ISO-10303-21;
HEADER;
/* Generated by software containing ST-Developer
 * from STEP Tools, Inc. (www.steptools.com) 
 */

FILE_DESCRIPTION(
/* description */ ('Compact handwheel screw vise'),
/* implementation_level */ '2;1');

FILE_NAME(
/* name */ 'Tr12x3 lead screw.step',
/* time_stamp */ '2026-10-29T16:08:22-07:00',
/* author */ (''),
/* organization */ (''),
/* preprocessor_version */ 'ST-DEVELOPER v20.2',
/* originating_system */ 'Autodesk Translation Framework v15.17.0.0',
/* authorisation */ '');

FILE_SCHEMA (('AUTOMOTIVE_DESIGN { 1 0 10303 214 3 1 1 }'));
ENDSEC;

DATA;
#10=MECHANICAL_DESIGN_GEOMETRIC_PRESENTATION_REPRESENTATION('',(#670),#25074);
#13=B_SPLINE_SURFACE_WITH_KNOTS('',3,3,((#20271,#20272,#20273,#20274,#20275,
#20276,#20277,#20278,#20279,#20280,#20281,#20282,#20283,#20284,#20285,#20286,
#20287,#20288,#20289,#20290,#20291,#20292,#20293,#20294,#20295,#20296,#20297,
#20298,#20299,#20300,#20301,#20302,#20303,#20304,#20305,#20306,#20307,#20308,
#20309,#20310,#20311,#20312,#20313,#20314,#20315,#20316,#20317,#20318,#20319,
#20320,#20321,#20322,#20323,#20324,#20325,#20326,#20327,#20328,#20329,#20330,
#20331,#20332,#20333,#20334,#20335,#20336,#20337,#20338,#20339,#20340,#20341,
#20342,#20343,#20344,#20345,#20346,#20347,#20348,#20349,#20350,#20351,#20352,
#20353,#20354,#20355,#20356,#20357,#20358,#20359,#20360,#20361,#20362,#20363,
#20364,#20365,#20366,#20367,#20368,#20369,#20370,#20371,#20372,#20373,#20374,
#20375,#20376,#20377,#20378,#20379,#20380,#20381,#20382,#20383,#20384,#20385,
#20386,#20387,#20388,#20389,#20390,#20391,#20392,#20393,#20394,#20395,#20396,
#20397,#20398,#20399,#20400,#20401,#20402,#20403,#20404,#20405,#20406,#20407,
#20408,#20409,#20410,#20411,#20412,#20413,#20414,#20415,#20416,#20417,#20418,
#20419,#20420,#20421,#20422,#20423,#20424,#20425,#20426,#20427,#20428,#20429,
#20430,#20431,#20432,#20433,#20434,#20435,#20436,#20437,#20438,#20439,#20440,
#20441,#20442,#20443,#20444,#20445,#20446,#20447,#20448,#20449,#20450,#20451,
#20452,#20453,#20454,#20455,#20456,#20457,#20458,#20459,#20460,#20461,#20462,
#20463,#20464,#20465,#20466,#20467,#20468,#20469,#20470,#20471,#20472,#20473,
#20474,#20475,#20476,#20477,#20478,#20479,#20480,#20481,#20482,#20483,#20484,
#20485,#20486,#20487,#20488,#20489,#20490,#20491,#20492,#20493,#20494,#20495,
#20496,#20497,#20498,#20499,#20500,#20501,#20502,#20503,#20504,#20505,#20506,
#20507,#20508,#20509,#20510,#20511,#20512,#20513,#20514,#20515,#20516,#20517,
#20518,#20519,#20520,#20521,#20522,#20523,#20524,#20525,#20526,#20527,#20528,
#20529,#20530,#20531,#20532,#20533,#20534,#20535,#20536,#20537,#20538,#20539,
#20540,#20541,#20542,#20543,#20544,#20545,#20546,#20547,#20548,#20549,#20550,
#20551,#20552,#20553,#20554,#20555,#20556,#20557,#20558,#20559,#20560,#20561,
#20562,#20563,#20564,#20565,#20566,#20567,#20568,#20569,#20570,#20571,#20572,
#20573,#20574,#20575,#20576,#20577,#20578,#20579,#20580,#20581,#20582,#20583,
#20584,#20585,#20586,#20587,#20588,#20589,#20590,#20591,#20592,#20593,#20594,
#20595,#20596,#20597,#20598,#20599,#20600,#20601,#20602,#20603,#20604,#20605,
#20606,#20607,#20608,#20609,#20610,#20611,#20612,#20613,#20614,#20615,#20616,
#20617,#20618,#20619,#20620,#20621,#20622,#20623,#20624,#20625,#20626,#20627,
#20628,#20629,#20630,#20631,#20632,#20633,#20634,#20635,#20636,#20637,#20638,
#20639,#20640,#20641,#20642,#20643,#20644,#20645,#20646,#20647,#20648,#20649,
#20650,#20651,#20652,#20653,#20654,#20655,#20656,#20657,#20658,#20659,#20660,
#20661,#20662,#20663,#20664,#20665,#20666,#20667,#20668,#20669,#20670,#20671,
#20672,#20673,#20674,#20675,#20676,#20677,#20678,#20679,#20680,#20681,#20682,
#20683,#20684,#20685,#20686,#20687,#20688,#20689,#20690,#20691,#20692,#20693,
#20694,#20695,#20696,#20697,#20698,#20699,#20700,#20701,#20702,#20703,#20704,
#20705,#20706,#20707,#20708,#20709,#20710,#20711,#20712,#20713,#20714,#20715,
#20716,#20717,#20718,#20719,#20720,#20721,#20722,#20723,#20724,#20725,#20726,
#20727,#20728,#20729,#20730,#20731,#20732,#20733,#20734,#20735,#20736,#20737,
#20738,#20739,#20740,#20741,#20742,#20743,#20744,#20745,#20746,#20747,#20748,
#20749,#20750,#20751,#20752,#20753,#20754,#20755,#20756,#20757,#20758,#20759,
#20760,#20761,#20762,#20763,#20764,#20765,#20766,#20767,#20768),(#20769,
#20770,#20771,#20772,#20773,#20774,#20775,#20776,#20777,#20778,#20779,#20780,
#20781,#20782,#20783,#20784,#20785,#20786,#20787,#20788,#20789,#20790,#20791,
#20792,#20793,#20794,#20795,#20796,#20797,#20798,#20799,#20800,#20801,#20802,
#20803,#20804,#20805,#20806,#20807,#20808,#20809,#20810,#20811,#20812,#20813,
#20814,#20815,#20816,#20817,#20818,#20819,#20820,#20821,#20822,#20823,#20824,
#20825,#20826,#20827,#20828,#20829,#20830,#20831,#20832,#20833,#20834,#20835,
#20836,#20837,#20838,#20839,#20840,#20841,#20842,#20843,#20844,#20845,#20846,
#20847,#20848,#20849,#20850,#20851,#20852,#20853,#20854,#20855,#20856,#20857,
#20858,#20859,#20860,#20861,#20862,#20863,#20864,#20865,#20866,#20867,#20868,
#20869,#20870,#20871,#20872,#20873,#20874,#20875,#20876,#20877,#20878,#20879,
#20880,#20881,#20882,#20883,#20884,#20885,#20886,#20887,#20888,#20889,#20890,
#20891,#20892,#20893,#20894,#20895,#20896,#20897,#20898,#20899,#20900,#20901,
#20902,#20903,#20904,#20905,#20906,#20907,#20908,#20909,#20910,#20911,#20912,
#20913,#20914,#20915,#20916,#20917,#20918,#20919,#20920,#20921,#20922,#20923,
#20924,#20925,#20926,#20927,#20928,#20929,#20930,#20931,#20932,#20933,#20934,
#20935,#20936,#20937,#20938,#20939,#20940,#20941,#20942,#20943,#20944,#20945,
#20946,#20947,#20948,#20949,#20950,#20951,#20952,#20953,#20954,#20955,#20956,
#20957,#20958,#20959,#20960,#20961,#20962,#20963,#20964,#20965,#20966,#20967,
#20968,#20969,#20970,#20971,#20972,#20973,#20974,#20975,#20976,#20977,#20978,
#20979,#20980,#20981,#20982,#20983,#20984,#20985,#20986,#20987,#20988,#20989,
#20990,#20991,#20992,#20993,#20994,#20995,#20996,#20997,#20998,#20999,#21000,
#21001,#21002,#21003,#21004,#21005,#21006,#21007,#21008,#21009,#21010,#21011,
#21012,#21013,#21014,#21015,#21016,#21017,#21018,#21019,#21020,#21021,#21022,
#21023,#21024,#21025,#21026,#21027,#21028,#21029,#21030,#21031,#21032,#21033,
#21034,#21035,#21036,#21037,#21038,#21039,#21040,#21041,#21042,#21043,#21044,
#21045,#21046,#21047,#21048,#21049,#21050,#21051,#21052,#21053,#21054,#21055,
#21056,#21057,#21058,#21059,#21060,#21061,#21062,#21063,#21064,#21065,#21066,
#21067,#21068,#21069,#21070,#21071,#21072,#21073,#21074,#21075,#21076,#21077,
#21078,#21079,#21080,#21081,#21082,#21083,#21084,#21085,#21086,#21087,#21088,
#21089,#21090,#21091,#21092,#21093,#21094,#21095,#21096,#21097,#21098,#21099,
#21100,#21101,#21102,#21103,#21104,#21105,#21106,#21107,#21108,#21109,#21110,
#21111,#21112,#21113,#21114,#21115,#21116,#21117,#21118,#21119,#21120,#21121,
#21122,#21123,#21124,#21125,#21126,#21127,#21128,#21129,#21130,#21131,#21132,
#21133,#21134,#21135,#21136,#21137,#21138,#21139,#21140,#21141,#21142,#21143,
#21144,#21145,#21146,#21147,#21148,#21149,#21150,#21151,#21152,#21153,#21154,
#21155,#21156,#21157,#21158,#21159,#21160,#21161,#21162,#21163,#21164,#21165,
#21166,#21167,#21168,#21169,#21170,#21171,#21172,#21173,#21174,#21175,#21176,
#21177,#21178,#21179,#21180,#21181,#21182,#21183,#21184,#21185,#21186,#21187,
#21188,#21189,#21190,#21191,#21192,#21193,#21194,#21195,#21196,#21197,#21198,
#21199,#21200,#21201,#21202,#21203,#21204,#21205,#21206,#21207,#21208,#21209,
#21210,#21211,#21212,#21213,#21214,#21215,#21216,#21217,#21218,#21219,#21220,
#21221,#21222,#21223,#21224,#21225,#21226,#21227,#21228,#21229,#21230,#21231,
#21232,#21233,#21234,#21235,#21236,#21237,#21238,#21239,#21240,#21241,#21242,
#21243,#21244,#21245,#21246,#21247,#21248,#21249,#21250,#21251,#21252,#21253,
#21254,#21255,#21256,#21257,#21258,#21259,#21260,#21261,#21262,#21263,#21264,
#21265,#21266),(#21267,#21268,#21269,#21270,#21271,#21272,#21273,#21274,
#21275,#21276,#21277,#21278,#21279,#21280,#21281,#21282,#21283,#21284,#21285,
#21286,#21287,#21288,#21289,#21290,#21291,#21292,#21293,#21294,#21295,#21296,
#21297,#21298,#21299,#21300,#21301,#21302,#21303,#21304,#21305,#21306,#21307,
#21308,#21309,#21310,#21311,#21312,#21313,#21314,#21315,#21316,#21317,#21318,
#21319,#21320,#21321,#21322,#21323,#21324,#21325,#21326,#21327,#21328,#21329,
#21330,#21331,#21332,#21333,#21334,#21335,#21336,#21337,#21338,#21339,#21340,
#21341,#21342,#21343,#21344,#21345,#21346,#21347,#21348,#21349,#21350,#21351,
#21352,#21353,#21354,#21355,#21356,#21357,#21358,#21359,#21360,#21361,#21362,
#21363,#21364,#21365,#21366,#21367,#21368,#21369,#21370,#21371,#21372,#21373,
#21374,#21375,#21376,#21377,#21378,#21379,#21380,#21381,#21382,#21383,#21384,
#21385,#21386,#21387,#21388,#21389,#21390,#21391,#21392,#21393,#21394,#21395,
#21396,#21397,#21398,#21399,#21400,#21401,#21402,#21403,#21404,#21405,#21406,
#21407,#21408,#21409,#21410,#21411,#21412,#21413,#21414,#21415,#21416,#21417,
#21418,#21419,#21420,#21421,#21422,#21423,#21424,#21425,#21426,#21427,#21428,
#21429,#21430,#21431,#21432,#21433,#21434,#21435,#21436,#21437,#21438,#21439,
#21440,#21441,#21442,#21443,#21444,#21445,#21446,#21447,#21448,#21449,#21450,
#21451,#21452,#21453,#21454,#21455,#21456,#21457,#21458,#21459,#21460,#21461,
#21462,#21463,#21464,#21465,#21466,#21467,#21468,#21469,#21470,#21471,#21472,
#21473,#21474,#21475,#21476,#21477,#21478,#21479,#21480,#21481,#21482,#21483,
#21484,#21485,#21486,#21487,#21488,#21489,#21490,#21491,#21492,#21493,#21494,
#21495,#21496,#21497,#21498,#21499,#21500,#21501,#21502,#21503,#21504,#21505,
#21506,#21507,#21508,#21509,#21510,#21511,#21512,#21513,#21514,#21515,#21516,
#21517,#21518,#21519,#21520,#21521,#21522,#21523,#21524,#21525,#21526,#21527,
#21528,#21529,#21530,#21531,#21532,#21533,#21534,#21535,#21536,#21537,#21538,
#21539,#21540,#21541,#21542,#21543,#21544,#21545,#21546,#21547,#21548,#21549,
#21550,#21551,#21552,#21553,#21554,#21555,#21556,#21557,#21558,#21559,#21560,
#21561,#21562,#21563,#21564,#21565,#21566,#21567,#21568,#21569,#21570,#21571,
#21572,#21573,#21574,#21575,#21576,#21577,#21578,#21579,#21580,#21581,#21582,
#21583,#21584,#21585,#21586,#21587,#21588,#21589,#21590,#21591,#21592,#21593,
#21594,#21595,#21596,#21597,#21598,#21599,#21600,#21601,#21602,#21603,#21604,
#21605,#21606,#21607,#21608,#21609,#21610,#21611,#21612,#21613,#21614,#21615,
#21616,#21617,#21618,#21619,#21620,#21621,#21622,#21623,#21624,#21625,#21626,
#21627,#21628,#21629,#21630,#21631,#21632,#21633,#21634,#21635,#21636,#21637,
#21638,#21639,#21640,#21641,#21642,#21643,#21644,#21645,#21646,#21647,#21648,
#21649,#21650,#21651,#21652,#21653,#21654,#21655,#21656,#21657,#21658,#21659,
#21660,#21661,#21662,#21663,#21664,#21665,#21666,#21667,#21668,#21669,#21670,
#21671,#21672,#21673,#21674,#21675,#21676,#21677,#21678,#21679,#21680,#21681,
#21682,#21683,#21684,#21685,#21686,#21687,#21688,#21689,#21690,#21691,#21692,
#21693,#21694,#21695,#21696,#21697,#21698,#21699,#21700,#21701,#21702,#21703,
#21704,#21705,#21706,#21707,#21708,#21709,#21710,#21711,#21712,#21713,#21714,
#21715,#21716,#21717,#21718,#21719,#21720,#21721,#21722,#21723,#21724,#21725,
#21726,#21727,#21728,#21729,#21730,#21731,#21732,#21733,#21734,#21735,#21736,
#21737,#21738,#21739,#21740,#21741,#21742,#21743,#21744,#21745,#21746,#21747,
#21748,#21749,#21750,#21751,#21752,#21753,#21754,#21755,#21756,#21757,#21758,
#21759,#21760,#21761,#21762,#21763,#21764),(#21765,#21766,#21767,#21768,
#21769,#21770,#21771,#21772,#21773,#21774,#21775,#21776,#21777,#21778,#21779,
#21780,#21781,#21782,#21783,#21784,#21785,#21786,#21787,#21788,#21789,#21790,
#21791,#21792,#21793,#21794,#21795,#21796,#21797,#21798,#21799,#21800,#21801,
#21802,#21803,#21804,#21805,#21806,#21807,#21808,#21809,#21810,#21811,#21812,
#21813,#21814,#21815,#21816,#21817,#21818,#21819,#21820,#21821,#21822,#21823,
#21824,#21825,#21826,#21827,#21828,#21829,#21830,#21831,#21832,#21833,#21834,
#21835,#21836,#21837,#21838,#21839,#21840,#21841,#21842,#21843,#21844,#21845,
#21846,#21847,#21848,#21849,#21850,#21851,#21852,#21853,#21854,#21855,#21856,
#21857,#21858,#21859,#21860,#21861,#21862,#21863,#21864,#21865,#21866,#21867,
#21868,#21869,#21870,#21871,#21872,#21873,#21874,#21875,#21876,#21877,#21878,
#21879,#21880,#21881,#21882,#21883,#21884,#21885,#21886,#21887,#21888,#21889,
#21890,#21891,#21892,#21893,#21894,#21895,#21896,#21897,#21898,#21899,#21900,
#21901,#21902,#21903,#21904,#21905,#21906,#21907,#21908,#21909,#21910,#21911,
#21912,#21913,#21914,#21915,#21916,#21917,#21918,#21919,#21920,#21921,#21922,
#21923,#21924,#21925,#21926,#21927,#21928,#21929,#21930,#21931,#21932,#21933,
#21934,#21935,#21936,#21937,#21938,#21939,#21940,#21941,#21942,#21943,#21944,
#21945,#21946,#21947,#21948,#21949,#21950,#21951,#21952,#21953,#21954,#21955,
#21956,#21957,#21958,#21959,#21960,#21961,#21962,#21963,#21964,#21965,#21966,
#21967,#21968,#21969,#21970,#21971,#21972,#21973,#21974,#21975,#21976,#21977,
#21978,#21979,#21980,#21981,#21982,#21983,#21984,#21985,#21986,#21987,#21988,
#21989,#21990,#21991,#21992,#21993,#21994,#21995,#21996,#21997,#21998,#21999,
#22000,#22001,#22002,#22003,#22004,#22005,#22006,#22007,#22008,#22009,#22010,
#22011,#22012,#22013,#22014,#22015,#22016,#22017,#22018,#22019,#22020,#22021,
#22022,#22023,#22024,#22025,#22026,#22027,#22028,#22029,#22030,#22031,#22032,
#22033,#22034,#22035,#22036,#22037,#22038,#22039,#22040,#22041,#22042,#22043,
#22044,#22045,#22046,#22047,#22048,#22049,#22050,#22051,#22052,#22053,#22054,
#22055,#22056,#22057,#22058,#22059,#22060,#22061,#22062,#22063,#22064,#22065,
#22066,#22067,#22068,#22069,#22070,#22071,#22072,#22073,#22074,#22075,#22076,
#22077,#22078,#22079,#22080,#22081,#22082,#22083,#22084,#22085,#22086,#22087,
#22088,#22089,#22090,#22091,#22092,#22093,#22094,#22095,#22096,#22097,#22098,
#22099,#22100,#22101,#22102,#22103,#22104,#22105,#22106,#22107,#22108,#22109,
#22110,#22111,#22112,#22113,#22114,#22115,#22116,#22117,#22118,#22119,#22120,
#22121,#22122,#22123,#22124,#22125,#22126,#22127,#22128,#22129,#22130,#22131,
#22132,#22133,#22134,#22135,#22136,#22137,#22138,#22139,#22140,#22141,#22142,
#22143,#22144,#22145,#22146,#22147,#22148,#22149,#22150,#22151,#22152,#22153,
#22154,#22155,#22156,#22157,#22158,#22159,#22160,#22161,#22162,#22163,#22164,
#22165,#22166,#22167,#22168,#22169,#22170,#22171,#22172,#22173,#22174,#22175,
#22176,#22177,#22178,#22179,#22180,#22181,#22182,#22183,#22184,#22185,#22186,
#22187,#22188,#22189,#22190,#22191,#22192,#22193,#22194,#22195,#22196,#22197,
#22198,#22199,#22200,#22201,#22202,#22203,#22204,#22205,#22206,#22207,#22208,
#22209,#22210,#22211,#22212,#22213,#22214,#22215,#22216,#22217,#22218,#22219,
#22220,#22221,#22222,#22223,#22224,#22225,#22226,#22227,#22228,#22229,#22230,
#22231,#22232,#22233,#22234,#22235,#22236,#22237,#22238,#22239,#22240,#22241,
#22242,#22243,#22244,#22245,#22246,#22247,#22248,#22249,#22250,#22251,#22252,
#22253,#22254,#22255,#22256,#22257,#22258,#22259,#22260,#22261,#22262)),
 .UNSPECIFIED.,.F.,.F.,.F.,(4,4),(4,1,1,1,1,1,1,1,1,1,1,1,1,1,1,1,1,1,1,
1,1,1,1,1,1,1,1,1,1,1,1,1,1,1,1,1,1,1,1,1,1,1,1,1,1,1,1,1,1,1,1,1,1,1,1,
1,1,1,1,1,1,1,1,1,1,1,1,1,1,1,1,1,1,1,1,1,1,1,1,1,1,1,1,1,1,1,1,1,1,1,1,
1,1,1,1,1,1,1,1,1,1,1,1,1,1,1,1,1,1,1,1,1,1,1,1,1,1,1,1,1,1,1,1,1,1,1,1,
1,1,1,1,1,1,1,1,1,1,1,1,1,1,1,1,1,1,1,1,1,1,1,1,1,1,1,1,1,1,1,1,1,1,1,1,
1,1,1,1,1,1,1,1,1,1,1,1,1,1,1,1,1,1,1,1,1,1,1,1,1,1,1,1,1,1,1,1,1,1,1,1,
1,1,1,1,1,1,1,1,1,1,1,1,1,1,1,1,1,1,1,1,1,1,1,1,1,1,1,1,1,1,1,1,1,1,1,1,
1,1,1,1,1,1,1,1,1,1,1,1,1,1,1,1,1,1,1,1,1,1,1,1,1,1,1,1,1,1,1,1,1,1,1,1,
1,1,1,1,1,1,1,1,1,1,1,1,1,1,1,1,1,1,1,1,1,1,1,1,1,1,1,1,1,1,1,1,1,1,1,1,
1,1,1,1,1,1,1,1,1,1,1,1,1,1,1,1,1,1,1,1,1,1,1,1,1,1,1,1,1,1,1,1,1,1,1,1,
1,1,1,1,1,1,1,1,1,1,1,1,1,1,1,1,1,1,1,1,1,1,1,1,1,1,1,1,1,1,1,1,1,1,1,1,
1,1,1,1,1,1,1,1,1,1,1,1,1,1,1,1,1,1,1,1,1,1,1,1,1,1,1,1,1,1,1,1,1,1,1,1,
1,1,1,1,1,1,1,1,1,1,1,1,1,1,1,1,1,1,1,1,1,1,1,1,1,1,1,1,1,1,1,1,1,1,1,1,
1,1,1,1,1,1,1,1,1,1,1,1,1,1,1,1,1,1,1,1,1,1,1,1,1,1,1,1,1,1,1,1,1,1,1,1,
1,1,1,1,1,1,1,1,4),(0.,0.184512097253587),(8.98171729021681,9.48139635699984,
9.98107542378286,10.4807544905659,10.9804335573489,11.4801126241319,11.979791690915,
12.479470757698,12.979149824481,13.478828891264,13.9785079580471,14.4781870248301,
14.9778660916131,15.4775451583961,15.9772242251791,16.4769032919622,16.9765823587452,
17.4762614255282,17.9759404923112,18.4756195590943,18.9752986258773,19.4749776926603,
19.9746567594433,20.4743358262264,20.9740148930094,21.4736939597924,21.9733730265754,
22.4730520933585,22.9727311601415,23.4724102269245,23.9720892937075,24.4717683604905,
24.9714474272736,25.4711264940566,25.9708055608396,26.4704846276226,26.9701636944057,
27.4698427611887,27.9695218279717,28.4692008947547,28.9688799615378,29.4685590283208,
29.9682380951038,30.4679171618868,30.9675962286699,31.4672752954529,31.9669543622359,
32.4666334290189,32.966312495802,33.465991562585,33.965670629368,34.465349696151,
34.965028762934,35.4647078297171,35.9643868965001,36.4640659632831,36.9637450300661,
37.4634240968492,37.9631031636322,38.4627822304152,38.9624612971982,39.4621403639813,
39.9618194307643,40.4614984975473,40.9611775643303,41.4608566311134,41.9605356978964,
42.4602147646794,42.9598938314624,43.4595728982454,43.9592519650285,44.4589310318115,
44.9586100985945,45.4582891653775,45.9579682321606,46.4576472989436,46.9573263657266,
47.4570054325096,47.9566844992927,48.4563635660757,48.9560426328587,49.4557216996417,
49.9554007664248,50.4550798332078,50.9547588999908,51.4544379667738,51.9541170335568,
52.4537961003399,52.9534751671229,53.4531542339059,53.9528333006889,54.452512367472,
54.952191434255,55.451870501038,55.951549567821,56.4512286346041,56.9509077013871,
57.4505867681701,57.9502658349531,58.4499449017362,58.9496239685192,59.9489821020852,
60.9483402356513,61.9476983692173,62.9470565027834,63.9464146363494,64.9457727699155,
65.9451309034815,66.9444890370476,67.9438471706136,68.9432053041797,69.9425634377457,
70.9419215713118,71.9412797048778,72.9406378384438,73.9399959720099,74.9393541055759,
75.938712239142,76.938070372708,77.9374285062741,78.9367866398401,79.9361447734062,
80.9355029069722,81.9348610405383,82.9342191741043,83.9335773076704,84.9329354412364,
85.9322935748025,86.9316517083685,87.9310098419346,88.9303679755006,89.9297261090666,
90.9290842426327,91.9284423761987,92.9278005097648,93.9271586433308,94.9265167768969,
95.9258749104629,96.925233044029,97.924591177595,98.9239493111611,99.9233074447271,
100.922665578293,101.922023711859,102.921381845425,103.920739978991,104.920098112557,
105.919456246123,106.918814379689,107.918172513255,108.917530646822,109.916888780388,
110.916246913954,111.91560504752,112.914963181086,113.914321314652,114.913679448218,
115.913037581784,116.91239571535,117.911753848916,118.911111982482,119.910470116048,
120.909828249614,121.90918638318,122.908544516746,123.907902650312,124.907260783878,
125.906618917444,126.90597705101,127.905335184576,128.904693318142,129.904051451709,
130.903409585275,131.902767718841,132.902125852407,133.901483985973,134.900842119539,
135.900200253105,136.899558386671,137.898916520237,138.898274653803,139.897632787369,
140.896990920935,141.896349054501,142.895707188067,143.895065321633,144.894423455199,
145.893781588765,146.893139722331,147.892497855897,148.891855989463,149.891214123029,
150.890572256596,151.889930390162,152.889288523728,153.888646657294,154.88800479086,
155.887362924426,156.886721057992,157.886079191558,158.885437325124,159.88479545869,
160.884153592256,161.883511725822,162.882869859388,163.882227992954,164.88158612652,
165.880944260086,166.880302393652,167.879660527218,168.879018660784,169.87837679435,
170.877734927916,171.877093061483,172.876451195049,173.875809328615,174.875167462181,
175.874525595747,176.873883729313,177.873241862879,178.872599996445,179.871958130011,
180.871316263577,181.870674397143,182.870032530709,183.869390664275,184.868748797841,
185.868106931407,186.867465064973,187.866823198539,188.866181332105,189.865539465671,
190.864897599237,191.864255732803,192.86361386637,193.862971999936,194.862330133502,
195.861688267068,196.861046400634,197.8604045342,198.859762667766,199.859120801332,
200.858478934898,201.857837068464,202.85719520203,203.856553335596,204.855911469162,
205.855269602728,206.854627736294,207.85398586986,208.853344003426,209.852702136992,
210.852060270558,211.851418404124,212.85077653769,213.850134671257,214.849492804823,
215.848850938389,216.848209071955,217.847567205521,218.846925339087,219.846283472653,
220.845641606219,221.844999739785,222.844357873351,223.843716006917,224.843074140483,
225.842432274049,226.841790407615,227.841148541181,228.840506674747,229.839864808313,
230.839222941879,231.838581075445,232.837939209011,233.837297342577,234.836655476144,
235.83601360971,236.835371743276,237.834729876842,238.834088010408,239.833446143974,
240.83280427754,241.832162411106,242.831520544672,243.830878678238,244.830236811804,
245.82959494537,246.828953078936,247.828311212502,248.827669346068,249.827027479634,
250.8263856132,251.825743746766,252.825101880332,253.824460013898,254.823818147464,
255.82317628103,256.822534414597,257.821892548163,258.821250681729,259.820608815295,
260.819966948861,261.819325082427,262.818683215993,263.818041349559,264.817399483125,
265.816757616691,266.816115750257,267.815473883823,268.814832017389,269.814190150955,
270.813548284521,271.812906418087,272.812264551653,273.811622685219,274.810980818785,
275.810338952351,276.809697085917,277.809055219484,278.80841335305,279.807771486616,
280.807129620182,281.806487753748,282.805845887314,283.80520402088,284.804562154446,
285.803920288012,286.803278421578,287.802636555144,288.80199468871,289.801352822276,
290.800710955842,291.800069089408,292.799427222974,293.79878535654,294.798143490106,
295.797501623672,296.796859757238,297.796217890804,298.795576024371,299.794934157937,
300.794292291503,301.793650425069,302.793008558635,303.792366692201,304.791724825767,
305.791082959333,306.790441092899,307.789799226465,308.789157360031,309.788515493597,
310.787873627163,311.787231760729,312.786589894295,313.785948027861,314.785306161427,
315.784664294993,316.784022428559,317.783380562125,318.782738695691,319.782096829258,
320.781454962824,321.78081309639,322.780171229956,323.779529363522,324.778887497088,
325.778245630654,326.77760376422,327.776961897786,328.776320031352,329.775678164918,
330.775036298484,331.77439443205,332.773752565616,333.773110699182,334.772468832748,
335.771826966314,336.77118509988,337.770543233446,338.769901367012,339.769259500578,
340.768617634145,341.767975767711,342.767333901277,343.766692034843,344.766050168409,
345.765408301975,346.764766435541,347.764124569107,348.763482702673,349.762840836239,
350.762198969805,351.761557103371,352.760915236937,353.760273370503,354.259952437286,
354.759631504069,355.259310570852,355.758989637635,356.258668704418,356.758347771201,
357.258026837984,357.757705904767,358.25738497155,358.757064038333,359.256743105116,
359.756422171899,360.256101238682,360.755780305465,361.255459372248,361.755138439031,
362.254817505815,362.754496572598,363.254175639381,363.753854706164,364.253533772947,
364.75321283973,365.252891906513,365.752570973296,366.252250040079,366.751929106862,
367.251608173645,367.751287240428,368.250966307211,368.750645373994,369.250324440777,
369.75000350756,370.249682574343,370.749361641126,371.249040707909,371.748719774692,
372.248398841475,372.748077908258,373.247756975041,373.747436041824,374.247115108607,
374.74679417539,375.246473242173,375.746152308956,376.245831375739,376.745510442522,
377.245189509305,377.744868576088,378.244547642871,378.744226709654,379.243905776437,
379.74358484322,380.243263910003,380.742942976786,381.242622043569,381.742301110352,
382.241980177135,382.741659243918,383.241338310702,383.741017377485,384.240696444268,
384.740375511051,385.240054577834,385.739733644617,386.2394127114,386.739091778183,
387.238770844966,387.738449911749,388.238128978532,388.737808045315,389.237487112098,
389.737166178881,390.236845245664,390.736524312447,391.23620337923,391.735882446013,
392.235561512796,392.735240579579,393.234919646362,393.734598713145,394.234277779928,
394.733956846711,395.233635913494,395.733314980277,396.23299404706,396.732673113843,
397.232352180626,397.732031247409,398.231710314192,398.731389380975,399.231068447758,
399.730747514541,400.230426581324,400.730105648107,401.22978471489,401.729463781673,
402.229142848456,402.728821915239,403.228500982022,403.728180048805),
 .UNSPECIFIED.);
#14=B_SPLINE_SURFACE_WITH_KNOTS('',3,3,((#22396,#22397,#22398,#22399,#22400,
#22401,#22402,#22403,#22404,#22405,#22406,#22407,#22408,#22409,#22410,#22411,
#22412,#22413,#22414,#22415,#22416,#22417,#22418,#22419,#22420,#22421,#22422,
#22423,#22424,#22425,#22426,#22427,#22428,#22429,#22430,#22431,#22432,#22433,
#22434,#22435,#22436,#22437,#22438,#22439,#22440,#22441,#22442,#22443,#22444,
#22445,#22446,#22447,#22448,#22449,#22450,#22451,#22452,#22453,#22454,#22455,
#22456,#22457,#22458,#22459,#22460,#22461,#22462,#22463,#22464,#22465,#22466,
#22467,#22468,#22469,#22470,#22471,#22472,#22473,#22474,#22475,#22476,#22477,
#22478,#22479,#22480,#22481,#22482,#22483,#22484,#22485,#22486,#22487,#22488,
#22489,#22490,#22491,#22492,#22493,#22494,#22495,#22496,#22497,#22498,#22499,
#22500,#22501,#22502,#22503,#22504,#22505,#22506,#22507,#22508,#22509,#22510,
#22511,#22512,#22513,#22514,#22515,#22516,#22517,#22518,#22519,#22520,#22521,
#22522,#22523,#22524,#22525,#22526,#22527,#22528,#22529,#22530,#22531,#22532,
#22533,#22534,#22535,#22536,#22537,#22538,#22539,#22540,#22541,#22542,#22543,
#22544,#22545,#22546,#22547,#22548,#22549,#22550,#22551,#22552,#22553,#22554,
#22555,#22556,#22557,#22558,#22559,#22560,#22561,#22562,#22563,#22564,#22565,
#22566,#22567,#22568,#22569,#22570,#22571,#22572,#22573,#22574,#22575,#22576,
#22577,#22578,#22579,#22580,#22581,#22582,#22583,#22584,#22585,#22586,#22587,
#22588,#22589,#22590,#22591,#22592,#22593,#22594,#22595,#22596,#22597,#22598,
#22599,#22600,#22601,#22602,#22603,#22604,#22605,#22606,#22607,#22608,#22609,
#22610,#22611,#22612,#22613,#22614,#22615,#22616,#22617,#22618,#22619,#22620,
#22621,#22622,#22623,#22624,#22625,#22626,#22627,#22628,#22629,#22630,#22631,
#22632,#22633,#22634,#22635,#22636,#22637,#22638,#22639,#22640,#22641,#22642,
#22643,#22644,#22645,#22646,#22647,#22648,#22649,#22650,#22651,#22652,#22653,
#22654,#22655,#22656,#22657,#22658,#22659,#22660,#22661,#22662,#22663,#22664,
#22665,#22666,#22667,#22668,#22669,#22670,#22671,#22672,#22673,#22674,#22675,
#22676,#22677,#22678,#22679,#22680,#22681,#22682,#22683,#22684,#22685,#22686,
#22687,#22688,#22689,#22690,#22691,#22692,#22693,#22694,#22695,#22696,#22697,
#22698,#22699,#22700,#22701,#22702,#22703,#22704,#22705,#22706,#22707,#22708,
#22709,#22710,#22711,#22712,#22713,#22714,#22715,#22716,#22717,#22718,#22719,
#22720,#22721,#22722,#22723,#22724,#22725,#22726,#22727,#22728,#22729,#22730,
#22731,#22732,#22733,#22734,#22735,#22736,#22737,#22738,#22739,#22740,#22741,
#22742,#22743,#22744,#22745,#22746,#22747,#22748,#22749,#22750,#22751,#22752,
#22753,#22754,#22755,#22756,#22757,#22758,#22759,#22760,#22761,#22762,#22763,
#22764,#22765,#22766,#22767,#22768,#22769,#22770,#22771,#22772,#22773,#22774,
#22775,#22776,#22777,#22778,#22779,#22780,#22781,#22782,#22783,#22784,#22785,
#22786,#22787,#22788,#22789,#22790,#22791,#22792,#22793,#22794,#22795,#22796,
#22797,#22798,#22799,#22800,#22801,#22802,#22803,#22804,#22805,#22806,#22807,
#22808,#22809,#22810,#22811,#22812,#22813,#22814,#22815,#22816,#22817,#22818,
#22819,#22820,#22821,#22822,#22823,#22824,#22825,#22826,#22827,#22828,#22829,
#22830,#22831,#22832,#22833,#22834,#22835,#22836,#22837,#22838,#22839,#22840,
#22841,#22842,#22843,#22844,#22845,#22846,#22847,#22848,#22849,#22850,#22851,
#22852,#22853,#22854,#22855,#22856,#22857,#22858,#22859,#22860,#22861,#22862,
#22863,#22864,#22865,#22866,#22867,#22868,#22869,#22870,#22871,#22872,#22873,
#22874,#22875,#22876,#22877,#22878,#22879,#22880,#22881,#22882,#22883,#22884,
#22885,#22886,#22887,#22888,#22889,#22890,#22891,#22892,#22893),(#22894,
#22895,#22896,#22897,#22898,#22899,#22900,#22901,#22902,#22903,#22904,#22905,
#22906,#22907,#22908,#22909,#22910,#22911,#22912,#22913,#22914,#22915,#22916,
#22917,#22918,#22919,#22920,#22921,#22922,#22923,#22924,#22925,#22926,#22927,
#22928,#22929,#22930,#22931,#22932,#22933,#22934,#22935,#22936,#22937,#22938,
#22939,#22940,#22941,#22942,#22943,#22944,#22945,#22946,#22947,#22948,#22949,
#22950,#22951,#22952,#22953,#22954,#22955,#22956,#22957,#22958,#22959,#22960,
#22961,#22962,#22963,#22964,#22965,#22966,#22967,#22968,#22969,#22970,#22971,
#22972,#22973,#22974,#22975,#22976,#22977,#22978,#22979,#22980,#22981,#22982,
#22983,#22984,#22985,#22986,#22987,#22988,#22989,#22990,#22991,#22992,#22993,
#22994,#22995,#22996,#22997,#22998,#22999,#23000,#23001,#23002,#23003,#23004,
#23005,#23006,#23007,#23008,#23009,#23010,#23011,#23012,#23013,#23014,#23015,
#23016,#23017,#23018,#23019,#23020,#23021,#23022,#23023,#23024,#23025,#23026,
#23027,#23028,#23029,#23030,#23031,#23032,#23033,#23034,#23035,#23036,#23037,
#23038,#23039,#23040,#23041,#23042,#23043,#23044,#23045,#23046,#23047,#23048,
#23049,#23050,#23051,#23052,#23053,#23054,#23055,#23056,#23057,#23058,#23059,
#23060,#23061,#23062,#23063,#23064,#23065,#23066,#23067,#23068,#23069,#23070,
#23071,#23072,#23073,#23074,#23075,#23076,#23077,#23078,#23079,#23080,#23081,
#23082,#23083,#23084,#23085,#23086,#23087,#23088,#23089,#23090,#23091,#23092,
#23093,#23094,#23095,#23096,#23097,#23098,#23099,#23100,#23101,#23102,#23103,
#23104,#23105,#23106,#23107,#23108,#23109,#23110,#23111,#23112,#23113,#23114,
#23115,#23116,#23117,#23118,#23119,#23120,#23121,#23122,#23123,#23124,#23125,
#23126,#23127,#23128,#23129,#23130,#23131,#23132,#23133,#23134,#23135,#23136,
#23137,#23138,#23139,#23140,#23141,#23142,#23143,#23144,#23145,#23146,#23147,
#23148,#23149,#23150,#23151,#23152,#23153,#23154,#23155,#23156,#23157,#23158,
#23159,#23160,#23161,#23162,#23163,#23164,#23165,#23166,#23167,#23168,#23169,
#23170,#23171,#23172,#23173,#23174,#23175,#23176,#23177,#23178,#23179,#23180,
#23181,#23182,#23183,#23184,#23185,#23186,#23187,#23188,#23189,#23190,#23191,
#23192,#23193,#23194,#23195,#23196,#23197,#23198,#23199,#23200,#23201,#23202,
#23203,#23204,#23205,#23206,#23207,#23208,#23209,#23210,#23211,#23212,#23213,
#23214,#23215,#23216,#23217,#23218,#23219,#23220,#23221,#23222,#23223,#23224,
#23225,#23226,#23227,#23228,#23229,#23230,#23231,#23232,#23233,#23234,#23235,
#23236,#23237,#23238,#23239,#23240,#23241,#23242,#23243,#23244,#23245,#23246,
#23247,#23248,#23249,#23250,#23251,#23252,#23253,#23254,#23255,#23256,#23257,
#23258,#23259,#23260,#23261,#23262,#23263,#23264,#23265,#23266,#23267,#23268,
#23269,#23270,#23271,#23272,#23273,#23274,#23275,#23276,#23277,#23278,#23279,
#23280,#23281,#23282,#23283,#23284,#23285,#23286,#23287,#23288,#23289,#23290,
#23291,#23292,#23293,#23294,#23295,#23296,#23297,#23298,#23299,#23300,#23301,
#23302,#23303,#23304,#23305,#23306,#23307,#23308,#23309,#23310,#23311,#23312,
#23313,#23314,#23315,#23316,#23317,#23318,#23319,#23320,#23321,#23322,#23323,
#23324,#23325,#23326,#23327,#23328,#23329,#23330,#23331,#23332,#23333,#23334,
#23335,#23336,#23337,#23338,#23339,#23340,#23341,#23342,#23343,#23344,#23345,
#23346,#23347,#23348,#23349,#23350,#23351,#23352,#23353,#23354,#23355,#23356,
#23357,#23358,#23359,#23360,#23361,#23362,#23363,#23364,#23365,#23366,#23367,
#23368,#23369,#23370,#23371,#23372,#23373,#23374,#23375,#23376,#23377,#23378,
#23379,#23380,#23381,#23382,#23383,#23384,#23385,#23386,#23387,#23388,#23389,
#23390,#23391),(#23392,#23393,#23394,#23395,#23396,#23397,#23398,#23399,
#23400,#23401,#23402,#23403,#23404,#23405,#23406,#23407,#23408,#23409,#23410,
#23411,#23412,#23413,#23414,#23415,#23416,#23417,#23418,#23419,#23420,#23421,
#23422,#23423,#23424,#23425,#23426,#23427,#23428,#23429,#23430,#23431,#23432,
#23433,#23434,#23435,#23436,#23437,#23438,#23439,#23440,#23441,#23442,#23443,
#23444,#23445,#23446,#23447,#23448,#23449,#23450,#23451,#23452,#23453,#23454,
#23455,#23456,#23457,#23458,#23459,#23460,#23461,#23462,#23463,#23464,#23465,
#23466,#23467,#23468,#23469,#23470,#23471,#23472,#23473,#23474,#23475,#23476,
#23477,#23478,#23479,#23480,#23481,#23482,#23483,#23484,#23485,#23486,#23487,
#23488,#23489,#23490,#23491,#23492,#23493,#23494,#23495,#23496,#23497,#23498,
#23499,#23500,#23501,#23502,#23503,#23504,#23505,#23506,#23507,#23508,#23509,
#23510,#23511,#23512,#23513,#23514,#23515,#23516,#23517,#23518,#23519,#23520,
#23521,#23522,#23523,#23524,#23525,#23526,#23527,#23528,#23529,#23530,#23531,
#23532,#23533,#23534,#23535,#23536,#23537,#23538,#23539,#23540,#23541,#23542,
#23543,#23544,#23545,#23546,#23547,#23548,#23549,#23550,#23551,#23552,#23553,
#23554,#23555,#23556,#23557,#23558,#23559,#23560,#23561,#23562,#23563,#23564,
#23565,#23566,#23567,#23568,#23569,#23570,#23571,#23572,#23573,#23574,#23575,
#23576,#23577,#23578,#23579,#23580,#23581,#23582,#23583,#23584,#23585,#23586,
#23587,#23588,#23589,#23590,#23591,#23592,#23593,#23594,#23595,#23596,#23597,
#23598,#23599,#23600,#23601,#23602,#23603,#23604,#23605,#23606,#23607,#23608,
#23609,#23610,#23611,#23612,#23613,#23614,#23615,#23616,#23617,#23618,#23619,
#23620,#23621,#23622,#23623,#23624,#23625,#23626,#23627,#23628,#23629,#23630,
#23631,#23632,#23633,#23634,#23635,#23636,#23637,#23638,#23639,#23640,#23641,
#23642,#23643,#23644,#23645,#23646,#23647,#23648,#23649,#23650,#23651,#23652,
#23653,#23654,#23655,#23656,#23657,#23658,#23659,#23660,#23661,#23662,#23663,
#23664,#23665,#23666,#23667,#23668,#23669,#23670,#23671,#23672,#23673,#23674,
#23675,#23676,#23677,#23678,#23679,#23680,#23681,#23682,#23683,#23684,#23685,
#23686,#23687,#23688,#23689,#23690,#23691,#23692,#23693,#23694,#23695,#23696,
#23697,#23698,#23699,#23700,#23701,#23702,#23703,#23704,#23705,#23706,#23707,
#23708,#23709,#23710,#23711,#23712,#23713,#23714,#23715,#23716,#23717,#23718,
#23719,#23720,#23721,#23722,#23723,#23724,#23725,#23726,#23727,#23728,#23729,
#23730,#23731,#23732,#23733,#23734,#23735,#23736,#23737,#23738,#23739,#23740,
#23741,#23742,#23743,#23744,#23745,#23746,#23747,#23748,#23749,#23750,#23751,
#23752,#23753,#23754,#23755,#23756,#23757,#23758,#23759,#23760,#23761,#23762,
#23763,#23764,#23765,#23766,#23767,#23768,#23769,#23770,#23771,#23772,#23773,
#23774,#23775,#23776,#23777,#23778,#23779,#23780,#23781,#23782,#23783,#23784,
#23785,#23786,#23787,#23788,#23789,#23790,#23791,#23792,#23793,#23794,#23795,
#23796,#23797,#23798,#23799,#23800,#23801,#23802,#23803,#23804,#23805,#23806,
#23807,#23808,#23809,#23810,#23811,#23812,#23813,#23814,#23815,#23816,#23817,
#23818,#23819,#23820,#23821,#23822,#23823,#23824,#23825,#23826,#23827,#23828,
#23829,#23830,#23831,#23832,#23833,#23834,#23835,#23836,#23837,#23838,#23839,
#23840,#23841,#23842,#23843,#23844,#23845,#23846,#23847,#23848,#23849,#23850,
#23851,#23852,#23853,#23854,#23855,#23856,#23857,#23858,#23859,#23860,#23861,
#23862,#23863,#23864,#23865,#23866,#23867,#23868,#23869,#23870,#23871,#23872,
#23873,#23874,#23875,#23876,#23877,#23878,#23879,#23880,#23881,#23882,#23883,
#23884,#23885,#23886,#23887,#23888,#23889),(#23890,#23891,#23892,#23893,
#23894,#23895,#23896,#23897,#23898,#23899,#23900,#23901,#23902,#23903,#23904,
#23905,#23906,#23907,#23908,#23909,#23910,#23911,#23912,#23913,#23914,#23915,
#23916,#23917,#23918,#23919,#23920,#23921,#23922,#23923,#23924,#23925,#23926,
#23927,#23928,#23929,#23930,#23931,#23932,#23933,#23934,#23935,#23936,#23937,
#23938,#23939,#23940,#23941,#23942,#23943,#23944,#23945,#23946,#23947,#23948,
#23949,#23950,#23951,#23952,#23953,#23954,#23955,#23956,#23957,#23958,#23959,
#23960,#23961,#23962,#23963,#23964,#23965,#23966,#23967,#23968,#23969,#23970,
#23971,#23972,#23973,#23974,#23975,#23976,#23977,#23978,#23979,#23980,#23981,
#23982,#23983,#23984,#23985,#23986,#23987,#23988,#23989,#23990,#23991,#23992,
#23993,#23994,#23995,#23996,#23997,#23998,#23999,#24000,#24001,#24002,#24003,
#24004,#24005,#24006,#24007,#24008,#24009,#24010,#24011,#24012,#24013,#24014,
#24015,#24016,#24017,#24018,#24019,#24020,#24021,#24022,#24023,#24024,#24025,
#24026,#24027,#24028,#24029,#24030,#24031,#24032,#24033,#24034,#24035,#24036,
#24037,#24038,#24039,#24040,#24041,#24042,#24043,#24044,#24045,#24046,#24047,
#24048,#24049,#24050,#24051,#24052,#24053,#24054,#24055,#24056,#24057,#24058,
#24059,#24060,#24061,#24062,#24063,#24064,#24065,#24066,#24067,#24068,#24069,
#24070,#24071,#24072,#24073,#24074,#24075,#24076,#24077,#24078,#24079,#24080,
#24081,#24082,#24083,#24084,#24085,#24086,#24087,#24088,#24089,#24090,#24091,
#24092,#24093,#24094,#24095,#24096,#24097,#24098,#24099,#24100,#24101,#24102,
#24103,#24104,#24105,#24106,#24107,#24108,#24109,#24110,#24111,#24112,#24113,
#24114,#24115,#24116,#24117,#24118,#24119,#24120,#24121,#24122,#24123,#24124,
#24125,#24126,#24127,#24128,#24129,#24130,#24131,#24132,#24133,#24134,#24135,
#24136,#24137,#24138,#24139,#24140,#24141,#24142,#24143,#24144,#24145,#24146,
#24147,#24148,#24149,#24150,#24151,#24152,#24153,#24154,#24155,#24156,#24157,
#24158,#24159,#24160,#24161,#24162,#24163,#24164,#24165,#24166,#24167,#24168,
#24169,#24170,#24171,#24172,#24173,#24174,#24175,#24176,#24177,#24178,#24179,
#24180,#24181,#24182,#24183,#24184,#24185,#24186,#24187,#24188,#24189,#24190,
#24191,#24192,#24193,#24194,#24195,#24196,#24197,#24198,#24199,#24200,#24201,
#24202,#24203,#24204,#24205,#24206,#24207,#24208,#24209,#24210,#24211,#24212,
#24213,#24214,#24215,#24216,#24217,#24218,#24219,#24220,#24221,#24222,#24223,
#24224,#24225,#24226,#24227,#24228,#24229,#24230,#24231,#24232,#24233,#24234,
#24235,#24236,#24237,#24238,#24239,#24240,#24241,#24242,#24243,#24244,#24245,
#24246,#24247,#24248,#24249,#24250,#24251,#24252,#24253,#24254,#24255,#24256,
#24257,#24258,#24259,#24260,#24261,#24262,#24263,#24264,#24265,#24266,#24267,
#24268,#24269,#24270,#24271,#24272,#24273,#24274,#24275,#24276,#24277,#24278,
#24279,#24280,#24281,#24282,#24283,#24284,#24285,#24286,#24287,#24288,#24289,
#24290,#24291,#24292,#24293,#24294,#24295,#24296,#24297,#24298,#24299,#24300,
#24301,#24302,#24303,#24304,#24305,#24306,#24307,#24308,#24309,#24310,#24311,
#24312,#24313,#24314,#24315,#24316,#24317,#24318,#24319,#24320,#24321,#24322,
#24323,#24324,#24325,#24326,#24327,#24328,#24329,#24330,#24331,#24332,#24333,
#24334,#24335,#24336,#24337,#24338,#24339,#24340,#24341,#24342,#24343,#24344,
#24345,#24346,#24347,#24348,#24349,#24350,#24351,#24352,#24353,#24354,#24355,
#24356,#24357,#24358,#24359,#24360,#24361,#24362,#24363,#24364,#24365,#24366,
#24367,#24368,#24369,#24370,#24371,#24372,#24373,#24374,#24375,#24376,#24377,
#24378,#24379,#24380,#24381,#24382,#24383,#24384,#24385,#24386,#24387)),
 .UNSPECIFIED.,.F.,.F.,.F.,(4,4),(4,1,1,1,1,1,1,1,1,1,1,1,1,1,1,1,1,1,1,
1,1,1,1,1,1,1,1,1,1,1,1,1,1,1,1,1,1,1,1,1,1,1,1,1,1,1,1,1,1,1,1,1,1,1,1,
1,1,1,1,1,1,1,1,1,1,1,1,1,1,1,1,1,1,1,1,1,1,1,1,1,1,1,1,1,1,1,1,1,1,1,1,
1,1,1,1,1,1,1,1,1,1,1,1,1,1,1,1,1,1,1,1,1,1,1,1,1,1,1,1,1,1,1,1,1,1,1,1,
1,1,1,1,1,1,1,1,1,1,1,1,1,1,1,1,1,1,1,1,1,1,1,1,1,1,1,1,1,1,1,1,1,1,1,1,
1,1,1,1,1,1,1,1,1,1,1,1,1,1,1,1,1,1,1,1,1,1,1,1,1,1,1,1,1,1,1,1,1,1,1,1,
1,1,1,1,1,1,1,1,1,1,1,1,1,1,1,1,1,1,1,1,1,1,1,1,1,1,1,1,1,1,1,1,1,1,1,1,
1,1,1,1,1,1,1,1,1,1,1,1,1,1,1,1,1,1,1,1,1,1,1,1,1,1,1,1,1,1,1,1,1,1,1,1,
1,1,1,1,1,1,1,1,1,1,1,1,1,1,1,1,1,1,1,1,1,1,1,1,1,1,1,1,1,1,1,1,1,1,1,1,
1,1,1,1,1,1,1,1,1,1,1,1,1,1,1,1,1,1,1,1,1,1,1,1,1,1,1,1,1,1,1,1,1,1,1,1,
1,1,1,1,1,1,1,1,1,1,1,1,1,1,1,1,1,1,1,1,1,1,1,1,1,1,1,1,1,1,1,1,1,1,1,1,
1,1,1,1,1,1,1,1,1,1,1,1,1,1,1,1,1,1,1,1,1,1,1,1,1,1,1,1,1,1,1,1,1,1,1,1,
1,1,1,1,1,1,1,1,1,1,1,1,1,1,1,1,1,1,1,1,1,1,1,1,1,1,1,1,1,1,1,1,1,1,1,1,
1,1,1,1,1,1,1,1,1,1,1,1,1,1,1,1,1,1,1,1,1,1,1,1,1,1,1,1,1,1,1,1,1,1,1,1,
1,1,1,1,1,1,1,1,4),(0.,0.184512097253587),(12.0092477762453,12.5089268430284,
13.0086059098114,13.5082849765944,14.0079640433774,14.5076431101605,15.0073221769435,
15.5070012437265,16.0066803105095,16.5063593772925,17.0060384440756,17.5057175108586,
18.0053965776416,18.5050756444246,19.0047547112077,19.5044337779907,20.0041128447737,
20.5037919115567,21.0034709783398,21.5031500451228,22.0028291119058,22.5025081786888,
23.0021872454719,23.5018663122549,24.0015453790379,24.5012244458209,25.0009035126039,
25.500582579387,26.00026164617,26.499940712953,26.999619779736,27.4992988465191,
27.9989779133021,28.4986569800851,28.9983360468681,29.4980151136512,29.9976941804342,
30.4973732472172,30.9970523140002,31.4967313807832,31.9964104475663,32.4960895143493,
32.9957685811323,33.4954476479153,33.9951267146984,34.4948057814814,34.9944848482644,
35.4941639150474,35.9938429818305,36.4935220486135,36.9932011153965,37.4928801821795,
37.9925592489626,38.4922383157456,38.9919173825286,39.4915964493116,39.9912755160946,
40.4909545828777,40.9906336496607,41.4903127164437,41.9899917832267,42.4896708500098,
42.9893499167928,43.4890289835758,43.9887080503588,44.4883871171419,44.9880661839249,
45.4877452507079,45.9874243174909,46.4871033842739,46.986782451057,47.48646151784,
47.986140584623,48.485819651406,48.9854987181891,49.4851777849721,49.9848568517551,
50.4845359185381,50.9842149853212,51.4838940521042,51.9835731188872,52.4832521856702,
52.9829312524532,53.4826103192363,53.9822893860193,54.4819684528023,54.9816475195853,
55.4813265863684,55.9810056531514,56.4806847199344,56.9803637867174,57.4800428535005,
57.9797219202835,58.4794009870665,58.9790800538495,59.4787591206325,59.9784381874156,
60.4781172541986,60.9777963209816,61.4774753877646,61.9771544545477,62.9765125881137,
63.9758707216798,64.9752288552458,65.9745869888119,66.9739451223779,67.9733032559439,
68.97266138951,69.972019523076,70.9713776566421,71.9707357902081,72.9700939237742,
73.9694520573402,74.9688101909063,75.9681683244723,76.9675264580384,77.9668845916044,
78.9662427251705,79.9656008587365,80.9649589923026,81.9643171258686,82.9636752594347,
83.9630333930007,84.9623915265667,85.9617496601328,86.9611077936988,87.9604659272649,
88.9598240608309,89.959182194397,90.958540327963,91.9578984615291,92.9572565950951,
93.9566147286612,94.9559728622272,95.9553309957932,96.9546891293593,97.9540472629253,
98.9534053964914,99.9527635300574,100.952121663623,101.95147979719,102.950837930756,
103.950196064322,104.949554197888,105.948912331454,106.94827046502,107.947628598586,
108.946986732152,109.946344865718,110.945702999284,111.94506113285,112.944419266416,
113.943777399982,114.943135533548,115.942493667114,116.94185180068,117.941209934246,
118.940568067812,119.939926201378,120.939284334944,121.93864246851,122.938000602077,
123.937358735643,124.936716869209,125.936075002775,126.935433136341,127.934791269907,
128.934149403473,129.933507537039,130.932865670605,131.932223804171,132.931581937737,
133.930940071303,134.930298204869,135.929656338435,136.929014472001,137.928372605567,
138.927730739133,139.927088872699,140.926447006265,141.925805139831,142.925163273397,
143.924521406963,144.92387954053,145.923237674096,146.922595807662,147.921953941228,
148.921312074794,149.92067020836,150.920028341926,151.919386475492,152.918744609058,
153.918102742624,154.91746087619,155.916819009756,156.916177143322,157.915535276888,
158.914893410454,159.91425154402,160.913609677586,161.912967811152,162.912325944718,
163.911684078284,164.91104221185,165.910400345416,166.909758478983,167.909116612549,
168.908474746115,169.907832879681,170.907191013247,171.906549146813,172.905907280379,
173.905265413945,174.904623547511,175.903981681077,176.903339814643,177.902697948209,
178.902056081775,179.901414215341,180.900772348907,181.900130482473,182.899488616039,
183.898846749605,184.898204883171,185.897563016737,186.896921150303,187.89627928387,
188.895637417436,189.894995551002,190.894353684568,191.893711818134,192.8930699517,
193.892428085266,194.891786218832,195.891144352398,196.890502485964,197.88986061953,
198.889218753096,199.888576886662,200.887935020228,201.887293153794,202.88665128736,
203.886009420926,204.885367554492,205.884725688058,206.884083821624,207.88344195519,
208.882800088756,209.882158222323,210.881516355889,211.880874489455,212.880232623021,
213.879590756587,214.878948890153,215.878307023719,216.877665157285,217.877023290851,
218.876381424417,219.875739557983,220.875097691549,221.874455825115,222.873813958681,
223.873172092247,224.872530225813,225.871888359379,226.871246492945,227.870604626511,
228.869962760077,229.869320893643,230.86867902721,231.868037160776,232.867395294342,
233.866753427908,234.866111561474,235.86546969504,236.864827828606,237.864185962172,
238.863544095738,239.862902229304,240.86226036287,241.861618496436,242.860976630002,
243.860334763568,244.859692897134,245.8590510307,246.858409164266,247.857767297832,
248.857125431398,249.856483564964,250.85584169853,251.855199832097,252.854557965663,
253.853916099229,254.853274232795,255.852632366361,256.851990499927,257.851348633493,
258.850706767059,259.850064900625,260.849423034191,261.848781167757,262.848139301323,
263.847497434889,264.846855568455,265.846213702021,266.845571835587,267.844929969153,
268.844288102719,269.843646236285,270.843004369851,271.842362503417,272.841720636983,
273.84107877055,274.840436904116,275.839795037682,276.839153171248,277.838511304814,
278.83786943838,279.837227571946,280.836585705512,281.835943839078,282.835301972644,
283.83466010621,284.834018239776,285.833376373342,286.832734506908,287.832092640474,
288.83145077404,289.830808907606,290.830167041172,291.829525174738,292.828883308304,
293.82824144187,294.827599575437,295.826957709003,296.826315842569,297.825673976135,
298.825032109701,299.824390243267,300.823748376833,301.823106510399,302.822464643965,
303.821822777531,304.821180911097,305.820539044663,306.819897178229,307.819255311795,
308.818613445361,309.817971578927,310.817329712493,311.816687846059,312.816045979625,
313.815404113191,314.814762246757,315.814120380323,316.81347851389,317.812836647456,
318.812194781022,319.811552914588,320.810911048154,321.81026918172,322.809627315286,
323.808985448852,324.808343582418,325.807701715984,326.80705984955,327.806417983116,
328.805776116682,329.805134250248,330.804492383814,331.80385051738,332.803208650946,
333.802566784512,334.801924918078,335.801283051644,336.80064118521,337.799999318776,
338.799357452343,339.798715585909,340.798073719475,341.797431853041,342.796789986607,
343.796148120173,344.795506253739,345.794864387305,346.794222520871,347.793580654437,
348.792938788003,349.792296921569,350.791655055135,351.791013188701,352.790371322267,
353.789729455833,354.789087589399,355.788445722965,356.787803856531,357.287482923314,
357.787161990097,358.28684105688,358.786520123663,359.286199190446,359.78587825723,
360.285557324013,360.785236390796,361.284915457579,361.784594524362,362.284273591145,
362.783952657928,363.283631724711,363.783310791494,364.282989858277,364.78266892506,
365.282347991843,365.782027058626,366.281706125409,366.781385192192,367.281064258975,
367.780743325758,368.280422392541,368.780101459324,369.279780526107,369.77945959289,
370.279138659673,370.778817726456,371.278496793239,371.778175860022,372.277854926805,
372.777533993588,373.277213060371,373.776892127154,374.276571193937,374.77625026072,
375.275929327503,375.775608394286,376.275287461069,376.774966527852,377.274645594635,
377.774324661418,378.274003728201,378.773682794984,379.273361861767,379.77304092855,
380.272719995333,380.772399062117,381.2720781289,381.771757195683,382.271436262466,
382.771115329249,383.270794396032,383.770473462815,384.270152529598,384.769831596381,
385.269510663164,385.769189729947,386.26886879673,386.768547863513,387.268226930296,
387.767905997079,388.267585063862,388.767264130645,389.266943197428,389.766622264211,
390.266301330994,390.765980397777,391.26565946456,391.765338531343,392.265017598126,
392.764696664909,393.264375731692,393.764054798475,394.263733865258,394.763412932041,
395.263091998824,395.762771065607,396.26245013239,396.762129199173,397.261808265956,
397.761487332739,398.261166399522,398.760845466305,399.260524533088,399.760203599871,
400.259882666654,400.759561733437,401.25924080022,401.758919867003,402.258598933787,
402.75827800057,403.257957067353,403.757636134136,404.257315200919,404.756994267702,
405.256673334485,405.756352401268,406.256031468051,406.755710534834),
 .UNSPECIFIED.);
#272=B_SPLINE_CURVE_WITH_KNOTS('',3,(#14873,#14874,#14875,#14876,#14877,
#14878,#14879,#14880,#14881,#14882,#14883,#14884,#14885,#14886,#14887,#14888,
#14889,#14890,#14891),.UNSPECIFIED.,.F.,.F.,(4,3,3,3,3,3,4),(-3.69871549170445,
-3.49775346748116,-2.99807440069814,-2.49839533391511,-1.99871626713209,
-1.49903720034907,-1.00018350866767),.UNSPECIFIED.);
#273=B_SPLINE_CURVE_WITH_KNOTS('',3,(#14894,#14895,#14896,#14897),
 .UNSPECIFIED.,.F.,.F.,(4,4),(0.,0.443060670554495),.UNSPECIFIED.);
#274=B_SPLINE_CURVE_WITH_KNOTS('',3,(#14902,#14903,#14904,#14905,#14906,
#14907,#14908,#14909,#14910,#14911,#14912,#14913,#14914,#14915,#14916,#14917,
#14918,#14919,#14920,#14921,#14922,#14923,#14924,#14925,#14926,#14927,#14928,
#14929,#14930,#14931,#14932,#14933,#14934,#14935,#14936,#14937,#14938,#14939,
#14940,#14941),.UNSPECIFIED.,.F.,.F.,(4,3,3,3,3,3,3,3,3,3,3,3,3,4),(-9.98190079888403,
-9.49390226887744,-8.99422320209442,-8.4945441353114,-7.99486506852837,
-7.49518600174535,-6.99550693496233,-6.4958278681793,-5.99614880139628,
-5.49646973461325,-4.99679066783023,-4.49711160104721,-3.99743253426419,
-3.69871549170445),.UNSPECIFIED.);
#275=B_SPLINE_CURVE_WITH_KNOTS('',3,(#14942,#14943,#14944,#14945,#14946,
#14947,#14948,#14949,#14950,#14951,#14952,#14953,#14954,#14955,#14956,#14957,
#14958,#14959,#14960,#14961,#14962,#14963,#14964,#14965,#14966,#14967,#14968,
#14969,#14970,#14971,#14972,#14973,#14974,#14975,#14976,#14977,#14978,#14979,
#14980,#14981,#14982,#14983,#14984),.UNSPECIFIED.,.F.,.F.,(4,3,3,3,3,3,
3,3,3,3,3,3,3,3,4),(0.443060670554495,0.49967906678306,0.999358133566079,
1.4990372003491,1.99871626713212,2.49839533391514,2.99807440069816,3.49775346748117,
3.99743253426419,4.49711160104721,4.99679066783023,5.49646973461325,5.99614880139627,
6.49582786817929,6.72624597773408),.UNSPECIFIED.);
#276=B_SPLINE_CURVE_WITH_KNOTS('',3,(#14989,#14990,#14991,#14992,#14993,
#14994,#14995,#14996,#14997,#14998,#14999,#15000,#15001,#15002,#15003,#15004,
#15005,#15006,#15007,#15008,#15009,#15010,#15011,#15012,#15013,#15014,#15015,
#15016,#15017,#15018,#15019,#15020,#15021,#15022,#15023,#15024,#15025,#15026,
#15027,#15028,#15029,#15030,#15031),.UNSPECIFIED.,.F.,.F.,(4,3,3,3,3,3,
3,3,3,3,3,3,3,3,4),(-16.2650861060636,-15.9897301370567,-15.4900510702737,
-14.9903720034907,-14.4906929367077,-13.9910138699247,-13.4913348031416,
-12.9916557363586,-12.4919766695756,-11.9922976027926,-11.4926185360095,
-10.9929394692265,-10.4932604024435,-9.99358133566046,-9.98190079888403),
 .UNSPECIFIED.);
#277=B_SPLINE_CURVE_WITH_KNOTS('',3,(#15032,#15033,#15034,#15035,#15036,
#15037,#15038,#15039,#15040,#15041,#15042,#15043,#15044,#15045,#15046,#15047,
#15048,#15049,#15050,#15051,#15052,#15053,#15054,#15055,#15056,#15057,#15058,
#15059,#15060,#15061,#15062,#15063,#15064,#15065,#15066,#15067,#15068,#15069,
#15070,#15071,#15072,#15073,#15074),.UNSPECIFIED.,.F.,.F.,(4,3,3,3,3,3,
3,3,3,3,3,3,3,3,4),(6.72624597773408,6.99550693496231,7.49518600174534,
7.99486506852837,8.49454413531139,8.99422320209442,9.49390226887745,9.99358133566048,
10.4932604024435,10.9929394692265,11.4926185360096,11.9922976027926,12.4919766695756,
12.9916557363586,13.0094312849137),.UNSPECIFIED.);
#278=B_SPLINE_CURVE_WITH_KNOTS('',3,(#15079,#15080,#15081,#15082,#15083,
#15084,#15085,#15086,#15087,#15088,#15089,#15090,#15091,#15092,#15093,#15094,
#15095,#15096,#15097,#15098,#15099,#15100,#15101,#15102,#15103,#15104,#15105,
#15106,#15107,#15108,#15109,#15110,#15111,#15112,#15113,#15114,#15115,#15116,
#15117,#15118,#15119,#15120,#15121),.UNSPECIFIED.,.F.,.F.,(4,3,3,3,3,3,
3,3,3,3,3,3,3,3,4),(-22.5482714132432,-22.485558005236,-21.985878938453,
-21.48619987167,-20.986520804887,-20.486841738104,-19.9871626713209,-19.4874836045379,
-18.9878045377549,-18.4881254709719,-17.9884464041888,-17.4887673374058,
-16.9890882706228,-16.4894092038398,-16.2650861060636),.UNSPECIFIED.);
#279=B_SPLINE_CURVE_WITH_KNOTS('',3,(#15122,#15123,#15124,#15125,#15126,
#15127,#15128,#15129,#15130,#15131,#15132,#15133,#15134,#15135,#15136,#15137,
#15138,#15139,#15140,#15141,#15142,#15143,#15144,#15145,#15146,#15147,#15148,
#15149,#15150,#15151,#15152,#15153,#15154,#15155,#15156,#15157,#15158,#15159,
#15160,#15161),.UNSPECIFIED.,.F.,.F.,(4,3,3,3,3,3,3,3,3,3,3,3,3,4),(13.0094312849137,
13.4913348031417,13.9910138699247,14.4906929367077,14.9903720034907,15.4900510702737,
15.9897301370568,16.4894092038398,16.9890882706228,17.4887673374058,17.9884464041888,
18.4881254709718,18.9878045377549,19.2926165920933),.UNSPECIFIED.);
#280=B_SPLINE_CURVE_WITH_KNOTS('',3,(#15166,#15167,#15168,#15169,#15170,
#15171,#15172,#15173,#15174,#15175,#15176,#15177,#15178,#15179,#15180,#15181,
#15182,#15183,#15184,#15185,#15186,#15187,#15188,#15189,#15190,#15191,#15192,
#15193,#15194,#15195,#15196,#15197,#15198,#15199,#15200,#15201,#15202,#15203,
#15204,#15205),.UNSPECIFIED.,.F.,.F.,(4,3,3,3,3,3,3,3,3,3,3,3,3,4),(-28.8314567204228,
-28.4817068066323,-27.9820277398493,-27.4823486730663,-26.9826696062833,
-26.4829905395002,-25.9833114727172,-25.4836324059342,-24.9839533391512,
-24.4842742723681,-23.9845952055851,-23.4849161388021,-22.9852370720191,
-22.5482714132432),.UNSPECIFIED.);
#281=B_SPLINE_CURVE_WITH_KNOTS('',3,(#15206,#15207,#15208,#15209,#15210,
#15211,#15212,#15213,#15214,#15215,#15216,#15217,#15218,#15219,#15220,#15221,
#15222,#15223,#15224,#15225,#15226,#15227,#15228,#15229,#15230,#15231,#15232,
#15233,#15234,#15235,#15236,#15237,#15238,#15239,#15240,#15241,#15242,#15243,
#15244,#15245,#15246,#15247,#15248),.UNSPECIFIED.,.F.,.F.,(4,3,3,3,3,3,
3,3,3,3,3,3,3,3,4),(19.2926165920933,19.4874836045379,19.9871626713209,
20.4868417381039,20.986520804887,21.48619987167,21.985878938453,22.4855580052361,
22.9852370720191,23.4849161388021,23.9845952055851,24.4842742723682,24.9839533391512,
25.4836324059342,25.5758018992728),.UNSPECIFIED.);
#282=B_SPLINE_CURVE_WITH_KNOTS('',3,(#15253,#15254,#15255,#15256,#15257,
#15258,#15259,#15260,#15261,#15262,#15263,#15264,#15265,#15266,#15267,#15268,
#15269,#15270,#15271,#15272,#15273,#15274,#15275,#15276,#15277,#15278,#15279,
#15280,#15281,#15282,#15283,#15284,#15285,#15286,#15287,#15288,#15289,#15290,
#15291,#15292,#15293,#15294,#15295),.UNSPECIFIED.,.F.,.F.,(4,3,3,3,3,3,
3,3,3,3,3,3,3,3,4),(-35.1146420276024,-34.9775346748116,-34.4778556080286,
-33.9781765412456,-33.4784974744626,-32.9788184076795,-32.4791393408965,
-31.9794602741135,-31.4797812073305,-30.9801021405474,-30.4804230737644,
-29.9807440069814,-29.4810649401984,-28.9813858734153,-28.8314567204228),
 .UNSPECIFIED.);
#283=B_SPLINE_CURVE_WITH_KNOTS('',3,(#15296,#15297,#15298,#15299,#15300,
#15301,#15302,#15303,#15304,#15305,#15306,#15307,#15308,#15309,#15310,#15311,
#15312,#15313,#15314,#15315,#15316,#15317,#15318,#15319,#15320,#15321,#15322,
#15323,#15324,#15325,#15326,#15327,#15328,#15329,#15330,#15331,#15332,#15333,
#15334,#15335),.UNSPECIFIED.,.F.,.F.,(4,3,3,3,3,3,3,3,3,3,3,3,3,4),(25.5758018992728,
25.9833114727172,26.4829905395003,26.9826696062833,27.4823486730663,27.9820277398493,
28.4817068066324,28.9813858734154,29.4810649401984,29.9807440069814,30.4804230737645,
30.9801021405475,31.4797812073305,31.8589872064524),.UNSPECIFIED.);
#284=B_SPLINE_CURVE_WITH_KNOTS('',3,(#15340,#15341,#15342,#15343,#15344,
#15345,#15346,#15347,#15348,#15349,#15350,#15351,#15352,#15353,#15354,#15355,
#15356,#15357,#15358,#15359,#15360,#15361,#15362,#15363,#15364,#15365,#15366,
#15367,#15368,#15369,#15370,#15371,#15372,#15373,#15374,#15375,#15376,#15377,
#15378,#15379),.UNSPECIFIED.,.F.,.F.,(4,3,3,3,3,3,3,3,3,3,3,3,3,4),(-41.397827334782,
-40.9736834762079,-40.4740044094249,-39.9743253426419,-39.4746462758588,
-38.9749672090758,-38.4752881422928,-37.9756090755098,-37.4759300087267,
-36.9762509419437,-36.4765718751607,-35.9768928083777,-35.4772137415947,
-35.1146420276024),.UNSPECIFIED.);
#285=B_SPLINE_CURVE_WITH_KNOTS('',3,(#15380,#15381,#15382,#15383,#15384,
#15385,#15386,#15387,#15388,#15389,#15390,#15391,#15392,#15393,#15394,#15395,
#15396,#15397,#15398,#15399,#15400,#15401,#15402,#15403,#15404,#15405,#15406,
#15407,#15408,#15409,#15410,#15411,#15412,#15413,#15414,#15415,#15416,#15417,
#15418,#15419,#15420,#15421,#15422),.UNSPECIFIED.,.F.,.F.,(4,3,3,3,3,3,
3,3,3,3,3,3,3,3,4),(31.8589872064524,31.9794602741135,32.4791393408966,
32.9788184076796,33.4784974744626,33.9781765412456,34.4778556080286,34.9775346748117,
35.4772137415947,35.9768928083777,36.4765718751607,36.9762509419437,37.4759300087267,
37.9756090755098,38.142172513632),.UNSPECIFIED.);
#286=B_SPLINE_CURVE_WITH_KNOTS('',3,(#15427,#15428,#15429,#15430,#15431,
#15432,#15433,#15434,#15435,#15436,#15437,#15438,#15439,#15440,#15441,#15442,
#15443,#15444,#15445,#15446,#15447,#15448,#15449,#15450,#15451,#15452,#15453,
#15454,#15455,#15456,#15457,#15458,#15459,#15460,#15461,#15462,#15463,#15464,
#15465,#15466,#15467,#15468,#15469),.UNSPECIFIED.,.F.,.F.,(4,3,3,3,3,3,
3,3,3,3,3,3,3,3,4),(-47.6810126419616,-47.4695113443872,-46.9698322776042,
-46.4701532108212,-45.9704741440381,-45.4707950772551,-44.9711160104721,
-44.4714369436891,-43.971757876906,-43.472078810123,-42.97239974334,-42.472720676557,
-41.973041609774,-41.4733625429909,-41.397827334782),.UNSPECIFIED.);
#287=B_SPLINE_CURVE_WITH_KNOTS('',3,(#15470,#15471,#15472,#15473,#15474,
#15475,#15476,#15477,#15478,#15479,#15480,#15481,#15482,#15483,#15484,#15485,
#15486,#15487,#15488,#15489,#15490,#15491,#15492,#15493,#15494,#15495,#15496,
#15497,#15498,#15499,#15500,#15501,#15502,#15503,#15504,#15505,#15506,#15507,
#15508,#15509),.UNSPECIFIED.,.F.,.F.,(4,3,3,3,3,3,3,3,3,3,3,3,3,4),(38.142172513632,
38.4752881422928,38.9749672090758,39.4746462758589,39.9743253426419,40.4740044094249,
40.973683476208,41.473362542991,41.973041609774,42.472720676557,42.9723997433401,
43.4720788101231,43.9717578769061,44.4253578208116),.UNSPECIFIED.);
#288=B_SPLINE_CURVE_WITH_KNOTS('',3,(#15514,#15515,#15516,#15517,#15518,
#15519,#15520,#15521,#15522,#15523,#15524,#15525,#15526,#15527,#15528,#15529,
#15530,#15531,#15532,#15533,#15534,#15535,#15536,#15537,#15538,#15539,#15540,
#15541),.UNSPECIFIED.,.F.,.F.,(4,3,3,3,3,3,3,3,3,4),(-53.9641979491412,
-52.9659810790005,-51.9666229454344,-50.9672648118684,-49.9679066783023,
-49.4682276115193,-48.9685485447363,-48.4688694779533,-47.9691904111702,
-47.6810126419616),.UNSPECIFIED.);
#289=B_SPLINE_CURVE_WITH_KNOTS('',3,(#15542,#15543,#15544,#15545,#15546,
#15547,#15548,#15549,#15550,#15551,#15552,#15553,#15554,#15555,#15556,#15557,
#15558,#15559,#15560,#15561,#15562,#15563,#15564,#15565,#15566,#15567,#15568,
#15569,#15570,#15571,#15572,#15573,#15574,#15575,#15576,#15577,#15578,#15579,
#15580,#15581),.UNSPECIFIED.,.F.,.F.,(4,3,3,3,3,3,3,3,3,3,3,3,3,4),(44.4253578208116,
44.4714369436892,44.9711160104722,45.4707950772552,45.9704741440382,46.4701532108212,
46.9698322776042,47.4695113443873,47.9691904111703,48.4688694779533,48.9685485447363,
49.4682276115193,49.9679066783024,50.7085431279912),.UNSPECIFIED.);
#290=B_SPLINE_CURVE_WITH_KNOTS('',3,(#15586,#15587,#15588,#15589,#15590,
#15591,#15592,#15593,#15594,#15595,#15596,#15597,#15598,#15599,#15600,#15601,
#15602,#15603,#15604,#15605,#15606,#15607),.UNSPECIFIED.,.F.,.F.,(4,3,3,
3,3,3,3,4),(-60.2473832563207,-59.9614880139628,-58.9621298803968,-57.9627717468307,
-56.9634136132647,-55.9640554796986,-54.9646973461326,-53.9641979491412),
 .UNSPECIFIED.);
#291=B_SPLINE_CURVE_WITH_KNOTS('',3,(#15608,#15609,#15610,#15611,#15612,
#15613,#15614,#15615,#15616,#15617,#15618,#15619,#15620,#15621,#15622,#15623,
#15624,#15625,#15626,#15627,#15628,#15629,#15630,#15631,#15632),
 .UNSPECIFIED.,.F.,.F.,(4,3,3,3,3,3,3,3,4),(50.7085431279912,50.9672648118684,
51.9666229454345,52.9659810790005,53.9653392125666,54.9646973461326,55.9640554796987,
56.9634136132647,56.9917284351708),.UNSPECIFIED.);
#292=B_SPLINE_CURVE_WITH_KNOTS('',3,(#15637,#15638,#15639,#15640,#15641,
#15642,#15643,#15644,#15645,#15646,#15647,#15648,#15649,#15650,#15651,#15652,
#15653,#15654,#15655,#15656,#15657,#15658),.UNSPECIFIED.,.F.,.F.,(4,3,3,
3,3,3,3,4),(-66.5305685635003,-65.9576368153591,-64.958278681793,-63.958920548227,
-62.9595624146609,-61.9602042810949,-60.9608461475288,-60.2473832563207),
 .UNSPECIFIED.);
#293=B_SPLINE_CURVE_WITH_KNOTS('',3,(#15659,#15660,#15661,#15662,#15663,
#15664,#15665,#15666,#15667,#15668,#15669,#15670,#15671,#15672,#15673,#15674,
#15675,#15676,#15677,#15678,#15679,#15680),.UNSPECIFIED.,.F.,.F.,(4,3,3,
3,3,3,3,4),(56.9917284351708,57.9627717468308,58.9621298803968,59.9614880139629,
60.9608461475289,61.960204281095,62.959562414661,63.2749137423504),
 .UNSPECIFIED.);
#294=B_SPLINE_CURVE_WITH_KNOTS('',3,(#15685,#15686,#15687,#15688,#15689,
#15690,#15691,#15692,#15693,#15694,#15695,#15696,#15697,#15698,#15699,#15700,
#15701,#15702,#15703,#15704,#15705,#15706),.UNSPECIFIED.,.F.,.F.,(4,3,3,
3,3,3,3,4),(-72.8137538706799,-71.9537856167554,-70.9544274831893,-69.9550693496233,
-68.9557112160572,-67.9563530824912,-66.9569949489251,-66.5305685635003),
 .UNSPECIFIED.);
#295=B_SPLINE_CURVE_WITH_KNOTS('',3,(#15707,#15708,#15709,#15710,#15711,
#15712,#15713,#15714,#15715,#15716,#15717,#15718,#15719,#15720,#15721,#15722,
#15723,#15724,#15725,#15726,#15727,#15728),.UNSPECIFIED.,.F.,.F.,(4,3,3,
3,3,3,3,4),(63.2749137423504,63.958920548227,64.9582786817931,65.9576368153591,
66.9569949489252,67.9563530824912,68.9557112160573,69.55809904953),
 .UNSPECIFIED.);
#296=B_SPLINE_CURVE_WITH_KNOTS('',3,(#15733,#15734,#15735,#15736,#15737,
#15738,#15739,#15740,#15741,#15742,#15743,#15744,#15745,#15746,#15747,#15748,
#15749,#15750,#15751,#15752,#15753,#15754,#15755,#15756,#15757),
 .UNSPECIFIED.,.F.,.F.,(4,3,3,3,3,3,3,3,4),(-79.0969391778595,-78.9492925517177,
-77.9499344181516,-76.9505762845856,-75.9512181510195,-74.9518600174535,
-73.9525018838875,-72.9531437503214,-72.8137538706799),.UNSPECIFIED.);
#297=B_SPLINE_CURVE_WITH_KNOTS('',3,(#15758,#15759,#15760,#15761,#15762,
#15763,#15764,#15765,#15766,#15767,#15768,#15769,#15770,#15771,#15772,#15773,
#15774,#15775,#15776,#15777,#15778,#15779),.UNSPECIFIED.,.F.,.F.,(4,3,3,
3,3,3,3,4),(69.55809904953,69.9550693496233,70.9544274831893,71.9537856167554,
72.9531437503215,73.9525018838875,74.9518600174536,75.8412843567096),
 .UNSPECIFIED.);
#298=B_SPLINE_CURVE_WITH_KNOTS('',3,(#15784,#15785,#15786,#15787,#15788,
#15789,#15790,#15791,#15792,#15793,#15794,#15795,#15796,#15797,#15798,#15799,
#15800,#15801,#15802,#15803,#15804,#15805),.UNSPECIFIED.,.F.,.F.,(4,3,3,
3,3,3,3,4),(-85.3801244850391,-84.945441353114,-83.9460832195479,-82.9467250859819,
-81.9473669524158,-80.9480088188498,-79.9486506852837,-79.0969391778595),
 .UNSPECIFIED.);
#299=B_SPLINE_CURVE_WITH_KNOTS('',3,(#15806,#15807,#15808,#15809,#15810,
#15811,#15812,#15813,#15814,#15815,#15816,#15817,#15818,#15819,#15820,#15821,
#15822,#15823,#15824,#15825,#15826,#15827,#15828,#15829,#15830),
 .UNSPECIFIED.,.F.,.F.,(4,3,3,3,3,3,3,3,4),(75.8412843567096,75.9512181510196,
76.9505762845857,77.9499344181517,78.9492925517178,79.9486506852838,80.9480088188499,
81.9473669524159,82.1244696638892),.UNSPECIFIED.);
#300=B_SPLINE_CURVE_WITH_KNOTS('',3,(#15835,#15836,#15837,#15838,#15839,
#15840,#15841,#15842,#15843,#15844,#15845,#15846,#15847,#15848,#15849,#15850,
#15851,#15852,#15853,#15854,#15855,#15856),.UNSPECIFIED.,.F.,.F.,(4,3,3,
3,3,3,3,4),(-91.6633097922187,-90.9415901545102,-89.9422320209442,-88.9428738873782,
-87.9435157538121,-86.944157620246,-85.94479948668,-85.3801244850391),
 .UNSPECIFIED.);
#301=B_SPLINE_CURVE_WITH_KNOTS('',3,(#15857,#15858,#15859,#15860,#15861,
#15862,#15863,#15864,#15865,#15866,#15867,#15868,#15869,#15870,#15871,#15872,
#15873,#15874,#15875,#15876,#15877,#15878),.UNSPECIFIED.,.F.,.F.,(4,3,3,
3,3,3,3,4),(82.1244696638892,82.946725085982,83.946083219548,84.9454413531141,
85.9447994866801,86.9441576202461,87.9435157538122,88.4076549710687),
 .UNSPECIFIED.);
#302=B_SPLINE_CURVE_WITH_KNOTS('',3,(#15883,#15884,#15885,#15886,#15887,
#15888,#15889,#15890,#15891,#15892,#15893,#15894,#15895,#15896,#15897,#15898,
#15899,#15900,#15901,#15902,#15903,#15904,#15905,#15906,#15907),
 .UNSPECIFIED.,.F.,.F.,(4,3,3,3,3,3,3,3,4),(-97.9464950993983,-97.9370970894726,
-96.9377389559065,-95.9383808223405,-94.9390226887744,-93.9396645552084,
-92.9403064216423,-91.9409482880763,-91.6633097922187),.UNSPECIFIED.);
#303=B_SPLINE_CURVE_WITH_KNOTS('',3,(#15908,#15909,#15910,#15911,#15912,
#15913,#15914,#15915,#15916,#15917,#15918,#15919,#15920,#15921,#15922,#15923,
#15924,#15925,#15926,#15927,#15928,#15929),.UNSPECIFIED.,.F.,.F.,(4,3,3,
3,3,3,3,4),(88.4076549710687,88.9428738873782,89.9422320209442,90.9415901545103,
91.9409482880763,92.9403064216424,93.9396645552084,94.6908402782483),
 .UNSPECIFIED.);
#304=B_SPLINE_CURVE_WITH_KNOTS('',3,(#15934,#15935,#15936,#15937,#15938,
#15939,#15940,#15941,#15942,#15943,#15944,#15945,#15946,#15947,#15948,#15949,
#15950,#15951,#15952,#15953,#15954,#15955),.UNSPECIFIED.,.F.,.F.,(4,3,3,
3,3,3,3,4),(-104.229680406578,-103.933245890869,-102.933887757303,-101.934529623737,
-100.935171490171,-99.9358133566047,-98.9364552230386,-97.9464950993983),
 .UNSPECIFIED.);
#305=B_SPLINE_CURVE_WITH_KNOTS('',3,(#15956,#15957,#15958,#15959,#15960,
#15961,#15962,#15963,#15964,#15965,#15966,#15967,#15968,#15969,#15970,#15971,
#15972,#15973,#15974,#15975,#15976,#15977,#15978,#15979,#15980),
 .UNSPECIFIED.,.F.,.F.,(4,3,3,3,3,3,3,3,4),(94.6908402782483,94.9390226887745,
95.9383808223405,96.9377389559065,97.9370970894726,98.9364552230386,99.9358133566047,
100.935171490171,100.974025585428),.UNSPECIFIED.);
#306=B_SPLINE_CURVE_WITH_KNOTS('',3,(#15985,#15986,#15987,#15988,#15989,
#15990,#15991,#15992,#15993,#15994,#15995,#15996,#15997,#15998,#15999,#16000,
#16001,#16002,#16003,#16004,#16005,#16006),.UNSPECIFIED.,.F.,.F.,(4,3,3,
3,3,3,3,4),(-110.512865713757,-109.929394692265,-108.930036558699,-107.930678425133,
-106.931320291567,-105.931962158001,-104.932604024435,-104.229680406578),
 .UNSPECIFIED.);
#307=B_SPLINE_CURVE_WITH_KNOTS('',3,(#16007,#16008,#16009,#16010,#16011,
#16012,#16013,#16014,#16015,#16016,#16017,#16018,#16019,#16020,#16021,#16022,
#16023,#16024,#16025,#16026,#16027,#16028),.UNSPECIFIED.,.F.,.F.,(4,3,3,
3,3,3,3,4),(100.974025585428,101.934529623737,102.933887757303,103.933245890869,
104.932604024435,105.931962158001,106.931320291567,107.257210892608),
 .UNSPECIFIED.);
#308=B_SPLINE_CURVE_WITH_KNOTS('',3,(#16033,#16034,#16035,#16036,#16037,
#16038,#16039,#16040,#16041,#16042,#16043,#16044,#16045,#16046,#16047,#16048,
#16049,#16050,#16051,#16052,#16053,#16054),.UNSPECIFIED.,.F.,.F.,(4,3,3,
3,3,3,3,4),(-116.796051020937,-115.925543493661,-114.926185360095,-113.926827226529,
-112.927469092963,-111.928110959397,-110.928752825831,-110.512865713757),
 .UNSPECIFIED.);
#309=B_SPLINE_CURVE_WITH_KNOTS('',3,(#16055,#16056,#16057,#16058,#16059,
#16060,#16061,#16062,#16063,#16064,#16065,#16066,#16067,#16068,#16069,#16070,
#16071,#16072,#16073,#16074,#16075,#16076),.UNSPECIFIED.,.F.,.F.,(4,3,3,
3,3,3,3,4),(107.257210892608,107.930678425133,108.930036558699,109.929394692265,
110.928752825831,111.928110959397,112.927469092963,113.540396199787),
 .UNSPECIFIED.);
#310=B_SPLINE_CURVE_WITH_KNOTS('',3,(#16081,#16082,#16083,#16084,#16085,
#16086,#16087,#16088,#16089,#16090,#16091,#16092,#16093,#16094,#16095,#16096,
#16097,#16098,#16099,#16100,#16101,#16102,#16103,#16104,#16105),
 .UNSPECIFIED.,.F.,.F.,(4,3,3,3,3,3,3,3,4),(-123.079236328117,-122.921050428624,
-121.921692295058,-120.922334161492,-119.922976027926,-118.92361789436,
-117.924259760793,-116.924901627227,-116.796051020937),.UNSPECIFIED.);
#311=B_SPLINE_CURVE_WITH_KNOTS('',3,(#16106,#16107,#16108,#16109,#16110,
#16111,#16112,#16113,#16114,#16115,#16116,#16117,#16118,#16119,#16120,#16121,
#16122,#16123,#16124,#16125,#16126,#16127),.UNSPECIFIED.,.F.,.F.,(4,3,3,
3,3,3,3,4),(113.540396199787,113.926827226529,114.926185360095,115.925543493661,
116.924901627228,117.924259760794,118.92361789436,119.823581506967),
 .UNSPECIFIED.);
#312=B_SPLINE_CURVE_WITH_KNOTS('',3,(#16132,#16133,#16134,#16135,#16136,
#16137,#16138,#16139,#16140,#16141,#16142,#16143,#16144,#16145,#16146,#16147,
#16148,#16149,#16150,#16151,#16152,#16153),.UNSPECIFIED.,.F.,.F.,(4,3,3,
3,3,3,3,4),(-129.362421635296,-128.91719923002,-127.917841096454,-126.918482962888,
-125.919124829322,-124.919766695756,-123.92040856219,-123.079236328117),
 .UNSPECIFIED.);
#313=B_SPLINE_CURVE_WITH_KNOTS('',3,(#16154,#16155,#16156,#16157,#16158,
#16159,#16160,#16161,#16162,#16163,#16164,#16165,#16166,#16167,#16168,#16169,
#16170,#16171,#16172,#16173,#16174,#16175,#16176,#16177,#16178),
 .UNSPECIFIED.,.F.,.F.,(4,3,3,3,3,3,3,3,4),(119.823581506967,119.922976027926,
120.922334161492,121.921692295058,122.921050428624,123.92040856219,124.919766695756,
125.919124829322,126.106766814146),.UNSPECIFIED.);
#314=B_SPLINE_CURVE_WITH_KNOTS('',3,(#16183,#16184,#16185,#16186,#16187,
#16188,#16189,#16190,#16191,#16192,#16193,#16194,#16195,#16196,#16197,#16198,
#16199,#16200,#16201,#16202,#16203,#16204),.UNSPECIFIED.,.F.,.F.,(4,3,3,
3,3,3,3,4),(-135.645606942476,-134.913348031416,-133.91398989785,-132.914631764284,
-131.915273630718,-130.915915497152,-129.916557363586,-129.362421635296),
 .UNSPECIFIED.);
#315=B_SPLINE_CURVE_WITH_KNOTS('',3,(#16205,#16206,#16207,#16208,#16209,
#16210,#16211,#16212,#16213,#16214,#16215,#16216,#16217,#16218,#16219,#16220,
#16221,#16222,#16223,#16224,#16225,#16226),.UNSPECIFIED.,.F.,.F.,(4,3,3,
3,3,3,3,4),(126.106766814146,126.918482962888,127.917841096454,128.91719923002,
129.916557363586,130.915915497152,131.915273630718,132.389952121326),
 .UNSPECIFIED.);
#316=B_SPLINE_CURVE_WITH_KNOTS('',3,(#16231,#16232,#16233,#16234,#16235,
#16236,#16237,#16238,#16239,#16240,#16241,#16242,#16243,#16244,#16245,#16246,
#16247,#16248,#16249,#16250,#16251,#16252,#16253,#16254,#16255),
 .UNSPECIFIED.,.F.,.F.,(4,3,3,3,3,3,3,3,4),(-141.928792249655,-141.908854966379,
-140.909496832813,-139.910138699247,-138.91078056568,-137.911422432114,
-136.912064298548,-135.912706164982,-135.645606942476),.UNSPECIFIED.);
#317=B_SPLINE_CURVE_WITH_KNOTS('',3,(#16256,#16257,#16258,#16259,#16260,
#16261,#16262,#16263,#16264,#16265,#16266,#16267,#16268,#16269,#16270,#16271,
#16272,#16273,#16274,#16275,#16276,#16277),.UNSPECIFIED.,.F.,.F.,(4,3,3,
3,3,3,3,4),(132.389952121326,132.914631764284,133.91398989785,134.913348031416,
135.912706164982,136.912064298549,137.911422432115,138.673137428505),
 .UNSPECIFIED.);
#318=B_SPLINE_CURVE_WITH_KNOTS('',3,(#16282,#16283,#16284,#16285,#16286,
#16287,#16288,#16289,#16290,#16291,#16292,#16293,#16294,#16295,#16296,#16297,
#16298,#16299,#16300,#16301,#16302,#16303),.UNSPECIFIED.,.F.,.F.,(4,3,3,
3,3,3,3,4),(-148.211977556835,-147.905003767775,-146.905645634209,-145.906287500643,
-144.906929367077,-143.907571233511,-142.908213099945,-141.928792249655),
 .UNSPECIFIED.);
#319=B_SPLINE_CURVE_WITH_KNOTS('',3,(#16304,#16305,#16306,#16307,#16308,
#16309,#16310,#16311,#16312,#16313,#16314,#16315,#16316,#16317,#16318,#16319,
#16320,#16321,#16322,#16323,#16324,#16325,#16326,#16327,#16328),
 .UNSPECIFIED.,.F.,.F.,(4,3,3,3,3,3,3,3,4),(138.673137428505,138.910780565681,
139.910138699247,140.909496832813,141.908854966379,142.908213099945,143.907571233511,
144.906929367077,144.956322735685),.UNSPECIFIED.);
#320=B_SPLINE_CURVE_WITH_KNOTS('',3,(#16333,#16334,#16335,#16336,#16337,
#16338,#16339,#16340,#16341,#16342,#16343,#16344,#16345,#16346,#16347,#16348,
#16349,#16350,#16351,#16352,#16353,#16354),.UNSPECIFIED.,.F.,.F.,(4,3,3,
3,3,3,3,4),(-154.495162864015,-153.901152569171,-152.901794435605,-151.902436302039,
-150.903078168473,-149.903720034907,-148.904361901341,-148.211977556835),
 .UNSPECIFIED.);
#321=B_SPLINE_CURVE_WITH_KNOTS('',3,(#16355,#16356,#16357,#16358,#16359,
#16360,#16361,#16362,#16363,#16364,#16365,#16366,#16367,#16368,#16369,#16370,
#16371,#16372,#16373,#16374,#16375,#16376),.UNSPECIFIED.,.F.,.F.,(4,3,3,
3,3,3,3,4),(144.956322735685,145.906287500643,146.905645634209,147.905003767775,
148.904361901341,149.903720034907,150.903078168473,151.239508042865),
 .UNSPECIFIED.);
#322=B_SPLINE_CURVE_WITH_KNOTS('',3,(#16381,#16382,#16383,#16384,#16385,
#16386,#16387,#16388,#16389,#16390,#16391,#16392,#16393,#16394,#16395,#16396,
#16397,#16398,#16399,#16400,#16401,#16402),.UNSPECIFIED.,.F.,.F.,(4,3,3,
3,3,3,3,4),(-160.778348171194,-159.897301370567,-158.897943237001,-157.898585103435,
-156.899226969869,-155.899868836303,-154.900510702737,-154.495162864015),
 .UNSPECIFIED.);
#323=B_SPLINE_CURVE_WITH_KNOTS('',3,(#16403,#16404,#16405,#16406,#16407,
#16408,#16409,#16410,#16411,#16412,#16413,#16414,#16415,#16416,#16417,#16418,
#16419,#16420,#16421,#16422,#16423,#16424),.UNSPECIFIED.,.F.,.F.,(4,3,3,
3,3,3,3,4),(151.239508042865,151.902436302039,152.901794435605,153.901152569171,
154.900510702737,155.899868836303,156.899226969869,157.522693350044),
 .UNSPECIFIED.);
#324=B_SPLINE_CURVE_WITH_KNOTS('',3,(#16429,#16430,#16431,#16432,#16433,
#16434,#16435,#16436,#16437,#16438,#16439,#16440,#16441,#16442,#16443,#16444,
#16445,#16446,#16447,#16448,#16449,#16450,#16451,#16452,#16453),
 .UNSPECIFIED.,.F.,.F.,(4,3,3,3,3,3,3,3,4),(-167.061533478374,-166.89280830553,
-165.893450171964,-164.894092038398,-163.894733904832,-162.895375771266,
-161.8960176377,-160.896659504134,-160.778348171194),.UNSPECIFIED.);
#325=B_SPLINE_CURVE_WITH_KNOTS('',3,(#16454,#16455,#16456,#16457,#16458,
#16459,#16460,#16461,#16462,#16463,#16464,#16465,#16466,#16467,#16468,#16469,
#16470,#16471,#16472,#16473,#16474,#16475),.UNSPECIFIED.,.F.,.F.,(4,3,3,
3,3,3,3,4),(157.522693350044,157.898585103435,158.897943237002,159.897301370568,
160.896659504134,161.8960176377,162.895375771266,163.805878657224),
 .UNSPECIFIED.);
#326=B_SPLINE_CURVE_WITH_KNOTS('',3,(#16480,#16481,#16482,#16483,#16484,
#16485,#16486,#16487,#16488,#16489,#16490,#16491,#16492,#16493,#16494,#16495,
#16496,#16497,#16498,#16499,#16500,#16501),.UNSPECIFIED.,.F.,.F.,(4,3,3,
3,3,3,3,4),(-173.344718785553,-172.888957106926,-171.88959897336,-170.890240839794,
-169.890882706228,-168.891524572662,-167.892166439096,-167.061533478374),
 .UNSPECIFIED.);
#327=B_SPLINE_CURVE_WITH_KNOTS('',3,(#16502,#16503,#16504,#16505,#16506,
#16507,#16508,#16509,#16510,#16511,#16512,#16513,#16514,#16515,#16516,#16517,
#16518,#16519,#16520,#16521,#16522,#16523,#16524,#16525,#16526),
 .UNSPECIFIED.,.F.,.F.,(4,3,3,3,3,3,3,3,4),(163.805878657224,163.894733904832,
164.894092038398,165.893450171964,166.89280830553,167.892166439096,168.891524572662,
169.890882706228,170.089063964403),.UNSPECIFIED.);
#328=B_SPLINE_CURVE_WITH_KNOTS('',3,(#16531,#16532,#16533,#16534,#16535,
#16536,#16537,#16538,#16539,#16540,#16541,#16542,#16543,#16544,#16545,#16546,
#16547,#16548,#16549,#16550,#16551,#16552),.UNSPECIFIED.,.F.,.F.,(4,3,3,
3,3,3,3,4),(-179.627904092733,-178.885105908322,-177.885747774756,-176.88638964119,
-175.887031507624,-174.887673374058,-173.888315240492,-173.344718785553),
 .UNSPECIFIED.);
#329=B_SPLINE_CURVE_WITH_KNOTS('',3,(#16553,#16554,#16555,#16556,#16557,
#16558,#16559,#16560,#16561,#16562,#16563,#16564,#16565,#16566,#16567,#16568,
#16569,#16570,#16571,#16572,#16573,#16574),.UNSPECIFIED.,.F.,.F.,(4,3,3,
3,3,3,3,4),(170.089063964403,170.890240839794,171.88959897336,172.888957106926,
173.888315240492,174.887673374058,175.887031507624,176.372249271583),
 .UNSPECIFIED.);
#330=B_SPLINE_CURVE_WITH_KNOTS('',3,(#16579,#16580,#16581,#16582,#16583,
#16584,#16585,#16586,#16587,#16588,#16589,#16590,#16591,#16592,#16593,#16594,
#16595,#16596,#16597,#16598,#16599,#16600,#16601,#16602,#16603),
 .UNSPECIFIED.,.F.,.F.,(4,3,3,3,3,3,3,3,4),(-185.911089399912,-185.880612843285,
-184.881254709719,-183.881896576153,-182.882538442587,-181.88318030902,
-180.883822175454,-179.884464041888,-179.627904092733),.UNSPECIFIED.);
#331=B_SPLINE_CURVE_WITH_KNOTS('',3,(#16604,#16605,#16606,#16607,#16608,
#16609,#16610,#16611,#16612,#16613,#16614,#16615,#16616,#16617,#16618,#16619,
#16620,#16621,#16622,#16623,#16624,#16625),.UNSPECIFIED.,.F.,.F.,(4,3,3,
3,3,3,3,4),(176.372249271583,176.88638964119,177.885747774756,178.885105908322,
179.884464041889,180.883822175455,181.883180309021,182.655434578762),
 .UNSPECIFIED.);
#332=B_SPLINE_CURVE_WITH_KNOTS('',3,(#16630,#16631,#16632,#16633,#16634,
#16635,#16636,#16637,#16638,#16639,#16640,#16641,#16642,#16643,#16644,#16645,
#16646,#16647,#16648,#16649,#16650,#16651),.UNSPECIFIED.,.F.,.F.,(4,3,3,
3,3,3,3,4),(-192.194274707092,-191.876761644681,-190.877403511115,-189.878045377549,
-188.878687243983,-187.879329110417,-186.879970976851,-185.911089399912),
 .UNSPECIFIED.);
#333=B_SPLINE_CURVE_WITH_KNOTS('',3,(#16652,#16653,#16654,#16655,#16656,
#16657,#16658,#16659,#16660,#16661,#16662,#16663,#16664,#16665,#16666,#16667,
#16668,#16669,#16670,#16671,#16672,#16673,#16674,#16675,#16676),
 .UNSPECIFIED.,.F.,.F.,(4,3,3,3,3,3,3,3,4),(182.655434578762,182.882538442587,
183.881896576153,184.881254709719,185.880612843285,186.879970976851,187.879329110417,
188.878687243983,188.938619885942),.UNSPECIFIED.);
#334=B_SPLINE_CURVE_WITH_KNOTS('',3,(#16681,#16682,#16683,#16684,#16685,
#16686,#16687,#16688,#16689,#16690,#16691,#16692,#16693,#16694,#16695,#16696,
#16697,#16698,#16699,#16700,#16701,#16702),.UNSPECIFIED.,.F.,.F.,(4,3,3,
3,3,3,3,4),(-198.477460014271,-197.872910446077,-196.873552312511,-195.874194178945,
-194.874836045379,-193.875477911813,-192.876119778247,-192.194274707092),
 .UNSPECIFIED.);
#335=B_SPLINE_CURVE_WITH_KNOTS('',3,(#16703,#16704,#16705,#16706,#16707,
#16708,#16709,#16710,#16711,#16712,#16713,#16714,#16715,#16716,#16717,#16718,
#16719,#16720,#16721,#16722,#16723,#16724),.UNSPECIFIED.,.F.,.F.,(4,3,3,
3,3,3,3,4),(188.938619885942,189.878045377549,190.877403511115,191.876761644681,
192.876119778247,193.875477911813,194.874836045379,195.221805193122),
 .UNSPECIFIED.);
#336=B_SPLINE_CURVE_WITH_KNOTS('',3,(#16729,#16730,#16731,#16732,#16733,
#16734,#16735,#16736,#16737,#16738,#16739,#16740,#16741,#16742,#16743,#16744,
#16745,#16746,#16747,#16748,#16749,#16750),.UNSPECIFIED.,.F.,.F.,(4,3,3,
3,3,3,3,4),(-204.760645321451,-203.869059247473,-202.869701113907,-201.870342980341,
-200.870984846775,-199.871626713209,-198.872268579643,-198.477460014271),
 .UNSPECIFIED.);
#337=B_SPLINE_CURVE_WITH_KNOTS('',3,(#16751,#16752,#16753,#16754,#16755,
#16756,#16757,#16758,#16759,#16760,#16761,#16762,#16763,#16764,#16765,#16766,
#16767,#16768,#16769,#16770,#16771,#16772),.UNSPECIFIED.,.F.,.F.,(4,3,3,
3,3,3,3,4),(195.221805193122,195.874194178945,196.873552312511,197.872910446077,
198.872268579643,199.871626713209,200.870984846776,201.504990500301),
 .UNSPECIFIED.);
#338=B_SPLINE_CURVE_WITH_KNOTS('',3,(#16777,#16778,#16779,#16780,#16781,
#16782,#16783,#16784,#16785,#16786,#16787,#16788,#16789,#16790,#16791,#16792,
#16793,#16794,#16795,#16796,#16797,#16798,#16799,#16800,#16801),
 .UNSPECIFIED.,.F.,.F.,(4,3,3,3,3,3,3,3,4),(-211.043830628631,-210.864566182436,
-209.86520804887,-208.865849915304,-207.866491781738,-206.867133648172,
-205.867775514606,-204.86841738104,-204.760645321451),.UNSPECIFIED.);
#339=B_SPLINE_CURVE_WITH_KNOTS('',3,(#16802,#16803,#16804,#16805,#16806,
#16807,#16808,#16809,#16810,#16811,#16812,#16813,#16814,#16815,#16816,#16817,
#16818,#16819,#16820,#16821,#16822,#16823),.UNSPECIFIED.,.F.,.F.,(4,3,3,
3,3,3,3,4),(201.504990500301,201.870342980342,202.869701113908,203.869059247474,
204.86841738104,205.867775514606,206.867133648172,207.788175807481),
 .UNSPECIFIED.);
#340=B_SPLINE_CURVE_WITH_KNOTS('',3,(#16828,#16829,#16830,#16831,#16832,
#16833,#16834,#16835,#16836,#16837,#16838,#16839,#16840,#16841,#16842,#16843,
#16844,#16845,#16846,#16847,#16848,#16849),.UNSPECIFIED.,.F.,.F.,(4,3,3,
3,3,3,3,4),(-217.32701593581,-216.860714983832,-215.861356850266,-214.8619987167,
-213.862640583134,-212.863282449568,-211.863924316002,-211.043830628631),
 .UNSPECIFIED.);
#341=B_SPLINE_CURVE_WITH_KNOTS('',3,(#16850,#16851,#16852,#16853,#16854,
#16855,#16856,#16857,#16858,#16859,#16860,#16861,#16862,#16863,#16864,#16865,
#16866,#16867,#16868,#16869,#16870,#16871,#16872,#16873,#16874),
 .UNSPECIFIED.,.F.,.F.,(4,3,3,3,3,3,3,3,4),(207.788175807481,207.866491781738,
208.865849915304,209.86520804887,210.864566182436,211.863924316002,212.863282449568,
213.862640583134,214.07136111466),.UNSPECIFIED.);
#342=B_SPLINE_CURVE_WITH_KNOTS('',3,(#16879,#16880,#16881,#16882,#16883,
#16884,#16885,#16886,#16887,#16888,#16889,#16890,#16891,#16892,#16893,#16894,
#16895,#16896,#16897,#16898,#16899,#16900),.UNSPECIFIED.,.F.,.F.,(4,3,3,
3,3,3,3,4),(-223.61020124299,-222.856863785228,-221.857505651662,-220.858147518096,
-219.85878938453,-218.859431250964,-217.860073117398,-217.32701593581),
 .UNSPECIFIED.);
#343=B_SPLINE_CURVE_WITH_KNOTS('',3,(#16901,#16902,#16903,#16904,#16905,
#16906,#16907,#16908,#16909,#16910,#16911,#16912,#16913,#16914,#16915,#16916,
#16917,#16918,#16919,#16920,#16921,#16922),.UNSPECIFIED.,.F.,.F.,(4,3,3,
3,3,3,3,4),(214.07136111466,214.8619987167,215.861356850266,216.860714983832,
217.860073117398,218.859431250964,219.85878938453,220.35454642184),
 .UNSPECIFIED.);
#344=B_SPLINE_CURVE_WITH_KNOTS('',3,(#16927,#16928,#16929,#16930,#16931,
#16932,#16933,#16934,#16935,#16936,#16937,#16938,#16939,#16940,#16941,#16942,
#16943,#16944,#16945,#16946,#16947,#16948,#16949,#16950,#16951),
 .UNSPECIFIED.,.F.,.F.,(4,3,3,3,3,3,3,3,4),(-229.893386550169,-229.852370720191,
-228.853012586625,-227.853654453059,-226.854296319493,-225.854938185927,
-224.85558005236,-223.856221918794,-223.61020124299),.UNSPECIFIED.);
#345=B_SPLINE_CURVE_WITH_KNOTS('',3,(#16952,#16953,#16954,#16955,#16956,
#16957,#16958,#16959,#16960,#16961,#16962,#16963,#16964,#16965,#16966,#16967,
#16968,#16969,#16970,#16971,#16972,#16973),.UNSPECIFIED.,.F.,.F.,(4,3,3,
3,3,3,3,4),(220.35454642184,220.858147518096,221.857505651663,222.856863785229,
223.856221918795,224.855580052361,225.854938185927,226.637731729019),
 .UNSPECIFIED.);
#346=B_SPLINE_CURVE_WITH_KNOTS('',3,(#16978,#16979,#16980,#16981,#16982,
#16983,#16984,#16985,#16986,#16987,#16988,#16989,#16990,#16991,#16992,#16993,
#16994,#16995,#16996,#16997,#16998,#16999),.UNSPECIFIED.,.F.,.F.,(4,3,3,
3,3,3,3,4),(-236.176571857349,-235.848519521587,-234.849161388021,-233.849803254455,
-232.850445120889,-231.851086987323,-230.851728853757,-229.893386550169),
 .UNSPECIFIED.);
#347=B_SPLINE_CURVE_WITH_KNOTS('',3,(#17000,#17001,#17002,#17003,#17004,
#17005,#17006,#17007,#17008,#17009,#17010,#17011,#17012,#17013,#17014,#17015,
#17016,#17017,#17018,#17019,#17020,#17021,#17022,#17023,#17024),
 .UNSPECIFIED.,.F.,.F.,(4,3,3,3,3,3,3,3,4),(226.637731729019,226.854296319493,
227.853654453059,228.853012586625,229.852370720191,230.851728853757,231.851086987323,
232.850445120889,232.920917036199),.UNSPECIFIED.);
#348=B_SPLINE_CURVE_WITH_KNOTS('',3,(#17029,#17030,#17031,#17032,#17033,
#17034,#17035,#17036,#17037,#17038,#17039,#17040,#17041,#17042,#17043,#17044,
#17045,#17046,#17047,#17048,#17049,#17050),.UNSPECIFIED.,.F.,.F.,(4,3,3,
3,3,3,3,4),(-242.459757164528,-241.844668322983,-240.845310189417,-239.845952055851,
-238.846593922285,-237.847235788719,-236.847877655153,-236.176571857349),
 .UNSPECIFIED.);
#349=B_SPLINE_CURVE_WITH_KNOTS('',3,(#17051,#17052,#17053,#17054,#17055,
#17056,#17057,#17058,#17059,#17060,#17061,#17062,#17063,#17064,#17065,#17066,
#17067,#17068,#17069,#17070,#17071,#17072),.UNSPECIFIED.,.F.,.F.,(4,3,3,
3,3,3,3,4),(232.920917036199,233.849803254455,234.849161388021,235.848519521587,
236.847877655153,237.847235788719,238.846593922285,239.204102343378),
 .UNSPECIFIED.);
#350=B_SPLINE_CURVE_WITH_KNOTS('',3,(#17077,#17078,#17079,#17080,#17081,
#17082,#17083,#17084,#17085,#17086,#17087,#17088,#17089,#17090,#17091,#17092,
#17093,#17094,#17095,#17096,#17097,#17098),.UNSPECIFIED.,.F.,.F.,(4,3,3,
3,3,3,3,4),(-248.742942471708,-247.84081712438,-246.841458990814,-245.842100857247,
-244.842742723681,-243.843384590115,-242.844026456549,-242.459757164528),
 .UNSPECIFIED.);
#351=B_SPLINE_CURVE_WITH_KNOTS('',3,(#17099,#17100,#17101,#17102,#17103,
#17104,#17105,#17106,#17107,#17108,#17109,#17110,#17111,#17112,#17113,#17114,
#17115,#17116,#17117,#17118,#17119,#17120),.UNSPECIFIED.,.F.,.F.,(4,3,3,
3,3,3,3,4),(239.204102343378,239.845952055851,240.845310189417,241.844668322983,
242.84402645655,243.843384590116,244.842742723682,245.487287650558),
 .UNSPECIFIED.);
#352=B_SPLINE_CURVE_WITH_KNOTS('',3,(#17125,#17126,#17127,#17128,#17129,
#17130,#17131,#17132,#17133,#17134,#17135,#17136,#17137,#17138,#17139,#17140,
#17141,#17142,#17143,#17144,#17145,#17146,#17147,#17148,#17149),
 .UNSPECIFIED.,.F.,.F.,(4,3,3,3,3,3,3,3,4),(-255.026127778888,-254.836324059342,
-253.836965925776,-252.83760779221,-251.838249658644,-250.838891525078,
-249.839533391512,-248.840175257946,-248.742942471708),.UNSPECIFIED.);
#353=B_SPLINE_CURVE_WITH_KNOTS('',3,(#17150,#17151,#17152,#17153,#17154,
#17155,#17156,#17157,#17158,#17159,#17160,#17161,#17162,#17163,#17164,#17165,
#17166,#17167,#17168,#17169,#17170,#17171),.UNSPECIFIED.,.F.,.F.,(4,3,3,
3,3,3,3,4),(245.487287650558,245.842100857248,246.841458990814,247.84081712438,
248.840175257946,249.839533391512,250.838891525078,251.770472957738),
 .UNSPECIFIED.);
#354=B_SPLINE_CURVE_WITH_KNOTS('',3,(#17176,#17177,#17178,#17179,#17180,
#17181,#17182,#17183,#17184,#17185,#17186,#17187,#17188,#17189,#17190,#17191,
#17192,#17193,#17194,#17195,#17196,#17197),.UNSPECIFIED.,.F.,.F.,(4,3,3,
3,3,3,3,4),(-261.309313086067,-260.832472860738,-259.833114727172,-258.833756593606,
-257.83439846004,-256.835040326474,-255.835682192908,-255.026127778888),
 .UNSPECIFIED.);
#355=B_SPLINE_CURVE_WITH_KNOTS('',3,(#17198,#17199,#17200,#17201,#17202,
#17203,#17204,#17205,#17206,#17207,#17208,#17209,#17210,#17211,#17212,#17213,
#17214,#17215,#17216,#17217,#17218,#17219,#17220,#17221,#17222),
 .UNSPECIFIED.,.F.,.F.,(4,3,3,3,3,3,3,3,4),(251.770472957738,251.838249658644,
252.83760779221,253.836965925776,254.836324059342,255.835682192908,256.835040326474,
257.83439846004,258.053658264917),.UNSPECIFIED.);
#356=B_SPLINE_CURVE_WITH_KNOTS('',3,(#17227,#17228,#17229,#17230,#17231,
#17232,#17233,#17234,#17235,#17236,#17237,#17238,#17239,#17240,#17241,#17242,
#17243,#17244,#17245,#17246,#17247,#17248),.UNSPECIFIED.,.F.,.F.,(4,3,3,
3,3,3,3,4),(-267.592498393247,-266.828621662134,-265.829263528568,-264.829905395002,
-263.830547261436,-262.83118912787,-261.831830994304,-261.309313086067),
 .UNSPECIFIED.);
#357=B_SPLINE_CURVE_WITH_KNOTS('',3,(#17249,#17250,#17251,#17252,#17253,
#17254,#17255,#17256,#17257,#17258,#17259,#17260,#17261,#17262,#17263,#17264,
#17265,#17266,#17267,#17268,#17269,#17270),.UNSPECIFIED.,.F.,.F.,(4,3,3,
3,3,3,3,4),(258.053658264917,258.833756593606,259.833114727172,260.832472860738,
261.831830994304,262.83118912787,263.830547261436,264.336843572097),
 .UNSPECIFIED.);
#358=B_SPLINE_CURVE_WITH_KNOTS('',3,(#17275,#17276,#17277,#17278,#17279,
#17280,#17281,#17282,#17283,#17284,#17285,#17286,#17287,#17288,#17289,#17290,
#17291,#17292,#17293,#17294,#17295,#17296,#17297,#17298,#17299),
 .UNSPECIFIED.,.F.,.F.,(4,3,3,3,3,3,3,3,4),(-273.875683700426,-273.824128597097,
-272.824770463531,-271.825412329965,-270.826054196399,-269.826696062833,
-268.827337929266,-267.8279797957,-267.592498393247),.UNSPECIFIED.);
#359=B_SPLINE_CURVE_WITH_KNOTS('',3,(#17300,#17301,#17302,#17303,#17304,
#17305,#17306,#17307,#17308,#17309,#17310,#17311,#17312,#17313,#17314,#17315,
#17316,#17317,#17318,#17319,#17320,#17321),.UNSPECIFIED.,.F.,.F.,(4,3,3,
3,3,3,3,4),(264.336843572097,264.829905395003,265.829263528569,266.828621662135,
267.827979795701,268.827337929267,269.826696062833,270.620028879276),
 .UNSPECIFIED.);
#360=B_SPLINE_CURVE_WITH_KNOTS('',3,(#17326,#17327,#17328,#17329,#17330,
#17331,#17332,#17333,#17334,#17335,#17336,#17337,#17338,#17339,#17340,#17341,
#17342,#17343,#17344,#17345,#17346,#17347),.UNSPECIFIED.,.F.,.F.,(4,3,3,
3,3,3,3,4),(-280.158869007606,-279.820277398493,-278.820919264927,-277.821561131361,
-276.822202997795,-275.822844864229,-274.823486730663,-273.875683700426),
 .UNSPECIFIED.);
#361=B_SPLINE_CURVE_WITH_KNOTS('',3,(#17348,#17349,#17350,#17351,#17352,
#17353,#17354,#17355,#17356,#17357,#17358,#17359,#17360,#17361,#17362,#17363,
#17364,#17365,#17366,#17367,#17368,#17369,#17370,#17371,#17372),
 .UNSPECIFIED.,.F.,.F.,(4,3,3,3,3,3,3,3,4),(270.620028879276,270.826054196399,
271.825412329965,272.824770463531,273.824128597097,274.823486730663,275.822844864229,
276.822202997795,276.903214186456),.UNSPECIFIED.);
#362=B_SPLINE_CURVE_WITH_KNOTS('',3,(#17377,#17378,#17379,#17380,#17381,
#17382,#17383,#17384,#17385,#17386,#17387,#17388,#17389,#17390,#17391,#17392,
#17393,#17394,#17395,#17396,#17397,#17398),.UNSPECIFIED.,.F.,.F.,(4,3,3,
3,3,3,3,4),(-286.442054314785,-285.816426199889,-284.817068066323,-283.817709932757,
-282.818351799191,-281.818993665625,-280.819635532059,-280.158869007606),
 .UNSPECIFIED.);
#363=B_SPLINE_CURVE_WITH_KNOTS('',3,(#17399,#17400,#17401,#17402,#17403,
#17404,#17405,#17406,#17407,#17408,#17409,#17410,#17411,#17412,#17413,#17414,
#17415,#17416,#17417,#17418,#17419,#17420),.UNSPECIFIED.,.F.,.F.,(4,3,3,
3,3,3,3,4),(276.903214186456,277.821561131361,278.820919264927,279.820277398493,
280.819635532059,281.818993665625,282.818351799191,283.186399493635),
 .UNSPECIFIED.);
#364=B_SPLINE_CURVE_WITH_KNOTS('',3,(#17425,#17426,#17427,#17428,#17429,
#17430,#17431,#17432,#17433,#17434,#17435,#17436,#17437,#17438,#17439,#17440,
#17441,#17442,#17443,#17444,#17445,#17446),.UNSPECIFIED.,.F.,.F.,(4,3,3,
3,3,3,3,4),(-292.725239621965,-291.812575001286,-290.81321686772,-289.813858734153,
-288.814500600587,-287.815142467021,-286.815784333455,-286.442054314785),
 .UNSPECIFIED.);
#365=B_SPLINE_CURVE_WITH_KNOTS('',3,(#17447,#17448,#17449,#17450,#17451,
#17452,#17453,#17454,#17455,#17456,#17457,#17458,#17459,#17460,#17461,#17462,
#17463,#17464,#17465,#17466,#17467,#17468),.UNSPECIFIED.,.F.,.F.,(4,3,3,
3,3,3,3,4),(283.186399493635,283.817709932757,284.817068066323,285.81642619989,
286.815784333456,287.815142467022,288.814500600588,289.469584800815),
 .UNSPECIFIED.);
#366=B_SPLINE_CURVE_WITH_KNOTS('',3,(#17473,#17474,#17475,#17476,#17477,
#17478,#17479,#17480,#17481,#17482,#17483,#17484,#17485,#17486,#17487,#17488,
#17489,#17490,#17491,#17492,#17493,#17494,#17495,#17496,#17497),
 .UNSPECIFIED.,.F.,.F.,(4,3,3,3,3,3,3,3,4),(-299.008424929145,-298.808081936248,
-297.808723802682,-296.809365669116,-295.81000753555,-294.810649401984,
-293.811291268418,-292.811933134852,-292.725239621965),.UNSPECIFIED.);
#367=B_SPLINE_CURVE_WITH_KNOTS('',3,(#17498,#17499,#17500,#17501,#17502,
#17503,#17504,#17505,#17506,#17507,#17508,#17509,#17510,#17511,#17512,#17513,
#17514,#17515,#17516,#17517,#17518,#17519),.UNSPECIFIED.,.F.,.F.,(4,3,3,
3,3,3,3,4),(289.469584800815,289.813858734154,290.81321686772,291.812575001286,
292.811933134852,293.811291268418,294.810649401984,295.752770107995),
 .UNSPECIFIED.);
#368=B_SPLINE_CURVE_WITH_KNOTS('',3,(#17524,#17525,#17526,#17527,#17528,
#17529,#17530,#17531,#17532,#17533,#17534,#17535,#17536,#17537,#17538,#17539,
#17540,#17541,#17542,#17543,#17544,#17545),.UNSPECIFIED.,.F.,.F.,(4,3,3,
3,3,3,3,4),(-305.291610236324,-304.804230737644,-303.804872604078,-302.805514470512,
-301.806156336946,-300.80679820338,-299.807440069814,-299.008424929145),
 .UNSPECIFIED.);
#369=B_SPLINE_CURVE_WITH_KNOTS('',3,(#17546,#17547,#17548,#17549,#17550,
#17551,#17552,#17553,#17554,#17555,#17556,#17557,#17558,#17559,#17560,#17561,
#17562,#17563,#17564,#17565,#17566,#17567,#17568,#17569,#17570),
 .UNSPECIFIED.,.F.,.F.,(4,3,3,3,3,3,3,3,4),(295.752770107995,295.81000753555,
296.809365669116,297.808723802682,298.808081936248,299.807440069814,300.80679820338,
301.806156336946,302.035955415174),.UNSPECIFIED.);
#370=B_SPLINE_CURVE_WITH_KNOTS('',3,(#17575,#17576,#17577,#17578,#17579,
#17580,#17581,#17582,#17583,#17584,#17585,#17586,#17587,#17588,#17589,#17590,
#17591,#17592,#17593,#17594,#17595,#17596),.UNSPECIFIED.,.F.,.F.,(4,3,3,
3,3,3,3,4),(-311.574795543504,-310.80037953904,-309.801021405475,-308.801663271908,
-307.802305138342,-306.802947004776,-305.80358887121,-305.291610236324),
 .UNSPECIFIED.);
#371=B_SPLINE_CURVE_WITH_KNOTS('',3,(#17597,#17598,#17599,#17600,#17601,
#17602,#17603,#17604,#17605,#17606,#17607,#17608,#17609,#17610,#17611,#17612,
#17613,#17614,#17615,#17616,#17617,#17618),.UNSPECIFIED.,.F.,.F.,(4,3,3,
3,3,3,3,4),(302.035955415174,302.805514470512,303.804872604078,304.804230737644,
305.80358887121,306.802947004777,307.802305138343,308.319140722354),
 .UNSPECIFIED.);
#372=B_SPLINE_CURVE_WITH_KNOTS('',3,(#17623,#17624,#17625,#17626,#17627,
#17628,#17629,#17630,#17631,#17632,#17633,#17634,#17635,#17636,#17637,#17638,
#17639,#17640,#17641,#17642,#17643,#17644,#17645,#17646,#17647),
 .UNSPECIFIED.,.F.,.F.,(4,3,3,3,3,3,3,3,4),(-317.857980850683,-317.795886474003,
-316.796528340437,-315.797170206871,-314.797812073305,-313.798453939739,
-312.799095806173,-311.799737672607,-311.574795543504),.UNSPECIFIED.);
#373=B_SPLINE_CURVE_WITH_KNOTS('',3,(#17648,#17649,#17650,#17651,#17652,
#17653,#17654,#17655,#17656,#17657,#17658,#17659,#17660,#17661,#17662,#17663,
#17664,#17665,#17666,#17667,#17668,#17669),.UNSPECIFIED.,.F.,.F.,(4,3,3,
3,3,3,3,4),(308.319140722354,308.801663271909,309.801021405475,310.800379539041,
311.799737672607,312.799095806173,313.798453939739,314.602326029533),
 .UNSPECIFIED.);
#374=B_SPLINE_CURVE_WITH_KNOTS('',3,(#17674,#17675,#17676,#17677,#17678,
#17679,#17680,#17681,#17682,#17683,#17684,#17685,#17686,#17687,#17688,#17689,
#17690,#17691,#17692,#17693,#17694,#17695),.UNSPECIFIED.,.F.,.F.,(4,3,3,
3,3,3,3,4),(-324.141166157863,-323.792035275399,-322.792677141833,-321.793319008267,
-320.793960874701,-319.794602741135,-318.795244607569,-317.857980850683),
 .UNSPECIFIED.);
#375=B_SPLINE_CURVE_WITH_KNOTS('',3,(#17696,#17697,#17698,#17699,#17700,
#17701,#17702,#17703,#17704,#17705,#17706,#17707,#17708,#17709,#17710,#17711,
#17712,#17713,#17714,#17715,#17716,#17717,#17718,#17719,#17720),
 .UNSPECIFIED.,.F.,.F.,(4,3,3,3,3,3,3,3,4),(314.602326029533,314.797812073305,
315.797170206871,316.796528340437,317.795886474003,318.795244607569,319.794602741135,
320.793960874701,320.885511336713),.UNSPECIFIED.);
#376=B_SPLINE_CURVE_WITH_KNOTS('',3,(#17725,#17726,#17727,#17728,#17729,
#17730,#17731,#17732,#17733,#17734,#17735,#17736,#17737,#17738,#17739,#17740,
#17741,#17742,#17743,#17744,#17745,#17746),.UNSPECIFIED.,.F.,.F.,(4,3,3,
3,3,3,3,4),(-330.424351465042,-329.788184076795,-328.788825943229,-327.789467809663,
-326.790109676097,-325.790751542531,-324.791393408965,-324.141166157863),
 .UNSPECIFIED.);
#377=B_SPLINE_CURVE_WITH_KNOTS('',3,(#17747,#17748,#17749,#17750,#17751,
#17752,#17753,#17754,#17755,#17756,#17757,#17758,#17759,#17760,#17761,#17762,
#17763,#17764,#17765,#17766,#17767,#17768),.UNSPECIFIED.,.F.,.F.,(4,3,3,
3,3,3,3,4),(320.885511336713,321.793319008267,322.792677141833,323.792035275399,
324.791393408965,325.790751542531,326.790109676097,327.168696643892),
 .UNSPECIFIED.);
#378=B_SPLINE_CURVE_WITH_KNOTS('',3,(#17773,#17774,#17775,#17776,#17777,
#17778,#17779,#17780,#17781,#17782,#17783,#17784,#17785,#17786,#17787,#17788,
#17789,#17790,#17791,#17792,#17793,#17794),.UNSPECIFIED.,.F.,.F.,(4,3,3,
3,3,3,3,4),(-336.707536772222,-335.784332878192,-334.784974744626,-333.78561661106,
-332.786258477494,-331.786900343927,-330.787542210361,-330.424351465042),
 .UNSPECIFIED.);
#379=B_SPLINE_CURVE_WITH_KNOTS('',3,(#17795,#17796,#17797,#17798,#17799,
#17800,#17801,#17802,#17803,#17804,#17805,#17806,#17807,#17808,#17809,#17810,
#17811,#17812,#17813,#17814,#17815,#17816),.UNSPECIFIED.,.F.,.F.,(4,3,3,
3,3,3,3,4),(327.168696643892,327.789467809663,328.78882594323,329.788184076796,
330.787542210362,331.786900343928,332.786258477494,333.451881951072),
 .UNSPECIFIED.);
#380=B_SPLINE_CURVE_WITH_KNOTS('',3,(#17821,#17822,#17823,#17824,#17825,
#17826,#17827,#17828,#17829,#17830,#17831,#17832,#17833,#17834,#17835,#17836,
#17837,#17838,#17839,#17840,#17841,#17842,#17843,#17844,#17845),
 .UNSPECIFIED.,.F.,.F.,(4,3,3,3,3,3,3,3,4),(-342.990722079402,-342.779839813154,
-341.780481679588,-340.781123546022,-339.781765412456,-338.78240727889,
-337.783049145324,-336.783691011758,-336.707536772222),.UNSPECIFIED.);
#381=B_SPLINE_CURVE_WITH_KNOTS('',3,(#17846,#17847,#17848,#17849,#17850,
#17851,#17852,#17853,#17854,#17855,#17856,#17857,#17858,#17859,#17860,#17861,
#17862,#17863,#17864,#17865,#17866,#17867),.UNSPECIFIED.,.F.,.F.,(4,3,3,
3,3,3,3,4),(333.451881951072,333.78561661106,334.784974744626,335.784332878192,
336.783691011758,337.783049145324,338.78240727889,339.735067258252),
 .UNSPECIFIED.);
#382=B_SPLINE_CURVE_WITH_KNOTS('',3,(#17872,#17873,#17874,#17875,#17876,
#17877,#17878,#17879,#17880,#17881,#17882,#17883,#17884,#17885,#17886,#17887,
#17888,#17889,#17890,#17891,#17892,#17893,#17894,#17895,#17896,#17897,#17898,
#17899,#17900,#17901,#17902,#17903,#17904,#17905),.UNSPECIFIED.,.F.,.F.,
(4,3,3,3,3,3,3,3,3,3,3,4),(-349.273907386581,-348.77598861455,-348.276309547767,
-347.776630480984,-347.276951414201,-346.777272347418,-346.277593280635,
-345.777914213852,-345.278235147069,-344.778556080286,-343.77919794672,
-342.990722079402),.UNSPECIFIED.);
#383=B_SPLINE_CURVE_WITH_KNOTS('',3,(#17906,#17907,#17908,#17909,#17910,
#17911,#17912,#17913,#17914,#17915,#17916,#17917,#17918,#17919,#17920,#17921,
#17922,#17923,#17924,#17925,#17926,#17927,#17928,#17929,#17930,#17931,#17932,
#17933),.UNSPECIFIED.,.F.,.F.,(4,3,3,3,3,3,3,3,3,4),(339.735067258252,339.781765412456,
340.781123546022,341.780481679588,342.779839813154,343.77919794672,344.778556080286,
345.278235147069,345.777914213852,346.018252565431),.UNSPECIFIED.);
#384=B_SPLINE_CURVE_WITH_KNOTS('',3,(#17938,#17939,#17940,#17941,#17942,
#17943,#17944,#17945,#17946,#17947,#17948,#17949,#17950,#17951,#17952,#17953,
#17954,#17955,#17956,#17957,#17958,#17959,#17960,#17961,#17962,#17963,#17964,
#17965,#17966,#17967,#17968,#17969,#17970,#17971,#17972,#17973,#17974,#17975,
#17976,#17977,#17978,#17979,#17980),.UNSPECIFIED.,.F.,.F.,(4,3,3,3,3,3,
3,3,3,3,3,3,3,3,4),(-355.557092693761,-355.27181648273,-354.772137415947,
-354.272458349164,-353.77277928238,-353.273100215597,-352.773421148814,
-352.273742082031,-351.774063015248,-351.274383948465,-350.774704881682,
-350.275025814899,-349.775346748116,-349.275667681333,-349.273907386581),
 .UNSPECIFIED.);
#385=B_SPLINE_CURVE_WITH_KNOTS('',3,(#17981,#17982,#17983,#17984,#17985,
#17986,#17987,#17988,#17989,#17990,#17991,#17992,#17993,#17994,#17995,#17996,
#17997,#17998,#17999,#18000,#18001,#18002,#18003,#18004,#18005,#18006,#18007,
#18008,#18009,#18010,#18011,#18012,#18013,#18014,#18015,#18016,#18017,#18018,
#18019,#18020,#18021,#18022,#18023),.UNSPECIFIED.,.F.,.F.,(4,3,3,3,3,3,
3,3,3,3,3,3,3,3,4),(346.018252565431,346.277593280635,346.777272347418,
347.276951414201,347.776630480984,348.276309547767,348.77598861455,349.275667681334,
349.775346748116,350.2750258149,350.774704881683,351.274383948466,351.774063015249,
352.273742082032,352.301437872611),.UNSPECIFIED.);
#386=B_SPLINE_CURVE_WITH_KNOTS('',3,(#18028,#18029,#18030,#18031,#18032,
#18033,#18034,#18035,#18036,#18037,#18038,#18039,#18040,#18041,#18042,#18043,
#18044,#18045,#18046,#18047,#18048,#18049,#18050,#18051,#18052,#18053,#18054,
#18055,#18056,#18057,#18058,#18059,#18060,#18061,#18062,#18063,#18064,#18065,
#18066,#18067,#18068,#18069,#18070),.UNSPECIFIED.,.F.,.F.,(4,3,3,3,3,3,
3,3,3,3,3,3,3,3,4),(-361.84027800094,-361.767644350909,-361.267965284126,
-360.768286217343,-360.26860715056,-359.768928083777,-359.269249016994,
-358.769569950211,-358.269890883428,-357.770211816645,-357.270532749862,
-356.770853683079,-356.271174616296,-355.771495549513,-355.557092693761),
 .UNSPECIFIED.);
#387=B_SPLINE_CURVE_WITH_KNOTS('',3,(#18071,#18072,#18073,#18074,#18075,
#18076,#18077,#18078,#18079,#18080,#18081,#18082,#18083,#18084,#18085,#18086,
#18087,#18088,#18089,#18090,#18091,#18092,#18093,#18094,#18095,#18096,#18097,
#18098,#18099,#18100,#18101,#18102,#18103,#18104,#18105,#18106,#18107,#18108,
#18109,#18110),.UNSPECIFIED.,.F.,.F.,(4,3,3,3,3,3,3,3,3,3,3,3,3,4),(352.301437872611,
352.773421148815,353.273100215598,353.772779282381,354.272458349164,354.772137415947,
355.27181648273,355.771495549513,356.271174616296,356.770853683079,357.270532749862,
357.770211816645,358.269890883428,358.58462317979),.UNSPECIFIED.);
#388=B_SPLINE_CURVE_WITH_KNOTS('',3,(#18115,#18116,#18117,#18118,#18119,
#18120,#18121,#18122,#18123,#18124,#18125,#18126,#18127,#18128,#18129,#18130,
#18131,#18132,#18133,#18134,#18135,#18136,#18137,#18138,#18139,#18140,#18141,
#18142,#18143,#18144,#18145,#18146,#18147,#18148,#18149,#18150,#18151,#18152,
#18153,#18154),.UNSPECIFIED.,.F.,.F.,(4,3,3,3,3,3,3,3,3,3,3,3,3,4),(-368.12346330812,
-367.763793152305,-367.264114085522,-366.764435018739,-366.264755951956,
-365.765076885173,-365.26539781839,-364.765718751607,-364.266039684824,
-363.766360618041,-363.266681551258,-362.767002484475,-362.267323417692,
-361.84027800094),.UNSPECIFIED.);
#389=B_SPLINE_CURVE_WITH_KNOTS('',3,(#18155,#18156,#18157,#18158,#18159,
#18160,#18161,#18162,#18163,#18164,#18165,#18166,#18167,#18168,#18169,#18170,
#18171,#18172,#18173,#18174,#18175,#18176,#18177,#18178,#18179,#18180,#18181,
#18182,#18183,#18184,#18185,#18186,#18187,#18188,#18189,#18190,#18191,#18192,
#18193,#18194,#18195,#18196,#18197),.UNSPECIFIED.,.F.,.F.,(4,3,3,3,3,3,
3,3,3,3,3,3,3,3,4),(358.58462317979,358.769569950211,359.269249016994,359.768928083777,
360.26860715056,360.768286217343,361.267965284126,361.767644350909,362.267323417692,
362.767002484475,363.266681551258,363.766360618041,364.266039684824,364.765718751607,
364.86780848697),.UNSPECIFIED.);
#390=B_SPLINE_CURVE_WITH_KNOTS('',3,(#18202,#18203,#18204,#18205,#18206,
#18207,#18208,#18209,#18210,#18211,#18212,#18213,#18214,#18215,#18216,#18217,
#18218,#18219,#18220,#18221,#18222,#18223,#18224,#18225,#18226,#18227,#18228,
#18229,#18230,#18231,#18232,#18233,#18234,#18235,#18236,#18237,#18238,#18239,
#18240,#18241,#18242,#18243,#18244),.UNSPECIFIED.,.F.,.F.,(4,3,3,3,3,3,
3,3,3,3,3,3,3,3,4),(-374.406648615299,-374.259621020484,-373.759941953701,
-373.260262886918,-372.760583820135,-372.260904753352,-371.761225686569,
-371.261546619786,-370.761867553003,-370.26218848622,-369.762509419437,
-369.262830352654,-368.763151285871,-368.263472219088,-368.12346330812),
 .UNSPECIFIED.);
#391=B_SPLINE_CURVE_WITH_KNOTS('',3,(#18245,#18246,#18247,#18248,#18249,
#18250,#18251,#18252,#18253,#18254,#18255,#18256,#18257,#18258,#18259,#18260,
#18261,#18262,#18263,#18264,#18265,#18266,#18267,#18268,#18269,#18270,#18271,
#18272,#18273,#18274,#18275,#18276,#18277,#18278,#18279,#18280,#18281,#18282,
#18283,#18284),.UNSPECIFIED.,.F.,.F.,(4,3,3,3,3,3,3,3,3,3,3,3,3,4),(364.86780848697,
365.26539781839,365.765076885173,366.264755951956,366.764435018739,367.264114085522,
367.763793152305,368.263472219088,368.763151285871,369.262830352654,369.762509419437,
370.26218848622,370.761867553004,371.150993794149),.UNSPECIFIED.);
#392=B_SPLINE_CURVE_WITH_KNOTS('',3,(#18289,#18290,#18291,#18292,#18293,
#18294,#18295,#18296,#18297,#18298,#18299,#18300,#18301,#18302,#18303,#18304,
#18305,#18306,#18307,#18308,#18309,#18310,#18311,#18312,#18313,#18314,#18315,
#18316,#18317,#18318,#18319,#18320,#18321,#18322,#18323,#18324,#18325,#18326,
#18327,#18328),.UNSPECIFIED.,.F.,.F.,(4,3,3,3,3,3,3,3,3,3,3,3,3,4),(-380.689833922479,
-380.255769821881,-379.756090755098,-379.256411688315,-378.756732621532,
-378.257053554749,-377.757374487966,-377.257695421183,-376.7580163544,-376.258337287616,
-375.758658220834,-375.25897915405,-374.759300087267,-374.406648615299),
 .UNSPECIFIED.);
#393=B_SPLINE_CURVE_WITH_KNOTS('',3,(#18329,#18330,#18331,#18332,#18333,
#18334,#18335,#18336,#18337,#18338,#18339,#18340,#18341,#18342,#18343,#18344,
#18345,#18346,#18347,#18348,#18349,#18350,#18351,#18352,#18353,#18354,#18355,
#18356,#18357,#18358,#18359,#18360,#18361,#18362,#18363,#18364,#18365,#18366,
#18367,#18368,#18369,#18370,#18371),.UNSPECIFIED.,.F.,.F.,(4,3,3,3,3,3,
3,3,3,3,3,3,3,3,4),(371.150993794149,371.261546619787,371.76122568657,372.260904753353,
372.760583820136,373.260262886919,373.759941953702,374.259621020485,374.759300087268,
375.258979154051,375.758658220834,376.258337287617,376.7580163544,377.257695421183,
377.434179101329),.UNSPECIFIED.);
#394=B_SPLINE_CURVE_WITH_KNOTS('',3,(#18376,#18377,#18378,#18379,#18380,
#18381,#18382,#18383,#18384,#18385,#18386,#18387,#18388,#18389,#18390,#18391,
#18392,#18393,#18394,#18395,#18396,#18397,#18398,#18399,#18400,#18401,#18402,
#18403,#18404,#18405,#18406,#18407,#18408,#18409,#18410,#18411,#18412,#18413,
#18414,#18415,#18416,#18417,#18418),.UNSPECIFIED.,.F.,.F.,(4,3,3,3,3,3,
3,3,3,3,3,3,3,3,4),(-386.973019229658,-386.75159769006,-386.251918623277,
-385.752239556494,-385.252560489711,-384.752881422928,-384.253202356145,
-383.753523289362,-383.253844222579,-382.754165155796,-382.254486089013,
-381.75480702223,-381.255127955447,-380.755448888664,-380.689833922479),
 .UNSPECIFIED.);
#395=B_SPLINE_CURVE_WITH_KNOTS('',3,(#18419,#18420,#18421,#18422,#18423,
#18424,#18425,#18426,#18427,#18428,#18429,#18430,#18431,#18432,#18433,#18434,
#18435,#18436,#18437,#18438,#18439,#18440,#18441,#18442,#18443,#18444,#18445,
#18446,#18447,#18448,#18449,#18450,#18451,#18452,#18453,#18454,#18455,#18456,
#18457,#18458),.UNSPECIFIED.,.F.,.F.,(4,3,3,3,3,3,3,3,3,3,3,3,3,4),(377.434179101329,
377.757374487966,378.257053554749,378.756732621532,379.256411688315,379.756090755098,
380.255769821881,380.755448888664,381.255127955447,381.75480702223,382.254486089013,
382.754165155796,383.253844222579,383.717364408508),.UNSPECIFIED.);
#396=B_SPLINE_CURVE_WITH_KNOTS('',3,(#18463,#18464,#18465,#18466,#18467,
#18468,#18469,#18470,#18471,#18472,#18473,#18474,#18475,#18476,#18477,#18478,
#18479,#18480,#18481,#18482,#18483,#18484,#18485,#18486,#18487,#18488,#18489,
#18490,#18491,#18492,#18493,#18494,#18495,#18496,#18497,#18498,#18499,#18500,
#18501,#18502,#18503,#18504,#18505),.UNSPECIFIED.,.F.,.F.,(4,3,3,3,3,3,
3,3,3,3,3,3,3,3,4),(-393.256204536838,-393.247425558239,-392.747746491456,
-392.248067424673,-391.74838835789,-391.248709291107,-390.749030224324,
-390.249351157541,-389.749672090758,-389.249993023975,-388.750313957192,
-388.250634890409,-387.750955823626,-387.251276756843,-386.973019229658),
 .UNSPECIFIED.);
#397=B_SPLINE_CURVE_WITH_KNOTS('',3,(#18506,#18507,#18508,#18509,#18510,
#18511,#18512,#18513,#18514,#18515,#18516,#18517,#18518,#18519,#18520,#18521,
#18522,#18523,#18524,#18525,#18526,#18527,#18528,#18529,#18530,#18531,#18532,
#18533,#18534,#18535,#18536,#18537,#18538,#18539,#18540,#18541,#18542,#18543,
#18544,#18545,#18546,#18547,#18548),.UNSPECIFIED.,.F.,.F.,(4,3,3,3,3,3,
3,3,3,3,3,3,3,3,4),(383.717364408508,383.753523289362,384.253202356145,
384.752881422928,385.252560489711,385.752239556494,386.251918623277,386.75159769006,
387.251276756843,387.750955823626,388.250634890409,388.750313957192,389.249993023975,
389.749672090758,390.000549715688),.UNSPECIFIED.);
#398=B_SPLINE_CURVE_WITH_KNOTS('',3,(#18554,#18555,#18556,#18557),
 .UNSPECIFIED.,.F.,.F.,(4,4),(405.265452313083,405.755527026166),
 .UNSPECIFIED.);
#399=B_SPLINE_CURVE_WITH_KNOTS('',3,(#18563,#18564,#18565,#18566,#18567,
#18568,#18569,#18570,#18571,#18572,#18573,#18574,#18575,#18576,#18577,#18578,
#18579),.UNSPECIFIED.,.F.,.F.,(4,1,1,1,1,1,1,1,1,1,1,1,1,1,4),(398.982267005903,
399.260524533088,399.760203599871,400.259882666654,400.759561733437,401.25924080022,
401.758919867003,402.258598933787,402.75827800057,403.257957067353,403.757636134136,
404.257315200919,404.756994267702,405.256673334485,405.265452313083),
 .UNSPECIFIED.);
#400=B_SPLINE_CURVE_WITH_KNOTS('',3,(#18582,#18583,#18584,#18585,#18586,
#18587,#18588,#18589,#18590,#18591,#18592,#18593,#18594),.UNSPECIFIED.,
 .F.,.F.,(4,1,1,1,1,1,1,1,1,1,4),(398.982267005904,399.231068447758,399.730747514541,
400.230426581324,400.730105648107,401.22978471489,401.729463781673,402.229142848456,
402.728821915239,403.228500982022,403.728180048805),.UNSPECIFIED.);
#401=B_SPLINE_CURVE_WITH_KNOTS('',3,(#18599,#18600,#18601,#18602,#18603,
#18604,#18605,#18606,#18607,#18608,#18609,#18610,#18611,#18612,#18613,#18614,
#18615),.UNSPECIFIED.,.F.,.F.,(4,1,1,1,1,1,1,1,1,1,1,1,1,1,4),(392.699081698724,
392.764696664909,393.264375731692,393.764054798475,394.263733865258,394.763412932041,
395.263091998824,395.762771065607,396.26245013239,396.762129199173,397.261808265956,
397.761487332739,398.261166399522,398.760845466305,398.982267005903),
 .UNSPECIFIED.);
#402=B_SPLINE_CURVE_WITH_KNOTS('',3,(#18616,#18617,#18618,#18619,#18620,
#18621,#18622,#18623,#18624,#18625,#18626,#18627,#18628,#18629,#18630,#18631,
#18632),.UNSPECIFIED.,.F.,.F.,(4,1,1,1,1,1,1,1,1,1,1,1,1,1,4),(392.699081698724,
392.735240579579,393.234919646362,393.734598713145,394.234277779928,394.733956846711,
395.233635913494,395.733314980277,396.23299404706,396.732673113843,397.232352180626,
397.732031247409,398.231710314192,398.731389380975,398.982267005904),
 .UNSPECIFIED.);
#403=B_SPLINE_CURVE_WITH_KNOTS('',3,(#18637,#18638,#18639,#18640,#18641,
#18642,#18643,#18644,#18645,#18646,#18647,#18648,#18649,#18650,#18651,#18652),
 .UNSPECIFIED.,.F.,.F.,(4,1,1,1,1,1,1,1,1,1,1,1,1,4),(386.415896391544,
386.768547863513,387.268226930296,387.767905997079,388.267585063862,388.767264130645,
389.266943197428,389.766622264211,390.266301330994,390.765980397777,391.26565946456,
391.765338531343,392.265017598126,392.699081698724),.UNSPECIFIED.);
#404=B_SPLINE_CURVE_WITH_KNOTS('',3,(#18653,#18654,#18655,#18656,#18657,
#18658,#18659,#18660,#18661,#18662,#18663,#18664,#18665,#18666,#18667,#18668),
 .UNSPECIFIED.,.F.,.F.,(4,1,1,1,1,1,1,1,1,1,1,1,1,4),(386.415896391545,
386.739091778183,387.238770844966,387.738449911749,388.238128978532,388.737808045315,
389.237487112098,389.737166178881,390.236845245664,390.736524312447,391.23620337923,
391.735882446013,392.235561512796,392.699081698724),.UNSPECIFIED.);
#405=B_SPLINE_CURVE_WITH_KNOTS('',3,(#18673,#18674,#18675,#18676,#18677,
#18678,#18679,#18680,#18681,#18682,#18683,#18684,#18685,#18686,#18687,#18688,
#18689),.UNSPECIFIED.,.F.,.F.,(4,1,1,1,1,1,1,1,1,1,1,1,1,1,4),(380.132711084365,
380.272719995333,380.772399062117,381.2720781289,381.771757195683,382.271436262466,
382.771115329249,383.270794396032,383.770473462815,384.270152529598,384.769831596381,
385.269510663164,385.769189729947,386.26886879673,386.415896391544),
 .UNSPECIFIED.);
#406=B_SPLINE_CURVE_WITH_KNOTS('',3,(#18690,#18691,#18692,#18693,#18694,
#18695,#18696,#18697,#18698,#18699,#18700,#18701,#18702,#18703,#18704,#18705,
#18706),.UNSPECIFIED.,.F.,.F.,(4,1,1,1,1,1,1,1,1,1,1,1,1,1,4),(380.132711084365,
380.243263910003,380.742942976786,381.242622043569,381.742301110352,382.241980177135,
382.741659243918,383.241338310702,383.741017377485,384.240696444268,384.740375511051,
385.240054577834,385.739733644617,386.2394127114,386.415896391545),
 .UNSPECIFIED.);
#407=B_SPLINE_CURVE_WITH_KNOTS('',3,(#18711,#18712,#18713,#18714,#18715,
#18716,#18717,#18718,#18719,#18720,#18721,#18722,#18723,#18724,#18725,#18726),
 .UNSPECIFIED.,.F.,.F.,(4,1,1,1,1,1,1,1,1,1,1,1,1,4),(373.849525777185,
374.276571193937,374.77625026072,375.275929327503,375.775608394286,376.275287461069,
376.774966527852,377.274645594635,377.774324661418,378.274003728201,378.773682794984,
379.273361861767,379.77304092855,380.132711084365),.UNSPECIFIED.);
#408=B_SPLINE_CURVE_WITH_KNOTS('',3,(#18727,#18728,#18729,#18730,#18731,
#18732,#18733,#18734,#18735,#18736,#18737,#18738,#18739,#18740,#18741,#18742),
 .UNSPECIFIED.,.F.,.F.,(4,1,1,1,1,1,1,1,1,1,1,1,1,4),(373.849525777185,
374.247115108607,374.74679417539,375.246473242173,375.746152308956,376.245831375739,
376.745510442522,377.245189509305,377.744868576088,378.244547642871,378.744226709654,
379.243905776437,379.74358484322,380.132711084365),.UNSPECIFIED.);
#409=B_SPLINE_CURVE_WITH_KNOTS('',3,(#18747,#18748,#18749,#18750,#18751,
#18752,#18753,#18754,#18755,#18756,#18757,#18758,#18759,#18760,#18761,#18762,
#18763),.UNSPECIFIED.,.F.,.F.,(4,1,1,1,1,1,1,1,1,1,1,1,1,1,4),(367.566340470006,
367.780743325758,368.280422392541,368.780101459324,369.279780526107,369.77945959289,
370.279138659673,370.778817726456,371.278496793239,371.778175860022,372.277854926805,
372.777533993588,373.277213060371,373.776892127154,373.849525777185),
 .UNSPECIFIED.);
#410=B_SPLINE_CURVE_WITH_KNOTS('',3,(#18764,#18765,#18766,#18767,#18768,
#18769,#18770,#18771,#18772,#18773,#18774,#18775,#18776,#18777,#18778,#18779,
#18780),.UNSPECIFIED.,.F.,.F.,(4,1,1,1,1,1,1,1,1,1,1,1,1,1,4),(367.566340470006,
367.751287240428,368.250966307211,368.750645373994,369.250324440777,369.75000350756,
370.249682574343,370.749361641126,371.249040707909,371.748719774692,372.248398841475,
372.748077908258,373.247756975041,373.747436041824,373.849525777185),
 .UNSPECIFIED.);
#411=B_SPLINE_CURVE_WITH_KNOTS('',3,(#18785,#18786,#18787,#18788,#18789,
#18790,#18791,#18792,#18793,#18794,#18795,#18796,#18797,#18798,#18799,#18800,
#18801),.UNSPECIFIED.,.F.,.F.,(4,1,1,1,1,1,1,1,1,1,1,1,1,1,4),(361.283155162826,
361.284915457579,361.784594524362,362.284273591145,362.783952657928,363.283631724711,
363.783310791494,364.282989858277,364.78266892506,365.282347991843,365.782027058626,
366.281706125409,366.781385192192,367.281064258975,367.566340470006),
 .UNSPECIFIED.);
#412=B_SPLINE_CURVE_WITH_KNOTS('',3,(#18802,#18803,#18804,#18805,#18806,
#18807,#18808,#18809,#18810,#18811,#18812,#18813,#18814,#18815,#18816,#18817),
 .UNSPECIFIED.,.F.,.F.,(4,1,1,1,1,1,1,1,1,1,1,1,1,4),(361.283155162826,
361.755138439031,362.254817505815,362.754496572598,363.254175639381,363.753854706164,
364.253533772947,364.75321283973,365.252891906513,365.752570973296,366.252250040079,
366.751929106862,367.251608173645,367.566340470006),.UNSPECIFIED.);
#413=B_SPLINE_CURVE_WITH_KNOTS('',3,(#18822,#18823,#18824,#18825,#18826,
#18827,#18828,#18829,#18830,#18831,#18832,#18833,#18834,#18835),
 .UNSPECIFIED.,.F.,.F.,(4,1,1,1,1,1,1,1,1,1,1,4),(354.999969855646,355.788445722965,
356.787803856531,357.287482923314,357.787161990097,358.28684105688,358.786520123663,
359.286199190446,359.78587825723,360.285557324013,360.785236390796,361.283155162826),
 .UNSPECIFIED.);
#414=B_SPLINE_CURVE_WITH_KNOTS('',3,(#18836,#18837,#18838,#18839,#18840,
#18841,#18842,#18843,#18844,#18845,#18846,#18847,#18848,#18849,#18850,#18851,
#18852),.UNSPECIFIED.,.F.,.F.,(4,1,1,1,1,1,1,1,1,1,1,1,1,1,4),(354.999969855647,
355.259310570852,355.758989637635,356.258668704418,356.758347771201,357.258026837984,
357.757705904767,358.25738497155,358.757064038333,359.256743105116,359.756422171899,
360.256101238682,360.755780305465,361.255459372248,361.283155162826),
 .UNSPECIFIED.);
#415=B_SPLINE_CURVE_WITH_KNOTS('',3,(#18857,#18858,#18859,#18860,#18861,
#18862,#18863,#18864,#18865,#18866,#18867),.UNSPECIFIED.,.F.,.F.,(4,1,1,
1,1,1,1,1,4),(348.716784548467,348.792938788003,349.792296921569,350.791655055135,
351.791013188701,352.790371322267,353.789729455833,354.789087589399,354.999969855646),
 .UNSPECIFIED.);
#416=B_SPLINE_CURVE_WITH_KNOTS('',3,(#18868,#18869,#18870,#18871,#18872,
#18873,#18874,#18875,#18876,#18877,#18878,#18879),.UNSPECIFIED.,.F.,.F.,
(4,1,1,1,1,1,1,1,1,4),(348.716784548467,348.763482702673,349.762840836239,
350.762198969805,351.761557103371,352.760915236937,353.760273370503,354.259952437286,
354.759631504069,354.999969855647),.UNSPECIFIED.);
#417=B_SPLINE_CURVE_WITH_KNOTS('',3,(#18884,#18885,#18886,#18887,#18888,
#18889,#18890,#18891,#18892,#18893),.UNSPECIFIED.,.F.,.F.,(4,1,1,1,1,1,
1,4),(342.433599241287,342.796789986607,343.796148120173,344.795506253739,
345.794864387305,346.794222520871,347.793580654437,348.716784548467),
 .UNSPECIFIED.);
#418=B_SPLINE_CURVE_WITH_KNOTS('',3,(#18894,#18895,#18896,#18897,#18898,
#18899,#18900,#18901,#18902,#18903),.UNSPECIFIED.,.F.,.F.,(4,1,1,1,1,1,
1,4),(342.433599241288,342.767333901277,343.766692034843,344.766050168409,
345.765408301975,346.764766435541,347.764124569107,348.716784548467),
 .UNSPECIFIED.);
#419=B_SPLINE_CURVE_WITH_KNOTS('',3,(#18908,#18909,#18910,#18911,#18912,
#18913,#18914,#18915,#18916,#18917),.UNSPECIFIED.,.F.,.F.,(4,1,1,1,1,1,
1,4),(336.150413934108,336.80064118521,337.799999318776,338.799357452343,
339.798715585909,340.798073719475,341.797431853041,342.433599241287),
 .UNSPECIFIED.);
#420=B_SPLINE_CURVE_WITH_KNOTS('',3,(#18918,#18919,#18920,#18921,#18922,
#18923,#18924,#18925,#18926,#18927),.UNSPECIFIED.,.F.,.F.,(4,1,1,1,1,1,
1,4),(336.150413934108,336.77118509988,337.770543233446,338.769901367012,
339.769259500578,340.768617634145,341.767975767711,342.433599241288),
 .UNSPECIFIED.);
#421=B_SPLINE_CURVE_WITH_KNOTS('',3,(#18932,#18933,#18934,#18935,#18936,
#18937,#18938,#18939,#18940,#18941),.UNSPECIFIED.,.F.,.F.,(4,1,1,1,1,1,
1,4),(329.867228626928,330.804492383814,331.80385051738,332.803208650946,
333.802566784512,334.801924918078,335.801283051644,336.150413934108),
 .UNSPECIFIED.);
#422=B_SPLINE_CURVE_WITH_KNOTS('',3,(#18942,#18943,#18944,#18945,#18946,
#18947,#18948,#18949,#18950,#18951),.UNSPECIFIED.,.F.,.F.,(4,1,1,1,1,1,
1,4),(329.867228626928,330.775036298484,331.77439443205,332.773752565616,
333.773110699182,334.772468832748,335.771826966314,336.150413934108),
 .UNSPECIFIED.);
#423=B_SPLINE_CURVE_WITH_KNOTS('',3,(#18956,#18957,#18958,#18959,#18960,
#18961,#18962,#18963,#18964,#18965,#18966),.UNSPECIFIED.,.F.,.F.,(4,1,1,
1,1,1,1,1,4),(323.584043319749,323.808985448852,324.808343582418,325.807701715984,
326.80705984955,327.806417983116,328.805776116682,329.805134250248,329.867228626928),
 .UNSPECIFIED.);
#424=B_SPLINE_CURVE_WITH_KNOTS('',3,(#18967,#18968,#18969,#18970,#18971,
#18972,#18973,#18974,#18975,#18976,#18977),.UNSPECIFIED.,.F.,.F.,(4,1,1,
1,1,1,1,1,4),(323.584043319749,323.779529363522,324.778887497088,325.778245630654,
326.77760376422,327.776961897786,328.776320031352,329.775678164918,329.867228626928),
 .UNSPECIFIED.);
#425=B_SPLINE_CURVE_WITH_KNOTS('',3,(#18982,#18983,#18984,#18985,#18986,
#18987,#18988,#18989,#18990,#18991),.UNSPECIFIED.,.F.,.F.,(4,1,1,1,1,1,
1,4),(317.300858012569,317.812836647456,318.812194781022,319.811552914588,
320.810911048154,321.81026918172,322.809627315286,323.584043319749),
 .UNSPECIFIED.);
#426=B_SPLINE_CURVE_WITH_KNOTS('',3,(#18992,#18993,#18994,#18995,#18996,
#18997,#18998,#18999,#19000,#19001),.UNSPECIFIED.,.F.,.F.,(4,1,1,1,1,1,
1,4),(317.300858012569,317.783380562125,318.782738695691,319.782096829258,
320.781454962824,321.78081309639,322.780171229956,323.584043319749),
 .UNSPECIFIED.);
#427=B_SPLINE_CURVE_WITH_KNOTS('',3,(#19006,#19007,#19008,#19009,#19010,
#19011,#19012,#19013,#19014,#19015),.UNSPECIFIED.,.F.,.F.,(4,1,1,1,1,1,
1,4),(311.017672705389,311.816687846059,312.816045979625,313.815404113191,
314.814762246757,315.814120380323,316.81347851389,317.300858012569),
 .UNSPECIFIED.);
#428=B_SPLINE_CURVE_WITH_KNOTS('',3,(#19016,#19017,#19018,#19019,#19020,
#19021,#19022,#19023,#19024,#19025),.UNSPECIFIED.,.F.,.F.,(4,1,1,1,1,1,
1,4),(311.01767270539,311.787231760729,312.786589894295,313.785948027861,
314.785306161427,315.784664294993,316.784022428559,317.300858012569),
 .UNSPECIFIED.);
#429=B_SPLINE_CURVE_WITH_KNOTS('',3,(#19030,#19031,#19032,#19033,#19034,
#19035,#19036,#19037,#19038,#19039,#19040),.UNSPECIFIED.,.F.,.F.,(4,1,1,
1,1,1,1,1,4),(304.73448739821,304.821180911097,305.820539044663,306.819897178229,
307.819255311795,308.818613445361,309.817971578927,310.817329712493,311.017672705389),
 .UNSPECIFIED.);
#430=B_SPLINE_CURVE_WITH_KNOTS('',3,(#19041,#19042,#19043,#19044,#19045,
#19046,#19047,#19048,#19049,#19050,#19051),.UNSPECIFIED.,.F.,.F.,(4,1,1,
1,1,1,1,1,4),(304.73448739821,304.791724825767,305.791082959333,306.790441092899,
307.789799226465,308.789157360031,309.788515493597,310.787873627163,311.01767270539),
 .UNSPECIFIED.);
#431=B_SPLINE_CURVE_WITH_KNOTS('',3,(#19056,#19057,#19058,#19059,#19060,
#19061,#19062,#19063,#19064,#19065),.UNSPECIFIED.,.F.,.F.,(4,1,1,1,1,1,
1,4),(298.45130209103,298.825032109701,299.824390243267,300.823748376833,
301.823106510399,302.822464643965,303.821822777531,304.73448739821),
 .UNSPECIFIED.);
#432=B_SPLINE_CURVE_WITH_KNOTS('',3,(#19066,#19067,#19068,#19069,#19070,
#19071,#19072,#19073,#19074,#19075),.UNSPECIFIED.,.F.,.F.,(4,1,1,1,1,1,
1,4),(298.451302091031,298.795576024371,299.794934157937,300.794292291503,
301.793650425069,302.793008558635,303.792366692201,304.73448739821),
 .UNSPECIFIED.);
#433=B_SPLINE_CURVE_WITH_KNOTS('',3,(#19080,#19081,#19082,#19083,#19084,
#19085,#19086,#19087,#19088,#19089),.UNSPECIFIED.,.F.,.F.,(4,1,1,1,1,1,
1,4),(292.168116783851,292.828883308304,293.82824144187,294.827599575437,
295.826957709003,296.826315842569,297.825673976135,298.45130209103),
 .UNSPECIFIED.);
#434=B_SPLINE_CURVE_WITH_KNOTS('',3,(#19090,#19091,#19092,#19093,#19094,
#19095,#19096,#19097,#19098,#19099),.UNSPECIFIED.,.F.,.F.,(4,1,1,1,1,1,
1,4),(292.168116783851,292.799427222974,293.79878535654,294.798143490106,
295.797501623672,296.796859757238,297.796217890804,298.451302091031),
 .UNSPECIFIED.);
#435=B_SPLINE_CURVE_WITH_KNOTS('',3,(#19104,#19105,#19106,#19107,#19108,
#19109,#19110,#19111,#19112,#19113),.UNSPECIFIED.,.F.,.F.,(4,1,1,1,1,1,
1,4),(285.884931476671,286.832734506908,287.832092640474,288.83145077404,
289.830808907606,290.830167041172,291.829525174738,292.168116783851),
 .UNSPECIFIED.);
#436=B_SPLINE_CURVE_WITH_KNOTS('',3,(#19114,#19115,#19116,#19117,#19118,
#19119,#19120,#19121,#19122,#19123),.UNSPECIFIED.,.F.,.F.,(4,1,1,1,1,1,
1,4),(285.884931476672,286.803278421578,287.802636555144,288.80199468871,
289.801352822276,290.800710955842,291.800069089408,292.168116783851),
 .UNSPECIFIED.);
#437=B_SPLINE_CURVE_WITH_KNOTS('',3,(#19128,#19129,#19130,#19131,#19132,
#19133,#19134,#19135,#19136,#19137,#19138),.UNSPECIFIED.,.F.,.F.,(4,1,1,
1,1,1,1,1,4),(279.601746169492,279.837227571946,280.836585705512,281.835943839078,
282.835301972644,283.83466010621,284.834018239776,285.833376373342,285.884931476671),
 .UNSPECIFIED.);
#438=B_SPLINE_CURVE_WITH_KNOTS('',3,(#19139,#19140,#19141,#19142,#19143,
#19144,#19145,#19146,#19147,#19148,#19149),.UNSPECIFIED.,.F.,.F.,(4,1,1,
1,1,1,1,1,4),(279.601746169492,279.807771486616,280.807129620182,281.806487753748,
282.805845887314,283.80520402088,284.804562154446,285.803920288012,285.884931476672),
 .UNSPECIFIED.);
#439=B_SPLINE_CURVE_WITH_KNOTS('',3,(#19154,#19155,#19156,#19157,#19158,
#19159,#19160,#19161,#19162,#19163),.UNSPECIFIED.,.F.,.F.,(4,1,1,1,1,1,
1,4),(273.318560862312,273.84107877055,274.840436904116,275.839795037682,
276.839153171248,277.838511304814,278.83786943838,279.601746169492),
 .UNSPECIFIED.);
#440=B_SPLINE_CURVE_WITH_KNOTS('',3,(#19164,#19165,#19166,#19167,#19168,
#19169,#19170,#19171,#19172,#19173),.UNSPECIFIED.,.F.,.F.,(4,1,1,1,1,1,
1,4),(273.318560862312,273.811622685219,274.810980818785,275.810338952351,
276.809697085917,277.809055219484,278.80841335305,279.601746169492),
 .UNSPECIFIED.);
#441=B_SPLINE_CURVE_WITH_KNOTS('',3,(#19178,#19179,#19180,#19181,#19182,
#19183,#19184,#19185,#19186,#19187),.UNSPECIFIED.,.F.,.F.,(4,1,1,1,1,1,
1,4),(267.035375555133,267.844929969153,268.844288102719,269.843646236285,
270.843004369851,271.842362503417,272.841720636983,273.318560862312),
 .UNSPECIFIED.);
#442=B_SPLINE_CURVE_WITH_KNOTS('',3,(#19188,#19189,#19190,#19191,#19192,
#19193,#19194,#19195,#19196,#19197),.UNSPECIFIED.,.F.,.F.,(4,1,1,1,1,1,
1,4),(267.035375555133,267.815473883823,268.814832017389,269.814190150955,
270.813548284521,271.812906418087,272.812264551653,273.318560862312),
 .UNSPECIFIED.);
#443=B_SPLINE_CURVE_WITH_KNOTS('',3,(#19202,#19203,#19204,#19205,#19206,
#19207,#19208,#19209,#19210,#19211,#19212),.UNSPECIFIED.,.F.,.F.,(4,1,1,
1,1,1,1,1,4),(260.752190247953,260.849423034191,261.848781167757,262.848139301323,
263.847497434889,264.846855568455,265.846213702021,266.845571835587,267.035375555133),
 .UNSPECIFIED.);
#444=B_SPLINE_CURVE_WITH_KNOTS('',3,(#19213,#19214,#19215,#19216,#19217,
#19218,#19219,#19220,#19221,#19222,#19223),.UNSPECIFIED.,.F.,.F.,(4,1,1,
1,1,1,1,1,4),(260.752190247953,260.819966948861,261.819325082427,262.818683215993,
263.818041349559,264.817399483125,265.816757616691,266.816115750257,267.035375555133),
 .UNSPECIFIED.);
#445=B_SPLINE_CURVE_WITH_KNOTS('',3,(#19228,#19229,#19230,#19231,#19232,
#19233,#19234,#19235,#19236,#19237),.UNSPECIFIED.,.F.,.F.,(4,1,1,1,1,1,
1,4),(254.469004940773,254.853274232795,255.852632366361,256.851990499927,
257.851348633493,258.850706767059,259.850064900625,260.752190247953),
 .UNSPECIFIED.);
#446=B_SPLINE_CURVE_WITH_KNOTS('',3,(#19238,#19239,#19240,#19241,#19242,
#19243,#19244,#19245,#19246,#19247),.UNSPECIFIED.,.F.,.F.,(4,1,1,1,1,1,
1,4),(254.469004940774,254.823818147464,255.82317628103,256.822534414597,
257.821892548163,258.821250681729,259.820608815295,260.752190247953),
 .UNSPECIFIED.);
#447=B_SPLINE_CURVE_WITH_KNOTS('',3,(#19252,#19253,#19254,#19255,#19256,
#19257,#19258,#19259,#19260,#19261),.UNSPECIFIED.,.F.,.F.,(4,1,1,1,1,1,
1,4),(248.185819633594,248.857125431398,249.856483564964,250.85584169853,
251.855199832097,252.854557965663,253.853916099229,254.469004940773),
 .UNSPECIFIED.);
#448=B_SPLINE_CURVE_WITH_KNOTS('',3,(#19262,#19263,#19264,#19265,#19266,
#19267,#19268,#19269,#19270,#19271),.UNSPECIFIED.,.F.,.F.,(4,1,1,1,1,1,
1,4),(248.185819633594,248.827669346068,249.827027479634,250.8263856132,
251.825743746766,252.825101880332,253.824460013898,254.469004940774),
 .UNSPECIFIED.);
#449=B_SPLINE_CURVE_WITH_KNOTS('',3,(#19276,#19277,#19278,#19279,#19280,
#19281,#19282,#19283,#19284,#19285),.UNSPECIFIED.,.F.,.F.,(4,1,1,1,1,1,
1,4),(241.902634326414,242.860976630002,243.860334763568,244.859692897134,
245.8590510307,246.858409164266,247.857767297832,248.185819633594),
 .UNSPECIFIED.);
#450=B_SPLINE_CURVE_WITH_KNOTS('',3,(#19286,#19287,#19288,#19289,#19290,
#19291,#19292,#19293,#19294,#19295),.UNSPECIFIED.,.F.,.F.,(4,1,1,1,1,1,
1,4),(241.902634326415,242.831520544672,243.830878678238,244.830236811804,
245.82959494537,246.828953078936,247.828311212502,248.185819633594),
 .UNSPECIFIED.);
#451=B_SPLINE_CURVE_WITH_KNOTS('',3,(#19300,#19301,#19302,#19303,#19304,
#19305,#19306,#19307,#19308,#19309,#19310),.UNSPECIFIED.,.F.,.F.,(4,1,1,
1,1,1,1,1,4),(235.619449019235,235.86546969504,236.864827828606,237.864185962172,
238.863544095738,239.862902229304,240.86226036287,241.861618496436,241.902634326414),
 .UNSPECIFIED.);
#452=B_SPLINE_CURVE_WITH_KNOTS('',3,(#19311,#19312,#19313,#19314,#19315,
#19316,#19317,#19318,#19319,#19320,#19321),.UNSPECIFIED.,.F.,.F.,(4,1,1,
1,1,1,1,1,4),(235.619449019235,235.83601360971,236.835371743276,237.834729876842,
238.834088010408,239.833446143974,240.83280427754,241.832162411106,241.902634326415),
 .UNSPECIFIED.);
#453=B_SPLINE_CURVE_WITH_KNOTS('',3,(#19326,#19327,#19328,#19329,#19330,
#19331,#19332,#19333,#19334,#19335),.UNSPECIFIED.,.F.,.F.,(4,1,1,1,1,1,
1,4),(229.336263712055,229.869320893643,230.86867902721,231.868037160776,
232.867395294342,233.866753427908,234.866111561474,235.619449019235),
 .UNSPECIFIED.);
#454=B_SPLINE_CURVE_WITH_KNOTS('',3,(#19336,#19337,#19338,#19339,#19340,
#19341,#19342,#19343,#19344,#19345),.UNSPECIFIED.,.F.,.F.,(4,1,1,1,1,1,
1,4),(229.336263712055,229.839864808313,230.839222941879,231.838581075445,
232.837939209011,233.837297342577,234.836655476144,235.619449019235),
 .UNSPECIFIED.);
#455=B_SPLINE_CURVE_WITH_KNOTS('',3,(#19350,#19351,#19352,#19353,#19354,
#19355,#19356,#19357,#19358,#19359),.UNSPECIFIED.,.F.,.F.,(4,1,1,1,1,1,
1,4),(223.053078404876,223.873172092247,224.872530225813,225.871888359379,
226.871246492945,227.870604626511,228.869962760077,229.336263712055),
 .UNSPECIFIED.);
#456=B_SPLINE_CURVE_WITH_KNOTS('',3,(#19360,#19361,#19362,#19363,#19364,
#19365,#19366,#19367,#19368,#19369),.UNSPECIFIED.,.F.,.F.,(4,1,1,1,1,1,
1,4),(223.053078404876,223.843716006917,224.843074140483,225.842432274049,
226.841790407615,227.841148541181,228.840506674747,229.336263712055),
 .UNSPECIFIED.);
#457=B_SPLINE_CURVE_WITH_KNOTS('',3,(#19374,#19375,#19376,#19377,#19378,
#19379,#19380,#19381,#19382,#19383,#19384),.UNSPECIFIED.,.F.,.F.,(4,1,1,
1,1,1,1,1,4),(216.769893097696,216.877665157285,217.877023290851,218.876381424417,
219.875739557983,220.875097691549,221.874455825115,222.873813958681,223.053078404876),
 .UNSPECIFIED.);
#458=B_SPLINE_CURVE_WITH_KNOTS('',3,(#19385,#19386,#19387,#19388,#19389,
#19390,#19391,#19392,#19393,#19394,#19395),.UNSPECIFIED.,.F.,.F.,(4,1,1,
1,1,1,1,1,4),(216.769893097696,216.848209071955,217.847567205521,218.846925339087,
219.846283472653,220.845641606219,221.844999739785,222.844357873351,223.053078404876),
 .UNSPECIFIED.);
#459=B_SPLINE_CURVE_WITH_KNOTS('',3,(#19400,#19401,#19402,#19403,#19404,
#19405,#19406,#19407,#19408,#19409),.UNSPECIFIED.,.F.,.F.,(4,1,1,1,1,1,
1,4),(210.486707790516,210.881516355889,211.880874489455,212.880232623021,
213.879590756587,214.878948890153,215.878307023719,216.769893097696),
 .UNSPECIFIED.);
#460=B_SPLINE_CURVE_WITH_KNOTS('',3,(#19410,#19411,#19412,#19413,#19414,
#19415,#19416,#19417,#19418,#19419),.UNSPECIFIED.,.F.,.F.,(4,1,1,1,1,1,
1,4),(210.486707790517,210.852060270558,211.851418404124,212.85077653769,
213.850134671257,214.849492804823,215.848850938389,216.769893097696),
 .UNSPECIFIED.);
#461=B_SPLINE_CURVE_WITH_KNOTS('',3,(#19424,#19425,#19426,#19427,#19428,
#19429,#19430,#19431,#19432,#19433),.UNSPECIFIED.,.F.,.F.,(4,1,1,1,1,1,
1,4),(204.203522483337,204.885367554492,205.884725688058,206.884083821624,
207.88344195519,208.882800088756,209.882158222323,210.486707790516),
 .UNSPECIFIED.);
#462=B_SPLINE_CURVE_WITH_KNOTS('',3,(#19434,#19435,#19436,#19437,#19438,
#19439,#19440,#19441,#19442,#19443),.UNSPECIFIED.,.F.,.F.,(4,1,1,1,1,1,
1,4),(204.203522483337,204.855911469162,205.855269602728,206.854627736294,
207.85398586986,208.853344003426,209.852702136992,210.486707790517),
 .UNSPECIFIED.);
#463=B_SPLINE_CURVE_WITH_KNOTS('',3,(#19448,#19449,#19450,#19451,#19452,
#19453,#19454,#19455,#19456,#19457),.UNSPECIFIED.,.F.,.F.,(4,1,1,1,1,1,
1,4),(197.920337176157,198.889218753096,199.888576886662,200.887935020228,
201.887293153794,202.88665128736,203.886009420926,204.203522483337),
 .UNSPECIFIED.);
#464=B_SPLINE_CURVE_WITH_KNOTS('',3,(#19458,#19459,#19460,#19461,#19462,
#19463,#19464,#19465,#19466,#19467),.UNSPECIFIED.,.F.,.F.,(4,1,1,1,1,1,
1,4),(197.920337176158,198.859762667766,199.859120801332,200.858478934898,
201.857837068464,202.85719520203,203.856553335596,204.203522483337),
 .UNSPECIFIED.);
#465=B_SPLINE_CURVE_WITH_KNOTS('',3,(#19472,#19473,#19474,#19475,#19476,
#19477,#19478,#19479,#19480,#19481,#19482),.UNSPECIFIED.,.F.,.F.,(4,1,1,
1,1,1,1,1,4),(191.637151868978,191.893711818134,192.8930699517,193.892428085266,
194.891786218832,195.891144352398,196.890502485964,197.88986061953,197.920337176157),
 .UNSPECIFIED.);
#466=B_SPLINE_CURVE_WITH_KNOTS('',3,(#19483,#19484,#19485,#19486,#19487,
#19488,#19489,#19490,#19491,#19492,#19493),.UNSPECIFIED.,.F.,.F.,(4,1,1,
1,1,1,1,1,4),(191.637151868978,191.864255732803,192.86361386637,193.862971999936,
194.862330133502,195.861688267068,196.861046400634,197.8604045342,197.920337176158),
 .UNSPECIFIED.);
#467=B_SPLINE_CURVE_WITH_KNOTS('',3,(#19498,#19499,#19500,#19501,#19502,
#19503,#19504,#19505,#19506,#19507),.UNSPECIFIED.,.F.,.F.,(4,1,1,1,1,1,
1,4),(185.353966561798,185.897563016737,186.896921150303,187.89627928387,
188.895637417436,189.894995551002,190.894353684568,191.637151868978),
 .UNSPECIFIED.);
#468=B_SPLINE_CURVE_WITH_KNOTS('',3,(#19508,#19509,#19510,#19511,#19512,
#19513,#19514,#19515,#19516,#19517),.UNSPECIFIED.,.F.,.F.,(4,1,1,1,1,1,
1,4),(185.353966561799,185.868106931407,186.867465064973,187.866823198539,
188.866181332105,189.865539465671,190.864897599237,191.637151868978),
 .UNSPECIFIED.);
#469=B_SPLINE_CURVE_WITH_KNOTS('',3,(#19522,#19523,#19524,#19525,#19526,
#19527,#19528,#19529,#19530,#19531),.UNSPECIFIED.,.F.,.F.,(4,1,1,1,1,1,
1,4),(179.070781254619,179.901414215341,180.900772348907,181.900130482473,
182.899488616039,183.898846749605,184.898204883171,185.353966561798),
 .UNSPECIFIED.);
#470=B_SPLINE_CURVE_WITH_KNOTS('',3,(#19532,#19533,#19534,#19535,#19536,
#19537,#19538,#19539,#19540,#19541),.UNSPECIFIED.,.F.,.F.,(4,1,1,1,1,1,
1,4),(179.070781254619,179.871958130011,180.871316263577,181.870674397143,
182.870032530709,183.869390664275,184.868748797841,185.353966561799),
 .UNSPECIFIED.);
#471=B_SPLINE_CURVE_WITH_KNOTS('',3,(#19546,#19547,#19548,#19549,#19550,
#19551,#19552,#19553,#19554,#19555,#19556),.UNSPECIFIED.,.F.,.F.,(4,1,1,
1,1,1,1,1,4),(172.787595947439,172.905907280379,173.905265413945,174.904623547511,
175.903981681077,176.903339814643,177.902697948209,178.902056081775,179.070781254619),
 .UNSPECIFIED.);
#472=B_SPLINE_CURVE_WITH_KNOTS('',3,(#19557,#19558,#19559,#19560,#19561,
#19562,#19563,#19564,#19565,#19566,#19567),.UNSPECIFIED.,.F.,.F.,(4,1,1,
1,1,1,1,1,4),(172.787595947439,172.876451195049,173.875809328615,174.875167462181,
175.874525595747,176.873883729313,177.873241862879,178.872599996445,179.070781254619),
 .UNSPECIFIED.);
#473=B_SPLINE_CURVE_WITH_KNOTS('',3,(#19572,#19573,#19574,#19575,#19576,
#19577,#19578,#19579,#19580,#19581),.UNSPECIFIED.,.F.,.F.,(4,1,1,1,1,1,
1,4),(166.504410640259,166.909758478983,167.909116612549,168.908474746115,
169.907832879681,170.907191013247,171.906549146813,172.787595947439),
 .UNSPECIFIED.);
#474=B_SPLINE_CURVE_WITH_KNOTS('',3,(#19582,#19583,#19584,#19585,#19586,
#19587,#19588,#19589,#19590,#19591),.UNSPECIFIED.,.F.,.F.,(4,1,1,1,1,1,
1,4),(166.50441064026,166.880302393652,167.879660527218,168.879018660784,
169.87837679435,170.877734927916,171.877093061483,172.787595947439),
 .UNSPECIFIED.);
#475=B_SPLINE_CURVE_WITH_KNOTS('',3,(#19596,#19597,#19598,#19599,#19600,
#19601,#19602,#19603,#19604,#19605),.UNSPECIFIED.,.F.,.F.,(4,1,1,1,1,1,
1,4),(160.22122533308,160.913609677586,161.912967811152,162.912325944718,
163.911684078284,164.91104221185,165.910400345416,166.504410640259),
 .UNSPECIFIED.);
#476=B_SPLINE_CURVE_WITH_KNOTS('',3,(#19606,#19607,#19608,#19609,#19610,
#19611,#19612,#19613,#19614,#19615),.UNSPECIFIED.,.F.,.F.,(4,1,1,1,1,1,
1,4),(160.22122533308,160.884153592256,161.883511725822,162.882869859388,
163.882227992954,164.88158612652,165.880944260086,166.50441064026),
 .UNSPECIFIED.);
#477=B_SPLINE_CURVE_WITH_KNOTS('',3,(#19620,#19621,#19622,#19623,#19624,
#19625,#19626,#19627,#19628,#19629),.UNSPECIFIED.,.F.,.F.,(4,1,1,1,1,1,
1,4),(153.9380400259,154.91746087619,155.916819009756,156.916177143322,
157.915535276888,158.914893410454,159.91425154402,160.22122533308),
 .UNSPECIFIED.);
#478=B_SPLINE_CURVE_WITH_KNOTS('',3,(#19630,#19631,#19632,#19633,#19634,
#19635,#19636,#19637,#19638,#19639),.UNSPECIFIED.,.F.,.F.,(4,1,1,1,1,1,
1,4),(153.938040025901,154.88800479086,155.887362924426,156.886721057992,
157.886079191558,158.885437325124,159.88479545869,160.22122533308),
 .UNSPECIFIED.);
#479=B_SPLINE_CURVE_WITH_KNOTS('',3,(#19644,#19645,#19646,#19647,#19648,
#19649,#19650,#19651,#19652,#19653,#19654),.UNSPECIFIED.,.F.,.F.,(4,1,1,
1,1,1,1,1,4),(147.654854718721,147.921953941228,148.921312074794,149.92067020836,
150.920028341926,151.919386475492,152.918744609058,153.918102742624,153.9380400259),
 .UNSPECIFIED.);
#480=B_SPLINE_CURVE_WITH_KNOTS('',3,(#19655,#19656,#19657,#19658,#19659,
#19660,#19661,#19662,#19663,#19664,#19665),.UNSPECIFIED.,.F.,.F.,(4,1,1,
1,1,1,1,1,4),(147.654854718721,147.892497855897,148.891855989463,149.891214123029,
150.890572256596,151.889930390162,152.889288523728,153.888646657294,153.938040025901),
 .UNSPECIFIED.);
#481=B_SPLINE_CURVE_WITH_KNOTS('',3,(#19670,#19671,#19672,#19673,#19674,
#19675,#19676,#19677,#19678,#19679),.UNSPECIFIED.,.F.,.F.,(4,1,1,1,1,1,
1,4),(141.371669411541,141.925805139831,142.925163273397,143.924521406963,
144.92387954053,145.923237674096,146.922595807662,147.654854718721),
 .UNSPECIFIED.);
#482=B_SPLINE_CURVE_WITH_KNOTS('',3,(#19680,#19681,#19682,#19683,#19684,
#19685,#19686,#19687,#19688,#19689),.UNSPECIFIED.,.F.,.F.,(4,1,1,1,1,1,
1,4),(141.371669411542,141.896349054501,142.895707188067,143.895065321633,
144.894423455199,145.893781588765,146.893139722331,147.654854718721),
 .UNSPECIFIED.);
#483=B_SPLINE_CURVE_WITH_KNOTS('',3,(#19694,#19695,#19696,#19697,#19698,
#19699,#19700,#19701,#19702,#19703),.UNSPECIFIED.,.F.,.F.,(4,1,1,1,1,1,
1,4),(135.088484104362,135.929656338435,136.929014472001,137.928372605567,
138.927730739133,139.927088872699,140.926447006265,141.371669411541),
 .UNSPECIFIED.);
#484=B_SPLINE_CURVE_WITH_KNOTS('',3,(#19704,#19705,#19706,#19707,#19708,
#19709,#19710,#19711,#19712,#19713),.UNSPECIFIED.,.F.,.F.,(4,1,1,1,1,1,
1,4),(135.088484104362,135.900200253105,136.899558386671,137.898916520237,
138.898274653803,139.897632787369,140.896990920935,141.371669411542),
 .UNSPECIFIED.);
#485=B_SPLINE_CURVE_WITH_KNOTS('',3,(#19718,#19719,#19720,#19721,#19722,
#19723,#19724,#19725,#19726,#19727,#19728),.UNSPECIFIED.,.F.,.F.,(4,1,1,
1,1,1,1,1,4),(128.805298797182,128.934149403473,129.933507537039,130.932865670605,
131.932223804171,132.931581937737,133.930940071303,134.930298204869,135.088484104362),
 .UNSPECIFIED.);
#486=B_SPLINE_CURVE_WITH_KNOTS('',3,(#19729,#19730,#19731,#19732,#19733,
#19734,#19735,#19736,#19737,#19738,#19739),.UNSPECIFIED.,.F.,.F.,(4,1,1,
1,1,1,1,1,4),(128.805298797182,128.904693318142,129.904051451709,130.903409585275,
131.902767718841,132.902125852407,133.901483985973,134.900842119539,135.088484104362),
 .UNSPECIFIED.);
#487=B_SPLINE_CURVE_WITH_KNOTS('',3,(#19744,#19745,#19746,#19747,#19748,
#19749,#19750,#19751,#19752,#19753),.UNSPECIFIED.,.F.,.F.,(4,1,1,1,1,1,
1,4),(122.522113490002,122.938000602077,123.937358735643,124.936716869209,
125.936075002775,126.935433136341,127.934791269907,128.805298797182),
 .UNSPECIFIED.);
#488=B_SPLINE_CURVE_WITH_KNOTS('',3,(#19754,#19755,#19756,#19757,#19758,
#19759,#19760,#19761,#19762,#19763),.UNSPECIFIED.,.F.,.F.,(4,1,1,1,1,1,
1,4),(122.522113490003,122.908544516746,123.907902650312,124.907260783878,
125.906618917444,126.90597705101,127.905335184576,128.805298797182),
 .UNSPECIFIED.);
#489=B_SPLINE_CURVE_WITH_KNOTS('',3,(#19768,#19769,#19770,#19771,#19772,
#19773,#19774,#19775,#19776,#19777),.UNSPECIFIED.,.F.,.F.,(4,1,1,1,1,1,
1,4),(116.238928182823,116.94185180068,117.941209934246,118.940568067812,
119.939926201378,120.939284334944,121.93864246851,122.522113490002),
 .UNSPECIFIED.);
#490=B_SPLINE_CURVE_WITH_KNOTS('',3,(#19778,#19779,#19780,#19781,#19782,
#19783,#19784,#19785,#19786,#19787),.UNSPECIFIED.,.F.,.F.,(4,1,1,1,1,1,
1,4),(116.238928182823,116.91239571535,117.911753848916,118.911111982482,
119.910470116048,120.909828249614,121.90918638318,122.522113490003),
 .UNSPECIFIED.);
#491=B_SPLINE_CURVE_WITH_KNOTS('',3,(#19792,#19793,#19794,#19795,#19796,
#19797,#19798,#19799,#19800,#19801),.UNSPECIFIED.,.F.,.F.,(4,1,1,1,1,1,
1,4),(109.955742875643,110.945702999284,111.94506113285,112.944419266416,
113.943777399982,114.943135533548,115.942493667114,116.238928182823),
 .UNSPECIFIED.);
#492=B_SPLINE_CURVE_WITH_KNOTS('',3,(#19802,#19803,#19804,#19805,#19806,
#19807,#19808,#19809,#19810,#19811),.UNSPECIFIED.,.F.,.F.,(4,1,1,1,1,1,
1,4),(109.955742875644,110.916246913954,111.91560504752,112.914963181086,
113.914321314652,114.913679448218,115.913037581784,116.238928182823),
 .UNSPECIFIED.);
#493=B_SPLINE_CURVE_WITH_KNOTS('',3,(#19816,#19817,#19818,#19819,#19820,
#19821,#19822,#19823,#19824,#19825,#19826),.UNSPECIFIED.,.F.,.F.,(4,1,1,
1,1,1,1,1,4),(103.672557568464,103.950196064322,104.949554197888,105.948912331454,
106.94827046502,107.947628598586,108.946986732152,109.946344865718,109.955742875643),
 .UNSPECIFIED.);
#494=B_SPLINE_CURVE_WITH_KNOTS('',3,(#19827,#19828,#19829,#19830,#19831,
#19832,#19833,#19834,#19835,#19836,#19837),.UNSPECIFIED.,.F.,.F.,(4,1,1,
1,1,1,1,1,4),(103.672557568464,103.920739978991,104.920098112557,105.919456246123,
106.918814379689,107.918172513255,108.917530646822,109.916888780388,109.955742875644),
 .UNSPECIFIED.);
#495=B_SPLINE_CURVE_WITH_KNOTS('',3,(#19842,#19843,#19844,#19845,#19846,
#19847,#19848,#19849,#19850,#19851),.UNSPECIFIED.,.F.,.F.,(4,1,1,1,1,1,
1,4),(97.3893722612841,97.9540472629253,98.9534053964914,99.9527635300574,
100.952121663623,101.95147979719,102.950837930756,103.672557568464),
 .UNSPECIFIED.);
#496=B_SPLINE_CURVE_WITH_KNOTS('',3,(#19852,#19853,#19854,#19855,#19856,
#19857,#19858,#19859,#19860,#19861),.UNSPECIFIED.,.F.,.F.,(4,1,1,1,1,1,
1,4),(97.3893722612845,97.924591177595,98.9239493111611,99.9233074447271,
100.922665578293,101.922023711859,102.921381845425,103.672557568464),
 .UNSPECIFIED.);
#497=B_SPLINE_CURVE_WITH_KNOTS('',3,(#19866,#19867,#19868,#19869,#19870,
#19871,#19872,#19873,#19874,#19875),.UNSPECIFIED.,.F.,.F.,(4,1,1,1,1,1,
1,4),(91.1061869541045,91.9578984615291,92.9572565950951,93.9566147286612,
94.9559728622272,95.9553309957932,96.9546891293593,97.3893722612841),
 .UNSPECIFIED.);
#498=B_SPLINE_CURVE_WITH_KNOTS('',3,(#19876,#19877,#19878,#19879,#19880,
#19881,#19882,#19883,#19884,#19885),.UNSPECIFIED.,.F.,.F.,(4,1,1,1,1,1,
1,4),(91.1061869541048,91.9284423761987,92.9278005097648,93.9271586433308,
94.9265167768969,95.9258749104629,96.925233044029,97.3893722612845),
 .UNSPECIFIED.);
#499=B_SPLINE_CURVE_WITH_KNOTS('',3,(#19890,#19891,#19892,#19893,#19894,
#19895,#19896,#19897,#19898,#19899,#19900),.UNSPECIFIED.,.F.,.F.,(4,1,1,
1,1,1,1,1,4),(84.8230016469249,84.9623915265667,85.9617496601328,86.9611077936988,
87.9604659272649,88.9598240608309,89.959182194397,90.958540327963,91.1061869541045),
 .UNSPECIFIED.);
#500=B_SPLINE_CURVE_WITH_KNOTS('',3,(#19901,#19902,#19903,#19904,#19905,
#19906,#19907,#19908,#19909,#19910,#19911),.UNSPECIFIED.,.F.,.F.,(4,1,1,
1,1,1,1,1,4),(84.8230016469253,84.9329354412364,85.9322935748025,86.9316517083685,
87.9310098419346,88.9303679755006,89.9297261090666,90.9290842426327,91.1061869541048),
 .UNSPECIFIED.);
#501=B_SPLINE_CURVE_WITH_KNOTS('',3,(#19916,#19917,#19918,#19919,#19920,
#19921,#19922,#19923,#19924,#19925),.UNSPECIFIED.,.F.,.F.,(4,1,1,1,1,1,
1,4),(78.5398163397454,78.9662427251705,79.9656008587365,80.9649589923026,
81.9643171258686,82.9636752594347,83.9630333930007,84.8230016469249),
 .UNSPECIFIED.);
#502=B_SPLINE_CURVE_WITH_KNOTS('',3,(#19926,#19927,#19928,#19929,#19930,
#19931,#19932,#19933,#19934,#19935),.UNSPECIFIED.,.F.,.F.,(4,1,1,1,1,1,
1,4),(78.5398163397457,78.9367866398401,79.9361447734062,80.9355029069722,
81.9348610405383,82.9342191741043,83.9335773076704,84.8230016469253),
 .UNSPECIFIED.);
#503=B_SPLINE_CURVE_WITH_KNOTS('',3,(#19940,#19941,#19942,#19943,#19944,
#19945,#19946,#19947,#19948,#19949),.UNSPECIFIED.,.F.,.F.,(4,1,1,1,1,1,
1,4),(72.2566310325658,72.9700939237742,73.9694520573402,74.9688101909063,
75.9681683244723,76.9675264580384,77.9668845916044,78.5398163397454),
 .UNSPECIFIED.);
#504=B_SPLINE_CURVE_WITH_KNOTS('',3,(#19950,#19951,#19952,#19953,#19954,
#19955,#19956,#19957,#19958,#19959),.UNSPECIFIED.,.F.,.F.,(4,1,1,1,1,1,
1,4),(72.2566310325661,72.9406378384438,73.9399959720099,74.9393541055759,
75.938712239142,76.938070372708,77.9374285062741,78.5398163397457),
 .UNSPECIFIED.);
#505=B_SPLINE_CURVE_WITH_KNOTS('',3,(#19964,#19965,#19966,#19967,#19968,
#19969,#19970,#19971,#19972,#19973,#19974),.UNSPECIFIED.,.F.,.F.,(4,1,1,
1,1,1,1,1,4),(65.9734457253862,65.9745869888119,66.9739451223779,67.9733032559439,
68.97266138951,69.972019523076,70.9713776566421,71.9707357902081,72.2566310325658),
 .UNSPECIFIED.);
#506=B_SPLINE_CURVE_WITH_KNOTS('',3,(#19975,#19976,#19977,#19978,#19979,
#19980,#19981,#19982,#19983,#19984),.UNSPECIFIED.,.F.,.F.,(4,1,1,1,1,1,
1,4),(65.9734457253865,66.9444890370476,67.9438471706136,68.9432053041797,
69.9425634377457,70.9419215713118,71.9412797048778,72.2566310325661),
 .UNSPECIFIED.);
#507=B_SPLINE_CURVE_WITH_KNOTS('',3,(#19989,#19990,#19991,#19992,#19993,
#19994,#19995,#19996,#19997,#19998,#19999,#20000),.UNSPECIFIED.,.F.,.F.,
(4,1,1,1,1,1,1,1,1,4),(59.6902604182066,59.9784381874156,60.4781172541986,
60.9777963209816,61.4774753877646,61.9771544545477,62.9765125881137,63.9758707216798,
64.9752288552458,65.9734457253862),.UNSPECIFIED.);
#508=B_SPLINE_CURVE_WITH_KNOTS('',3,(#20001,#20002,#20003,#20004,#20005,
#20006,#20007,#20008,#20009,#20010,#20011),.UNSPECIFIED.,.F.,.F.,(4,1,1,
1,1,1,1,1,4),(59.6902604182069,59.9489821020852,60.9483402356513,61.9476983692173,
62.9470565027834,63.9464146363494,64.9457727699155,65.9451309034815,65.9734457253865),
 .UNSPECIFIED.);
#509=B_SPLINE_CURVE_WITH_KNOTS('',3,(#20016,#20017,#20018,#20019,#20020,
#20021,#20022,#20023,#20024,#20025,#20026,#20027,#20028,#20029,#20030,#20031,
#20032),.UNSPECIFIED.,.F.,.F.,(4,1,1,1,1,1,1,1,1,1,1,1,1,1,4),(53.407075111027,
53.4826103192363,53.9822893860193,54.4819684528023,54.9816475195853,55.4813265863684,
55.9810056531514,56.4806847199344,56.9803637867174,57.4800428535005,57.9797219202835,
58.4794009870665,58.9790800538495,59.4787591206325,59.6902604182066),
 .UNSPECIFIED.);
#510=B_SPLINE_CURVE_WITH_KNOTS('',3,(#20033,#20034,#20035,#20036,#20037,
#20038,#20039,#20040,#20041,#20042,#20043,#20044,#20045,#20046,#20047,#20048),
 .UNSPECIFIED.,.F.,.F.,(4,1,1,1,1,1,1,1,1,1,1,1,1,4),(53.4070751110273,
53.4531542339059,53.9528333006889,54.452512367472,54.952191434255,55.451870501038,
55.951549567821,56.4512286346041,56.9509077013871,57.4505867681701,57.9502658349531,
58.4499449017362,58.9496239685192,59.6902604182069),.UNSPECIFIED.);
#511=B_SPLINE_CURVE_WITH_KNOTS('',3,(#20053,#20054,#20055,#20056,#20057,
#20058,#20059,#20060,#20061,#20062,#20063,#20064,#20065,#20066,#20067,#20068),
 .UNSPECIFIED.,.F.,.F.,(4,1,1,1,1,1,1,1,1,1,1,1,1,4),(47.1238898038474,
47.48646151784,47.986140584623,48.485819651406,48.9854987181891,49.4851777849721,
49.9848568517551,50.4845359185381,50.9842149853212,51.4838940521042,51.9835731188872,
52.4832521856702,52.9829312524532,53.407075111027),.UNSPECIFIED.);
#512=B_SPLINE_CURVE_WITH_KNOTS('',3,(#20069,#20070,#20071,#20072,#20073,
#20074,#20075,#20076,#20077,#20078,#20079,#20080,#20081,#20082,#20083,#20084),
 .UNSPECIFIED.,.F.,.F.,(4,1,1,1,1,1,1,1,1,1,1,1,1,4),(47.1238898038477,
47.4570054325096,47.9566844992927,48.4563635660757,48.9560426328587,49.4557216996417,
49.9554007664248,50.4550798332078,50.9547588999908,51.4544379667738,51.9541170335568,
52.4537961003399,52.9534751671229,53.4070751110273),.UNSPECIFIED.);
#513=B_SPLINE_CURVE_WITH_KNOTS('',3,(#20089,#20090,#20091,#20092,#20093,
#20094,#20095,#20096,#20097,#20098,#20099,#20100,#20101,#20102,#20103,#20104,
#20105),.UNSPECIFIED.,.F.,.F.,(4,1,1,1,1,1,1,1,1,1,1,1,1,1,4),(40.8407044966678,
40.9906336496607,41.4903127164437,41.9899917832267,42.4896708500098,42.9893499167928,
43.4890289835758,43.9887080503588,44.4883871171419,44.9880661839249,45.4877452507079,
45.9874243174909,46.4871033842739,46.986782451057,47.1238898038474),
 .UNSPECIFIED.);
#514=B_SPLINE_CURVE_WITH_KNOTS('',3,(#20106,#20107,#20108,#20109,#20110,
#20111,#20112,#20113,#20114,#20115,#20116,#20117,#20118,#20119,#20120,#20121,
#20122),.UNSPECIFIED.,.F.,.F.,(4,1,1,1,1,1,1,1,1,1,1,1,1,1,4),(40.8407044966681,
40.9611775643303,41.4608566311134,41.9605356978964,42.4602147646794,42.9598938314624,
43.4595728982454,43.9592519650285,44.4589310318115,44.9586100985945,45.4582891653775,
45.9579682321606,46.4576472989436,46.9573263657266,47.1238898038477),
 .UNSPECIFIED.);
#515=B_SPLINE_CURVE_WITH_KNOTS('',3,(#20127,#20128,#20129,#20130,#20131,
#20132,#20133,#20134,#20135,#20136,#20137,#20138,#20139,#20140,#20141,#20142),
 .UNSPECIFIED.,.F.,.F.,(4,1,1,1,1,1,1,1,1,1,1,1,1,4),(34.5575191894882,
34.9944848482644,35.4941639150474,35.9938429818305,36.4935220486135,36.9932011153965,
37.4928801821795,37.9925592489626,38.4922383157456,38.9919173825286,39.4915964493116,
39.9912755160946,40.4909545828777,40.8407044966678),.UNSPECIFIED.);
#516=B_SPLINE_CURVE_WITH_KNOTS('',3,(#20143,#20144,#20145,#20146,#20147,
#20148,#20149,#20150,#20151,#20152,#20153,#20154,#20155,#20156,#20157,#20158),
 .UNSPECIFIED.,.F.,.F.,(4,1,1,1,1,1,1,1,1,1,1,1,1,4),(34.5575191894886,
34.965028762934,35.4647078297171,35.9643868965001,36.4640659632831,36.9637450300661,
37.4634240968492,37.9631031636322,38.4627822304152,38.9624612971982,39.4621403639813,
39.9618194307643,40.4614984975473,40.8407044966681),.UNSPECIFIED.);
#517=B_SPLINE_CURVE_WITH_KNOTS('',3,(#20163,#20164,#20165,#20166,#20167,
#20168,#20169,#20170,#20171,#20172,#20173,#20174,#20175,#20176,#20177,#20178,
#20179),.UNSPECIFIED.,.F.,.F.,(4,1,1,1,1,1,1,1,1,1,1,1,1,1,4),(28.2743338823086,
28.4986569800851,28.9983360468681,29.4980151136512,29.9976941804342,30.4973732472172,
30.9970523140002,31.4967313807832,31.9964104475663,32.4960895143493,32.9957685811323,
33.4954476479153,33.9951267146984,34.4948057814814,34.5575191894882),
 .UNSPECIFIED.);
#518=B_SPLINE_CURVE_WITH_KNOTS('',3,(#20180,#20181,#20182,#20183,#20184,
#20185,#20186,#20187,#20188,#20189,#20190,#20191,#20192,#20193,#20194,#20195,
#20196),.UNSPECIFIED.,.F.,.F.,(4,1,1,1,1,1,1,1,1,1,1,1,1,1,4),(28.2743338823089,
28.4692008947547,28.9688799615378,29.4685590283208,29.9682380951038,30.4679171618868,
30.9675962286699,31.4672752954529,31.9669543622359,32.4666334290189,32.966312495802,
33.465991562585,33.965670629368,34.465349696151,34.5575191894886),
 .UNSPECIFIED.);
#519=B_SPLINE_CURVE_WITH_KNOTS('',3,(#20201,#20202,#20203,#20204,#20205,
#20206,#20207,#20208,#20209,#20210,#20211,#20212,#20213,#20214,#20215,#20216,
#20217),.UNSPECIFIED.,.F.,.F.,(4,1,1,1,1,1,1,1,1,1,1,1,1,1,4),(21.991148575129,
22.0028291119058,22.5025081786888,23.0021872454719,23.5018663122549,24.0015453790379,
24.5012244458209,25.0009035126039,25.500582579387,26.00026164617,26.499940712953,
26.999619779736,27.4992988465191,27.9989779133021,28.2743338823086),
 .UNSPECIFIED.);
#520=B_SPLINE_CURVE_WITH_KNOTS('',3,(#20218,#20219,#20220,#20221,#20222,
#20223,#20224,#20225,#20226,#20227,#20228,#20229,#20230,#20231,#20232,#20233),
 .UNSPECIFIED.,.F.,.F.,(4,1,1,1,1,1,1,1,1,1,1,1,1,4),(21.9911485751294,
22.4730520933585,22.9727311601415,23.4724102269245,23.9720892937075,24.4717683604905,
24.9714474272736,25.4711264940566,25.9708055608396,26.4704846276226,26.9701636944057,
27.4698427611887,27.9695218279717,28.2743338823089),.UNSPECIFIED.);
#521=B_SPLINE_CURVE_WITH_KNOTS('',3,(#20238,#20239,#20240,#20241,#20242,
#20243,#20244,#20245,#20246,#20247,#20248,#20249,#20250,#20251,#20252,#20253),
 .UNSPECIFIED.,.F.,.F.,(4,1,1,1,1,1,1,1,1,1,1,1,1,4),(15.7079632679495,
16.0066803105095,16.5063593772925,17.0060384440756,17.5057175108586,18.0053965776416,
18.5050756444246,19.0047547112077,19.5044337779907,20.0041128447737,20.5037919115567,
21.0034709783398,21.5031500451228,21.991148575129),.UNSPECIFIED.);
#522=B_SPLINE_CURVE_WITH_KNOTS('',3,(#20254,#20255,#20256,#20257,#20258,
#20259,#20260,#20261,#20262,#20263,#20264,#20265,#20266,#20267,#20268,#20269,
#20270),.UNSPECIFIED.,.F.,.F.,(4,1,1,1,1,1,1,1,1,1,1,1,1,1,4),(15.7079632679498,
15.9772242251791,16.4769032919622,16.9765823587452,17.4762614255282,17.9759404923112,
18.4756195590943,18.9752986258773,19.4749776926603,19.9746567594433,20.4743358262264,
20.9740148930094,21.4736939597924,21.9733730265754,21.9911485751294),
 .UNSPECIFIED.);
#523=B_SPLINE_CURVE_WITH_KNOTS('',3,(#22264,#22265,#22266,#22267,#22268,
#22269,#22270,#22271,#22272,#22273,#22274,#22275,#22276,#22277,#22278,#22279,
#22280,#22281,#22282,#22283,#22284,#22285,#22286,#22287,#22288,#22289,#22290,
#22291,#22292,#22293,#22294,#22295,#22296,#22297,#22298,#22299,#22300,#22301,
#22302,#22303),.UNSPECIFIED.,.F.,.F.,(4,3,3,3,3,3,3,3,3,3,3,3,3,4),(-0.53478501993692,
-0.534277081309421,-0.456439695901019,-0.38064245929011,-0.348102919117109,
-0.328886681298388,-0.258595553176405,-0.246742105655551,-0.185056579241663,
-0.163339235199672,-0.143463957830519,-0.0808484674142256,-0.0206857924044652,
0.),.UNSPECIFIED.);
#524=B_SPLINE_CURVE_WITH_KNOTS('',3,(#22304,#22305,#22306,#22307,#22308,
#22309,#22310,#22311,#22312,#22313,#22314,#22315,#22316,#22317,#22318,#22319,
#22320,#22321,#22322,#22323,#22324,#22325,#22326,#22327,#22328),
 .UNSPECIFIED.,.F.,.F.,(4,3,3,3,3,3,3,3,4),(390.000549715688,390.249351157541,
390.749030224325,391.248709291108,391.748388357891,392.248067424674,392.747746491457,
393.24742555824,393.746279249921),.UNSPECIFIED.);
#525=B_SPLINE_CURVE_WITH_KNOTS('',3,(#22330,#22331,#22332,#22333,#22334,
#22335,#22336,#22337,#22338,#22339,#22340,#22341,#22342,#22343,#22344,#22345,
#22346,#22347,#22348,#22349,#22350,#22351,#22352,#22353,#22354,#22355,#22356,
#22357,#22358,#22359,#22360,#22361,#22362,#22363,#22364,#22365,#22366),
 .UNSPECIFIED.,.F.,.F.,(4,3,3,3,3,3,3,3,3,3,3,3,4),(0.,0.000373494560508806,
0.0620760815771024,0.112839239637108,0.153038169722591,0.175804963675793,
0.247183842626883,0.319084136954533,0.344742425233931,0.363606980156396,
0.439518700737557,0.51795432283266,0.534785019937482),.UNSPECIFIED.);
#526=B_SPLINE_CURVE_WITH_KNOTS('',3,(#22367,#22368,#22369,#22370,#22371,
#22372,#22373,#22374,#22375,#22376,#22377,#22378,#22379,#22380,#22381),
 .UNSPECIFIED.,.F.,.F.,(4,1,1,1,1,1,1,1,1,1,1,1,4),(9.98190079888485,10.4807544905659,
10.9804335573489,11.4801126241319,11.979791690915,12.479470757698,12.979149824481,
13.478828891264,13.9785079580471,14.4781870248301,14.9778660916131,15.4775451583961,
15.7079632679498),.UNSPECIFIED.);
#527=B_SPLINE_CURVE_WITH_KNOTS('',3,(#22385,#22386,#22387,#22388,#22389,
#22390,#22391,#22392,#22393,#22394,#22395),.UNSPECIFIED.,.F.,.F.,(4,1,1,
1,1,1,1,1,4),(12.0092477762453,12.5089268430284,13.0086059098114,13.5082849765944,
14.0079640433774,14.5076431101605,15.0073221769435,15.5070012437265,15.7079632679495),
 .UNSPECIFIED.);
#528=B_SPLINE_CURVE_WITH_KNOTS('',3,(#24389,#24390,#24391,#24392,#24393,
#24394,#24395,#24396,#24397,#24398,#24399,#24400,#24401,#24402,#24403,#24404,
#24405,#24406,#24407,#24408,#24409,#24410,#24411,#24412,#24413,#24414,#24415,
#24416,#24417,#24418,#24419,#24420,#24421,#24422,#24423,#24424,#24425,#24426,
#24427,#24428),.UNSPECIFIED.,.F.,.F.,(4,3,3,3,3,3,3,3,3,3,3,3,3,4),(-0.539097184344981,
-0.538720824057998,-0.476544551511477,-0.429912347101587,-0.401091234701428,
-0.381803774975435,-0.313681369269712,-0.290015733871917,-0.24230273417063,
-0.214804629165427,-0.192593514291413,-0.116696500404398,-0.0381316372362206,
0.),.UNSPECIFIED.);
#529=B_SPLINE_CURVE_WITH_KNOTS('',3,(#24429,#24430,#24431,#24432,#24433,
#24434,#24435,#24436,#24437,#24438,#24439,#24440,#24441,#24442,#24443,#24444,
#24445,#24446,#24447,#24448,#24449,#24450,#24451,#24452,#24453,#24454,#24455,
#24456,#24457,#24458,#24459,#24460,#24461,#24462,#24463,#24464,#24465),
 .UNSPECIFIED.,.F.,.F.,(4,3,3,3,3,3,3,3,3,3,3,3,4),(0.,0.000511892384038064,
0.078754853834616,0.155070466132989,0.20164291816609,0.227017770490094,
0.290460834304131,0.352619921814331,0.383703668213755,0.403796492255862,
0.466621120797767,0.52704524650008,0.539097184344933),.UNSPECIFIED.);
#530=B_SPLINE_CURVE_WITH_KNOTS('',3,(#24466,#24467,#24468,#24469,#24470,
#24471,#24472,#24473,#24474,#24475),.UNSPECIFIED.,.F.,.F.,(4,3,3,4),(-394.746462758588,
-394.246783691805,-393.747104625022,-393.256204536838),.UNSPECIFIED.);
#606=SHAPE_REPRESENTATION_RELATIONSHIP('SRR','None',#25217,#634);
#634=ADVANCED_BREP_SHAPE_REPRESENTATION('',(#703),#25064);
#670=STYLED_ITEM('',(#25446),#703);
#703=MANIFOLD_SOLID_BREP('Body1',#8081);
#799=FACE_BOUND('',#1958,.T.);
#800=FACE_BOUND('',#1961,.T.);
#801=FACE_BOUND('',#1964,.T.);
#953=PLANE('',#9024);
#954=PLANE('',#9025);
#955=PLANE('',#9027);
#956=PLANE('',#9028);
#957=PLANE('',#9029);
#958=PLANE('',#9034);
#959=PLANE('',#9035);
#960=PLANE('',#9040);
#961=PLANE('',#9042);
#1266=FACE_OUTER_BOUND('',#1823,.T.);
#1267=FACE_OUTER_BOUND('',#1824,.T.);
#1268=FACE_OUTER_BOUND('',#1825,.T.);
#1269=FACE_OUTER_BOUND('',#1826,.T.);
#1270=FACE_OUTER_BOUND('',#1827,.T.);
#1271=FACE_OUTER_BOUND('',#1828,.T.);
#1272=FACE_OUTER_BOUND('',#1829,.T.);
#1273=FACE_OUTER_BOUND('',#1830,.T.);
#1274=FACE_OUTER_BOUND('',#1831,.T.);
#1275=FACE_OUTER_BOUND('',#1832,.T.);
#1276=FACE_OUTER_BOUND('',#1833,.T.);
#1277=FACE_OUTER_BOUND('',#1834,.T.);
#1278=FACE_OUTER_BOUND('',#1835,.T.);
#1279=FACE_OUTER_BOUND('',#1836,.T.);
#1280=FACE_OUTER_BOUND('',#1837,.T.);
#1281=FACE_OUTER_BOUND('',#1838,.T.);
#1282=FACE_OUTER_BOUND('',#1839,.T.);
#1283=FACE_OUTER_BOUND('',#1840,.T.);
#1284=FACE_OUTER_BOUND('',#1841,.T.);
#1285=FACE_OUTER_BOUND('',#1842,.T.);
#1286=FACE_OUTER_BOUND('',#1843,.T.);
#1287=FACE_OUTER_BOUND('',#1844,.T.);
#1288=FACE_OUTER_BOUND('',#1845,.T.);
#1289=FACE_OUTER_BOUND('',#1846,.T.);
#1290=FACE_OUTER_BOUND('',#1847,.T.);
#1291=FACE_OUTER_BOUND('',#1848,.T.);
#1292=FACE_OUTER_BOUND('',#1849,.T.);
#1293=FACE_OUTER_BOUND('',#1850,.T.);
#1294=FACE_OUTER_BOUND('',#1851,.T.);
#1295=FACE_OUTER_BOUND('',#1852,.T.);
#1296=FACE_OUTER_BOUND('',#1853,.T.);
#1297=FACE_OUTER_BOUND('',#1854,.T.);
#1298=FACE_OUTER_BOUND('',#1855,.T.);
#1299=FACE_OUTER_BOUND('',#1856,.T.);
#1300=FACE_OUTER_BOUND('',#1857,.T.);
#1301=FACE_OUTER_BOUND('',#1858,.T.);
#1302=FACE_OUTER_BOUND('',#1859,.T.);
#1303=FACE_OUTER_BOUND('',#1860,.T.);
#1304=FACE_OUTER_BOUND('',#1861,.T.);
#1305=FACE_OUTER_BOUND('',#1862,.T.);
#1306=FACE_OUTER_BOUND('',#1863,.T.);
#1307=FACE_OUTER_BOUND('',#1864,.T.);
#1308=FACE_OUTER_BOUND('',#1865,.T.);
#1309=FACE_OUTER_BOUND('',#1866,.T.);
#1310=FACE_OUTER_BOUND('',#1867,.T.);
#1311=FACE_OUTER_BOUND('',#1868,.T.);
#1312=FACE_OUTER_BOUND('',#1869,.T.);
#1313=FACE_OUTER_BOUND('',#1870,.T.);
#1314=FACE_OUTER_BOUND('',#1871,.T.);
#1315=FACE_OUTER_BOUND('',#1872,.T.);
#1316=FACE_OUTER_BOUND('',#1873,.T.);
#1317=FACE_OUTER_BOUND('',#1874,.T.);
#1318=FACE_OUTER_BOUND('',#1875,.T.);
#1319=FACE_OUTER_BOUND('',#1876,.T.);
#1320=FACE_OUTER_BOUND('',#1877,.T.);
#1321=FACE_OUTER_BOUND('',#1878,.T.);
#1322=FACE_OUTER_BOUND('',#1879,.T.);
#1323=FACE_OUTER_BOUND('',#1880,.T.);
#1324=FACE_OUTER_BOUND('',#1881,.T.);
#1325=FACE_OUTER_BOUND('',#1882,.T.);
#1326=FACE_OUTER_BOUND('',#1883,.T.);
#1327=FACE_OUTER_BOUND('',#1884,.T.);
#1328=FACE_OUTER_BOUND('',#1885,.T.);
#1329=FACE_OUTER_BOUND('',#1886,.T.);
#1330=FACE_OUTER_BOUND('',#1887,.T.);
#1331=FACE_OUTER_BOUND('',#1888,.T.);
#1332=FACE_OUTER_BOUND('',#1889,.T.);
#1333=FACE_OUTER_BOUND('',#1890,.T.);
#1334=FACE_OUTER_BOUND('',#1891,.T.);
#1335=FACE_OUTER_BOUND('',#1892,.T.);
#1336=FACE_OUTER_BOUND('',#1893,.T.);
#1337=FACE_OUTER_BOUND('',#1894,.T.);
#1338=FACE_OUTER_BOUND('',#1895,.T.);
#1339=FACE_OUTER_BOUND('',#1896,.T.);
#1340=FACE_OUTER_BOUND('',#1897,.T.);
#1341=FACE_OUTER_BOUND('',#1898,.T.);
#1342=FACE_OUTER_BOUND('',#1899,.T.);
#1343=FACE_OUTER_BOUND('',#1900,.T.);
#1344=FACE_OUTER_BOUND('',#1901,.T.);
#1345=FACE_OUTER_BOUND('',#1902,.T.);
#1346=FACE_OUTER_BOUND('',#1903,.T.);
#1347=FACE_OUTER_BOUND('',#1904,.T.);
#1348=FACE_OUTER_BOUND('',#1905,.T.);
#1349=FACE_OUTER_BOUND('',#1906,.T.);
#1350=FACE_OUTER_BOUND('',#1907,.T.);
#1351=FACE_OUTER_BOUND('',#1908,.T.);
#1352=FACE_OUTER_BOUND('',#1909,.T.);
#1353=FACE_OUTER_BOUND('',#1910,.T.);
#1354=FACE_OUTER_BOUND('',#1911,.T.);
#1355=FACE_OUTER_BOUND('',#1912,.T.);
#1356=FACE_OUTER_BOUND('',#1913,.T.);
#1357=FACE_OUTER_BOUND('',#1914,.T.);
#1358=FACE_OUTER_BOUND('',#1915,.T.);
#1359=FACE_OUTER_BOUND('',#1916,.T.);
#1360=FACE_OUTER_BOUND('',#1917,.T.);
#1361=FACE_OUTER_BOUND('',#1918,.T.);
#1362=FACE_OUTER_BOUND('',#1919,.T.);
#1363=FACE_OUTER_BOUND('',#1920,.T.);
#1364=FACE_OUTER_BOUND('',#1921,.T.);
#1365=FACE_OUTER_BOUND('',#1922,.T.);
#1366=FACE_OUTER_BOUND('',#1923,.T.);
#1367=FACE_OUTER_BOUND('',#1924,.T.);
#1368=FACE_OUTER_BOUND('',#1925,.T.);
#1369=FACE_OUTER_BOUND('',#1926,.T.);
#1370=FACE_OUTER_BOUND('',#1927,.T.);
#1371=FACE_OUTER_BOUND('',#1928,.T.);
#1372=FACE_OUTER_BOUND('',#1929,.T.);
#1373=FACE_OUTER_BOUND('',#1930,.T.);
#1374=FACE_OUTER_BOUND('',#1931,.T.);
#1375=FACE_OUTER_BOUND('',#1932,.T.);
#1376=FACE_OUTER_BOUND('',#1933,.T.);
#1377=FACE_OUTER_BOUND('',#1934,.T.);
#1378=FACE_OUTER_BOUND('',#1935,.T.);
#1379=FACE_OUTER_BOUND('',#1936,.T.);
#1380=FACE_OUTER_BOUND('',#1937,.T.);
#1381=FACE_OUTER_BOUND('',#1938,.T.);
#1382=FACE_OUTER_BOUND('',#1939,.T.);
#1383=FACE_OUTER_BOUND('',#1940,.T.);
#1384=FACE_OUTER_BOUND('',#1941,.T.);
#1385=FACE_OUTER_BOUND('',#1942,.T.);
#1386=FACE_OUTER_BOUND('',#1943,.T.);
#1387=FACE_OUTER_BOUND('',#1944,.T.);
#1388=FACE_OUTER_BOUND('',#1945,.T.);
#1389=FACE_OUTER_BOUND('',#1946,.T.);
#1390=FACE_OUTER_BOUND('',#1947,.T.);
#1391=FACE_OUTER_BOUND('',#1948,.T.);
#1392=FACE_OUTER_BOUND('',#1949,.T.);
#1393=FACE_OUTER_BOUND('',#1950,.T.);
#1394=FACE_OUTER_BOUND('',#1951,.T.);
#1395=FACE_OUTER_BOUND('',#1952,.T.);
#1396=FACE_OUTER_BOUND('',#1953,.T.);
#1397=FACE_OUTER_BOUND('',#1954,.T.);
#1398=FACE_OUTER_BOUND('',#1955,.T.);
#1399=FACE_OUTER_BOUND('',#1956,.T.);
#1400=FACE_OUTER_BOUND('',#1957,.T.);
#1401=FACE_OUTER_BOUND('',#1959,.T.);
#1402=FACE_OUTER_BOUND('',#1960,.T.);
#1403=FACE_OUTER_BOUND('',#1962,.T.);
#1404=FACE_OUTER_BOUND('',#1963,.T.);
#1405=FACE_OUTER_BOUND('',#1965,.T.);
#1406=FACE_OUTER_BOUND('',#1966,.T.);
#1823=EDGE_LOOP('',(#6219,#6220,#6221,#6222));
#1824=EDGE_LOOP('',(#6223,#6224,#6225,#6226));
#1825=EDGE_LOOP('',(#6227,#6228,#6229,#6230));
#1826=EDGE_LOOP('',(#6231,#6232,#6233,#6234));
#1827=EDGE_LOOP('',(#6235,#6236,#6237,#6238));
#1828=EDGE_LOOP('',(#6239,#6240,#6241,#6242));
#1829=EDGE_LOOP('',(#6243,#6244,#6245,#6246));
#1830=EDGE_LOOP('',(#6247,#6248,#6249,#6250));
#1831=EDGE_LOOP('',(#6251,#6252,#6253,#6254));
#1832=EDGE_LOOP('',(#6255,#6256,#6257,#6258));
#1833=EDGE_LOOP('',(#6259,#6260,#6261,#6262));
#1834=EDGE_LOOP('',(#6263,#6264,#6265,#6266));
#1835=EDGE_LOOP('',(#6267,#6268,#6269,#6270));
#1836=EDGE_LOOP('',(#6271,#6272,#6273,#6274));
#1837=EDGE_LOOP('',(#6275,#6276,#6277,#6278));
#1838=EDGE_LOOP('',(#6279,#6280,#6281,#6282));
#1839=EDGE_LOOP('',(#6283,#6284,#6285,#6286));
#1840=EDGE_LOOP('',(#6287,#6288,#6289,#6290));
#1841=EDGE_LOOP('',(#6291,#6292,#6293,#6294));
#1842=EDGE_LOOP('',(#6295,#6296,#6297,#6298));
#1843=EDGE_LOOP('',(#6299,#6300,#6301,#6302));
#1844=EDGE_LOOP('',(#6303,#6304,#6305,#6306));
#1845=EDGE_LOOP('',(#6307,#6308,#6309,#6310));
#1846=EDGE_LOOP('',(#6311,#6312,#6313,#6314));
#1847=EDGE_LOOP('',(#6315,#6316,#6317,#6318));
#1848=EDGE_LOOP('',(#6319,#6320,#6321,#6322));
#1849=EDGE_LOOP('',(#6323,#6324,#6325,#6326));
#1850=EDGE_LOOP('',(#6327,#6328,#6329,#6330));
#1851=EDGE_LOOP('',(#6331,#6332,#6333,#6334));
#1852=EDGE_LOOP('',(#6335,#6336,#6337,#6338));
#1853=EDGE_LOOP('',(#6339,#6340,#6341,#6342));
#1854=EDGE_LOOP('',(#6343,#6344,#6345,#6346));
#1855=EDGE_LOOP('',(#6347,#6348,#6349,#6350));
#1856=EDGE_LOOP('',(#6351,#6352,#6353,#6354));
#1857=EDGE_LOOP('',(#6355,#6356,#6357,#6358));
#1858=EDGE_LOOP('',(#6359,#6360,#6361,#6362));
#1859=EDGE_LOOP('',(#6363,#6364,#6365,#6366));
#1860=EDGE_LOOP('',(#6367,#6368,#6369,#6370));
#1861=EDGE_LOOP('',(#6371,#6372,#6373,#6374));
#1862=EDGE_LOOP('',(#6375,#6376,#6377,#6378));
#1863=EDGE_LOOP('',(#6379,#6380,#6381,#6382));
#1864=EDGE_LOOP('',(#6383,#6384,#6385,#6386));
#1865=EDGE_LOOP('',(#6387,#6388,#6389,#6390));
#1866=EDGE_LOOP('',(#6391,#6392,#6393,#6394));
#1867=EDGE_LOOP('',(#6395,#6396,#6397,#6398));
#1868=EDGE_LOOP('',(#6399,#6400,#6401,#6402));
#1869=EDGE_LOOP('',(#6403,#6404,#6405,#6406));
#1870=EDGE_LOOP('',(#6407,#6408,#6409,#6410));
#1871=EDGE_LOOP('',(#6411,#6412,#6413,#6414));
#1872=EDGE_LOOP('',(#6415,#6416,#6417,#6418));
#1873=EDGE_LOOP('',(#6419,#6420,#6421,#6422));
#1874=EDGE_LOOP('',(#6423,#6424,#6425,#6426));
#1875=EDGE_LOOP('',(#6427,#6428,#6429,#6430));
#1876=EDGE_LOOP('',(#6431,#6432,#6433,#6434));
#1877=EDGE_LOOP('',(#6435,#6436,#6437,#6438));
#1878=EDGE_LOOP('',(#6439,#6440,#6441,#6442));
#1879=EDGE_LOOP('',(#6443,#6444,#6445,#6446));
#1880=EDGE_LOOP('',(#6447,#6448,#6449,#6450));
#1881=EDGE_LOOP('',(#6451,#6452,#6453,#6454));
#1882=EDGE_LOOP('',(#6455,#6456,#6457,#6458));
#1883=EDGE_LOOP('',(#6459,#6460,#6461,#6462));
#1884=EDGE_LOOP('',(#6463,#6464,#6465,#6466));
#1885=EDGE_LOOP('',(#6467,#6468,#6469,#6470));
#1886=EDGE_LOOP('',(#6471,#6472,#6473));
#1887=EDGE_LOOP('',(#6474,#6475,#6476,#6477,#6478));
#1888=EDGE_LOOP('',(#6479,#6480,#6481,#6482));
#1889=EDGE_LOOP('',(#6483,#6484,#6485,#6486));
#1890=EDGE_LOOP('',(#6487,#6488,#6489,#6490));
#1891=EDGE_LOOP('',(#6491,#6492,#6493,#6494));
#1892=EDGE_LOOP('',(#6495,#6496,#6497,#6498));
#1893=EDGE_LOOP('',(#6499,#6500,#6501,#6502));
#1894=EDGE_LOOP('',(#6503,#6504,#6505,#6506));
#1895=EDGE_LOOP('',(#6507,#6508,#6509,#6510));
#1896=EDGE_LOOP('',(#6511,#6512,#6513,#6514));
#1897=EDGE_LOOP('',(#6515,#6516,#6517,#6518));
#1898=EDGE_LOOP('',(#6519,#6520,#6521,#6522));
#1899=EDGE_LOOP('',(#6523,#6524,#6525,#6526));
#1900=EDGE_LOOP('',(#6527,#6528,#6529,#6530));
#1901=EDGE_LOOP('',(#6531,#6532,#6533,#6534));
#1902=EDGE_LOOP('',(#6535,#6536,#6537,#6538));
#1903=EDGE_LOOP('',(#6539,#6540,#6541,#6542));
#1904=EDGE_LOOP('',(#6543,#6544,#6545,#6546));
#1905=EDGE_LOOP('',(#6547,#6548,#6549,#6550));
#1906=EDGE_LOOP('',(#6551,#6552,#6553,#6554));
#1907=EDGE_LOOP('',(#6555,#6556,#6557,#6558));
#1908=EDGE_LOOP('',(#6559,#6560,#6561,#6562));
#1909=EDGE_LOOP('',(#6563,#6564,#6565,#6566));
#1910=EDGE_LOOP('',(#6567,#6568,#6569,#6570));
#1911=EDGE_LOOP('',(#6571,#6572,#6573,#6574));
#1912=EDGE_LOOP('',(#6575,#6576,#6577,#6578));
#1913=EDGE_LOOP('',(#6579,#6580,#6581,#6582));
#1914=EDGE_LOOP('',(#6583,#6584,#6585,#6586));
#1915=EDGE_LOOP('',(#6587,#6588,#6589,#6590));
#1916=EDGE_LOOP('',(#6591,#6592,#6593,#6594));
#1917=EDGE_LOOP('',(#6595,#6596,#6597,#6598));
#1918=EDGE_LOOP('',(#6599,#6600,#6601,#6602));
#1919=EDGE_LOOP('',(#6603,#6604,#6605,#6606));
#1920=EDGE_LOOP('',(#6607,#6608,#6609,#6610));
#1921=EDGE_LOOP('',(#6611,#6612,#6613,#6614));
#1922=EDGE_LOOP('',(#6615,#6616,#6617,#6618));
#1923=EDGE_LOOP('',(#6619,#6620,#6621,#6622));
#1924=EDGE_LOOP('',(#6623,#6624,#6625,#6626));
#1925=EDGE_LOOP('',(#6627,#6628,#6629,#6630));
#1926=EDGE_LOOP('',(#6631,#6632,#6633,#6634));
#1927=EDGE_LOOP('',(#6635,#6636,#6637,#6638));
#1928=EDGE_LOOP('',(#6639,#6640,#6641,#6642));
#1929=EDGE_LOOP('',(#6643,#6644,#6645,#6646));
#1930=EDGE_LOOP('',(#6647,#6648,#6649,#6650));
#1931=EDGE_LOOP('',(#6651,#6652,#6653,#6654));
#1932=EDGE_LOOP('',(#6655,#6656,#6657,#6658));
#1933=EDGE_LOOP('',(#6659,#6660,#6661,#6662));
#1934=EDGE_LOOP('',(#6663,#6664,#6665,#6666));
#1935=EDGE_LOOP('',(#6667,#6668,#6669,#6670));
#1936=EDGE_LOOP('',(#6671,#6672,#6673,#6674));
#1937=EDGE_LOOP('',(#6675,#6676,#6677,#6678));
#1938=EDGE_LOOP('',(#6679,#6680,#6681,#6682));
#1939=EDGE_LOOP('',(#6683,#6684,#6685,#6686));
#1940=EDGE_LOOP('',(#6687,#6688,#6689,#6690));
#1941=EDGE_LOOP('',(#6691,#6692,#6693,#6694));
#1942=EDGE_LOOP('',(#6695,#6696,#6697,#6698));
#1943=EDGE_LOOP('',(#6699,#6700,#6701,#6702));
#1944=EDGE_LOOP('',(#6703,#6704,#6705,#6706));
#1945=EDGE_LOOP('',(#6707,#6708,#6709,#6710));
#1946=EDGE_LOOP('',(#6711,#6712,#6713,#6714));
#1947=EDGE_LOOP('',(#6715,#6716,#6717,#6718));
#1948=EDGE_LOOP('',(#6719,#6720,#6721,#6722));
#1949=EDGE_LOOP('',(#6723,#6724,#6725,#6726,#6727,#6728,#6729,#6730,#6731,
#6732,#6733,#6734,#6735,#6736,#6737,#6738,#6739,#6740,#6741,#6742,#6743,
#6744,#6745,#6746,#6747,#6748,#6749,#6750,#6751,#6752,#6753,#6754,#6755,
#6756,#6757,#6758,#6759,#6760,#6761,#6762,#6763,#6764,#6765,#6766,#6767,
#6768,#6769,#6770,#6771,#6772,#6773,#6774,#6775,#6776,#6777,#6778,#6779,
#6780,#6781,#6782,#6783,#6784,#6785,#6786,#6787,#6788,#6789,#6790,#6791,
#6792,#6793,#6794,#6795,#6796,#6797,#6798,#6799,#6800,#6801,#6802,#6803,
#6804,#6805,#6806,#6807,#6808,#6809,#6810,#6811,#6812,#6813,#6814,#6815,
#6816,#6817,#6818,#6819,#6820,#6821,#6822,#6823,#6824,#6825,#6826,#6827,
#6828,#6829,#6830,#6831,#6832,#6833,#6834,#6835,#6836,#6837,#6838,#6839,
#6840,#6841,#6842,#6843,#6844,#6845,#6846,#6847,#6848,#6849,#6850,#6851));
#1950=EDGE_LOOP('',(#6852,#6853,#6854,#6855));
#1951=EDGE_LOOP('',(#6856,#6857,#6858,#6859,#6860,#6861,#6862,#6863,#6864,
#6865,#6866,#6867,#6868,#6869,#6870,#6871,#6872,#6873,#6874,#6875,#6876,
#6877,#6878,#6879,#6880,#6881,#6882,#6883,#6884,#6885,#6886,#6887,#6888,
#6889,#6890,#6891,#6892,#6893,#6894,#6895,#6896,#6897,#6898,#6899,#6900,
#6901,#6902,#6903,#6904,#6905,#6906,#6907,#6908,#6909,#6910,#6911,#6912,
#6913,#6914,#6915,#6916,#6917,#6918,#6919,#6920,#6921,#6922,#6923,#6924,
#6925,#6926,#6927,#6928,#6929,#6930,#6931,#6932,#6933,#6934,#6935,#6936,
#6937,#6938,#6939,#6940,#6941,#6942,#6943,#6944,#6945,#6946,#6947,#6948,
#6949,#6950,#6951,#6952,#6953,#6954,#6955,#6956,#6957,#6958,#6959,#6960,
#6961,#6962,#6963,#6964,#6965,#6966,#6967,#6968,#6969,#6970,#6971,#6972,
#6973,#6974,#6975,#6976,#6977,#6978,#6979,#6980,#6981,#6982,#6983,#6984,
#6985));
#1952=EDGE_LOOP('',(#6986,#6987,#6988,#6989));
#1953=EDGE_LOOP('',(#6990,#6991,#6992,#6993));
#1954=EDGE_LOOP('',(#6994,#6995,#6996,#6997));
#1955=EDGE_LOOP('',(#6998,#6999,#7000,#7001));
#1956=EDGE_LOOP('',(#7002,#7003,#7004,#7005));
#1957=EDGE_LOOP('',(#7006,#7007,#7008,#7009));
#1958=EDGE_LOOP('',(#7010,#7011,#7012,#7013));
#1959=EDGE_LOOP('',(#7014));
#1960=EDGE_LOOP('',(#7015));
#1961=EDGE_LOOP('',(#7016,#7017,#7018,#7019,#7020));
#1962=EDGE_LOOP('',(#7021,#7022,#7023,#7024));
#1963=EDGE_LOOP('',(#7025));
#1964=EDGE_LOOP('',(#7026));
#1965=EDGE_LOOP('',(#7027,#7028,#7029,#7030));
#1966=EDGE_LOOP('',(#7031,#7032,#7033,#7034));
#2331=LINE('',#14871,#2839);
#2332=LINE('',#14901,#2840);
#2333=LINE('',#14988,#2841);
#2334=LINE('',#15078,#2842);
#2335=LINE('',#15165,#2843);
#2336=LINE('',#15252,#2844);
#2337=LINE('',#15339,#2845);
#2338=LINE('',#15426,#2846);
#2339=LINE('',#15513,#2847);
#2340=LINE('',#15585,#2848);
#2341=LINE('',#15636,#2849);
#2342=LINE('',#15684,#2850);
#2343=LINE('',#15732,#2851);
#2344=LINE('',#15783,#2852);
#2345=LINE('',#15834,#2853);
#2346=LINE('',#15882,#2854);
#2347=LINE('',#15933,#2855);
#2348=LINE('',#15984,#2856);
#2349=LINE('',#16032,#2857);
#2350=LINE('',#16080,#2858);
#2351=LINE('',#16131,#2859);
#2352=LINE('',#16182,#2860);
#2353=LINE('',#16230,#2861);
#2354=LINE('',#16281,#2862);
#2355=LINE('',#16332,#2863);
#2356=LINE('',#16380,#2864);
#2357=LINE('',#16428,#2865);
#2358=LINE('',#16479,#2866);
#2359=LINE('',#16530,#2867);
#2360=LINE('',#16578,#2868);
#2361=LINE('',#16629,#2869);
#2362=LINE('',#16680,#2870);
#2363=LINE('',#16728,#2871);
#2364=LINE('',#16776,#2872);
#2365=LINE('',#16827,#2873);
#2366=LINE('',#16878,#2874);
#2367=LINE('',#16926,#2875);
#2368=LINE('',#16977,#2876);
#2369=LINE('',#17028,#2877);
#2370=LINE('',#17076,#2878);
#2371=LINE('',#17124,#2879);
#2372=LINE('',#17175,#2880);
#2373=LINE('',#17226,#2881);
#2374=LINE('',#17274,#2882);
#2375=LINE('',#17325,#2883);
#2376=LINE('',#17376,#2884);
#2377=LINE('',#17424,#2885);
#2378=LINE('',#17472,#2886);
#2379=LINE('',#17523,#2887);
#2380=LINE('',#17574,#2888);
#2381=LINE('',#17622,#2889);
#2382=LINE('',#17673,#2890);
#2383=LINE('',#17724,#2891);
#2384=LINE('',#17772,#2892);
#2385=LINE('',#17820,#2893);
#2386=LINE('',#17871,#2894);
#2387=LINE('',#17937,#2895);
#2388=LINE('',#18027,#2896);
#2389=LINE('',#18114,#2897);
#2390=LINE('',#18201,#2898);
#2391=LINE('',#18288,#2899);
#2392=LINE('',#18375,#2900);
#2393=LINE('',#18462,#2901);
#2394=LINE('',#18552,#2902);
#2395=LINE('',#18562,#2903);
#2396=LINE('',#18598,#2904);
#2397=LINE('',#18636,#2905);
#2398=LINE('',#18672,#2906);
#2399=LINE('',#18710,#2907);
#2400=LINE('',#18746,#2908);
#2401=LINE('',#18784,#2909);
#2402=LINE('',#18821,#2910);
#2403=LINE('',#18856,#2911);
#2404=LINE('',#18883,#2912);
#2405=LINE('',#18907,#2913);
#2406=LINE('',#18931,#2914);
#2407=LINE('',#18955,#2915);
#2408=LINE('',#18981,#2916);
#2409=LINE('',#19005,#2917);
#2410=LINE('',#19029,#2918);
#2411=LINE('',#19055,#2919);
#2412=LINE('',#19079,#2920);
#2413=LINE('',#19103,#2921);
#2414=LINE('',#19127,#2922);
#2415=LINE('',#19153,#2923);
#2416=LINE('',#19177,#2924);
#2417=LINE('',#19201,#2925);
#2418=LINE('',#19227,#2926);
#2419=LINE('',#19251,#2927);
#2420=LINE('',#19275,#2928);
#2421=LINE('',#19299,#2929);
#2422=LINE('',#19325,#2930);
#2423=LINE('',#19349,#2931);
#2424=LINE('',#19373,#2932);
#2425=LINE('',#19399,#2933);
#2426=LINE('',#19423,#2934);
#2427=LINE('',#19447,#2935);
#2428=LINE('',#19471,#2936);
#2429=LINE('',#19497,#2937);
#2430=LINE('',#19521,#2938);
#2431=LINE('',#19545,#2939);
#2432=LINE('',#19571,#2940);
#2433=LINE('',#19595,#2941);
#2434=LINE('',#19619,#2942);
#2435=LINE('',#19643,#2943);
#2436=LINE('',#19669,#2944);
#2437=LINE('',#19693,#2945);
#2438=LINE('',#19717,#2946);
#2439=LINE('',#19743,#2947);
#2440=LINE('',#19767,#2948);
#2441=LINE('',#19791,#2949);
#2442=LINE('',#19815,#2950);
#2443=LINE('',#19841,#2951);
#2444=LINE('',#19865,#2952);
#2445=LINE('',#19889,#2953);
#2446=LINE('',#19915,#2954);
#2447=LINE('',#19939,#2955);
#2448=LINE('',#19963,#2956);
#2449=LINE('',#19988,#2957);
#2450=LINE('',#20015,#2958);
#2451=LINE('',#20052,#2959);
#2452=LINE('',#20088,#2960);
#2453=LINE('',#20126,#2961);
#2454=LINE('',#20162,#2962);
#2455=LINE('',#20200,#2963);
#2456=LINE('',#20237,#2964);
#2457=LINE('',#24479,#2965);
#2458=LINE('',#24481,#2966);
#2459=LINE('',#24483,#2967);
#2460=LINE('',#24484,#2968);
#2461=LINE('',#24489,#2969);
#2462=LINE('',#24490,#2970);
#2463=LINE('',#24493,#2971);
#2464=LINE('',#24494,#2972);
#2465=LINE('',#24497,#2973);
#2466=LINE('',#24498,#2974);
#2467=LINE('',#24505,#2975);
#2468=LINE('',#24515,#2976);
#2839=VECTOR('',#10459,0.6);
#2840=VECTOR('',#10464,0.6);
#2841=VECTOR('',#10467,0.6);
#2842=VECTOR('',#10470,0.6);
#2843=VECTOR('',#10473,0.6);
#2844=VECTOR('',#10476,0.6);
#2845=VECTOR('',#10479,0.6);
#2846=VECTOR('',#10482,0.6);
#2847=VECTOR('',#10485,0.6);
#2848=VECTOR('',#10488,0.6);
#2849=VECTOR('',#10491,0.6);
#2850=VECTOR('',#10494,0.6);
#2851=VECTOR('',#10497,0.6);
#2852=VECTOR('',#10500,0.6);
#2853=VECTOR('',#10503,0.6);
#2854=VECTOR('',#10506,0.6);
#2855=VECTOR('',#10509,0.6);
#2856=VECTOR('',#10512,0.6);
#2857=VECTOR('',#10515,0.6);
#2858=VECTOR('',#10518,0.6);
#2859=VECTOR('',#10521,0.6);
#2860=VECTOR('',#10524,0.6);
#2861=VECTOR('',#10527,0.6);
#2862=VECTOR('',#10530,0.6);
#2863=VECTOR('',#10533,0.6);
#2864=VECTOR('',#10536,0.6);
#2865=VECTOR('',#10539,0.6);
#2866=VECTOR('',#10542,0.6);
#2867=VECTOR('',#10545,0.6);
#2868=VECTOR('',#10548,0.6);
#2869=VECTOR('',#10551,0.6);
#2870=VECTOR('',#10554,0.6);
#2871=VECTOR('',#10557,0.6);
#2872=VECTOR('',#10560,0.6);
#2873=VECTOR('',#10563,0.6);
#2874=VECTOR('',#10566,0.6);
#2875=VECTOR('',#10569,0.6);
#2876=VECTOR('',#10572,0.6);
#2877=VECTOR('',#10575,0.6);
#2878=VECTOR('',#10578,0.6);
#2879=VECTOR('',#10581,0.6);
#2880=VECTOR('',#10584,0.6);
#2881=VECTOR('',#10587,0.6);
#2882=VECTOR('',#10590,0.6);
#2883=VECTOR('',#10593,0.6);
#2884=VECTOR('',#10596,0.6);
#2885=VECTOR('',#10599,0.6);
#2886=VECTOR('',#10602,0.6);
#2887=VECTOR('',#10605,0.6);
#2888=VECTOR('',#10608,0.6);
#2889=VECTOR('',#10611,0.6);
#2890=VECTOR('',#10614,0.6);
#2891=VECTOR('',#10617,0.6);
#2892=VECTOR('',#10620,0.6);
#2893=VECTOR('',#10623,0.6);
#2894=VECTOR('',#10626,0.6);
#2895=VECTOR('',#10629,0.6);
#2896=VECTOR('',#10632,0.6);
#2897=VECTOR('',#10635,0.6);
#2898=VECTOR('',#10638,0.6);
#2899=VECTOR('',#10641,0.6);
#2900=VECTOR('',#10644,0.6);
#2901=VECTOR('',#10647,0.6);
#2902=VECTOR('',#10650,0.415875);
#2903=VECTOR('',#10655,0.415875);
#2904=VECTOR('',#10660,0.415875);
#2905=VECTOR('',#10663,0.415875);
#2906=VECTOR('',#10666,0.415875);
#2907=VECTOR('',#10669,0.415875);
#2908=VECTOR('',#10672,0.415875);
#2909=VECTOR('',#10675,0.415875);
#2910=VECTOR('',#10678,0.415875);
#2911=VECTOR('',#10681,0.415875);
#2912=VECTOR('',#10684,0.415875);
#2913=VECTOR('',#10687,0.415875);
#2914=VECTOR('',#10690,0.415875);
#2915=VECTOR('',#10693,0.415875);
#2916=VECTOR('',#10696,0.415875);
#2917=VECTOR('',#10699,0.415875);
#2918=VECTOR('',#10702,0.415875);
#2919=VECTOR('',#10705,0.415875);
#2920=VECTOR('',#10708,0.415875);
#2921=VECTOR('',#10711,0.415875);
#2922=VECTOR('',#10714,0.415875);
#2923=VECTOR('',#10717,0.415875);
#2924=VECTOR('',#10720,0.415875);
#2925=VECTOR('',#10723,0.415875);
#2926=VECTOR('',#10726,0.415875);
#2927=VECTOR('',#10729,0.415875);
#2928=VECTOR('',#10732,0.415875);
#2929=VECTOR('',#10735,0.415875);
#2930=VECTOR('',#10738,0.415875);
#2931=VECTOR('',#10741,0.415875);
#2932=VECTOR('',#10744,0.415875);
#2933=VECTOR('',#10747,0.415875);
#2934=VECTOR('',#10750,0.415875);
#2935=VECTOR('',#10753,0.415875);
#2936=VECTOR('',#10756,0.415875);
#2937=VECTOR('',#10759,0.415875);
#2938=VECTOR('',#10762,0.415875);
#2939=VECTOR('',#10765,0.415875);
#2940=VECTOR('',#10768,0.415875);
#2941=VECTOR('',#10771,0.415875);
#2942=VECTOR('',#10774,0.415875);
#2943=VECTOR('',#10777,0.415875);
#2944=VECTOR('',#10780,0.415875);
#2945=VECTOR('',#10783,0.415875);
#2946=VECTOR('',#10786,0.415875);
#2947=VECTOR('',#10789,0.415875);
#2948=VECTOR('',#10792,0.415875);
#2949=VECTOR('',#10795,0.415875);
#2950=VECTOR('',#10798,0.415875);
#2951=VECTOR('',#10801,0.415875);
#2952=VECTOR('',#10804,0.415875);
#2953=VECTOR('',#10807,0.415875);
#2954=VECTOR('',#10810,0.415875);
#2955=VECTOR('',#10813,0.415875);
#2956=VECTOR('',#10816,0.415875);
#2957=VECTOR('',#10819,0.415875);
#2958=VECTOR('',#10822,0.415875);
#2959=VECTOR('',#10825,0.415875);
#2960=VECTOR('',#10828,0.415875);
#2961=VECTOR('',#10831,0.415875);
#2962=VECTOR('',#10834,0.415875);
#2963=VECTOR('',#10837,0.415875);
#2964=VECTOR('',#10840,0.415875);
#2965=VECTOR('',#10847,1.);
#2966=VECTOR('',#10848,1.);
#2967=VECTOR('',#10849,1.);
#2968=VECTOR('',#10850,1.);
#2969=VECTOR('',#10855,1.);
#2970=VECTOR('',#10856,1.);
#2971=VECTOR('',#10859,1.);
#2972=VECTOR('',#10860,1.);
#2973=VECTOR('',#10863,1.);
#2974=VECTOR('',#10864,1.);
#2975=VECTOR('',#10873,1.);
#2976=VECTOR('',#10888,1.35);
#3278=CIRCLE('',#8894,0.5941);
#3279=CIRCLE('',#8958,0.415875);
#3280=CIRCLE('',#8960,0.415875);
#3281=CIRCLE('',#9023,0.415875);
#3282=CIRCLE('',#9026,1.);
#3283=CIRCLE('',#9030,1.);
#3284=CIRCLE('',#9032,1.);
#3285=CIRCLE('',#9033,1.);
#3286=CIRCLE('',#9036,1.35);
#3287=CIRCLE('',#9037,0.5941);
#3288=CIRCLE('',#9039,1.35);
#3692=VERTEX_POINT('',#14869);
#3693=VERTEX_POINT('',#14870);
#3694=VERTEX_POINT('',#14872);
#3695=VERTEX_POINT('',#14892);
#3696=VERTEX_POINT('',#14899);
#3697=VERTEX_POINT('',#14900);
#3698=VERTEX_POINT('',#14986);
#3699=VERTEX_POINT('',#14987);
#3700=VERTEX_POINT('',#15076);
#3701=VERTEX_POINT('',#15077);
#3702=VERTEX_POINT('',#15163);
#3703=VERTEX_POINT('',#15164);
#3704=VERTEX_POINT('',#15250);
#3705=VERTEX_POINT('',#15251);
#3706=VERTEX_POINT('',#15337);
#3707=VERTEX_POINT('',#15338);
#3708=VERTEX_POINT('',#15424);
#3709=VERTEX_POINT('',#15425);
#3710=VERTEX_POINT('',#15511);
#3711=VERTEX_POINT('',#15512);
#3712=VERTEX_POINT('',#15583);
#3713=VERTEX_POINT('',#15584);
#3714=VERTEX_POINT('',#15634);
#3715=VERTEX_POINT('',#15635);
#3716=VERTEX_POINT('',#15682);
#3717=VERTEX_POINT('',#15683);
#3718=VERTEX_POINT('',#15730);
#3719=VERTEX_POINT('',#15731);
#3720=VERTEX_POINT('',#15781);
#3721=VERTEX_POINT('',#15782);
#3722=VERTEX_POINT('',#15832);
#3723=VERTEX_POINT('',#15833);
#3724=VERTEX_POINT('',#15880);
#3725=VERTEX_POINT('',#15881);
#3726=VERTEX_POINT('',#15931);
#3727=VERTEX_POINT('',#15932);
#3728=VERTEX_POINT('',#15982);
#3729=VERTEX_POINT('',#15983);
#3730=VERTEX_POINT('',#16030);
#3731=VERTEX_POINT('',#16031);
#3732=VERTEX_POINT('',#16078);
#3733=VERTEX_POINT('',#16079);
#3734=VERTEX_POINT('',#16129);
#3735=VERTEX_POINT('',#16130);
#3736=VERTEX_POINT('',#16180);
#3737=VERTEX_POINT('',#16181);
#3738=VERTEX_POINT('',#16228);
#3739=VERTEX_POINT('',#16229);
#3740=VERTEX_POINT('',#16279);
#3741=VERTEX_POINT('',#16280);
#3742=VERTEX_POINT('',#16330);
#3743=VERTEX_POINT('',#16331);
#3744=VERTEX_POINT('',#16378);
#3745=VERTEX_POINT('',#16379);
#3746=VERTEX_POINT('',#16426);
#3747=VERTEX_POINT('',#16427);
#3748=VERTEX_POINT('',#16477);
#3749=VERTEX_POINT('',#16478);
#3750=VERTEX_POINT('',#16528);
#3751=VERTEX_POINT('',#16529);
#3752=VERTEX_POINT('',#16576);
#3753=VERTEX_POINT('',#16577);
#3754=VERTEX_POINT('',#16627);
#3755=VERTEX_POINT('',#16628);
#3756=VERTEX_POINT('',#16678);
#3757=VERTEX_POINT('',#16679);
#3758=VERTEX_POINT('',#16726);
#3759=VERTEX_POINT('',#16727);
#3760=VERTEX_POINT('',#16774);
#3761=VERTEX_POINT('',#16775);
#3762=VERTEX_POINT('',#16825);
#3763=VERTEX_POINT('',#16826);
#3764=VERTEX_POINT('',#16876);
#3765=VERTEX_POINT('',#16877);
#3766=VERTEX_POINT('',#16924);
#3767=VERTEX_POINT('',#16925);
#3768=VERTEX_POINT('',#16975);
#3769=VERTEX_POINT('',#16976);
#3770=VERTEX_POINT('',#17026);
#3771=VERTEX_POINT('',#17027);
#3772=VERTEX_POINT('',#17074);
#3773=VERTEX_POINT('',#17075);
#3774=VERTEX_POINT('',#17122);
#3775=VERTEX_POINT('',#17123);
#3776=VERTEX_POINT('',#17173);
#3777=VERTEX_POINT('',#17174);
#3778=VERTEX_POINT('',#17224);
#3779=VERTEX_POINT('',#17225);
#3780=VERTEX_POINT('',#17272);
#3781=VERTEX_POINT('',#17273);
#3782=VERTEX_POINT('',#17323);
#3783=VERTEX_POINT('',#17324);
#3784=VERTEX_POINT('',#17374);
#3785=VERTEX_POINT('',#17375);
#3786=VERTEX_POINT('',#17422);
#3787=VERTEX_POINT('',#17423);
#3788=VERTEX_POINT('',#17470);
#3789=VERTEX_POINT('',#17471);
#3790=VERTEX_POINT('',#17521);
#3791=VERTEX_POINT('',#17522);
#3792=VERTEX_POINT('',#17572);
#3793=VERTEX_POINT('',#17573);
#3794=VERTEX_POINT('',#17620);
#3795=VERTEX_POINT('',#17621);
#3796=VERTEX_POINT('',#17671);
#3797=VERTEX_POINT('',#17672);
#3798=VERTEX_POINT('',#17722);
#3799=VERTEX_POINT('',#17723);
#3800=VERTEX_POINT('',#17770);
#3801=VERTEX_POINT('',#17771);
#3802=VERTEX_POINT('',#17818);
#3803=VERTEX_POINT('',#17819);
#3804=VERTEX_POINT('',#17869);
#3805=VERTEX_POINT('',#17870);
#3806=VERTEX_POINT('',#17935);
#3807=VERTEX_POINT('',#17936);
#3808=VERTEX_POINT('',#18025);
#3809=VERTEX_POINT('',#18026);
#3810=VERTEX_POINT('',#18112);
#3811=VERTEX_POINT('',#18113);
#3812=VERTEX_POINT('',#18199);
#3813=VERTEX_POINT('',#18200);
#3814=VERTEX_POINT('',#18286);
#3815=VERTEX_POINT('',#18287);
#3816=VERTEX_POINT('',#18373);
#3817=VERTEX_POINT('',#18374);
#3818=VERTEX_POINT('',#18460);
#3819=VERTEX_POINT('',#18461);
#3820=VERTEX_POINT('',#18550);
#3821=VERTEX_POINT('',#18551);
#3822=VERTEX_POINT('',#18553);
#3823=VERTEX_POINT('',#18560);
#3824=VERTEX_POINT('',#18561);
#3825=VERTEX_POINT('',#18580);
#3826=VERTEX_POINT('',#18596);
#3827=VERTEX_POINT('',#18597);
#3828=VERTEX_POINT('',#18634);
#3829=VERTEX_POINT('',#18635);
#3830=VERTEX_POINT('',#18670);
#3831=VERTEX_POINT('',#18671);
#3832=VERTEX_POINT('',#18708);
#3833=VERTEX_POINT('',#18709);
#3834=VERTEX_POINT('',#18744);
#3835=VERTEX_POINT('',#18745);
#3836=VERTEX_POINT('',#18782);
#3837=VERTEX_POINT('',#18783);
#3838=VERTEX_POINT('',#18819);
#3839=VERTEX_POINT('',#18820);
#3840=VERTEX_POINT('',#18854);
#3841=VERTEX_POINT('',#18855);
#3842=VERTEX_POINT('',#18881);
#3843=VERTEX_POINT('',#18882);
#3844=VERTEX_POINT('',#18905);
#3845=VERTEX_POINT('',#18906);
#3846=VERTEX_POINT('',#18929);
#3847=VERTEX_POINT('',#18930);
#3848=VERTEX_POINT('',#18953);
#3849=VERTEX_POINT('',#18954);
#3850=VERTEX_POINT('',#18979);
#3851=VERTEX_POINT('',#18980);
#3852=VERTEX_POINT('',#19003);
#3853=VERTEX_POINT('',#19004);
#3854=VERTEX_POINT('',#19027);
#3855=VERTEX_POINT('',#19028);
#3856=VERTEX_POINT('',#19053);
#3857=VERTEX_POINT('',#19054);
#3858=VERTEX_POINT('',#19077);
#3859=VERTEX_POINT('',#19078);
#3860=VERTEX_POINT('',#19101);
#3861=VERTEX_POINT('',#19102);
#3862=VERTEX_POINT('',#19125);
#3863=VERTEX_POINT('',#19126);
#3864=VERTEX_POINT('',#19151);
#3865=VERTEX_POINT('',#19152);
#3866=VERTEX_POINT('',#19175);
#3867=VERTEX_POINT('',#19176);
#3868=VERTEX_POINT('',#19199);
#3869=VERTEX_POINT('',#19200);
#3870=VERTEX_POINT('',#19225);
#3871=VERTEX_POINT('',#19226);
#3872=VERTEX_POINT('',#19249);
#3873=VERTEX_POINT('',#19250);
#3874=VERTEX_POINT('',#19273);
#3875=VERTEX_POINT('',#19274);
#3876=VERTEX_POINT('',#19297);
#3877=VERTEX_POINT('',#19298);
#3878=VERTEX_POINT('',#19323);
#3879=VERTEX_POINT('',#19324);
#3880=VERTEX_POINT('',#19347);
#3881=VERTEX_POINT('',#19348);
#3882=VERTEX_POINT('',#19371);
#3883=VERTEX_POINT('',#19372);
#3884=VERTEX_POINT('',#19397);
#3885=VERTEX_POINT('',#19398);
#3886=VERTEX_POINT('',#19421);
#3887=VERTEX_POINT('',#19422);
#3888=VERTEX_POINT('',#19445);
#3889=VERTEX_POINT('',#19446);
#3890=VERTEX_POINT('',#19469);
#3891=VERTEX_POINT('',#19470);
#3892=VERTEX_POINT('',#19495);
#3893=VERTEX_POINT('',#19496);
#3894=VERTEX_POINT('',#19519);
#3895=VERTEX_POINT('',#19520);
#3896=VERTEX_POINT('',#19543);
#3897=VERTEX_POINT('',#19544);
#3898=VERTEX_POINT('',#19569);
#3899=VERTEX_POINT('',#19570);
#3900=VERTEX_POINT('',#19593);
#3901=VERTEX_POINT('',#19594);
#3902=VERTEX_POINT('',#19617);
#3903=VERTEX_POINT('',#19618);
#3904=VERTEX_POINT('',#19641);
#3905=VERTEX_POINT('',#19642);
#3906=VERTEX_POINT('',#19667);
#3907=VERTEX_POINT('',#19668);
#3908=VERTEX_POINT('',#19691);
#3909=VERTEX_POINT('',#19692);
#3910=VERTEX_POINT('',#19715);
#3911=VERTEX_POINT('',#19716);
#3912=VERTEX_POINT('',#19741);
#3913=VERTEX_POINT('',#19742);
#3914=VERTEX_POINT('',#19765);
#3915=VERTEX_POINT('',#19766);
#3916=VERTEX_POINT('',#19789);
#3917=VERTEX_POINT('',#19790);
#3918=VERTEX_POINT('',#19813);
#3919=VERTEX_POINT('',#19814);
#3920=VERTEX_POINT('',#19839);
#3921=VERTEX_POINT('',#19840);
#3922=VERTEX_POINT('',#19863);
#3923=VERTEX_POINT('',#19864);
#3924=VERTEX_POINT('',#19887);
#3925=VERTEX_POINT('',#19888);
#3926=VERTEX_POINT('',#19913);
#3927=VERTEX_POINT('',#19914);
#3928=VERTEX_POINT('',#19937);
#3929=VERTEX_POINT('',#19938);
#3930=VERTEX_POINT('',#19961);
#3931=VERTEX_POINT('',#19962);
#3932=VERTEX_POINT('',#19986);
#3933=VERTEX_POINT('',#19987);
#3934=VERTEX_POINT('',#20013);
#3935=VERTEX_POINT('',#20014);
#3936=VERTEX_POINT('',#20050);
#3937=VERTEX_POINT('',#20051);
#3938=VERTEX_POINT('',#20086);
#3939=VERTEX_POINT('',#20087);
#3940=VERTEX_POINT('',#20124);
#3941=VERTEX_POINT('',#20125);
#3942=VERTEX_POINT('',#20160);
#3943=VERTEX_POINT('',#20161);
#3944=VERTEX_POINT('',#20198);
#3945=VERTEX_POINT('',#20199);
#3946=VERTEX_POINT('',#20235);
#3947=VERTEX_POINT('',#20236);
#3948=VERTEX_POINT('',#22263);
#3949=VERTEX_POINT('',#22329);
#3950=VERTEX_POINT('',#22383);
#3951=VERTEX_POINT('',#24388);
#3952=VERTEX_POINT('',#24477);
#3953=VERTEX_POINT('',#24478);
#3954=VERTEX_POINT('',#24480);
#3955=VERTEX_POINT('',#24482);
#3956=VERTEX_POINT('',#24486);
#3957=VERTEX_POINT('',#24488);
#3958=VERTEX_POINT('',#24492);
#3959=VERTEX_POINT('',#24496);
#3960=VERTEX_POINT('',#24502);
#3961=VERTEX_POINT('',#24504);
#3962=VERTEX_POINT('',#24509);
#3963=VERTEX_POINT('',#24513);
#4596=EDGE_CURVE('',#3692,#3693,#2331,.T.);
#4597=EDGE_CURVE('',#3692,#3694,#272,.T.);
#4598=EDGE_CURVE('',#3694,#3695,#3278,.F.);
#4599=EDGE_CURVE('',#3695,#3693,#273,.T.);
#4600=EDGE_CURVE('',#3696,#3697,#2332,.T.);
#4601=EDGE_CURVE('',#3696,#3692,#274,.T.);
#4602=EDGE_CURVE('',#3693,#3697,#275,.T.);
#4603=EDGE_CURVE('',#3698,#3699,#2333,.T.);
#4604=EDGE_CURVE('',#3698,#3696,#276,.T.);
#4605=EDGE_CURVE('',#3697,#3699,#277,.T.);
#4606=EDGE_CURVE('',#3700,#3701,#2334,.T.);
#4607=EDGE_CURVE('',#3700,#3698,#278,.T.);
#4608=EDGE_CURVE('',#3699,#3701,#279,.T.);
#4609=EDGE_CURVE('',#3702,#3703,#2335,.T.);
#4610=EDGE_CURVE('',#3702,#3700,#280,.T.);
#4611=EDGE_CURVE('',#3701,#3703,#281,.T.);
#4612=EDGE_CURVE('',#3704,#3705,#2336,.T.);
#4613=EDGE_CURVE('',#3704,#3702,#282,.T.);
#4614=EDGE_CURVE('',#3703,#3705,#283,.T.);
#4615=EDGE_CURVE('',#3706,#3707,#2337,.T.);
#4616=EDGE_CURVE('',#3706,#3704,#284,.T.);
#4617=EDGE_CURVE('',#3705,#3707,#285,.T.);
#4618=EDGE_CURVE('',#3708,#3709,#2338,.T.);
#4619=EDGE_CURVE('',#3708,#3706,#286,.T.);
#4620=EDGE_CURVE('',#3707,#3709,#287,.T.);
#4621=EDGE_CURVE('',#3710,#3711,#2339,.T.);
#4622=EDGE_CURVE('',#3710,#3708,#288,.T.);
#4623=EDGE_CURVE('',#3709,#3711,#289,.T.);
#4624=EDGE_CURVE('',#3712,#3713,#2340,.T.);
#4625=EDGE_CURVE('',#3712,#3710,#290,.T.);
#4626=EDGE_CURVE('',#3711,#3713,#291,.T.);
#4627=EDGE_CURVE('',#3714,#3715,#2341,.T.);
#4628=EDGE_CURVE('',#3714,#3712,#292,.T.);
#4629=EDGE_CURVE('',#3713,#3715,#293,.T.);
#4630=EDGE_CURVE('',#3716,#3717,#2342,.T.);
#4631=EDGE_CURVE('',#3716,#3714,#294,.T.);
#4632=EDGE_CURVE('',#3715,#3717,#295,.T.);
#4633=EDGE_CURVE('',#3718,#3719,#2343,.T.);
#4634=EDGE_CURVE('',#3718,#3716,#296,.T.);
#4635=EDGE_CURVE('',#3717,#3719,#297,.T.);
#4636=EDGE_CURVE('',#3720,#3721,#2344,.T.);
#4637=EDGE_CURVE('',#3720,#3718,#298,.T.);
#4638=EDGE_CURVE('',#3719,#3721,#299,.T.);
#4639=EDGE_CURVE('',#3722,#3723,#2345,.T.);
#4640=EDGE_CURVE('',#3722,#3720,#300,.T.);
#4641=EDGE_CURVE('',#3721,#3723,#301,.T.);
#4642=EDGE_CURVE('',#3724,#3725,#2346,.T.);
#4643=EDGE_CURVE('',#3724,#3722,#302,.T.);
#4644=EDGE_CURVE('',#3723,#3725,#303,.T.);
#4645=EDGE_CURVE('',#3726,#3727,#2347,.T.);
#4646=EDGE_CURVE('',#3726,#3724,#304,.T.);
#4647=EDGE_CURVE('',#3725,#3727,#305,.T.);
#4648=EDGE_CURVE('',#3728,#3729,#2348,.T.);
#4649=EDGE_CURVE('',#3728,#3726,#306,.T.);
#4650=EDGE_CURVE('',#3727,#3729,#307,.T.);
#4651=EDGE_CURVE('',#3730,#3731,#2349,.T.);
#4652=EDGE_CURVE('',#3730,#3728,#308,.T.);
#4653=EDGE_CURVE('',#3729,#3731,#309,.T.);
#4654=EDGE_CURVE('',#3732,#3733,#2350,.T.);
#4655=EDGE_CURVE('',#3732,#3730,#310,.T.);
#4656=EDGE_CURVE('',#3731,#3733,#311,.T.);
#4657=EDGE_CURVE('',#3734,#3735,#2351,.T.);
#4658=EDGE_CURVE('',#3734,#3732,#312,.T.);
#4659=EDGE_CURVE('',#3733,#3735,#313,.T.);
#4660=EDGE_CURVE('',#3736,#3737,#2352,.T.);
#4661=EDGE_CURVE('',#3736,#3734,#314,.T.);
#4662=EDGE_CURVE('',#3735,#3737,#315,.T.);
#4663=EDGE_CURVE('',#3738,#3739,#2353,.T.);
#4664=EDGE_CURVE('',#3738,#3736,#316,.T.);
#4665=EDGE_CURVE('',#3737,#3739,#317,.T.);
#4666=EDGE_CURVE('',#3740,#3741,#2354,.T.);
#4667=EDGE_CURVE('',#3740,#3738,#318,.T.);
#4668=EDGE_CURVE('',#3739,#3741,#319,.T.);
#4669=EDGE_CURVE('',#3742,#3743,#2355,.T.);
#4670=EDGE_CURVE('',#3742,#3740,#320,.T.);
#4671=EDGE_CURVE('',#3741,#3743,#321,.T.);
#4672=EDGE_CURVE('',#3744,#3745,#2356,.T.);
#4673=EDGE_CURVE('',#3744,#3742,#322,.T.);
#4674=EDGE_CURVE('',#3743,#3745,#323,.T.);
#4675=EDGE_CURVE('',#3746,#3747,#2357,.T.);
#4676=EDGE_CURVE('',#3746,#3744,#324,.T.);
#4677=EDGE_CURVE('',#3745,#3747,#325,.T.);
#4678=EDGE_CURVE('',#3748,#3749,#2358,.T.);
#4679=EDGE_CURVE('',#3748,#3746,#326,.T.);
#4680=EDGE_CURVE('',#3747,#3749,#327,.T.);
#4681=EDGE_CURVE('',#3750,#3751,#2359,.T.);
#4682=EDGE_CURVE('',#3750,#3748,#328,.T.);
#4683=EDGE_CURVE('',#3749,#3751,#329,.T.);
#4684=EDGE_CURVE('',#3752,#3753,#2360,.T.);
#4685=EDGE_CURVE('',#3752,#3750,#330,.T.);
#4686=EDGE_CURVE('',#3751,#3753,#331,.T.);
#4687=EDGE_CURVE('',#3754,#3755,#2361,.T.);
#4688=EDGE_CURVE('',#3754,#3752,#332,.T.);
#4689=EDGE_CURVE('',#3753,#3755,#333,.T.);
#4690=EDGE_CURVE('',#3756,#3757,#2362,.T.);
#4691=EDGE_CURVE('',#3756,#3754,#334,.T.);
#4692=EDGE_CURVE('',#3755,#3757,#335,.T.);
#4693=EDGE_CURVE('',#3758,#3759,#2363,.T.);
#4694=EDGE_CURVE('',#3758,#3756,#336,.T.);
#4695=EDGE_CURVE('',#3757,#3759,#337,.T.);
#4696=EDGE_CURVE('',#3760,#3761,#2364,.T.);
#4697=EDGE_CURVE('',#3760,#3758,#338,.T.);
#4698=EDGE_CURVE('',#3759,#3761,#339,.T.);
#4699=EDGE_CURVE('',#3762,#3763,#2365,.T.);
#4700=EDGE_CURVE('',#3762,#3760,#340,.T.);
#4701=EDGE_CURVE('',#3761,#3763,#341,.T.);
#4702=EDGE_CURVE('',#3764,#3765,#2366,.T.);
#4703=EDGE_CURVE('',#3764,#3762,#342,.T.);
#4704=EDGE_CURVE('',#3763,#3765,#343,.T.);
#4705=EDGE_CURVE('',#3766,#3767,#2367,.T.);
#4706=EDGE_CURVE('',#3766,#3764,#344,.T.);
#4707=EDGE_CURVE('',#3765,#3767,#345,.T.);
#4708=EDGE_CURVE('',#3768,#3769,#2368,.T.);
#4709=EDGE_CURVE('',#3768,#3766,#346,.T.);
#4710=EDGE_CURVE('',#3767,#3769,#347,.T.);
#4711=EDGE_CURVE('',#3770,#3771,#2369,.T.);
#4712=EDGE_CURVE('',#3770,#3768,#348,.T.);
#4713=EDGE_CURVE('',#3769,#3771,#349,.T.);
#4714=EDGE_CURVE('',#3772,#3773,#2370,.T.);
#4715=EDGE_CURVE('',#3772,#3770,#350,.T.);
#4716=EDGE_CURVE('',#3771,#3773,#351,.T.);
#4717=EDGE_CURVE('',#3774,#3775,#2371,.T.);
#4718=EDGE_CURVE('',#3774,#3772,#352,.T.);
#4719=EDGE_CURVE('',#3773,#3775,#353,.T.);
#4720=EDGE_CURVE('',#3776,#3777,#2372,.T.);
#4721=EDGE_CURVE('',#3776,#3774,#354,.T.);
#4722=EDGE_CURVE('',#3775,#3777,#355,.T.);
#4723=EDGE_CURVE('',#3778,#3779,#2373,.T.);
#4724=EDGE_CURVE('',#3778,#3776,#356,.T.);
#4725=EDGE_CURVE('',#3777,#3779,#357,.T.);
#4726=EDGE_CURVE('',#3780,#3781,#2374,.T.);
#4727=EDGE_CURVE('',#3780,#3778,#358,.T.);
#4728=EDGE_CURVE('',#3779,#3781,#359,.T.);
#4729=EDGE_CURVE('',#3782,#3783,#2375,.T.);
#4730=EDGE_CURVE('',#3782,#3780,#360,.T.);
#4731=EDGE_CURVE('',#3781,#3783,#361,.T.);
#4732=EDGE_CURVE('',#3784,#3785,#2376,.T.);
#4733=EDGE_CURVE('',#3784,#3782,#362,.T.);
#4734=EDGE_CURVE('',#3783,#3785,#363,.T.);
#4735=EDGE_CURVE('',#3786,#3787,#2377,.T.);
#4736=EDGE_CURVE('',#3786,#3784,#364,.T.);
#4737=EDGE_CURVE('',#3785,#3787,#365,.T.);
#4738=EDGE_CURVE('',#3788,#3789,#2378,.T.);
#4739=EDGE_CURVE('',#3788,#3786,#366,.T.);
#4740=EDGE_CURVE('',#3787,#3789,#367,.T.);
#4741=EDGE_CURVE('',#3790,#3791,#2379,.T.);
#4742=EDGE_CURVE('',#3790,#3788,#368,.T.);
#4743=EDGE_CURVE('',#3789,#3791,#369,.T.);
#4744=EDGE_CURVE('',#3792,#3793,#2380,.T.);
#4745=EDGE_CURVE('',#3792,#3790,#370,.T.);
#4746=EDGE_CURVE('',#3791,#3793,#371,.T.);
#4747=EDGE_CURVE('',#3794,#3795,#2381,.T.);
#4748=EDGE_CURVE('',#3794,#3792,#372,.T.);
#4749=EDGE_CURVE('',#3793,#3795,#373,.T.);
#4750=EDGE_CURVE('',#3796,#3797,#2382,.T.);
#4751=EDGE_CURVE('',#3796,#3794,#374,.T.);
#4752=EDGE_CURVE('',#3795,#3797,#375,.T.);
#4753=EDGE_CURVE('',#3798,#3799,#2383,.T.);
#4754=EDGE_CURVE('',#3798,#3796,#376,.T.);
#4755=EDGE_CURVE('',#3797,#3799,#377,.T.);
#4756=EDGE_CURVE('',#3800,#3801,#2384,.T.);
#4757=EDGE_CURVE('',#3800,#3798,#378,.T.);
#4758=EDGE_CURVE('',#3799,#3801,#379,.T.);
#4759=EDGE_CURVE('',#3802,#3803,#2385,.T.);
#4760=EDGE_CURVE('',#3802,#3800,#380,.T.);
#4761=EDGE_CURVE('',#3801,#3803,#381,.T.);
#4762=EDGE_CURVE('',#3804,#3805,#2386,.T.);
#4763=EDGE_CURVE('',#3804,#3802,#382,.T.);
#4764=EDGE_CURVE('',#3803,#3805,#383,.T.);
#4765=EDGE_CURVE('',#3806,#3807,#2387,.T.);
#4766=EDGE_CURVE('',#3806,#3804,#384,.T.);
#4767=EDGE_CURVE('',#3805,#3807,#385,.T.);
#4768=EDGE_CURVE('',#3808,#3809,#2388,.T.);
#4769=EDGE_CURVE('',#3808,#3806,#386,.T.);
#4770=EDGE_CURVE('',#3807,#3809,#387,.T.);
#4771=EDGE_CURVE('',#3810,#3811,#2389,.T.);
#4772=EDGE_CURVE('',#3810,#3808,#388,.T.);
#4773=EDGE_CURVE('',#3809,#3811,#389,.T.);
#4774=EDGE_CURVE('',#3812,#3813,#2390,.T.);
#4775=EDGE_CURVE('',#3812,#3810,#390,.T.);
#4776=EDGE_CURVE('',#3811,#3813,#391,.T.);
#4777=EDGE_CURVE('',#3814,#3815,#2391,.T.);
#4778=EDGE_CURVE('',#3814,#3812,#392,.T.);
#4779=EDGE_CURVE('',#3813,#3815,#393,.T.);
#4780=EDGE_CURVE('',#3816,#3817,#2392,.T.);
#4781=EDGE_CURVE('',#3816,#3814,#394,.T.);
#4782=EDGE_CURVE('',#3815,#3817,#395,.T.);
#4783=EDGE_CURVE('',#3818,#3819,#2393,.T.);
#4784=EDGE_CURVE('',#3818,#3816,#396,.T.);
#4785=EDGE_CURVE('',#3817,#3819,#397,.T.);
#4786=EDGE_CURVE('',#3820,#3821,#2394,.T.);
#4787=EDGE_CURVE('',#3820,#3822,#398,.T.);
#4788=EDGE_CURVE('',#3821,#3822,#3279,.T.);
#4789=EDGE_CURVE('',#3823,#3824,#2395,.T.);
#4790=EDGE_CURVE('',#3823,#3820,#399,.T.);
#4791=EDGE_CURVE('',#3825,#3821,#3280,.T.);
#4792=EDGE_CURVE('',#3824,#3825,#400,.T.);
#4793=EDGE_CURVE('',#3826,#3827,#2396,.T.);
#4794=EDGE_CURVE('',#3826,#3823,#401,.T.);
#4795=EDGE_CURVE('',#3827,#3824,#402,.T.);
#4796=EDGE_CURVE('',#3828,#3829,#2397,.T.);
#4797=EDGE_CURVE('',#3828,#3826,#403,.T.);
#4798=EDGE_CURVE('',#3829,#3827,#404,.T.);
#4799=EDGE_CURVE('',#3830,#3831,#2398,.T.);
#4800=EDGE_CURVE('',#3830,#3828,#405,.T.);
#4801=EDGE_CURVE('',#3831,#3829,#406,.T.);
#4802=EDGE_CURVE('',#3832,#3833,#2399,.T.);
#4803=EDGE_CURVE('',#3832,#3830,#407,.T.);
#4804=EDGE_CURVE('',#3833,#3831,#408,.T.);
#4805=EDGE_CURVE('',#3834,#3835,#2400,.T.);
#4806=EDGE_CURVE('',#3834,#3832,#409,.T.);
#4807=EDGE_CURVE('',#3835,#3833,#410,.T.);
#4808=EDGE_CURVE('',#3836,#3837,#2401,.T.);
#4809=EDGE_CURVE('',#3836,#3834,#411,.T.);
#4810=EDGE_CURVE('',#3837,#3835,#412,.T.);
#4811=EDGE_CURVE('',#3838,#3839,#2402,.T.);
#4812=EDGE_CURVE('',#3838,#3836,#413,.T.);
#4813=EDGE_CURVE('',#3839,#3837,#414,.T.);
#4814=EDGE_CURVE('',#3840,#3841,#2403,.T.);
#4815=EDGE_CURVE('',#3840,#3838,#415,.T.);
#4816=EDGE_CURVE('',#3841,#3839,#416,.T.);
#4817=EDGE_CURVE('',#3842,#3843,#2404,.T.);
#4818=EDGE_CURVE('',#3842,#3840,#417,.T.);
#4819=EDGE_CURVE('',#3843,#3841,#418,.T.);
#4820=EDGE_CURVE('',#3844,#3845,#2405,.T.);
#4821=EDGE_CURVE('',#3844,#3842,#419,.T.);
#4822=EDGE_CURVE('',#3845,#3843,#420,.T.);
#4823=EDGE_CURVE('',#3846,#3847,#2406,.T.);
#4824=EDGE_CURVE('',#3846,#3844,#421,.T.);
#4825=EDGE_CURVE('',#3847,#3845,#422,.T.);
#4826=EDGE_CURVE('',#3848,#3849,#2407,.T.);
#4827=EDGE_CURVE('',#3848,#3846,#423,.T.);
#4828=EDGE_CURVE('',#3849,#3847,#424,.T.);
#4829=EDGE_CURVE('',#3850,#3851,#2408,.T.);
#4830=EDGE_CURVE('',#3850,#3848,#425,.T.);
#4831=EDGE_CURVE('',#3851,#3849,#426,.T.);
#4832=EDGE_CURVE('',#3852,#3853,#2409,.T.);
#4833=EDGE_CURVE('',#3852,#3850,#427,.T.);
#4834=EDGE_CURVE('',#3853,#3851,#428,.T.);
#4835=EDGE_CURVE('',#3854,#3855,#2410,.T.);
#4836=EDGE_CURVE('',#3854,#3852,#429,.T.);
#4837=EDGE_CURVE('',#3855,#3853,#430,.T.);
#4838=EDGE_CURVE('',#3856,#3857,#2411,.T.);
#4839=EDGE_CURVE('',#3856,#3854,#431,.T.);
#4840=EDGE_CURVE('',#3857,#3855,#432,.T.);
#4841=EDGE_CURVE('',#3858,#3859,#2412,.T.);
#4842=EDGE_CURVE('',#3858,#3856,#433,.T.);
#4843=EDGE_CURVE('',#3859,#3857,#434,.T.);
#4844=EDGE_CURVE('',#3860,#3861,#2413,.T.);
#4845=EDGE_CURVE('',#3860,#3858,#435,.T.);
#4846=EDGE_CURVE('',#3861,#3859,#436,.T.);
#4847=EDGE_CURVE('',#3862,#3863,#2414,.T.);
#4848=EDGE_CURVE('',#3862,#3860,#437,.T.);
#4849=EDGE_CURVE('',#3863,#3861,#438,.T.);
#4850=EDGE_CURVE('',#3864,#3865,#2415,.T.);
#4851=EDGE_CURVE('',#3864,#3862,#439,.T.);
#4852=EDGE_CURVE('',#3865,#3863,#440,.T.);
#4853=EDGE_CURVE('',#3866,#3867,#2416,.T.);
#4854=EDGE_CURVE('',#3866,#3864,#441,.T.);
#4855=EDGE_CURVE('',#3867,#3865,#442,.T.);
#4856=EDGE_CURVE('',#3868,#3869,#2417,.T.);
#4857=EDGE_CURVE('',#3868,#3866,#443,.T.);
#4858=EDGE_CURVE('',#3869,#3867,#444,.T.);
#4859=EDGE_CURVE('',#3870,#3871,#2418,.T.);
#4860=EDGE_CURVE('',#3870,#3868,#445,.T.);
#4861=EDGE_CURVE('',#3871,#3869,#446,.T.);
#4862=EDGE_CURVE('',#3872,#3873,#2419,.T.);
#4863=EDGE_CURVE('',#3872,#3870,#447,.T.);
#4864=EDGE_CURVE('',#3873,#3871,#448,.T.);
#4865=EDGE_CURVE('',#3874,#3875,#2420,.T.);
#4866=EDGE_CURVE('',#3874,#3872,#449,.T.);
#4867=EDGE_CURVE('',#3875,#3873,#450,.T.);
#4868=EDGE_CURVE('',#3876,#3877,#2421,.T.);
#4869=EDGE_CURVE('',#3876,#3874,#451,.T.);
#4870=EDGE_CURVE('',#3877,#3875,#452,.T.);
#4871=EDGE_CURVE('',#3878,#3879,#2422,.T.);
#4872=EDGE_CURVE('',#3878,#3876,#453,.T.);
#4873=EDGE_CURVE('',#3879,#3877,#454,.T.);
#4874=EDGE_CURVE('',#3880,#3881,#2423,.T.);
#4875=EDGE_CURVE('',#3880,#3878,#455,.T.);
#4876=EDGE_CURVE('',#3881,#3879,#456,.T.);
#4877=EDGE_CURVE('',#3882,#3883,#2424,.T.);
#4878=EDGE_CURVE('',#3882,#3880,#457,.T.);
#4879=EDGE_CURVE('',#3883,#3881,#458,.T.);
#4880=EDGE_CURVE('',#3884,#3885,#2425,.T.);
#4881=EDGE_CURVE('',#3884,#3882,#459,.T.);
#4882=EDGE_CURVE('',#3885,#3883,#460,.T.);
#4883=EDGE_CURVE('',#3886,#3887,#2426,.T.);
#4884=EDGE_CURVE('',#3886,#3884,#461,.T.);
#4885=EDGE_CURVE('',#3887,#3885,#462,.T.);
#4886=EDGE_CURVE('',#3888,#3889,#2427,.T.);
#4887=EDGE_CURVE('',#3888,#3886,#463,.T.);
#4888=EDGE_CURVE('',#3889,#3887,#464,.T.);
#4889=EDGE_CURVE('',#3890,#3891,#2428,.T.);
#4890=EDGE_CURVE('',#3890,#3888,#465,.T.);
#4891=EDGE_CURVE('',#3891,#3889,#466,.T.);
#4892=EDGE_CURVE('',#3892,#3893,#2429,.T.);
#4893=EDGE_CURVE('',#3892,#3890,#467,.T.);
#4894=EDGE_CURVE('',#3893,#3891,#468,.T.);
#4895=EDGE_CURVE('',#3894,#3895,#2430,.T.);
#4896=EDGE_CURVE('',#3894,#3892,#469,.T.);
#4897=EDGE_CURVE('',#3895,#3893,#470,.T.);
#4898=EDGE_CURVE('',#3896,#3897,#2431,.T.);
#4899=EDGE_CURVE('',#3896,#3894,#471,.T.);
#4900=EDGE_CURVE('',#3897,#3895,#472,.T.);
#4901=EDGE_CURVE('',#3898,#3899,#2432,.T.);
#4902=EDGE_CURVE('',#3898,#3896,#473,.T.);
#4903=EDGE_CURVE('',#3899,#3897,#474,.T.);
#4904=EDGE_CURVE('',#3900,#3901,#2433,.T.);
#4905=EDGE_CURVE('',#3900,#3898,#475,.T.);
#4906=EDGE_CURVE('',#3901,#3899,#476,.T.);
#4907=EDGE_CURVE('',#3902,#3903,#2434,.T.);
#4908=EDGE_CURVE('',#3902,#3900,#477,.T.);
#4909=EDGE_CURVE('',#3903,#3901,#478,.T.);
#4910=EDGE_CURVE('',#3904,#3905,#2435,.T.);
#4911=EDGE_CURVE('',#3904,#3902,#479,.T.);
#4912=EDGE_CURVE('',#3905,#3903,#480,.T.);
#4913=EDGE_CURVE('',#3906,#3907,#2436,.T.);
#4914=EDGE_CURVE('',#3906,#3904,#481,.T.);
#4915=EDGE_CURVE('',#3907,#3905,#482,.T.);
#4916=EDGE_CURVE('',#3908,#3909,#2437,.T.);
#4917=EDGE_CURVE('',#3908,#3906,#483,.T.);
#4918=EDGE_CURVE('',#3909,#3907,#484,.T.);
#4919=EDGE_CURVE('',#3910,#3911,#2438,.T.);
#4920=EDGE_CURVE('',#3910,#3908,#485,.T.);
#4921=EDGE_CURVE('',#3911,#3909,#486,.T.);
#4922=EDGE_CURVE('',#3912,#3913,#2439,.T.);
#4923=EDGE_CURVE('',#3912,#3910,#487,.T.);
#4924=EDGE_CURVE('',#3913,#3911,#488,.T.);
#4925=EDGE_CURVE('',#3914,#3915,#2440,.T.);
#4926=EDGE_CURVE('',#3914,#3912,#489,.T.);
#4927=EDGE_CURVE('',#3915,#3913,#490,.T.);
#4928=EDGE_CURVE('',#3916,#3917,#2441,.T.);
#4929=EDGE_CURVE('',#3916,#3914,#491,.T.);
#4930=EDGE_CURVE('',#3917,#3915,#492,.T.);
#4931=EDGE_CURVE('',#3918,#3919,#2442,.T.);
#4932=EDGE_CURVE('',#3918,#3916,#493,.T.);
#4933=EDGE_CURVE('',#3919,#3917,#494,.T.);
#4934=EDGE_CURVE('',#3920,#3921,#2443,.T.);
#4935=EDGE_CURVE('',#3920,#3918,#495,.T.);
#4936=EDGE_CURVE('',#3921,#3919,#496,.T.);
#4937=EDGE_CURVE('',#3922,#3923,#2444,.T.);
#4938=EDGE_CURVE('',#3922,#3920,#497,.T.);
#4939=EDGE_CURVE('',#3923,#3921,#498,.T.);
#4940=EDGE_CURVE('',#3924,#3925,#2445,.T.);
#4941=EDGE_CURVE('',#3924,#3922,#499,.T.);
#4942=EDGE_CURVE('',#3925,#3923,#500,.T.);
#4943=EDGE_CURVE('',#3926,#3927,#2446,.T.);
#4944=EDGE_CURVE('',#3926,#3924,#501,.T.);
#4945=EDGE_CURVE('',#3927,#3925,#502,.T.);
#4946=EDGE_CURVE('',#3928,#3929,#2447,.T.);
#4947=EDGE_CURVE('',#3928,#3926,#503,.T.);
#4948=EDGE_CURVE('',#3929,#3927,#504,.T.);
#4949=EDGE_CURVE('',#3930,#3931,#2448,.T.);
#4950=EDGE_CURVE('',#3930,#3928,#505,.T.);
#4951=EDGE_CURVE('',#3931,#3929,#506,.T.);
#4952=EDGE_CURVE('',#3932,#3933,#2449,.T.);
#4953=EDGE_CURVE('',#3932,#3930,#507,.T.);
#4954=EDGE_CURVE('',#3933,#3931,#508,.T.);
#4955=EDGE_CURVE('',#3934,#3935,#2450,.T.);
#4956=EDGE_CURVE('',#3934,#3932,#509,.T.);
#4957=EDGE_CURVE('',#3935,#3933,#510,.T.);
#4958=EDGE_CURVE('',#3936,#3937,#2451,.T.);
#4959=EDGE_CURVE('',#3936,#3934,#511,.T.);
#4960=EDGE_CURVE('',#3937,#3935,#512,.T.);
#4961=EDGE_CURVE('',#3938,#3939,#2452,.T.);
#4962=EDGE_CURVE('',#3938,#3936,#513,.T.);
#4963=EDGE_CURVE('',#3939,#3937,#514,.T.);
#4964=EDGE_CURVE('',#3940,#3941,#2453,.T.);
#4965=EDGE_CURVE('',#3940,#3938,#515,.T.);
#4966=EDGE_CURVE('',#3941,#3939,#516,.T.);
#4967=EDGE_CURVE('',#3942,#3943,#2454,.T.);
#4968=EDGE_CURVE('',#3942,#3940,#517,.T.);
#4969=EDGE_CURVE('',#3943,#3941,#518,.T.);
#4970=EDGE_CURVE('',#3944,#3945,#2455,.T.);
#4971=EDGE_CURVE('',#3944,#3942,#519,.T.);
#4972=EDGE_CURVE('',#3945,#3943,#520,.T.);
#4973=EDGE_CURVE('',#3946,#3947,#2456,.T.);
#4974=EDGE_CURVE('',#3946,#3944,#521,.T.);
#4975=EDGE_CURVE('',#3947,#3945,#522,.T.);
#4976=EDGE_CURVE('',#3948,#3825,#523,.T.);
#4977=EDGE_CURVE('',#3819,#3948,#524,.T.);
#4978=EDGE_CURVE('',#3949,#3695,#525,.T.);
#4979=EDGE_CURVE('',#3949,#3947,#526,.T.);
#4980=EDGE_CURVE('',#3950,#3949,#3281,.T.);
#4981=EDGE_CURVE('',#3950,#3946,#527,.T.);
#4982=EDGE_CURVE('',#3822,#3951,#528,.T.);
#4983=EDGE_CURVE('',#3694,#3950,#529,.T.);
#4984=EDGE_CURVE('',#3951,#3818,#530,.T.);
#4985=EDGE_CURVE('',#3952,#3953,#2457,.T.);
#4986=EDGE_CURVE('',#3952,#3954,#2458,.T.);
#4987=EDGE_CURVE('',#3955,#3954,#2459,.T.);
#4988=EDGE_CURVE('',#3953,#3955,#2460,.T.);
#4989=EDGE_CURVE('',#3953,#3956,#3282,.T.);
#4990=EDGE_CURVE('',#3955,#3957,#2461,.T.);
#4991=EDGE_CURVE('',#3957,#3956,#2462,.T.);
#4992=EDGE_CURVE('',#3954,#3958,#2463,.T.);
#4993=EDGE_CURVE('',#3957,#3958,#2464,.T.);
#4994=EDGE_CURVE('',#3956,#3959,#2465,.T.);
#4995=EDGE_CURVE('',#3958,#3959,#2466,.T.);
#4996=EDGE_CURVE('',#3959,#3952,#3283,.T.);
#4997=EDGE_CURVE('',#3960,#3960,#3284,.T.);
#4998=EDGE_CURVE('',#3960,#3961,#2467,.T.);
#4999=EDGE_CURVE('',#3961,#3961,#3285,.T.);
#5000=EDGE_CURVE('',#3962,#3962,#3286,.T.);
#5001=EDGE_CURVE('',#3951,#3948,#3287,.F.);
#5002=EDGE_CURVE('',#3963,#3963,#3288,.T.);
#5003=EDGE_CURVE('',#3963,#3962,#2468,.T.);
#6219=ORIENTED_EDGE('',*,*,#4596,.F.);
#6220=ORIENTED_EDGE('',*,*,#4597,.T.);
#6221=ORIENTED_EDGE('',*,*,#4598,.T.);
#6222=ORIENTED_EDGE('',*,*,#4599,.T.);
#6223=ORIENTED_EDGE('',*,*,#4600,.F.);
#6224=ORIENTED_EDGE('',*,*,#4601,.T.);
#6225=ORIENTED_EDGE('',*,*,#4596,.T.);
#6226=ORIENTED_EDGE('',*,*,#4602,.T.);
#6227=ORIENTED_EDGE('',*,*,#4603,.F.);
#6228=ORIENTED_EDGE('',*,*,#4604,.T.);
#6229=ORIENTED_EDGE('',*,*,#4600,.T.);
#6230=ORIENTED_EDGE('',*,*,#4605,.T.);
#6231=ORIENTED_EDGE('',*,*,#4606,.F.);
#6232=ORIENTED_EDGE('',*,*,#4607,.T.);
#6233=ORIENTED_EDGE('',*,*,#4603,.T.);
#6234=ORIENTED_EDGE('',*,*,#4608,.T.);
#6235=ORIENTED_EDGE('',*,*,#4609,.F.);
#6236=ORIENTED_EDGE('',*,*,#4610,.T.);
#6237=ORIENTED_EDGE('',*,*,#4606,.T.);
#6238=ORIENTED_EDGE('',*,*,#4611,.T.);
#6239=ORIENTED_EDGE('',*,*,#4612,.F.);
#6240=ORIENTED_EDGE('',*,*,#4613,.T.);
#6241=ORIENTED_EDGE('',*,*,#4609,.T.);
#6242=ORIENTED_EDGE('',*,*,#4614,.T.);
#6243=ORIENTED_EDGE('',*,*,#4615,.F.);
#6244=ORIENTED_EDGE('',*,*,#4616,.T.);
#6245=ORIENTED_EDGE('',*,*,#4612,.T.);
#6246=ORIENTED_EDGE('',*,*,#4617,.T.);
#6247=ORIENTED_EDGE('',*,*,#4618,.F.);
#6248=ORIENTED_EDGE('',*,*,#4619,.T.);
#6249=ORIENTED_EDGE('',*,*,#4615,.T.);
#6250=ORIENTED_EDGE('',*,*,#4620,.T.);
#6251=ORIENTED_EDGE('',*,*,#4621,.F.);
#6252=ORIENTED_EDGE('',*,*,#4622,.T.);
#6253=ORIENTED_EDGE('',*,*,#4618,.T.);
#6254=ORIENTED_EDGE('',*,*,#4623,.T.);
#6255=ORIENTED_EDGE('',*,*,#4624,.F.);
#6256=ORIENTED_EDGE('',*,*,#4625,.T.);
#6257=ORIENTED_EDGE('',*,*,#4621,.T.);
#6258=ORIENTED_EDGE('',*,*,#4626,.T.);
#6259=ORIENTED_EDGE('',*,*,#4627,.F.);
#6260=ORIENTED_EDGE('',*,*,#4628,.T.);
#6261=ORIENTED_EDGE('',*,*,#4624,.T.);
#6262=ORIENTED_EDGE('',*,*,#4629,.T.);
#6263=ORIENTED_EDGE('',*,*,#4630,.F.);
#6264=ORIENTED_EDGE('',*,*,#4631,.T.);
#6265=ORIENTED_EDGE('',*,*,#4627,.T.);
#6266=ORIENTED_EDGE('',*,*,#4632,.T.);
#6267=ORIENTED_EDGE('',*,*,#4633,.F.);
#6268=ORIENTED_EDGE('',*,*,#4634,.T.);
#6269=ORIENTED_EDGE('',*,*,#4630,.T.);
#6270=ORIENTED_EDGE('',*,*,#4635,.T.);
#6271=ORIENTED_EDGE('',*,*,#4636,.F.);
#6272=ORIENTED_EDGE('',*,*,#4637,.T.);
#6273=ORIENTED_EDGE('',*,*,#4633,.T.);
#6274=ORIENTED_EDGE('',*,*,#4638,.T.);
#6275=ORIENTED_EDGE('',*,*,#4639,.F.);
#6276=ORIENTED_EDGE('',*,*,#4640,.T.);
#6277=ORIENTED_EDGE('',*,*,#4636,.T.);
#6278=ORIENTED_EDGE('',*,*,#4641,.T.);
#6279=ORIENTED_EDGE('',*,*,#4642,.F.);
#6280=ORIENTED_EDGE('',*,*,#4643,.T.);
#6281=ORIENTED_EDGE('',*,*,#4639,.T.);
#6282=ORIENTED_EDGE('',*,*,#4644,.T.);
#6283=ORIENTED_EDGE('',*,*,#4645,.F.);
#6284=ORIENTED_EDGE('',*,*,#4646,.T.);
#6285=ORIENTED_EDGE('',*,*,#4642,.T.);
#6286=ORIENTED_EDGE('',*,*,#4647,.T.);
#6287=ORIENTED_EDGE('',*,*,#4648,.F.);
#6288=ORIENTED_EDGE('',*,*,#4649,.T.);
#6289=ORIENTED_EDGE('',*,*,#4645,.T.);
#6290=ORIENTED_EDGE('',*,*,#4650,.T.);
#6291=ORIENTED_EDGE('',*,*,#4651,.F.);
#6292=ORIENTED_EDGE('',*,*,#4652,.T.);
#6293=ORIENTED_EDGE('',*,*,#4648,.T.);
#6294=ORIENTED_EDGE('',*,*,#4653,.T.);
#6295=ORIENTED_EDGE('',*,*,#4654,.F.);
#6296=ORIENTED_EDGE('',*,*,#4655,.T.);
#6297=ORIENTED_EDGE('',*,*,#4651,.T.);
#6298=ORIENTED_EDGE('',*,*,#4656,.T.);
#6299=ORIENTED_EDGE('',*,*,#4657,.F.);
#6300=ORIENTED_EDGE('',*,*,#4658,.T.);
#6301=ORIENTED_EDGE('',*,*,#4654,.T.);
#6302=ORIENTED_EDGE('',*,*,#4659,.T.);
#6303=ORIENTED_EDGE('',*,*,#4660,.F.);
#6304=ORIENTED_EDGE('',*,*,#4661,.T.);
#6305=ORIENTED_EDGE('',*,*,#4657,.T.);
#6306=ORIENTED_EDGE('',*,*,#4662,.T.);
#6307=ORIENTED_EDGE('',*,*,#4663,.F.);
#6308=ORIENTED_EDGE('',*,*,#4664,.T.);
#6309=ORIENTED_EDGE('',*,*,#4660,.T.);
#6310=ORIENTED_EDGE('',*,*,#4665,.T.);
#6311=ORIENTED_EDGE('',*,*,#4666,.F.);
#6312=ORIENTED_EDGE('',*,*,#4667,.T.);
#6313=ORIENTED_EDGE('',*,*,#4663,.T.);
#6314=ORIENTED_EDGE('',*,*,#4668,.T.);
#6315=ORIENTED_EDGE('',*,*,#4669,.F.);
#6316=ORIENTED_EDGE('',*,*,#4670,.T.);
#6317=ORIENTED_EDGE('',*,*,#4666,.T.);
#6318=ORIENTED_EDGE('',*,*,#4671,.T.);
#6319=ORIENTED_EDGE('',*,*,#4672,.F.);
#6320=ORIENTED_EDGE('',*,*,#4673,.T.);
#6321=ORIENTED_EDGE('',*,*,#4669,.T.);
#6322=ORIENTED_EDGE('',*,*,#4674,.T.);
#6323=ORIENTED_EDGE('',*,*,#4675,.F.);
#6324=ORIENTED_EDGE('',*,*,#4676,.T.);
#6325=ORIENTED_EDGE('',*,*,#4672,.T.);
#6326=ORIENTED_EDGE('',*,*,#4677,.T.);
#6327=ORIENTED_EDGE('',*,*,#4678,.F.);
#6328=ORIENTED_EDGE('',*,*,#4679,.T.);
#6329=ORIENTED_EDGE('',*,*,#4675,.T.);
#6330=ORIENTED_EDGE('',*,*,#4680,.T.);
#6331=ORIENTED_EDGE('',*,*,#4681,.F.);
#6332=ORIENTED_EDGE('',*,*,#4682,.T.);
#6333=ORIENTED_EDGE('',*,*,#4678,.T.);
#6334=ORIENTED_EDGE('',*,*,#4683,.T.);
#6335=ORIENTED_EDGE('',*,*,#4684,.F.);
#6336=ORIENTED_EDGE('',*,*,#4685,.T.);
#6337=ORIENTED_EDGE('',*,*,#4681,.T.);
#6338=ORIENTED_EDGE('',*,*,#4686,.T.);
#6339=ORIENTED_EDGE('',*,*,#4687,.F.);
#6340=ORIENTED_EDGE('',*,*,#4688,.T.);
#6341=ORIENTED_EDGE('',*,*,#4684,.T.);
#6342=ORIENTED_EDGE('',*,*,#4689,.T.);
#6343=ORIENTED_EDGE('',*,*,#4690,.F.);
#6344=ORIENTED_EDGE('',*,*,#4691,.T.);
#6345=ORIENTED_EDGE('',*,*,#4687,.T.);
#6346=ORIENTED_EDGE('',*,*,#4692,.T.);
#6347=ORIENTED_EDGE('',*,*,#4693,.F.);
#6348=ORIENTED_EDGE('',*,*,#4694,.T.);
#6349=ORIENTED_EDGE('',*,*,#4690,.T.);
#6350=ORIENTED_EDGE('',*,*,#4695,.T.);
#6351=ORIENTED_EDGE('',*,*,#4696,.F.);
#6352=ORIENTED_EDGE('',*,*,#4697,.T.);
#6353=ORIENTED_EDGE('',*,*,#4693,.T.);
#6354=ORIENTED_EDGE('',*,*,#4698,.T.);
#6355=ORIENTED_EDGE('',*,*,#4699,.F.);
#6356=ORIENTED_EDGE('',*,*,#4700,.T.);
#6357=ORIENTED_EDGE('',*,*,#4696,.T.);
#6358=ORIENTED_EDGE('',*,*,#4701,.T.);
#6359=ORIENTED_EDGE('',*,*,#4702,.F.);
#6360=ORIENTED_EDGE('',*,*,#4703,.T.);
#6361=ORIENTED_EDGE('',*,*,#4699,.T.);
#6362=ORIENTED_EDGE('',*,*,#4704,.T.);
#6363=ORIENTED_EDGE('',*,*,#4705,.F.);
#6364=ORIENTED_EDGE('',*,*,#4706,.T.);
#6365=ORIENTED_EDGE('',*,*,#4702,.T.);
#6366=ORIENTED_EDGE('',*,*,#4707,.T.);
#6367=ORIENTED_EDGE('',*,*,#4708,.F.);
#6368=ORIENTED_EDGE('',*,*,#4709,.T.);
#6369=ORIENTED_EDGE('',*,*,#4705,.T.);
#6370=ORIENTED_EDGE('',*,*,#4710,.T.);
#6371=ORIENTED_EDGE('',*,*,#4711,.F.);
#6372=ORIENTED_EDGE('',*,*,#4712,.T.);
#6373=ORIENTED_EDGE('',*,*,#4708,.T.);
#6374=ORIENTED_EDGE('',*,*,#4713,.T.);
#6375=ORIENTED_EDGE('',*,*,#4714,.F.);
#6376=ORIENTED_EDGE('',*,*,#4715,.T.);
#6377=ORIENTED_EDGE('',*,*,#4711,.T.);
#6378=ORIENTED_EDGE('',*,*,#4716,.T.);
#6379=ORIENTED_EDGE('',*,*,#4717,.F.);
#6380=ORIENTED_EDGE('',*,*,#4718,.T.);
#6381=ORIENTED_EDGE('',*,*,#4714,.T.);
#6382=ORIENTED_EDGE('',*,*,#4719,.T.);
#6383=ORIENTED_EDGE('',*,*,#4720,.F.);
#6384=ORIENTED_EDGE('',*,*,#4721,.T.);
#6385=ORIENTED_EDGE('',*,*,#4717,.T.);
#6386=ORIENTED_EDGE('',*,*,#4722,.T.);
#6387=ORIENTED_EDGE('',*,*,#4723,.F.);
#6388=ORIENTED_EDGE('',*,*,#4724,.T.);
#6389=ORIENTED_EDGE('',*,*,#4720,.T.);
#6390=ORIENTED_EDGE('',*,*,#4725,.T.);
#6391=ORIENTED_EDGE('',*,*,#4726,.F.);
#6392=ORIENTED_EDGE('',*,*,#4727,.T.);
#6393=ORIENTED_EDGE('',*,*,#4723,.T.);
#6394=ORIENTED_EDGE('',*,*,#4728,.T.);
#6395=ORIENTED_EDGE('',*,*,#4729,.F.);
#6396=ORIENTED_EDGE('',*,*,#4730,.T.);
#6397=ORIENTED_EDGE('',*,*,#4726,.T.);
#6398=ORIENTED_EDGE('',*,*,#4731,.T.);
#6399=ORIENTED_EDGE('',*,*,#4732,.F.);
#6400=ORIENTED_EDGE('',*,*,#4733,.T.);
#6401=ORIENTED_EDGE('',*,*,#4729,.T.);
#6402=ORIENTED_EDGE('',*,*,#4734,.T.);
#6403=ORIENTED_EDGE('',*,*,#4735,.F.);
#6404=ORIENTED_EDGE('',*,*,#4736,.T.);
#6405=ORIENTED_EDGE('',*,*,#4732,.T.);
#6406=ORIENTED_EDGE('',*,*,#4737,.T.);
#6407=ORIENTED_EDGE('',*,*,#4738,.F.);
#6408=ORIENTED_EDGE('',*,*,#4739,.T.);
#6409=ORIENTED_EDGE('',*,*,#4735,.T.);
#6410=ORIENTED_EDGE('',*,*,#4740,.T.);
#6411=ORIENTED_EDGE('',*,*,#4741,.F.);
#6412=ORIENTED_EDGE('',*,*,#4742,.T.);
#6413=ORIENTED_EDGE('',*,*,#4738,.T.);
#6414=ORIENTED_EDGE('',*,*,#4743,.T.);
#6415=ORIENTED_EDGE('',*,*,#4744,.F.);
#6416=ORIENTED_EDGE('',*,*,#4745,.T.);
#6417=ORIENTED_EDGE('',*,*,#4741,.T.);
#6418=ORIENTED_EDGE('',*,*,#4746,.T.);
#6419=ORIENTED_EDGE('',*,*,#4747,.F.);
#6420=ORIENTED_EDGE('',*,*,#4748,.T.);
#6421=ORIENTED_EDGE('',*,*,#4744,.T.);
#6422=ORIENTED_EDGE('',*,*,#4749,.T.);
#6423=ORIENTED_EDGE('',*,*,#4750,.F.);
#6424=ORIENTED_EDGE('',*,*,#4751,.T.);
#6425=ORIENTED_EDGE('',*,*,#4747,.T.);
#6426=ORIENTED_EDGE('',*,*,#4752,.T.);
#6427=ORIENTED_EDGE('',*,*,#4753,.F.);
#6428=ORIENTED_EDGE('',*,*,#4754,.T.);
#6429=ORIENTED_EDGE('',*,*,#4750,.T.);
#6430=ORIENTED_EDGE('',*,*,#4755,.T.);
#6431=ORIENTED_EDGE('',*,*,#4756,.F.);
#6432=ORIENTED_EDGE('',*,*,#4757,.T.);
#6433=ORIENTED_EDGE('',*,*,#4753,.T.);
#6434=ORIENTED_EDGE('',*,*,#4758,.T.);
#6435=ORIENTED_EDGE('',*,*,#4759,.F.);
#6436=ORIENTED_EDGE('',*,*,#4760,.T.);
#6437=ORIENTED_EDGE('',*,*,#4756,.T.);
#6438=ORIENTED_EDGE('',*,*,#4761,.T.);
#6439=ORIENTED_EDGE('',*,*,#4762,.F.);
#6440=ORIENTED_EDGE('',*,*,#4763,.T.);
#6441=ORIENTED_EDGE('',*,*,#4759,.T.);
#6442=ORIENTED_EDGE('',*,*,#4764,.T.);
#6443=ORIENTED_EDGE('',*,*,#4765,.F.);
#6444=ORIENTED_EDGE('',*,*,#4766,.T.);
#6445=ORIENTED_EDGE('',*,*,#4762,.T.);
#6446=ORIENTED_EDGE('',*,*,#4767,.T.);
#6447=ORIENTED_EDGE('',*,*,#4768,.F.);
#6448=ORIENTED_EDGE('',*,*,#4769,.T.);
#6449=ORIENTED_EDGE('',*,*,#4765,.T.);
#6450=ORIENTED_EDGE('',*,*,#4770,.T.);
#6451=ORIENTED_EDGE('',*,*,#4771,.F.);
#6452=ORIENTED_EDGE('',*,*,#4772,.T.);
#6453=ORIENTED_EDGE('',*,*,#4768,.T.);
#6454=ORIENTED_EDGE('',*,*,#4773,.T.);
#6455=ORIENTED_EDGE('',*,*,#4774,.F.);
#6456=ORIENTED_EDGE('',*,*,#4775,.T.);
#6457=ORIENTED_EDGE('',*,*,#4771,.T.);
#6458=ORIENTED_EDGE('',*,*,#4776,.T.);
#6459=ORIENTED_EDGE('',*,*,#4777,.F.);
#6460=ORIENTED_EDGE('',*,*,#4778,.T.);
#6461=ORIENTED_EDGE('',*,*,#4774,.T.);
#6462=ORIENTED_EDGE('',*,*,#4779,.T.);
#6463=ORIENTED_EDGE('',*,*,#4780,.F.);
#6464=ORIENTED_EDGE('',*,*,#4781,.T.);
#6465=ORIENTED_EDGE('',*,*,#4777,.T.);
#6466=ORIENTED_EDGE('',*,*,#4782,.T.);
#6467=ORIENTED_EDGE('',*,*,#4783,.F.);
#6468=ORIENTED_EDGE('',*,*,#4784,.T.);
#6469=ORIENTED_EDGE('',*,*,#4780,.T.);
#6470=ORIENTED_EDGE('',*,*,#4785,.T.);
#6471=ORIENTED_EDGE('',*,*,#4786,.F.);
#6472=ORIENTED_EDGE('',*,*,#4787,.T.);
#6473=ORIENTED_EDGE('',*,*,#4788,.F.);
#6474=ORIENTED_EDGE('',*,*,#4789,.F.);
#6475=ORIENTED_EDGE('',*,*,#4790,.T.);
#6476=ORIENTED_EDGE('',*,*,#4786,.T.);
#6477=ORIENTED_EDGE('',*,*,#4791,.F.);
#6478=ORIENTED_EDGE('',*,*,#4792,.F.);
#6479=ORIENTED_EDGE('',*,*,#4793,.F.);
#6480=ORIENTED_EDGE('',*,*,#4794,.T.);
#6481=ORIENTED_EDGE('',*,*,#4789,.T.);
#6482=ORIENTED_EDGE('',*,*,#4795,.F.);
#6483=ORIENTED_EDGE('',*,*,#4796,.F.);
#6484=ORIENTED_EDGE('',*,*,#4797,.T.);
#6485=ORIENTED_EDGE('',*,*,#4793,.T.);
#6486=ORIENTED_EDGE('',*,*,#4798,.F.);
#6487=ORIENTED_EDGE('',*,*,#4799,.F.);
#6488=ORIENTED_EDGE('',*,*,#4800,.T.);
#6489=ORIENTED_EDGE('',*,*,#4796,.T.);
#6490=ORIENTED_EDGE('',*,*,#4801,.F.);
#6491=ORIENTED_EDGE('',*,*,#4802,.F.);
#6492=ORIENTED_EDGE('',*,*,#4803,.T.);
#6493=ORIENTED_EDGE('',*,*,#4799,.T.);
#6494=ORIENTED_EDGE('',*,*,#4804,.F.);
#6495=ORIENTED_EDGE('',*,*,#4805,.F.);
#6496=ORIENTED_EDGE('',*,*,#4806,.T.);
#6497=ORIENTED_EDGE('',*,*,#4802,.T.);
#6498=ORIENTED_EDGE('',*,*,#4807,.F.);
#6499=ORIENTED_EDGE('',*,*,#4808,.F.);
#6500=ORIENTED_EDGE('',*,*,#4809,.T.);
#6501=ORIENTED_EDGE('',*,*,#4805,.T.);
#6502=ORIENTED_EDGE('',*,*,#4810,.F.);
#6503=ORIENTED_EDGE('',*,*,#4811,.F.);
#6504=ORIENTED_EDGE('',*,*,#4812,.T.);
#6505=ORIENTED_EDGE('',*,*,#4808,.T.);
#6506=ORIENTED_EDGE('',*,*,#4813,.F.);
#6507=ORIENTED_EDGE('',*,*,#4814,.F.);
#6508=ORIENTED_EDGE('',*,*,#4815,.T.);
#6509=ORIENTED_EDGE('',*,*,#4811,.T.);
#6510=ORIENTED_EDGE('',*,*,#4816,.F.);
#6511=ORIENTED_EDGE('',*,*,#4817,.F.);
#6512=ORIENTED_EDGE('',*,*,#4818,.T.);
#6513=ORIENTED_EDGE('',*,*,#4814,.T.);
#6514=ORIENTED_EDGE('',*,*,#4819,.F.);
#6515=ORIENTED_EDGE('',*,*,#4820,.F.);
#6516=ORIENTED_EDGE('',*,*,#4821,.T.);
#6517=ORIENTED_EDGE('',*,*,#4817,.T.);
#6518=ORIENTED_EDGE('',*,*,#4822,.F.);
#6519=ORIENTED_EDGE('',*,*,#4823,.F.);
#6520=ORIENTED_EDGE('',*,*,#4824,.T.);
#6521=ORIENTED_EDGE('',*,*,#4820,.T.);
#6522=ORIENTED_EDGE('',*,*,#4825,.F.);
#6523=ORIENTED_EDGE('',*,*,#4826,.F.);
#6524=ORIENTED_EDGE('',*,*,#4827,.T.);
#6525=ORIENTED_EDGE('',*,*,#4823,.T.);
#6526=ORIENTED_EDGE('',*,*,#4828,.F.);
#6527=ORIENTED_EDGE('',*,*,#4829,.F.);
#6528=ORIENTED_EDGE('',*,*,#4830,.T.);
#6529=ORIENTED_EDGE('',*,*,#4826,.T.);
#6530=ORIENTED_EDGE('',*,*,#4831,.F.);
#6531=ORIENTED_EDGE('',*,*,#4832,.F.);
#6532=ORIENTED_EDGE('',*,*,#4833,.T.);
#6533=ORIENTED_EDGE('',*,*,#4829,.T.);
#6534=ORIENTED_EDGE('',*,*,#4834,.F.);
#6535=ORIENTED_EDGE('',*,*,#4835,.F.);
#6536=ORIENTED_EDGE('',*,*,#4836,.T.);
#6537=ORIENTED_EDGE('',*,*,#4832,.T.);
#6538=ORIENTED_EDGE('',*,*,#4837,.F.);
#6539=ORIENTED_EDGE('',*,*,#4838,.F.);
#6540=ORIENTED_EDGE('',*,*,#4839,.T.);
#6541=ORIENTED_EDGE('',*,*,#4835,.T.);
#6542=ORIENTED_EDGE('',*,*,#4840,.F.);
#6543=ORIENTED_EDGE('',*,*,#4841,.F.);
#6544=ORIENTED_EDGE('',*,*,#4842,.T.);
#6545=ORIENTED_EDGE('',*,*,#4838,.T.);
#6546=ORIENTED_EDGE('',*,*,#4843,.F.);
#6547=ORIENTED_EDGE('',*,*,#4844,.F.);
#6548=ORIENTED_EDGE('',*,*,#4845,.T.);
#6549=ORIENTED_EDGE('',*,*,#4841,.T.);
#6550=ORIENTED_EDGE('',*,*,#4846,.F.);
#6551=ORIENTED_EDGE('',*,*,#4847,.F.);
#6552=ORIENTED_EDGE('',*,*,#4848,.T.);
#6553=ORIENTED_EDGE('',*,*,#4844,.T.);
#6554=ORIENTED_EDGE('',*,*,#4849,.F.);
#6555=ORIENTED_EDGE('',*,*,#4850,.F.);
#6556=ORIENTED_EDGE('',*,*,#4851,.T.);
#6557=ORIENTED_EDGE('',*,*,#4847,.T.);
#6558=ORIENTED_EDGE('',*,*,#4852,.F.);
#6559=ORIENTED_EDGE('',*,*,#4853,.F.);
#6560=ORIENTED_EDGE('',*,*,#4854,.T.);
#6561=ORIENTED_EDGE('',*,*,#4850,.T.);
#6562=ORIENTED_EDGE('',*,*,#4855,.F.);
#6563=ORIENTED_EDGE('',*,*,#4856,.F.);
#6564=ORIENTED_EDGE('',*,*,#4857,.T.);
#6565=ORIENTED_EDGE('',*,*,#4853,.T.);
#6566=ORIENTED_EDGE('',*,*,#4858,.F.);
#6567=ORIENTED_EDGE('',*,*,#4859,.F.);
#6568=ORIENTED_EDGE('',*,*,#4860,.T.);
#6569=ORIENTED_EDGE('',*,*,#4856,.T.);
#6570=ORIENTED_EDGE('',*,*,#4861,.F.);
#6571=ORIENTED_EDGE('',*,*,#4862,.F.);
#6572=ORIENTED_EDGE('',*,*,#4863,.T.);
#6573=ORIENTED_EDGE('',*,*,#4859,.T.);
#6574=ORIENTED_EDGE('',*,*,#4864,.F.);
#6575=ORIENTED_EDGE('',*,*,#4865,.F.);
#6576=ORIENTED_EDGE('',*,*,#4866,.T.);
#6577=ORIENTED_EDGE('',*,*,#4862,.T.);
#6578=ORIENTED_EDGE('',*,*,#4867,.F.);
#6579=ORIENTED_EDGE('',*,*,#4868,.F.);
#6580=ORIENTED_EDGE('',*,*,#4869,.T.);
#6581=ORIENTED_EDGE('',*,*,#4865,.T.);
#6582=ORIENTED_EDGE('',*,*,#4870,.F.);
#6583=ORIENTED_EDGE('',*,*,#4871,.F.);
#6584=ORIENTED_EDGE('',*,*,#4872,.T.);
#6585=ORIENTED_EDGE('',*,*,#4868,.T.);
#6586=ORIENTED_EDGE('',*,*,#4873,.F.);
#6587=ORIENTED_EDGE('',*,*,#4874,.F.);
#6588=ORIENTED_EDGE('',*,*,#4875,.T.);
#6589=ORIENTED_EDGE('',*,*,#4871,.T.);
#6590=ORIENTED_EDGE('',*,*,#4876,.F.);
#6591=ORIENTED_EDGE('',*,*,#4877,.F.);
#6592=ORIENTED_EDGE('',*,*,#4878,.T.);
#6593=ORIENTED_EDGE('',*,*,#4874,.T.);
#6594=ORIENTED_EDGE('',*,*,#4879,.F.);
#6595=ORIENTED_EDGE('',*,*,#4880,.F.);
#6596=ORIENTED_EDGE('',*,*,#4881,.T.);
#6597=ORIENTED_EDGE('',*,*,#4877,.T.);
#6598=ORIENTED_EDGE('',*,*,#4882,.F.);
#6599=ORIENTED_EDGE('',*,*,#4883,.F.);
#6600=ORIENTED_EDGE('',*,*,#4884,.T.);
#6601=ORIENTED_EDGE('',*,*,#4880,.T.);
#6602=ORIENTED_EDGE('',*,*,#4885,.F.);
#6603=ORIENTED_EDGE('',*,*,#4886,.F.);
#6604=ORIENTED_EDGE('',*,*,#4887,.T.);
#6605=ORIENTED_EDGE('',*,*,#4883,.T.);
#6606=ORIENTED_EDGE('',*,*,#4888,.F.);
#6607=ORIENTED_EDGE('',*,*,#4889,.F.);
#6608=ORIENTED_EDGE('',*,*,#4890,.T.);
#6609=ORIENTED_EDGE('',*,*,#4886,.T.);
#6610=ORIENTED_EDGE('',*,*,#4891,.F.);
#6611=ORIENTED_EDGE('',*,*,#4892,.F.);
#6612=ORIENTED_EDGE('',*,*,#4893,.T.);
#6613=ORIENTED_EDGE('',*,*,#4889,.T.);
#6614=ORIENTED_EDGE('',*,*,#4894,.F.);
#6615=ORIENTED_EDGE('',*,*,#4895,.F.);
#6616=ORIENTED_EDGE('',*,*,#4896,.T.);
#6617=ORIENTED_EDGE('',*,*,#4892,.T.);
#6618=ORIENTED_EDGE('',*,*,#4897,.F.);
#6619=ORIENTED_EDGE('',*,*,#4898,.F.);
#6620=ORIENTED_EDGE('',*,*,#4899,.T.);
#6621=ORIENTED_EDGE('',*,*,#4895,.T.);
#6622=ORIENTED_EDGE('',*,*,#4900,.F.);
#6623=ORIENTED_EDGE('',*,*,#4901,.F.);
#6624=ORIENTED_EDGE('',*,*,#4902,.T.);
#6625=ORIENTED_EDGE('',*,*,#4898,.T.);
#6626=ORIENTED_EDGE('',*,*,#4903,.F.);
#6627=ORIENTED_EDGE('',*,*,#4904,.F.);
#6628=ORIENTED_EDGE('',*,*,#4905,.T.);
#6629=ORIENTED_EDGE('',*,*,#4901,.T.);
#6630=ORIENTED_EDGE('',*,*,#4906,.F.);
#6631=ORIENTED_EDGE('',*,*,#4907,.F.);
#6632=ORIENTED_EDGE('',*,*,#4908,.T.);
#6633=ORIENTED_EDGE('',*,*,#4904,.T.);
#6634=ORIENTED_EDGE('',*,*,#4909,.F.);
#6635=ORIENTED_EDGE('',*,*,#4910,.F.);
#6636=ORIENTED_EDGE('',*,*,#4911,.T.);
#6637=ORIENTED_EDGE('',*,*,#4907,.T.);
#6638=ORIENTED_EDGE('',*,*,#4912,.F.);
#6639=ORIENTED_EDGE('',*,*,#4913,.F.);
#6640=ORIENTED_EDGE('',*,*,#4914,.T.);
#6641=ORIENTED_EDGE('',*,*,#4910,.T.);
#6642=ORIENTED_EDGE('',*,*,#4915,.F.);
#6643=ORIENTED_EDGE('',*,*,#4916,.F.);
#6644=ORIENTED_EDGE('',*,*,#4917,.T.);
#6645=ORIENTED_EDGE('',*,*,#4913,.T.);
#6646=ORIENTED_EDGE('',*,*,#4918,.F.);
#6647=ORIENTED_EDGE('',*,*,#4919,.F.);
#6648=ORIENTED_EDGE('',*,*,#4920,.T.);
#6649=ORIENTED_EDGE('',*,*,#4916,.T.);
#6650=ORIENTED_EDGE('',*,*,#4921,.F.);
#6651=ORIENTED_EDGE('',*,*,#4922,.F.);
#6652=ORIENTED_EDGE('',*,*,#4923,.T.);
#6653=ORIENTED_EDGE('',*,*,#4919,.T.);
#6654=ORIENTED_EDGE('',*,*,#4924,.F.);
#6655=ORIENTED_EDGE('',*,*,#4925,.F.);
#6656=ORIENTED_EDGE('',*,*,#4926,.T.);
#6657=ORIENTED_EDGE('',*,*,#4922,.T.);
#6658=ORIENTED_EDGE('',*,*,#4927,.F.);
#6659=ORIENTED_EDGE('',*,*,#4928,.F.);
#6660=ORIENTED_EDGE('',*,*,#4929,.T.);
#6661=ORIENTED_EDGE('',*,*,#4925,.T.);
#6662=ORIENTED_EDGE('',*,*,#4930,.F.);
#6663=ORIENTED_EDGE('',*,*,#4931,.F.);
#6664=ORIENTED_EDGE('',*,*,#4932,.T.);
#6665=ORIENTED_EDGE('',*,*,#4928,.T.);
#6666=ORIENTED_EDGE('',*,*,#4933,.F.);
#6667=ORIENTED_EDGE('',*,*,#4934,.F.);
#6668=ORIENTED_EDGE('',*,*,#4935,.T.);
#6669=ORIENTED_EDGE('',*,*,#4931,.T.);
#6670=ORIENTED_EDGE('',*,*,#4936,.F.);
#6671=ORIENTED_EDGE('',*,*,#4937,.F.);
#6672=ORIENTED_EDGE('',*,*,#4938,.T.);
#6673=ORIENTED_EDGE('',*,*,#4934,.T.);
#6674=ORIENTED_EDGE('',*,*,#4939,.F.);
#6675=ORIENTED_EDGE('',*,*,#4940,.F.);
#6676=ORIENTED_EDGE('',*,*,#4941,.T.);
#6677=ORIENTED_EDGE('',*,*,#4937,.T.);
#6678=ORIENTED_EDGE('',*,*,#4942,.F.);
#6679=ORIENTED_EDGE('',*,*,#4943,.F.);
#6680=ORIENTED_EDGE('',*,*,#4944,.T.);
#6681=ORIENTED_EDGE('',*,*,#4940,.T.);
#6682=ORIENTED_EDGE('',*,*,#4945,.F.);
#6683=ORIENTED_EDGE('',*,*,#4946,.F.);
#6684=ORIENTED_EDGE('',*,*,#4947,.T.);
#6685=ORIENTED_EDGE('',*,*,#4943,.T.);
#6686=ORIENTED_EDGE('',*,*,#4948,.F.);
#6687=ORIENTED_EDGE('',*,*,#4949,.F.);
#6688=ORIENTED_EDGE('',*,*,#4950,.T.);
#6689=ORIENTED_EDGE('',*,*,#4946,.T.);
#6690=ORIENTED_EDGE('',*,*,#4951,.F.);
#6691=ORIENTED_EDGE('',*,*,#4952,.F.);
#6692=ORIENTED_EDGE('',*,*,#4953,.T.);
#6693=ORIENTED_EDGE('',*,*,#4949,.T.);
#6694=ORIENTED_EDGE('',*,*,#4954,.F.);
#6695=ORIENTED_EDGE('',*,*,#4955,.F.);
#6696=ORIENTED_EDGE('',*,*,#4956,.T.);
#6697=ORIENTED_EDGE('',*,*,#4952,.T.);
#6698=ORIENTED_EDGE('',*,*,#4957,.F.);
#6699=ORIENTED_EDGE('',*,*,#4958,.F.);
#6700=ORIENTED_EDGE('',*,*,#4959,.T.);
#6701=ORIENTED_EDGE('',*,*,#4955,.T.);
#6702=ORIENTED_EDGE('',*,*,#4960,.F.);
#6703=ORIENTED_EDGE('',*,*,#4961,.F.);
#6704=ORIENTED_EDGE('',*,*,#4962,.T.);
#6705=ORIENTED_EDGE('',*,*,#4958,.T.);
#6706=ORIENTED_EDGE('',*,*,#4963,.F.);
#6707=ORIENTED_EDGE('',*,*,#4964,.F.);
#6708=ORIENTED_EDGE('',*,*,#4965,.T.);
#6709=ORIENTED_EDGE('',*,*,#4961,.T.);
#6710=ORIENTED_EDGE('',*,*,#4966,.F.);
#6711=ORIENTED_EDGE('',*,*,#4967,.F.);
#6712=ORIENTED_EDGE('',*,*,#4968,.T.);
#6713=ORIENTED_EDGE('',*,*,#4964,.T.);
#6714=ORIENTED_EDGE('',*,*,#4969,.F.);
#6715=ORIENTED_EDGE('',*,*,#4970,.F.);
#6716=ORIENTED_EDGE('',*,*,#4971,.T.);
#6717=ORIENTED_EDGE('',*,*,#4967,.T.);
#6718=ORIENTED_EDGE('',*,*,#4972,.F.);
#6719=ORIENTED_EDGE('',*,*,#4973,.F.);
#6720=ORIENTED_EDGE('',*,*,#4974,.T.);
#6721=ORIENTED_EDGE('',*,*,#4970,.T.);
#6722=ORIENTED_EDGE('',*,*,#4975,.F.);
#6723=ORIENTED_EDGE('',*,*,#4976,.F.);
#6724=ORIENTED_EDGE('',*,*,#4977,.F.);
#6725=ORIENTED_EDGE('',*,*,#4785,.F.);
#6726=ORIENTED_EDGE('',*,*,#4782,.F.);
#6727=ORIENTED_EDGE('',*,*,#4779,.F.);
#6728=ORIENTED_EDGE('',*,*,#4776,.F.);
#6729=ORIENTED_EDGE('',*,*,#4773,.F.);
#6730=ORIENTED_EDGE('',*,*,#4770,.F.);
#6731=ORIENTED_EDGE('',*,*,#4767,.F.);
#6732=ORIENTED_EDGE('',*,*,#4764,.F.);
#6733=ORIENTED_EDGE('',*,*,#4761,.F.);
#6734=ORIENTED_EDGE('',*,*,#4758,.F.);
#6735=ORIENTED_EDGE('',*,*,#4755,.F.);
#6736=ORIENTED_EDGE('',*,*,#4752,.F.);
#6737=ORIENTED_EDGE('',*,*,#4749,.F.);
#6738=ORIENTED_EDGE('',*,*,#4746,.F.);
#6739=ORIENTED_EDGE('',*,*,#4743,.F.);
#6740=ORIENTED_EDGE('',*,*,#4740,.F.);
#6741=ORIENTED_EDGE('',*,*,#4737,.F.);
#6742=ORIENTED_EDGE('',*,*,#4734,.F.);
#6743=ORIENTED_EDGE('',*,*,#4731,.F.);
#6744=ORIENTED_EDGE('',*,*,#4728,.F.);
#6745=ORIENTED_EDGE('',*,*,#4725,.F.);
#6746=ORIENTED_EDGE('',*,*,#4722,.F.);
#6747=ORIENTED_EDGE('',*,*,#4719,.F.);
#6748=ORIENTED_EDGE('',*,*,#4716,.F.);
#6749=ORIENTED_EDGE('',*,*,#4713,.F.);
#6750=ORIENTED_EDGE('',*,*,#4710,.F.);
#6751=ORIENTED_EDGE('',*,*,#4707,.F.);
#6752=ORIENTED_EDGE('',*,*,#4704,.F.);
#6753=ORIENTED_EDGE('',*,*,#4701,.F.);
#6754=ORIENTED_EDGE('',*,*,#4698,.F.);
#6755=ORIENTED_EDGE('',*,*,#4695,.F.);
#6756=ORIENTED_EDGE('',*,*,#4692,.F.);
#6757=ORIENTED_EDGE('',*,*,#4689,.F.);
#6758=ORIENTED_EDGE('',*,*,#4686,.F.);
#6759=ORIENTED_EDGE('',*,*,#4683,.F.);
#6760=ORIENTED_EDGE('',*,*,#4680,.F.);
#6761=ORIENTED_EDGE('',*,*,#4677,.F.);
#6762=ORIENTED_EDGE('',*,*,#4674,.F.);
#6763=ORIENTED_EDGE('',*,*,#4671,.F.);
#6764=ORIENTED_EDGE('',*,*,#4668,.F.);
#6765=ORIENTED_EDGE('',*,*,#4665,.F.);
#6766=ORIENTED_EDGE('',*,*,#4662,.F.);
#6767=ORIENTED_EDGE('',*,*,#4659,.F.);
#6768=ORIENTED_EDGE('',*,*,#4656,.F.);
#6769=ORIENTED_EDGE('',*,*,#4653,.F.);
#6770=ORIENTED_EDGE('',*,*,#4650,.F.);
#6771=ORIENTED_EDGE('',*,*,#4647,.F.);
#6772=ORIENTED_EDGE('',*,*,#4644,.F.);
#6773=ORIENTED_EDGE('',*,*,#4641,.F.);
#6774=ORIENTED_EDGE('',*,*,#4638,.F.);
#6775=ORIENTED_EDGE('',*,*,#4635,.F.);
#6776=ORIENTED_EDGE('',*,*,#4632,.F.);
#6777=ORIENTED_EDGE('',*,*,#4629,.F.);
#6778=ORIENTED_EDGE('',*,*,#4626,.F.);
#6779=ORIENTED_EDGE('',*,*,#4623,.F.);
#6780=ORIENTED_EDGE('',*,*,#4620,.F.);
#6781=ORIENTED_EDGE('',*,*,#4617,.F.);
#6782=ORIENTED_EDGE('',*,*,#4614,.F.);
#6783=ORIENTED_EDGE('',*,*,#4611,.F.);
#6784=ORIENTED_EDGE('',*,*,#4608,.F.);
#6785=ORIENTED_EDGE('',*,*,#4605,.F.);
#6786=ORIENTED_EDGE('',*,*,#4602,.F.);
#6787=ORIENTED_EDGE('',*,*,#4599,.F.);
#6788=ORIENTED_EDGE('',*,*,#4978,.F.);
#6789=ORIENTED_EDGE('',*,*,#4979,.T.);
#6790=ORIENTED_EDGE('',*,*,#4975,.T.);
#6791=ORIENTED_EDGE('',*,*,#4972,.T.);
#6792=ORIENTED_EDGE('',*,*,#4969,.T.);
#6793=ORIENTED_EDGE('',*,*,#4966,.T.);
#6794=ORIENTED_EDGE('',*,*,#4963,.T.);
#6795=ORIENTED_EDGE('',*,*,#4960,.T.);
#6796=ORIENTED_EDGE('',*,*,#4957,.T.);
#6797=ORIENTED_EDGE('',*,*,#4954,.T.);
#6798=ORIENTED_EDGE('',*,*,#4951,.T.);
#6799=ORIENTED_EDGE('',*,*,#4948,.T.);
#6800=ORIENTED_EDGE('',*,*,#4945,.T.);
#6801=ORIENTED_EDGE('',*,*,#4942,.T.);
#6802=ORIENTED_EDGE('',*,*,#4939,.T.);
#6803=ORIENTED_EDGE('',*,*,#4936,.T.);
#6804=ORIENTED_EDGE('',*,*,#4933,.T.);
#6805=ORIENTED_EDGE('',*,*,#4930,.T.);
#6806=ORIENTED_EDGE('',*,*,#4927,.T.);
#6807=ORIENTED_EDGE('',*,*,#4924,.T.);
#6808=ORIENTED_EDGE('',*,*,#4921,.T.);
#6809=ORIENTED_EDGE('',*,*,#4918,.T.);
#6810=ORIENTED_EDGE('',*,*,#4915,.T.);
#6811=ORIENTED_EDGE('',*,*,#4912,.T.);
#6812=ORIENTED_EDGE('',*,*,#4909,.T.);
#6813=ORIENTED_EDGE('',*,*,#4906,.T.);
#6814=ORIENTED_EDGE('',*,*,#4903,.T.);
#6815=ORIENTED_EDGE('',*,*,#4900,.T.);
#6816=ORIENTED_EDGE('',*,*,#4897,.T.);
#6817=ORIENTED_EDGE('',*,*,#4894,.T.);
#6818=ORIENTED_EDGE('',*,*,#4891,.T.);
#6819=ORIENTED_EDGE('',*,*,#4888,.T.);
#6820=ORIENTED_EDGE('',*,*,#4885,.T.);
#6821=ORIENTED_EDGE('',*,*,#4882,.T.);
#6822=ORIENTED_EDGE('',*,*,#4879,.T.);
#6823=ORIENTED_EDGE('',*,*,#4876,.T.);
#6824=ORIENTED_EDGE('',*,*,#4873,.T.);
#6825=ORIENTED_EDGE('',*,*,#4870,.T.);
#6826=ORIENTED_EDGE('',*,*,#4867,.T.);
#6827=ORIENTED_EDGE('',*,*,#4864,.T.);
#6828=ORIENTED_EDGE('',*,*,#4861,.T.);
#6829=ORIENTED_EDGE('',*,*,#4858,.T.);
#6830=ORIENTED_EDGE('',*,*,#4855,.T.);
#6831=ORIENTED_EDGE('',*,*,#4852,.T.);
#6832=ORIENTED_EDGE('',*,*,#4849,.T.);
#6833=ORIENTED_EDGE('',*,*,#4846,.T.);
#6834=ORIENTED_EDGE('',*,*,#4843,.T.);
#6835=ORIENTED_EDGE('',*,*,#4840,.T.);
#6836=ORIENTED_EDGE('',*,*,#4837,.T.);
#6837=ORIENTED_EDGE('',*,*,#4834,.T.);
#6838=ORIENTED_EDGE('',*,*,#4831,.T.);
#6839=ORIENTED_EDGE('',*,*,#4828,.T.);
#6840=ORIENTED_EDGE('',*,*,#4825,.T.);
#6841=ORIENTED_EDGE('',*,*,#4822,.T.);
#6842=ORIENTED_EDGE('',*,*,#4819,.T.);
#6843=ORIENTED_EDGE('',*,*,#4816,.T.);
#6844=ORIENTED_EDGE('',*,*,#4813,.T.);
#6845=ORIENTED_EDGE('',*,*,#4810,.T.);
#6846=ORIENTED_EDGE('',*,*,#4807,.T.);
#6847=ORIENTED_EDGE('',*,*,#4804,.T.);
#6848=ORIENTED_EDGE('',*,*,#4801,.T.);
#6849=ORIENTED_EDGE('',*,*,#4798,.T.);
#6850=ORIENTED_EDGE('',*,*,#4795,.T.);
#6851=ORIENTED_EDGE('',*,*,#4792,.T.);
#6852=ORIENTED_EDGE('',*,*,#4973,.T.);
#6853=ORIENTED_EDGE('',*,*,#4979,.F.);
#6854=ORIENTED_EDGE('',*,*,#4980,.F.);
#6855=ORIENTED_EDGE('',*,*,#4981,.T.);
#6856=ORIENTED_EDGE('',*,*,#4982,.F.);
#6857=ORIENTED_EDGE('',*,*,#4787,.F.);
#6858=ORIENTED_EDGE('',*,*,#4790,.F.);
#6859=ORIENTED_EDGE('',*,*,#4794,.F.);
#6860=ORIENTED_EDGE('',*,*,#4797,.F.);
#6861=ORIENTED_EDGE('',*,*,#4800,.F.);
#6862=ORIENTED_EDGE('',*,*,#4803,.F.);
#6863=ORIENTED_EDGE('',*,*,#4806,.F.);
#6864=ORIENTED_EDGE('',*,*,#4809,.F.);
#6865=ORIENTED_EDGE('',*,*,#4812,.F.);
#6866=ORIENTED_EDGE('',*,*,#4815,.F.);
#6867=ORIENTED_EDGE('',*,*,#4818,.F.);
#6868=ORIENTED_EDGE('',*,*,#4821,.F.);
#6869=ORIENTED_EDGE('',*,*,#4824,.F.);
#6870=ORIENTED_EDGE('',*,*,#4827,.F.);
#6871=ORIENTED_EDGE('',*,*,#4830,.F.);
#6872=ORIENTED_EDGE('',*,*,#4833,.F.);
#6873=ORIENTED_EDGE('',*,*,#4836,.F.);
#6874=ORIENTED_EDGE('',*,*,#4839,.F.);
#6875=ORIENTED_EDGE('',*,*,#4842,.F.);
#6876=ORIENTED_EDGE('',*,*,#4845,.F.);
#6877=ORIENTED_EDGE('',*,*,#4848,.F.);
#6878=ORIENTED_EDGE('',*,*,#4851,.F.);
#6879=ORIENTED_EDGE('',*,*,#4854,.F.);
#6880=ORIENTED_EDGE('',*,*,#4857,.F.);
#6881=ORIENTED_EDGE('',*,*,#4860,.F.);
#6882=ORIENTED_EDGE('',*,*,#4863,.F.);
#6883=ORIENTED_EDGE('',*,*,#4866,.F.);
#6884=ORIENTED_EDGE('',*,*,#4869,.F.);
#6885=ORIENTED_EDGE('',*,*,#4872,.F.);
#6886=ORIENTED_EDGE('',*,*,#4875,.F.);
#6887=ORIENTED_EDGE('',*,*,#4878,.F.);
#6888=ORIENTED_EDGE('',*,*,#4881,.F.);
#6889=ORIENTED_EDGE('',*,*,#4884,.F.);
#6890=ORIENTED_EDGE('',*,*,#4887,.F.);
#6891=ORIENTED_EDGE('',*,*,#4890,.F.);
#6892=ORIENTED_EDGE('',*,*,#4893,.F.);
#6893=ORIENTED_EDGE('',*,*,#4896,.F.);
#6894=ORIENTED_EDGE('',*,*,#4899,.F.);
#6895=ORIENTED_EDGE('',*,*,#4902,.F.);
#6896=ORIENTED_EDGE('',*,*,#4905,.F.);
#6897=ORIENTED_EDGE('',*,*,#4908,.F.);
#6898=ORIENTED_EDGE('',*,*,#4911,.F.);
#6899=ORIENTED_EDGE('',*,*,#4914,.F.);
#6900=ORIENTED_EDGE('',*,*,#4917,.F.);
#6901=ORIENTED_EDGE('',*,*,#4920,.F.);
#6902=ORIENTED_EDGE('',*,*,#4923,.F.);
#6903=ORIENTED_EDGE('',*,*,#4926,.F.);
#6904=ORIENTED_EDGE('',*,*,#4929,.F.);
#6905=ORIENTED_EDGE('',*,*,#4932,.F.);
#6906=ORIENTED_EDGE('',*,*,#4935,.F.);
#6907=ORIENTED_EDGE('',*,*,#4938,.F.);
#6908=ORIENTED_EDGE('',*,*,#4941,.F.);
#6909=ORIENTED_EDGE('',*,*,#4944,.F.);
#6910=ORIENTED_EDGE('',*,*,#4947,.F.);
#6911=ORIENTED_EDGE('',*,*,#4950,.F.);
#6912=ORIENTED_EDGE('',*,*,#4953,.F.);
#6913=ORIENTED_EDGE('',*,*,#4956,.F.);
#6914=ORIENTED_EDGE('',*,*,#4959,.F.);
#6915=ORIENTED_EDGE('',*,*,#4962,.F.);
#6916=ORIENTED_EDGE('',*,*,#4965,.F.);
#6917=ORIENTED_EDGE('',*,*,#4968,.F.);
#6918=ORIENTED_EDGE('',*,*,#4971,.F.);
#6919=ORIENTED_EDGE('',*,*,#4974,.F.);
#6920=ORIENTED_EDGE('',*,*,#4981,.F.);
#6921=ORIENTED_EDGE('',*,*,#4983,.F.);
#6922=ORIENTED_EDGE('',*,*,#4597,.F.);
#6923=ORIENTED_EDGE('',*,*,#4601,.F.);
#6924=ORIENTED_EDGE('',*,*,#4604,.F.);
#6925=ORIENTED_EDGE('',*,*,#4607,.F.);
#6926=ORIENTED_EDGE('',*,*,#4610,.F.);
#6927=ORIENTED_EDGE('',*,*,#4613,.F.);
#6928=ORIENTED_EDGE('',*,*,#4616,.F.);
#6929=ORIENTED_EDGE('',*,*,#4619,.F.);
#6930=ORIENTED_EDGE('',*,*,#4622,.F.);
#6931=ORIENTED_EDGE('',*,*,#4625,.F.);
#6932=ORIENTED_EDGE('',*,*,#4628,.F.);
#6933=ORIENTED_EDGE('',*,*,#4631,.F.);
#6934=ORIENTED_EDGE('',*,*,#4634,.F.);
#6935=ORIENTED_EDGE('',*,*,#4637,.F.);
#6936=ORIENTED_EDGE('',*,*,#4640,.F.);
#6937=ORIENTED_EDGE('',*,*,#4643,.F.);
#6938=ORIENTED_EDGE('',*,*,#4646,.F.);
#6939=ORIENTED_EDGE('',*,*,#4649,.F.);
#6940=ORIENTED_EDGE('',*,*,#4652,.F.);
#6941=ORIENTED_EDGE('',*,*,#4655,.F.);
#6942=ORIENTED_EDGE('',*,*,#4658,.F.);
#6943=ORIENTED_EDGE('',*,*,#4661,.F.);
#6944=ORIENTED_EDGE('',*,*,#4664,.F.);
#6945=ORIENTED_EDGE('',*,*,#4667,.F.);
#6946=ORIENTED_EDGE('',*,*,#4670,.F.);
#6947=ORIENTED_EDGE('',*,*,#4673,.F.);
#6948=ORIENTED_EDGE('',*,*,#4676,.F.);
#6949=ORIENTED_EDGE('',*,*,#4679,.F.);
#6950=ORIENTED_EDGE('',*,*,#4682,.F.);
#6951=ORIENTED_EDGE('',*,*,#4685,.F.);
#6952=ORIENTED_EDGE('',*,*,#4688,.F.);
#6953=ORIENTED_EDGE('',*,*,#4691,.F.);
#6954=ORIENTED_EDGE('',*,*,#4694,.F.);
#6955=ORIENTED_EDGE('',*,*,#4697,.F.);
#6956=ORIENTED_EDGE('',*,*,#4700,.F.);
#6957=ORIENTED_EDGE('',*,*,#4703,.F.);
#6958=ORIENTED_EDGE('',*,*,#4706,.F.);
#6959=ORIENTED_EDGE('',*,*,#4709,.F.);
#6960=ORIENTED_EDGE('',*,*,#4712,.F.);
#6961=ORIENTED_EDGE('',*,*,#4715,.F.);
#6962=ORIENTED_EDGE('',*,*,#4718,.F.);
#6963=ORIENTED_EDGE('',*,*,#4721,.F.);
#6964=ORIENTED_EDGE('',*,*,#4724,.F.);
#6965=ORIENTED_EDGE('',*,*,#4727,.F.);
#6966=ORIENTED_EDGE('',*,*,#4730,.F.);
#6967=ORIENTED_EDGE('',*,*,#4733,.F.);
#6968=ORIENTED_EDGE('',*,*,#4736,.F.);
#6969=ORIENTED_EDGE('',*,*,#4739,.F.);
#6970=ORIENTED_EDGE('',*,*,#4742,.F.);
#6971=ORIENTED_EDGE('',*,*,#4745,.F.);
#6972=ORIENTED_EDGE('',*,*,#4748,.F.);
#6973=ORIENTED_EDGE('',*,*,#4751,.F.);
#6974=ORIENTED_EDGE('',*,*,#4754,.F.);
#6975=ORIENTED_EDGE('',*,*,#4757,.F.);
#6976=ORIENTED_EDGE('',*,*,#4760,.F.);
#6977=ORIENTED_EDGE('',*,*,#4763,.F.);
#6978=ORIENTED_EDGE('',*,*,#4766,.F.);
#6979=ORIENTED_EDGE('',*,*,#4769,.F.);
#6980=ORIENTED_EDGE('',*,*,#4772,.F.);
#6981=ORIENTED_EDGE('',*,*,#4775,.F.);
#6982=ORIENTED_EDGE('',*,*,#4778,.F.);
#6983=ORIENTED_EDGE('',*,*,#4781,.F.);
#6984=ORIENTED_EDGE('',*,*,#4784,.F.);
#6985=ORIENTED_EDGE('',*,*,#4984,.F.);
#6986=ORIENTED_EDGE('',*,*,#4985,.F.);
#6987=ORIENTED_EDGE('',*,*,#4986,.T.);
#6988=ORIENTED_EDGE('',*,*,#4987,.F.);
#6989=ORIENTED_EDGE('',*,*,#4988,.F.);
#6990=ORIENTED_EDGE('',*,*,#4989,.F.);
#6991=ORIENTED_EDGE('',*,*,#4988,.T.);
#6992=ORIENTED_EDGE('',*,*,#4990,.T.);
#6993=ORIENTED_EDGE('',*,*,#4991,.T.);
#6994=ORIENTED_EDGE('',*,*,#4990,.F.);
#6995=ORIENTED_EDGE('',*,*,#4987,.T.);
#6996=ORIENTED_EDGE('',*,*,#4992,.T.);
#6997=ORIENTED_EDGE('',*,*,#4993,.F.);
#6998=ORIENTED_EDGE('',*,*,#4994,.F.);
#6999=ORIENTED_EDGE('',*,*,#4991,.F.);
#7000=ORIENTED_EDGE('',*,*,#4993,.T.);
#7001=ORIENTED_EDGE('',*,*,#4995,.T.);
#7002=ORIENTED_EDGE('',*,*,#4996,.F.);
#7003=ORIENTED_EDGE('',*,*,#4995,.F.);
#7004=ORIENTED_EDGE('',*,*,#4992,.F.);
#7005=ORIENTED_EDGE('',*,*,#4986,.F.);
#7006=ORIENTED_EDGE('',*,*,#4997,.F.);
#7007=ORIENTED_EDGE('',*,*,#4998,.T.);
#7008=ORIENTED_EDGE('',*,*,#4999,.F.);
#7009=ORIENTED_EDGE('',*,*,#4998,.F.);
#7010=ORIENTED_EDGE('',*,*,#4994,.T.);
#7011=ORIENTED_EDGE('',*,*,#4996,.T.);
#7012=ORIENTED_EDGE('',*,*,#4985,.T.);
#7013=ORIENTED_EDGE('',*,*,#4989,.T.);
#7014=ORIENTED_EDGE('',*,*,#4997,.T.);
#7015=ORIENTED_EDGE('',*,*,#5000,.F.);
#7016=ORIENTED_EDGE('',*,*,#5001,.T.);
#7017=ORIENTED_EDGE('',*,*,#4976,.T.);
#7018=ORIENTED_EDGE('',*,*,#4791,.T.);
#7019=ORIENTED_EDGE('',*,*,#4788,.T.);
#7020=ORIENTED_EDGE('',*,*,#4982,.T.);
#7021=ORIENTED_EDGE('',*,*,#5002,.F.);
#7022=ORIENTED_EDGE('',*,*,#5003,.T.);
#7023=ORIENTED_EDGE('',*,*,#5000,.T.);
#7024=ORIENTED_EDGE('',*,*,#5003,.F.);
#7025=ORIENTED_EDGE('',*,*,#5002,.T.);
#7026=ORIENTED_EDGE('',*,*,#4999,.T.);
#7027=ORIENTED_EDGE('',*,*,#4783,.T.);
#7028=ORIENTED_EDGE('',*,*,#4977,.T.);
#7029=ORIENTED_EDGE('',*,*,#5001,.F.);
#7030=ORIENTED_EDGE('',*,*,#4984,.T.);
#7031=ORIENTED_EDGE('',*,*,#4978,.T.);
#7032=ORIENTED_EDGE('',*,*,#4598,.F.);
#7033=ORIENTED_EDGE('',*,*,#4983,.T.);
#7034=ORIENTED_EDGE('',*,*,#4980,.T.);
#7433=CYLINDRICAL_SURFACE('',#8893,0.5941);
#7434=CYLINDRICAL_SURFACE('',#8895,0.5941);
#7435=CYLINDRICAL_SURFACE('',#8896,0.5941);
#7436=CYLINDRICAL_SURFACE('',#8897,0.5941);
#7437=CYLINDRICAL_SURFACE('',#8898,0.5941);
#7438=CYLINDRICAL_SURFACE('',#8899,0.5941);
#7439=CYLINDRICAL_SURFACE('',#8900,0.5941);
#7440=CYLINDRICAL_SURFACE('',#8901,0.5941);
#7441=CYLINDRICAL_SURFACE('',#8902,0.5941);
#7442=CYLINDRICAL_SURFACE('',#8903,0.5941);
#7443=CYLINDRICAL_SURFACE('',#8904,0.5941);
#7444=CYLINDRICAL_SURFACE('',#8905,0.5941);
#7445=CYLINDRICAL_SURFACE('',#8906,0.5941);
#7446=CYLINDRICAL_SURFACE('',#8907,0.5941);
#7447=CYLINDRICAL_SURFACE('',#8908,0.5941);
#7448=CYLINDRICAL_SURFACE('',#8909,0.5941);
#7449=CYLINDRICAL_SURFACE('',#8910,0.5941);
#7450=CYLINDRICAL_SURFACE('',#8911,0.5941);
#7451=CYLINDRICAL_SURFACE('',#8912,0.5941);
#7452=CYLINDRICAL_SURFACE('',#8913,0.5941);
#7453=CYLINDRICAL_SURFACE('',#8914,0.5941);
#7454=CYLINDRICAL_SURFACE('',#8915,0.5941);
#7455=CYLINDRICAL_SURFACE('',#8916,0.5941);
#7456=CYLINDRICAL_SURFACE('',#8917,0.5941);
#7457=CYLINDRICAL_SURFACE('',#8918,0.5941);
#7458=CYLINDRICAL_SURFACE('',#8919,0.5941);
#7459=CYLINDRICAL_SURFACE('',#8920,0.5941);
#7460=CYLINDRICAL_SURFACE('',#8921,0.5941);
#7461=CYLINDRICAL_SURFACE('',#8922,0.5941);
#7462=CYLINDRICAL_SURFACE('',#8923,0.5941);
#7463=CYLINDRICAL_SURFACE('',#8924,0.5941);
#7464=CYLINDRICAL_SURFACE('',#8925,0.5941);
#7465=CYLINDRICAL_SURFACE('',#8926,0.5941);
#7466=CYLINDRICAL_SURFACE('',#8927,0.5941);
#7467=CYLINDRICAL_SURFACE('',#8928,0.5941);
#7468=CYLINDRICAL_SURFACE('',#8929,0.5941);
#7469=CYLINDRICAL_SURFACE('',#8930,0.5941);
#7470=CYLINDRICAL_SURFACE('',#8931,0.5941);
#7471=CYLINDRICAL_SURFACE('',#8932,0.5941);
#7472=CYLINDRICAL_SURFACE('',#8933,0.5941);
#7473=CYLINDRICAL_SURFACE('',#8934,0.5941);
#7474=CYLINDRICAL_SURFACE('',#8935,0.5941);
#7475=CYLINDRICAL_SURFACE('',#8936,0.5941);
#7476=CYLINDRICAL_SURFACE('',#8937,0.5941);
#7477=CYLINDRICAL_SURFACE('',#8938,0.5941);
#7478=CYLINDRICAL_SURFACE('',#8939,0.5941);
#7479=CYLINDRICAL_SURFACE('',#8940,0.5941);
#7480=CYLINDRICAL_SURFACE('',#8941,0.5941);
#7481=CYLINDRICAL_SURFACE('',#8942,0.5941);
#7482=CYLINDRICAL_SURFACE('',#8943,0.5941);
#7483=CYLINDRICAL_SURFACE('',#8944,0.5941);
#7484=CYLINDRICAL_SURFACE('',#8945,0.5941);
#7485=CYLINDRICAL_SURFACE('',#8946,0.5941);
#7486=CYLINDRICAL_SURFACE('',#8947,0.5941);
#7487=CYLINDRICAL_SURFACE('',#8948,0.5941);
#7488=CYLINDRICAL_SURFACE('',#8949,0.5941);
#7489=CYLINDRICAL_SURFACE('',#8950,0.5941);
#7490=CYLINDRICAL_SURFACE('',#8951,0.5941);
#7491=CYLINDRICAL_SURFACE('',#8952,0.5941);
#7492=CYLINDRICAL_SURFACE('',#8953,0.5941);
#7493=CYLINDRICAL_SURFACE('',#8954,0.5941);
#7494=CYLINDRICAL_SURFACE('',#8955,0.5941);
#7495=CYLINDRICAL_SURFACE('',#8956,0.5941);
#7496=CYLINDRICAL_SURFACE('',#8957,0.415875);
#7497=CYLINDRICAL_SURFACE('',#8959,0.415875);
#7498=CYLINDRICAL_SURFACE('',#8961,0.415875);
#7499=CYLINDRICAL_SURFACE('',#8962,0.415875);
#7500=CYLINDRICAL_SURFACE('',#8963,0.415875);
#7501=CYLINDRICAL_SURFACE('',#8964,0.415875);
#7502=CYLINDRICAL_SURFACE('',#8965,0.415875);
#7503=CYLINDRICAL_SURFACE('',#8966,0.415875);
#7504=CYLINDRICAL_SURFACE('',#8967,0.415875);
#7505=CYLINDRICAL_SURFACE('',#8968,0.415875);
#7506=CYLINDRICAL_SURFACE('',#8969,0.415875);
#7507=CYLINDRICAL_SURFACE('',#8970,0.415875);
#7508=CYLINDRICAL_SURFACE('',#8971,0.415875);
#7509=CYLINDRICAL_SURFACE('',#8972,0.415875);
#7510=CYLINDRICAL_SURFACE('',#8973,0.415875);
#7511=CYLINDRICAL_SURFACE('',#8974,0.415875);
#7512=CYLINDRICAL_SURFACE('',#8975,0.415875);
#7513=CYLINDRICAL_SURFACE('',#8976,0.415875);
#7514=CYLINDRICAL_SURFACE('',#8977,0.415875);
#7515=CYLINDRICAL_SURFACE('',#8978,0.415875);
#7516=CYLINDRICAL_SURFACE('',#8979,0.415875);
#7517=CYLINDRICAL_SURFACE('',#8980,0.415875);
#7518=CYLINDRICAL_SURFACE('',#8981,0.415875);
#7519=CYLINDRICAL_SURFACE('',#8982,0.415875);
#7520=CYLINDRICAL_SURFACE('',#8983,0.415875);
#7521=CYLINDRICAL_SURFACE('',#8984,0.415875);
#7522=CYLINDRICAL_SURFACE('',#8985,0.415875);
#7523=CYLINDRICAL_SURFACE('',#8986,0.415875);
#7524=CYLINDRICAL_SURFACE('',#8987,0.415875);
#7525=CYLINDRICAL_SURFACE('',#8988,0.415875);
#7526=CYLINDRICAL_SURFACE('',#8989,0.415875);
#7527=CYLINDRICAL_SURFACE('',#8990,0.415875);
#7528=CYLINDRICAL_SURFACE('',#8991,0.415875);
#7529=CYLINDRICAL_SURFACE('',#8992,0.415875);
#7530=CYLINDRICAL_SURFACE('',#8993,0.415875);
#7531=CYLINDRICAL_SURFACE('',#8994,0.415875);
#7532=CYLINDRICAL_SURFACE('',#8995,0.415875);
#7533=CYLINDRICAL_SURFACE('',#8996,0.415875);
#7534=CYLINDRICAL_SURFACE('',#8997,0.415875);
#7535=CYLINDRICAL_SURFACE('',#8998,0.415875);
#7536=CYLINDRICAL_SURFACE('',#8999,0.415875);
#7537=CYLINDRICAL_SURFACE('',#9000,0.415875);
#7538=CYLINDRICAL_SURFACE('',#9001,0.415875);
#7539=CYLINDRICAL_SURFACE('',#9002,0.415875);
#7540=CYLINDRICAL_SURFACE('',#9003,0.415875);
#7541=CYLINDRICAL_SURFACE('',#9004,0.415875);
#7542=CYLINDRICAL_SURFACE('',#9005,0.415875);
#7543=CYLINDRICAL_SURFACE('',#9006,0.415875);
#7544=CYLINDRICAL_SURFACE('',#9007,0.415875);
#7545=CYLINDRICAL_SURFACE('',#9008,0.415875);
#7546=CYLINDRICAL_SURFACE('',#9009,0.415875);
#7547=CYLINDRICAL_SURFACE('',#9010,0.415875);
#7548=CYLINDRICAL_SURFACE('',#9011,0.415875);
#7549=CYLINDRICAL_SURFACE('',#9012,0.415875);
#7550=CYLINDRICAL_SURFACE('',#9013,0.415875);
#7551=CYLINDRICAL_SURFACE('',#9014,0.415875);
#7552=CYLINDRICAL_SURFACE('',#9015,0.415875);
#7553=CYLINDRICAL_SURFACE('',#9016,0.415875);
#7554=CYLINDRICAL_SURFACE('',#9017,0.415875);
#7555=CYLINDRICAL_SURFACE('',#9018,0.415875);
#7556=CYLINDRICAL_SURFACE('',#9019,0.415875);
#7557=CYLINDRICAL_SURFACE('',#9020,0.415875);
#7558=CYLINDRICAL_SURFACE('',#9021,0.415875);
#7559=CYLINDRICAL_SURFACE('',#9022,0.415875);
#7560=CYLINDRICAL_SURFACE('',#9031,1.);
#7561=CYLINDRICAL_SURFACE('',#9038,1.35);
#7562=CYLINDRICAL_SURFACE('',#9041,0.5941);
#7836=ADVANCED_FACE('',(#1266),#7433,.T.);
#7837=ADVANCED_FACE('',(#1267),#7434,.T.);
#7838=ADVANCED_FACE('',(#1268),#7435,.T.);
#7839=ADVANCED_FACE('',(#1269),#7436,.T.);
#7840=ADVANCED_FACE('',(#1270),#7437,.T.);
#7841=ADVANCED_FACE('',(#1271),#7438,.T.);
#7842=ADVANCED_FACE('',(#1272),#7439,.T.);
#7843=ADVANCED_FACE('',(#1273),#7440,.T.);
#7844=ADVANCED_FACE('',(#1274),#7441,.T.);
#7845=ADVANCED_FACE('',(#1275),#7442,.T.);
#7846=ADVANCED_FACE('',(#1276),#7443,.T.);
#7847=ADVANCED_FACE('',(#1277),#7444,.T.);
#7848=ADVANCED_FACE('',(#1278),#7445,.T.);
#7849=ADVANCED_FACE('',(#1279),#7446,.T.);
#7850=ADVANCED_FACE('',(#1280),#7447,.T.);
#7851=ADVANCED_FACE('',(#1281),#7448,.T.);
#7852=ADVANCED_FACE('',(#1282),#7449,.T.);
#7853=ADVANCED_FACE('',(#1283),#7450,.T.);
#7854=ADVANCED_FACE('',(#1284),#7451,.T.);
#7855=ADVANCED_FACE('',(#1285),#7452,.T.);
#7856=ADVANCED_FACE('',(#1286),#7453,.T.);
#7857=ADVANCED_FACE('',(#1287),#7454,.T.);
#7858=ADVANCED_FACE('',(#1288),#7455,.T.);
#7859=ADVANCED_FACE('',(#1289),#7456,.T.);
#7860=ADVANCED_FACE('',(#1290),#7457,.T.);
#7861=ADVANCED_FACE('',(#1291),#7458,.T.);
#7862=ADVANCED_FACE('',(#1292),#7459,.T.);
#7863=ADVANCED_FACE('',(#1293),#7460,.T.);
#7864=ADVANCED_FACE('',(#1294),#7461,.T.);
#7865=ADVANCED_FACE('',(#1295),#7462,.T.);
#7866=ADVANCED_FACE('',(#1296),#7463,.T.);
#7867=ADVANCED_FACE('',(#1297),#7464,.T.);
#7868=ADVANCED_FACE('',(#1298),#7465,.T.);
#7869=ADVANCED_FACE('',(#1299),#7466,.T.);
#7870=ADVANCED_FACE('',(#1300),#7467,.T.);
#7871=ADVANCED_FACE('',(#1301),#7468,.T.);
#7872=ADVANCED_FACE('',(#1302),#7469,.T.);
#7873=ADVANCED_FACE('',(#1303),#7470,.T.);
#7874=ADVANCED_FACE('',(#1304),#7471,.T.);
#7875=ADVANCED_FACE('',(#1305),#7472,.T.);
#7876=ADVANCED_FACE('',(#1306),#7473,.T.);
#7877=ADVANCED_FACE('',(#1307),#7474,.T.);
#7878=ADVANCED_FACE('',(#1308),#7475,.T.);
#7879=ADVANCED_FACE('',(#1309),#7476,.T.);
#7880=ADVANCED_FACE('',(#1310),#7477,.T.);
#7881=ADVANCED_FACE('',(#1311),#7478,.T.);
#7882=ADVANCED_FACE('',(#1312),#7479,.T.);
#7883=ADVANCED_FACE('',(#1313),#7480,.T.);
#7884=ADVANCED_FACE('',(#1314),#7481,.T.);
#7885=ADVANCED_FACE('',(#1315),#7482,.T.);
#7886=ADVANCED_FACE('',(#1316),#7483,.T.);
#7887=ADVANCED_FACE('',(#1317),#7484,.T.);
#7888=ADVANCED_FACE('',(#1318),#7485,.T.);
#7889=ADVANCED_FACE('',(#1319),#7486,.T.);
#7890=ADVANCED_FACE('',(#1320),#7487,.T.);
#7891=ADVANCED_FACE('',(#1321),#7488,.T.);
#7892=ADVANCED_FACE('',(#1322),#7489,.T.);
#7893=ADVANCED_FACE('',(#1323),#7490,.T.);
#7894=ADVANCED_FACE('',(#1324),#7491,.T.);
#7895=ADVANCED_FACE('',(#1325),#7492,.T.);
#7896=ADVANCED_FACE('',(#1326),#7493,.T.);
#7897=ADVANCED_FACE('',(#1327),#7494,.T.);
#7898=ADVANCED_FACE('',(#1328),#7495,.T.);
#7899=ADVANCED_FACE('',(#1329),#7496,.T.);
#7900=ADVANCED_FACE('',(#1330),#7497,.T.);
#7901=ADVANCED_FACE('',(#1331),#7498,.T.);
#7902=ADVANCED_FACE('',(#1332),#7499,.T.);
#7903=ADVANCED_FACE('',(#1333),#7500,.T.);
#7904=ADVANCED_FACE('',(#1334),#7501,.T.);
#7905=ADVANCED_FACE('',(#1335),#7502,.T.);
#7906=ADVANCED_FACE('',(#1336),#7503,.T.);
#7907=ADVANCED_FACE('',(#1337),#7504,.T.);
#7908=ADVANCED_FACE('',(#1338),#7505,.T.);
#7909=ADVANCED_FACE('',(#1339),#7506,.T.);
#7910=ADVANCED_FACE('',(#1340),#7507,.T.);
#7911=ADVANCED_FACE('',(#1341),#7508,.T.);
#7912=ADVANCED_FACE('',(#1342),#7509,.T.);
#7913=ADVANCED_FACE('',(#1343),#7510,.T.);
#7914=ADVANCED_FACE('',(#1344),#7511,.T.);
#7915=ADVANCED_FACE('',(#1345),#7512,.T.);
#7916=ADVANCED_FACE('',(#1346),#7513,.T.);
#7917=ADVANCED_FACE('',(#1347),#7514,.T.);
#7918=ADVANCED_FACE('',(#1348),#7515,.T.);
#7919=ADVANCED_FACE('',(#1349),#7516,.T.);
#7920=ADVANCED_FACE('',(#1350),#7517,.T.);
#7921=ADVANCED_FACE('',(#1351),#7518,.T.);
#7922=ADVANCED_FACE('',(#1352),#7519,.T.);
#7923=ADVANCED_FACE('',(#1353),#7520,.T.);
#7924=ADVANCED_FACE('',(#1354),#7521,.T.);
#7925=ADVANCED_FACE('',(#1355),#7522,.T.);
#7926=ADVANCED_FACE('',(#1356),#7523,.T.);
#7927=ADVANCED_FACE('',(#1357),#7524,.T.);
#7928=ADVANCED_FACE('',(#1358),#7525,.T.);
#7929=ADVANCED_FACE('',(#1359),#7526,.T.);
#7930=ADVANCED_FACE('',(#1360),#7527,.T.);
#7931=ADVANCED_FACE('',(#1361),#7528,.T.);
#7932=ADVANCED_FACE('',(#1362),#7529,.T.);
#7933=ADVANCED_FACE('',(#1363),#7530,.T.);
#7934=ADVANCED_FACE('',(#1364),#7531,.T.);
#7935=ADVANCED_FACE('',(#1365),#7532,.T.);
#7936=ADVANCED_FACE('',(#1366),#7533,.T.);
#7937=ADVANCED_FACE('',(#1367),#7534,.T.);
#7938=ADVANCED_FACE('',(#1368),#7535,.T.);
#7939=ADVANCED_FACE('',(#1369),#7536,.T.);
#7940=ADVANCED_FACE('',(#1370),#7537,.T.);
#7941=ADVANCED_FACE('',(#1371),#7538,.T.);
#7942=ADVANCED_FACE('',(#1372),#7539,.T.);
#7943=ADVANCED_FACE('',(#1373),#7540,.T.);
#7944=ADVANCED_FACE('',(#1374),#7541,.T.);
#7945=ADVANCED_FACE('',(#1375),#7542,.T.);
#7946=ADVANCED_FACE('',(#1376),#7543,.T.);
#7947=ADVANCED_FACE('',(#1377),#7544,.T.);
#7948=ADVANCED_FACE('',(#1378),#7545,.T.);
#7949=ADVANCED_FACE('',(#1379),#7546,.T.);
#7950=ADVANCED_FACE('',(#1380),#7547,.T.);
#7951=ADVANCED_FACE('',(#1381),#7548,.T.);
#7952=ADVANCED_FACE('',(#1382),#7549,.T.);
#7953=ADVANCED_FACE('',(#1383),#7550,.T.);
#7954=ADVANCED_FACE('',(#1384),#7551,.T.);
#7955=ADVANCED_FACE('',(#1385),#7552,.T.);
#7956=ADVANCED_FACE('',(#1386),#7553,.T.);
#7957=ADVANCED_FACE('',(#1387),#7554,.T.);
#7958=ADVANCED_FACE('',(#1388),#7555,.T.);
#7959=ADVANCED_FACE('',(#1389),#7556,.T.);
#7960=ADVANCED_FACE('',(#1390),#7557,.T.);
#7961=ADVANCED_FACE('',(#1391),#7558,.T.);
#7962=ADVANCED_FACE('',(#1392),#13,.F.);
#7963=ADVANCED_FACE('',(#1393),#7559,.T.);
#7964=ADVANCED_FACE('',(#1394),#14,.F.);
#7965=ADVANCED_FACE('',(#1395),#953,.F.);
#7966=ADVANCED_FACE('',(#1396),#954,.T.);
#7967=ADVANCED_FACE('',(#1397),#955,.F.);
#7968=ADVANCED_FACE('',(#1398),#956,.F.);
#7969=ADVANCED_FACE('',(#1399),#957,.F.);
#7970=ADVANCED_FACE('',(#1400,#799),#7560,.T.);
#7971=ADVANCED_FACE('',(#1401),#958,.T.);
#7972=ADVANCED_FACE('',(#1402,#800),#959,.F.);
#7973=ADVANCED_FACE('',(#1403),#7561,.T.);
#7974=ADVANCED_FACE('',(#1404,#801),#960,.T.);
#7975=ADVANCED_FACE('',(#1405),#7562,.T.);
#7976=ADVANCED_FACE('',(#1406),#961,.F.);
#8081=CLOSED_SHELL('',(#7836,#7837,#7838,#7839,#7840,#7841,#7842,#7843,
#7844,#7845,#7846,#7847,#7848,#7849,#7850,#7851,#7852,#7853,#7854,#7855,
#7856,#7857,#7858,#7859,#7860,#7861,#7862,#7863,#7864,#7865,#7866,#7867,
#7868,#7869,#7870,#7871,#7872,#7873,#7874,#7875,#7876,#7877,#7878,#7879,
#7880,#7881,#7882,#7883,#7884,#7885,#7886,#7887,#7888,#7889,#7890,#7891,
#7892,#7893,#7894,#7895,#7896,#7897,#7898,#7899,#7900,#7901,#7902,#7903,
#7904,#7905,#7906,#7907,#7908,#7909,#7910,#7911,#7912,#7913,#7914,#7915,
#7916,#7917,#7918,#7919,#7920,#7921,#7922,#7923,#7924,#7925,#7926,#7927,
#7928,#7929,#7930,#7931,#7932,#7933,#7934,#7935,#7936,#7937,#7938,#7939,
#7940,#7941,#7942,#7943,#7944,#7945,#7946,#7947,#7948,#7949,#7950,#7951,
#7952,#7953,#7954,#7955,#7956,#7957,#7958,#7959,#7960,#7961,#7962,#7963,
#7964,#7965,#7966,#7967,#7968,#7969,#7970,#7971,#7972,#7973,#7974,#7975,
#7976));
#8892=AXIS2_PLACEMENT_3D('',#14867,#10455,#10456);
#8893=AXIS2_PLACEMENT_3D('',#14868,#10457,#10458);
#8894=AXIS2_PLACEMENT_3D('',#14893,#10460,#10461);
#8895=AXIS2_PLACEMENT_3D('',#14898,#10462,#10463);
#8896=AXIS2_PLACEMENT_3D('',#14985,#10465,#10466);
#8897=AXIS2_PLACEMENT_3D('',#15075,#10468,#10469);
#8898=AXIS2_PLACEMENT_3D('',#15162,#10471,#10472);
#8899=AXIS2_PLACEMENT_3D('',#15249,#10474,#10475);
#8900=AXIS2_PLACEMENT_3D('',#15336,#10477,#10478);
#8901=AXIS2_PLACEMENT_3D('',#15423,#10480,#10481);
#8902=AXIS2_PLACEMENT_3D('',#15510,#10483,#10484);
#8903=AXIS2_PLACEMENT_3D('',#15582,#10486,#10487);
#8904=AXIS2_PLACEMENT_3D('',#15633,#10489,#10490);
#8905=AXIS2_PLACEMENT_3D('',#15681,#10492,#10493);
#8906=AXIS2_PLACEMENT_3D('',#15729,#10495,#10496);
#8907=AXIS2_PLACEMENT_3D('',#15780,#10498,#10499);
#8908=AXIS2_PLACEMENT_3D('',#15831,#10501,#10502);
#8909=AXIS2_PLACEMENT_3D('',#15879,#10504,#10505);
#8910=AXIS2_PLACEMENT_3D('',#15930,#10507,#10508);
#8911=AXIS2_PLACEMENT_3D('',#15981,#10510,#10511);
#8912=AXIS2_PLACEMENT_3D('',#16029,#10513,#10514);
#8913=AXIS2_PLACEMENT_3D('',#16077,#10516,#10517);
#8914=AXIS2_PLACEMENT_3D('',#16128,#10519,#10520);
#8915=AXIS2_PLACEMENT_3D('',#16179,#10522,#10523);
#8916=AXIS2_PLACEMENT_3D('',#16227,#10525,#10526);
#8917=AXIS2_PLACEMENT_3D('',#16278,#10528,#10529);
#8918=AXIS2_PLACEMENT_3D('',#16329,#10531,#10532);
#8919=AXIS2_PLACEMENT_3D('',#16377,#10534,#10535);
#8920=AXIS2_PLACEMENT_3D('',#16425,#10537,#10538);
#8921=AXIS2_PLACEMENT_3D('',#16476,#10540,#10541);
#8922=AXIS2_PLACEMENT_3D('',#16527,#10543,#10544);
#8923=AXIS2_PLACEMENT_3D('',#16575,#10546,#10547);
#8924=AXIS2_PLACEMENT_3D('',#16626,#10549,#10550);
#8925=AXIS2_PLACEMENT_3D('',#16677,#10552,#10553);
#8926=AXIS2_PLACEMENT_3D('',#16725,#10555,#10556);
#8927=AXIS2_PLACEMENT_3D('',#16773,#10558,#10559);
#8928=AXIS2_PLACEMENT_3D('',#16824,#10561,#10562);
#8929=AXIS2_PLACEMENT_3D('',#16875,#10564,#10565);
#8930=AXIS2_PLACEMENT_3D('',#16923,#10567,#10568);
#8931=AXIS2_PLACEMENT_3D('',#16974,#10570,#10571);
#8932=AXIS2_PLACEMENT_3D('',#17025,#10573,#10574);
#8933=AXIS2_PLACEMENT_3D('',#17073,#10576,#10577);
#8934=AXIS2_PLACEMENT_3D('',#17121,#10579,#10580);
#8935=AXIS2_PLACEMENT_3D('',#17172,#10582,#10583);
#8936=AXIS2_PLACEMENT_3D('',#17223,#10585,#10586);
#8937=AXIS2_PLACEMENT_3D('',#17271,#10588,#10589);
#8938=AXIS2_PLACEMENT_3D('',#17322,#10591,#10592);
#8939=AXIS2_PLACEMENT_3D('',#17373,#10594,#10595);
#8940=AXIS2_PLACEMENT_3D('',#17421,#10597,#10598);
#8941=AXIS2_PLACEMENT_3D('',#17469,#10600,#10601);
#8942=AXIS2_PLACEMENT_3D('',#17520,#10603,#10604);
#8943=AXIS2_PLACEMENT_3D('',#17571,#10606,#10607);
#8944=AXIS2_PLACEMENT_3D('',#17619,#10609,#10610);
#8945=AXIS2_PLACEMENT_3D('',#17670,#10612,#10613);
#8946=AXIS2_PLACEMENT_3D('',#17721,#10615,#10616);
#8947=AXIS2_PLACEMENT_3D('',#17769,#10618,#10619);
#8948=AXIS2_PLACEMENT_3D('',#17817,#10621,#10622);
#8949=AXIS2_PLACEMENT_3D('',#17868,#10624,#10625);
#8950=AXIS2_PLACEMENT_3D('',#17934,#10627,#10628);
#8951=AXIS2_PLACEMENT_3D('',#18024,#10630,#10631);
#8952=AXIS2_PLACEMENT_3D('',#18111,#10633,#10634);
#8953=AXIS2_PLACEMENT_3D('',#18198,#10636,#10637);
#8954=AXIS2_PLACEMENT_3D('',#18285,#10639,#10640);
#8955=AXIS2_PLACEMENT_3D('',#18372,#10642,#10643);
#8956=AXIS2_PLACEMENT_3D('',#18459,#10645,#10646);
#8957=AXIS2_PLACEMENT_3D('',#18549,#10648,#10649);
#8958=AXIS2_PLACEMENT_3D('',#18558,#10651,#10652);
#8959=AXIS2_PLACEMENT_3D('',#18559,#10653,#10654);
#8960=AXIS2_PLACEMENT_3D('',#18581,#10656,#10657);
#8961=AXIS2_PLACEMENT_3D('',#18595,#10658,#10659);
#8962=AXIS2_PLACEMENT_3D('',#18633,#10661,#10662);
#8963=AXIS2_PLACEMENT_3D('',#18669,#10664,#10665);
#8964=AXIS2_PLACEMENT_3D('',#18707,#10667,#10668);
#8965=AXIS2_PLACEMENT_3D('',#18743,#10670,#10671);
#8966=AXIS2_PLACEMENT_3D('',#18781,#10673,#10674);
#8967=AXIS2_PLACEMENT_3D('',#18818,#10676,#10677);
#8968=AXIS2_PLACEMENT_3D('',#18853,#10679,#10680);
#8969=AXIS2_PLACEMENT_3D('',#18880,#10682,#10683);
#8970=AXIS2_PLACEMENT_3D('',#18904,#10685,#10686);
#8971=AXIS2_PLACEMENT_3D('',#18928,#10688,#10689);
#8972=AXIS2_PLACEMENT_3D('',#18952,#10691,#10692);
#8973=AXIS2_PLACEMENT_3D('',#18978,#10694,#10695);
#8974=AXIS2_PLACEMENT_3D('',#19002,#10697,#10698);
#8975=AXIS2_PLACEMENT_3D('',#19026,#10700,#10701);
#8976=AXIS2_PLACEMENT_3D('',#19052,#10703,#10704);
#8977=AXIS2_PLACEMENT_3D('',#19076,#10706,#10707);
#8978=AXIS2_PLACEMENT_3D('',#19100,#10709,#10710);
#8979=AXIS2_PLACEMENT_3D('',#19124,#10712,#10713);
#8980=AXIS2_PLACEMENT_3D('',#19150,#10715,#10716);
#8981=AXIS2_PLACEMENT_3D('',#19174,#10718,#10719);
#8982=AXIS2_PLACEMENT_3D('',#19198,#10721,#10722);
#8983=AXIS2_PLACEMENT_3D('',#19224,#10724,#10725);
#8984=AXIS2_PLACEMENT_3D('',#19248,#10727,#10728);
#8985=AXIS2_PLACEMENT_3D('',#19272,#10730,#10731);
#8986=AXIS2_PLACEMENT_3D('',#19296,#10733,#10734);
#8987=AXIS2_PLACEMENT_3D('',#19322,#10736,#10737);
#8988=AXIS2_PLACEMENT_3D('',#19346,#10739,#10740);
#8989=AXIS2_PLACEMENT_3D('',#19370,#10742,#10743);
#8990=AXIS2_PLACEMENT_3D('',#19396,#10745,#10746);
#8991=AXIS2_PLACEMENT_3D('',#19420,#10748,#10749);
#8992=AXIS2_PLACEMENT_3D('',#19444,#10751,#10752);
#8993=AXIS2_PLACEMENT_3D('',#19468,#10754,#10755);
#8994=AXIS2_PLACEMENT_3D('',#19494,#10757,#10758);
#8995=AXIS2_PLACEMENT_3D('',#19518,#10760,#10761);
#8996=AXIS2_PLACEMENT_3D('',#19542,#10763,#10764);
#8997=AXIS2_PLACEMENT_3D('',#19568,#10766,#10767);
#8998=AXIS2_PLACEMENT_3D('',#19592,#10769,#10770);
#8999=AXIS2_PLACEMENT_3D('',#19616,#10772,#10773);
#9000=AXIS2_PLACEMENT_3D('',#19640,#10775,#10776);
#9001=AXIS2_PLACEMENT_3D('',#19666,#10778,#10779);
#9002=AXIS2_PLACEMENT_3D('',#19690,#10781,#10782);
#9003=AXIS2_PLACEMENT_3D('',#19714,#10784,#10785);
#9004=AXIS2_PLACEMENT_3D('',#19740,#10787,#10788);
#9005=AXIS2_PLACEMENT_3D('',#19764,#10790,#10791);
#9006=AXIS2_PLACEMENT_3D('',#19788,#10793,#10794);
#9007=AXIS2_PLACEMENT_3D('',#19812,#10796,#10797);
#9008=AXIS2_PLACEMENT_3D('',#19838,#10799,#10800);
#9009=AXIS2_PLACEMENT_3D('',#19862,#10802,#10803);
#9010=AXIS2_PLACEMENT_3D('',#19886,#10805,#10806);
#9011=AXIS2_PLACEMENT_3D('',#19912,#10808,#10809);
#9012=AXIS2_PLACEMENT_3D('',#19936,#10811,#10812);
#9013=AXIS2_PLACEMENT_3D('',#19960,#10814,#10815);
#9014=AXIS2_PLACEMENT_3D('',#19985,#10817,#10818);
#9015=AXIS2_PLACEMENT_3D('',#20012,#10820,#10821);
#9016=AXIS2_PLACEMENT_3D('',#20049,#10823,#10824);
#9017=AXIS2_PLACEMENT_3D('',#20085,#10826,#10827);
#9018=AXIS2_PLACEMENT_3D('',#20123,#10829,#10830);
#9019=AXIS2_PLACEMENT_3D('',#20159,#10832,#10833);
#9020=AXIS2_PLACEMENT_3D('',#20197,#10835,#10836);
#9021=AXIS2_PLACEMENT_3D('',#20234,#10838,#10839);
#9022=AXIS2_PLACEMENT_3D('',#22382,#10841,#10842);
#9023=AXIS2_PLACEMENT_3D('',#22384,#10843,#10844);
#9024=AXIS2_PLACEMENT_3D('',#24476,#10845,#10846);
#9025=AXIS2_PLACEMENT_3D('',#24485,#10851,#10852);
#9026=AXIS2_PLACEMENT_3D('',#24487,#10853,#10854);
#9027=AXIS2_PLACEMENT_3D('',#24491,#10857,#10858);
#9028=AXIS2_PLACEMENT_3D('',#24495,#10861,#10862);
#9029=AXIS2_PLACEMENT_3D('',#24499,#10865,#10866);
#9030=AXIS2_PLACEMENT_3D('',#24500,#10867,#10868);
#9031=AXIS2_PLACEMENT_3D('',#24501,#10869,#10870);
#9032=AXIS2_PLACEMENT_3D('',#24503,#10871,#10872);
#9033=AXIS2_PLACEMENT_3D('',#24506,#10874,#10875);
#9034=AXIS2_PLACEMENT_3D('',#24507,#10876,#10877);
#9035=AXIS2_PLACEMENT_3D('',#24508,#10878,#10879);
#9036=AXIS2_PLACEMENT_3D('',#24510,#10880,#10881);
#9037=AXIS2_PLACEMENT_3D('',#24511,#10882,#10883);
#9038=AXIS2_PLACEMENT_3D('',#24512,#10884,#10885);
#9039=AXIS2_PLACEMENT_3D('',#24514,#10886,#10887);
#9040=AXIS2_PLACEMENT_3D('',#24516,#10889,#10890);
#9041=AXIS2_PLACEMENT_3D('',#24517,#10891,#10892);
#9042=AXIS2_PLACEMENT_3D('',#24518,#10893,#10894);
#10455=DIRECTION('axis',(0.,0.,1.));
#10456=DIRECTION('refdir',(1.,0.,0.));
#10457=DIRECTION('center_axis',(1.,0.,0.));
#10458=DIRECTION('ref_axis',(0.,0.975560628713931,0.219730425074181));
#10459=DIRECTION('',(-1.,0.,0.));
#10460=DIRECTION('center_axis',(-1.,0.,0.));
#10461=DIRECTION('ref_axis',(0.,0.,-1.));
#10462=DIRECTION('center_axis',(1.,0.,0.));
#10463=DIRECTION('ref_axis',(0.,0.,-1.));
#10464=DIRECTION('',(-1.,0.,0.));
#10465=DIRECTION('center_axis',(1.,0.,0.));
#10466=DIRECTION('ref_axis',(0.,0.,-1.));
#10467=DIRECTION('',(-1.,0.,0.));
#10468=DIRECTION('center_axis',(1.,0.,0.));
#10469=DIRECTION('ref_axis',(0.,0.,-1.));
#10470=DIRECTION('',(-1.,0.,0.));
#10471=DIRECTION('center_axis',(1.,0.,0.));
#10472=DIRECTION('ref_axis',(0.,0.,-1.));
#10473=DIRECTION('',(-1.,0.,0.));
#10474=DIRECTION('center_axis',(1.,0.,0.));
#10475=DIRECTION('ref_axis',(0.,0.,-1.));
#10476=DIRECTION('',(-1.,0.,0.));
#10477=DIRECTION('center_axis',(1.,0.,0.));
#10478=DIRECTION('ref_axis',(0.,0.,-1.));
#10479=DIRECTION('',(-1.,0.,0.));
#10480=DIRECTION('center_axis',(1.,0.,0.));
#10481=DIRECTION('ref_axis',(0.,0.,-1.));
#10482=DIRECTION('',(-1.,0.,0.));
#10483=DIRECTION('center_axis',(1.,0.,0.));
#10484=DIRECTION('ref_axis',(0.,0.,-1.));
#10485=DIRECTION('',(-1.,0.,0.));
#10486=DIRECTION('center_axis',(1.,0.,0.));
#10487=DIRECTION('ref_axis',(0.,0.,-1.));
#10488=DIRECTION('',(-1.,0.,0.));
#10489=DIRECTION('center_axis',(1.,0.,0.));
#10490=DIRECTION('ref_axis',(0.,0.,-1.));
#10491=DIRECTION('',(-1.,0.,0.));
#10492=DIRECTION('center_axis',(1.,0.,0.));
#10493=DIRECTION('ref_axis',(0.,0.,-1.));
#10494=DIRECTION('',(-1.,0.,0.));
#10495=DIRECTION('center_axis',(1.,0.,0.));
#10496=DIRECTION('ref_axis',(0.,0.,-1.));
#10497=DIRECTION('',(-1.,0.,0.));
#10498=DIRECTION('center_axis',(1.,0.,0.));
#10499=DIRECTION('ref_axis',(0.,0.,-1.));
#10500=DIRECTION('',(-1.,0.,0.));
#10501=DIRECTION('center_axis',(1.,0.,0.));
#10502=DIRECTION('ref_axis',(0.,0.,-1.));
#10503=DIRECTION('',(-1.,0.,0.));
#10504=DIRECTION('center_axis',(1.,0.,0.));
#10505=DIRECTION('ref_axis',(0.,0.,-1.));
#10506=DIRECTION('',(-1.,0.,0.));
#10507=DIRECTION('center_axis',(1.,0.,0.));
#10508=DIRECTION('ref_axis',(0.,0.,-1.));
#10509=DIRECTION('',(-1.,0.,0.));
#10510=DIRECTION('center_axis',(1.,0.,0.));
#10511=DIRECTION('ref_axis',(0.,0.,-1.));
#10512=DIRECTION('',(-1.,0.,0.));
#10513=DIRECTION('center_axis',(1.,0.,0.));
#10514=DIRECTION('ref_axis',(0.,0.,-1.));
#10515=DIRECTION('',(-1.,0.,0.));
#10516=DIRECTION('center_axis',(1.,0.,0.));
#10517=DIRECTION('ref_axis',(0.,0.,-1.));
#10518=DIRECTION('',(-1.,0.,0.));
#10519=DIRECTION('center_axis',(1.,0.,0.));
#10520=DIRECTION('ref_axis',(0.,0.,-1.));
#10521=DIRECTION('',(-1.,0.,0.));
#10522=DIRECTION('center_axis',(1.,0.,0.));
#10523=DIRECTION('ref_axis',(0.,0.,-1.));
#10524=DIRECTION('',(-1.,0.,0.));
#10525=DIRECTION('center_axis',(1.,0.,0.));
#10526=DIRECTION('ref_axis',(0.,0.,-1.));
#10527=DIRECTION('',(-1.,0.,0.));
#10528=DIRECTION('center_axis',(1.,0.,0.));
#10529=DIRECTION('ref_axis',(0.,0.,-1.));
#10530=DIRECTION('',(-1.,0.,0.));
#10531=DIRECTION('center_axis',(1.,0.,0.));
#10532=DIRECTION('ref_axis',(0.,0.,-1.));
#10533=DIRECTION('',(-1.,0.,0.));
#10534=DIRECTION('center_axis',(1.,0.,0.));
#10535=DIRECTION('ref_axis',(0.,0.,-1.));
#10536=DIRECTION('',(-1.,0.,0.));
#10537=DIRECTION('center_axis',(1.,0.,0.));
#10538=DIRECTION('ref_axis',(0.,0.,-1.));
#10539=DIRECTION('',(-1.,0.,0.));
#10540=DIRECTION('center_axis',(1.,0.,0.));
#10541=DIRECTION('ref_axis',(0.,0.,-1.));
#10542=DIRECTION('',(-1.,0.,0.));
#10543=DIRECTION('center_axis',(1.,0.,0.));
#10544=DIRECTION('ref_axis',(0.,0.,-1.));
#10545=DIRECTION('',(-1.,0.,0.));
#10546=DIRECTION('center_axis',(1.,0.,0.));
#10547=DIRECTION('ref_axis',(0.,0.,-1.));
#10548=DIRECTION('',(-1.,0.,0.));
#10549=DIRECTION('center_axis',(1.,0.,0.));
#10550=DIRECTION('ref_axis',(0.,0.,-1.));
#10551=DIRECTION('',(-1.,0.,0.));
#10552=DIRECTION('center_axis',(1.,0.,0.));
#10553=DIRECTION('ref_axis',(0.,0.,-1.));
#10554=DIRECTION('',(-1.,0.,0.));
#10555=DIRECTION('center_axis',(1.,0.,0.));
#10556=DIRECTION('ref_axis',(0.,0.,-1.));
#10557=DIRECTION('',(-1.,0.,0.));
#10558=DIRECTION('center_axis',(1.,0.,0.));
#10559=DIRECTION('ref_axis',(0.,0.,-1.));
#10560=DIRECTION('',(-1.,0.,0.));
#10561=DIRECTION('center_axis',(1.,0.,0.));
#10562=DIRECTION('ref_axis',(0.,0.,-1.));
#10563=DIRECTION('',(-1.,0.,0.));
#10564=DIRECTION('center_axis',(1.,0.,0.));
#10565=DIRECTION('ref_axis',(0.,0.,-1.));
#10566=DIRECTION('',(-1.,0.,0.));
#10567=DIRECTION('center_axis',(1.,0.,0.));
#10568=DIRECTION('ref_axis',(0.,0.,-1.));
#10569=DIRECTION('',(-1.,0.,0.));
#10570=DIRECTION('center_axis',(1.,0.,0.));
#10571=DIRECTION('ref_axis',(0.,0.,-1.));
#10572=DIRECTION('',(-1.,0.,0.));
#10573=DIRECTION('center_axis',(1.,0.,0.));
#10574=DIRECTION('ref_axis',(0.,0.,-1.));
#10575=DIRECTION('',(-1.,0.,0.));
#10576=DIRECTION('center_axis',(1.,0.,0.));
#10577=DIRECTION('ref_axis',(0.,0.,-1.));
#10578=DIRECTION('',(-1.,0.,0.));
#10579=DIRECTION('center_axis',(1.,0.,0.));
#10580=DIRECTION('ref_axis',(0.,0.,-1.));
#10581=DIRECTION('',(-1.,0.,0.));
#10582=DIRECTION('center_axis',(1.,0.,0.));
#10583=DIRECTION('ref_axis',(0.,0.,-1.));
#10584=DIRECTION('',(-1.,0.,0.));
#10585=DIRECTION('center_axis',(1.,0.,0.));
#10586=DIRECTION('ref_axis',(0.,0.,-1.));
#10587=DIRECTION('',(-1.,0.,0.));
#10588=DIRECTION('center_axis',(1.,0.,0.));
#10589=DIRECTION('ref_axis',(0.,0.,-1.));
#10590=DIRECTION('',(-1.,0.,0.));
#10591=DIRECTION('center_axis',(1.,0.,0.));
#10592=DIRECTION('ref_axis',(0.,0.,-1.));
#10593=DIRECTION('',(-1.,0.,0.));
#10594=DIRECTION('center_axis',(1.,0.,0.));
#10595=DIRECTION('ref_axis',(0.,0.,-1.));
#10596=DIRECTION('',(-1.,0.,0.));
#10597=DIRECTION('center_axis',(1.,0.,0.));
#10598=DIRECTION('ref_axis',(0.,0.,-1.));
#10599=DIRECTION('',(-1.,0.,0.));
#10600=DIRECTION('center_axis',(1.,0.,0.));
#10601=DIRECTION('ref_axis',(0.,0.,-1.));
#10602=DIRECTION('',(-1.,0.,0.));
#10603=DIRECTION('center_axis',(1.,0.,0.));
#10604=DIRECTION('ref_axis',(0.,0.,-1.));
#10605=DIRECTION('',(-1.,0.,0.));
#10606=DIRECTION('center_axis',(1.,0.,0.));
#10607=DIRECTION('ref_axis',(0.,0.,-1.));
#10608=DIRECTION('',(-1.,0.,0.));
#10609=DIRECTION('center_axis',(1.,0.,0.));
#10610=DIRECTION('ref_axis',(0.,0.,-1.));
#10611=DIRECTION('',(-1.,0.,0.));
#10612=DIRECTION('center_axis',(1.,0.,0.));
#10613=DIRECTION('ref_axis',(0.,0.,-1.));
#10614=DIRECTION('',(-1.,0.,0.));
#10615=DIRECTION('center_axis',(1.,0.,0.));
#10616=DIRECTION('ref_axis',(0.,0.,-1.));
#10617=DIRECTION('',(-1.,0.,0.));
#10618=DIRECTION('center_axis',(1.,0.,0.));
#10619=DIRECTION('ref_axis',(0.,0.,-1.));
#10620=DIRECTION('',(-1.,0.,0.));
#10621=DIRECTION('center_axis',(1.,0.,0.));
#10622=DIRECTION('ref_axis',(0.,0.,-1.));
#10623=DIRECTION('',(-1.,0.,0.));
#10624=DIRECTION('center_axis',(1.,0.,0.));
#10625=DIRECTION('ref_axis',(0.,0.,-1.));
#10626=DIRECTION('',(-1.,0.,0.));
#10627=DIRECTION('center_axis',(1.,0.,0.));
#10628=DIRECTION('ref_axis',(0.,0.,-1.));
#10629=DIRECTION('',(-1.,0.,0.));
#10630=DIRECTION('center_axis',(1.,0.,0.));
#10631=DIRECTION('ref_axis',(0.,0.,-1.));
#10632=DIRECTION('',(-1.,0.,0.));
#10633=DIRECTION('center_axis',(1.,0.,0.));
#10634=DIRECTION('ref_axis',(0.,0.,-1.));
#10635=DIRECTION('',(-1.,0.,0.));
#10636=DIRECTION('center_axis',(1.,0.,0.));
#10637=DIRECTION('ref_axis',(0.,0.,-1.));
#10638=DIRECTION('',(-1.,0.,0.));
#10639=DIRECTION('center_axis',(1.,0.,0.));
#10640=DIRECTION('ref_axis',(0.,0.,-1.));
#10641=DIRECTION('',(-1.,0.,0.));
#10642=DIRECTION('center_axis',(1.,0.,0.));
#10643=DIRECTION('ref_axis',(0.,0.,-1.));
#10644=DIRECTION('',(-1.,0.,0.));
#10645=DIRECTION('center_axis',(1.,0.,0.));
#10646=DIRECTION('ref_axis',(0.,0.,-1.));
#10647=DIRECTION('',(-1.,0.,0.));
#10648=DIRECTION('center_axis',(1.,0.,0.));
#10649=DIRECTION('ref_axis',(0.,-1.17203152359781E-12,-1.));
#10650=DIRECTION('',(1.,0.,0.));
#10651=DIRECTION('center_axis',(1.,0.,0.));
#10652=DIRECTION('ref_axis',(0.,-1.17203152359781E-12,-1.));
#10653=DIRECTION('center_axis',(1.,0.,0.));
#10654=DIRECTION('ref_axis',(0.,-1.17203152359781E-12,-1.));
#10655=DIRECTION('',(1.,0.,0.));
#10656=DIRECTION('center_axis',(1.,0.,0.));
#10657=DIRECTION('ref_axis',(0.,-1.17203152359781E-12,-1.));
#10658=DIRECTION('center_axis',(1.,0.,0.));
#10659=DIRECTION('ref_axis',(0.,-1.17203152359781E-12,-1.));
#10660=DIRECTION('',(1.,0.,0.));
#10661=DIRECTION('center_axis',(1.,0.,0.));
#10662=DIRECTION('ref_axis',(0.,-1.17203152359781E-12,-1.));
#10663=DIRECTION('',(1.,0.,0.));
#10664=DIRECTION('center_axis',(1.,0.,0.));
#10665=DIRECTION('ref_axis',(0.,-1.17203152359781E-12,-1.));
#10666=DIRECTION('',(1.,0.,0.));
#10667=DIRECTION('center_axis',(1.,0.,0.));
#10668=DIRECTION('ref_axis',(0.,-1.17203152359781E-12,-1.));
#10669=DIRECTION('',(1.,0.,0.));
#10670=DIRECTION('center_axis',(1.,0.,0.));
#10671=DIRECTION('ref_axis',(0.,-1.17203152359781E-12,-1.));
#10672=DIRECTION('',(1.,0.,0.));
#10673=DIRECTION('center_axis',(1.,0.,0.));
#10674=DIRECTION('ref_axis',(0.,-1.17203152359781E-12,-1.));
#10675=DIRECTION('',(1.,0.,0.));
#10676=DIRECTION('center_axis',(1.,0.,0.));
#10677=DIRECTION('ref_axis',(0.,-1.17203152359781E-12,-1.));
#10678=DIRECTION('',(1.,0.,0.));
#10679=DIRECTION('center_axis',(1.,0.,0.));
#10680=DIRECTION('ref_axis',(0.,-1.17203152359781E-12,-1.));
#10681=DIRECTION('',(1.,0.,0.));
#10682=DIRECTION('center_axis',(1.,0.,0.));
#10683=DIRECTION('ref_axis',(0.,-1.17203152359781E-12,-1.));
#10684=DIRECTION('',(1.,0.,0.));
#10685=DIRECTION('center_axis',(1.,0.,0.));
#10686=DIRECTION('ref_axis',(0.,-1.17203152359781E-12,-1.));
#10687=DIRECTION('',(1.,0.,0.));
#10688=DIRECTION('center_axis',(1.,0.,0.));
#10689=DIRECTION('ref_axis',(0.,-1.17203152359781E-12,-1.));
#10690=DIRECTION('',(1.,0.,0.));
#10691=DIRECTION('center_axis',(1.,0.,0.));
#10692=DIRECTION('ref_axis',(0.,-1.17203152359781E-12,-1.));
#10693=DIRECTION('',(1.,0.,0.));
#10694=DIRECTION('center_axis',(1.,0.,0.));
#10695=DIRECTION('ref_axis',(0.,-1.17203152359781E-12,-1.));
#10696=DIRECTION('',(1.,0.,0.));
#10697=DIRECTION('center_axis',(1.,0.,0.));
#10698=DIRECTION('ref_axis',(0.,-1.17203152359781E-12,-1.));
#10699=DIRECTION('',(1.,0.,0.));
#10700=DIRECTION('center_axis',(1.,0.,0.));
#10701=DIRECTION('ref_axis',(0.,-1.17203152359781E-12,-1.));
#10702=DIRECTION('',(1.,0.,0.));
#10703=DIRECTION('center_axis',(1.,0.,0.));
#10704=DIRECTION('ref_axis',(0.,-1.17203152359781E-12,-1.));
#10705=DIRECTION('',(1.,0.,0.));
#10706=DIRECTION('center_axis',(1.,0.,0.));
#10707=DIRECTION('ref_axis',(0.,-1.17203152359781E-12,-1.));
#10708=DIRECTION('',(1.,0.,0.));
#10709=DIRECTION('center_axis',(1.,0.,0.));
#10710=DIRECTION('ref_axis',(0.,-1.17203152359781E-12,-1.));
#10711=DIRECTION('',(1.,0.,0.));
#10712=DIRECTION('center_axis',(1.,0.,0.));
#10713=DIRECTION('ref_axis',(0.,-1.17203152359781E-12,-1.));
#10714=DIRECTION('',(1.,0.,0.));
#10715=DIRECTION('center_axis',(1.,0.,0.));
#10716=DIRECTION('ref_axis',(0.,-1.17203152359781E-12,-1.));
#10717=DIRECTION('',(1.,0.,0.));
#10718=DIRECTION('center_axis',(1.,0.,0.));
#10719=DIRECTION('ref_axis',(0.,-1.17203152359781E-12,-1.));
#10720=DIRECTION('',(1.,0.,0.));
#10721=DIRECTION('center_axis',(1.,0.,0.));
#10722=DIRECTION('ref_axis',(0.,-1.17203152359781E-12,-1.));
#10723=DIRECTION('',(1.,0.,0.));
#10724=DIRECTION('center_axis',(1.,0.,0.));
#10725=DIRECTION('ref_axis',(0.,-1.17203152359781E-12,-1.));
#10726=DIRECTION('',(1.,0.,0.));
#10727=DIRECTION('center_axis',(1.,0.,0.));
#10728=DIRECTION('ref_axis',(0.,-1.17203152359781E-12,-1.));
#10729=DIRECTION('',(1.,0.,0.));
#10730=DIRECTION('center_axis',(1.,0.,0.));
#10731=DIRECTION('ref_axis',(0.,-1.17203152359781E-12,-1.));
#10732=DIRECTION('',(1.,0.,0.));
#10733=DIRECTION('center_axis',(1.,0.,0.));
#10734=DIRECTION('ref_axis',(0.,-1.17203152359781E-12,-1.));
#10735=DIRECTION('',(1.,0.,0.));
#10736=DIRECTION('center_axis',(1.,0.,0.));
#10737=DIRECTION('ref_axis',(0.,-1.17203152359781E-12,-1.));
#10738=DIRECTION('',(1.,0.,0.));
#10739=DIRECTION('center_axis',(1.,0.,0.));
#10740=DIRECTION('ref_axis',(0.,-1.17203152359781E-12,-1.));
#10741=DIRECTION('',(1.,0.,0.));
#10742=DIRECTION('center_axis',(1.,0.,0.));
#10743=DIRECTION('ref_axis',(0.,-1.17203152359781E-12,-1.));
#10744=DIRECTION('',(1.,0.,0.));
#10745=DIRECTION('center_axis',(1.,0.,0.));
#10746=DIRECTION('ref_axis',(0.,-1.17203152359781E-12,-1.));
#10747=DIRECTION('',(1.,0.,0.));
#10748=DIRECTION('center_axis',(1.,0.,0.));
#10749=DIRECTION('ref_axis',(0.,-1.17203152359781E-12,-1.));
#10750=DIRECTION('',(1.,0.,0.));
#10751=DIRECTION('center_axis',(1.,0.,0.));
#10752=DIRECTION('ref_axis',(0.,-1.17203152359781E-12,-1.));
#10753=DIRECTION('',(1.,0.,0.));
#10754=DIRECTION('center_axis',(1.,0.,0.));
#10755=DIRECTION('ref_axis',(0.,-1.17203152359781E-12,-1.));
#10756=DIRECTION('',(1.,0.,0.));
#10757=DIRECTION('center_axis',(1.,0.,0.));
#10758=DIRECTION('ref_axis',(0.,-1.17203152359781E-12,-1.));
#10759=DIRECTION('',(1.,0.,0.));
#10760=DIRECTION('center_axis',(1.,0.,0.));
#10761=DIRECTION('ref_axis',(0.,-1.17203152359781E-12,-1.));
#10762=DIRECTION('',(1.,0.,0.));
#10763=DIRECTION('center_axis',(1.,0.,0.));
#10764=DIRECTION('ref_axis',(0.,-1.17203152359781E-12,-1.));
#10765=DIRECTION('',(1.,0.,0.));
#10766=DIRECTION('center_axis',(1.,0.,0.));
#10767=DIRECTION('ref_axis',(0.,-1.17203152359781E-12,-1.));
#10768=DIRECTION('',(1.,0.,0.));
#10769=DIRECTION('center_axis',(1.,0.,0.));
#10770=DIRECTION('ref_axis',(0.,-1.17203152359781E-12,-1.));
#10771=DIRECTION('',(1.,0.,0.));
#10772=DIRECTION('center_axis',(1.,0.,0.));
#10773=DIRECTION('ref_axis',(0.,-1.17203152359781E-12,-1.));
#10774=DIRECTION('',(1.,0.,0.));
#10775=DIRECTION('center_axis',(1.,0.,0.));
#10776=DIRECTION('ref_axis',(0.,-1.17203152359781E-12,-1.));
#10777=DIRECTION('',(1.,0.,0.));
#10778=DIRECTION('center_axis',(1.,0.,0.));
#10779=DIRECTION('ref_axis',(0.,-1.17203152359781E-12,-1.));
#10780=DIRECTION('',(1.,0.,0.));
#10781=DIRECTION('center_axis',(1.,0.,0.));
#10782=DIRECTION('ref_axis',(0.,-1.17203152359781E-12,-1.));
#10783=DIRECTION('',(1.,0.,0.));
#10784=DIRECTION('center_axis',(1.,0.,0.));
#10785=DIRECTION('ref_axis',(0.,-1.17203152359781E-12,-1.));
#10786=DIRECTION('',(1.,0.,0.));
#10787=DIRECTION('center_axis',(1.,0.,0.));
#10788=DIRECTION('ref_axis',(0.,-1.17203152359781E-12,-1.));
#10789=DIRECTION('',(1.,0.,0.));
#10790=DIRECTION('center_axis',(1.,0.,0.));
#10791=DIRECTION('ref_axis',(0.,-1.17203152359781E-12,-1.));
#10792=DIRECTION('',(1.,0.,0.));
#10793=DIRECTION('center_axis',(1.,0.,0.));
#10794=DIRECTION('ref_axis',(0.,-1.17203152359781E-12,-1.));
#10795=DIRECTION('',(1.,0.,0.));
#10796=DIRECTION('center_axis',(1.,0.,0.));
#10797=DIRECTION('ref_axis',(0.,-1.17203152359781E-12,-1.));
#10798=DIRECTION('',(1.,0.,0.));
#10799=DIRECTION('center_axis',(1.,0.,0.));
#10800=DIRECTION('ref_axis',(0.,-1.17203152359781E-12,-1.));
#10801=DIRECTION('',(1.,0.,0.));
#10802=DIRECTION('center_axis',(1.,0.,0.));
#10803=DIRECTION('ref_axis',(0.,-1.17203152359781E-12,-1.));
#10804=DIRECTION('',(1.,0.,0.));
#10805=DIRECTION('center_axis',(1.,0.,0.));
#10806=DIRECTION('ref_axis',(0.,-1.17203152359781E-12,-1.));
#10807=DIRECTION('',(1.,0.,0.));
#10808=DIRECTION('center_axis',(1.,0.,0.));
#10809=DIRECTION('ref_axis',(0.,-1.17203152359781E-12,-1.));
#10810=DIRECTION('',(1.,0.,0.));
#10811=DIRECTION('center_axis',(1.,0.,0.));
#10812=DIRECTION('ref_axis',(0.,-1.17203152359781E-12,-1.));
#10813=DIRECTION('',(1.,0.,0.));
#10814=DIRECTION('center_axis',(1.,0.,0.));
#10815=DIRECTION('ref_axis',(0.,-1.17203152359781E-12,-1.));
#10816=DIRECTION('',(1.,0.,0.));
#10817=DIRECTION('center_axis',(1.,0.,0.));
#10818=DIRECTION('ref_axis',(0.,-1.17203152359781E-12,-1.));
#10819=DIRECTION('',(1.,0.,0.));
#10820=DIRECTION('center_axis',(1.,0.,0.));
#10821=DIRECTION('ref_axis',(0.,-1.17203152359781E-12,-1.));
#10822=DIRECTION('',(1.,0.,0.));
#10823=DIRECTION('center_axis',(1.,0.,0.));
#10824=DIRECTION('ref_axis',(0.,-1.17203152359781E-12,-1.));
#10825=DIRECTION('',(1.,0.,0.));
#10826=DIRECTION('center_axis',(1.,0.,0.));
#10827=DIRECTION('ref_axis',(0.,-1.17203152359781E-12,-1.));
#10828=DIRECTION('',(1.,0.,0.));
#10829=DIRECTION('center_axis',(1.,0.,0.));
#10830=DIRECTION('ref_axis',(0.,-1.17203152359781E-12,-1.));
#10831=DIRECTION('',(1.,0.,0.));
#10832=DIRECTION('center_axis',(1.,0.,0.));
#10833=DIRECTION('ref_axis',(0.,-1.17203152359781E-12,-1.));
#10834=DIRECTION('',(1.,0.,0.));
#10835=DIRECTION('center_axis',(1.,0.,0.));
#10836=DIRECTION('ref_axis',(0.,-1.17203152359781E-12,-1.));
#10837=DIRECTION('',(1.,0.,0.));
#10838=DIRECTION('center_axis',(1.,0.,0.));
#10839=DIRECTION('ref_axis',(0.,-1.17203152359781E-12,-1.));
#10840=DIRECTION('',(1.,0.,0.));
#10841=DIRECTION('center_axis',(1.,0.,0.));
#10842=DIRECTION('ref_axis',(0.,-1.17203152359781E-12,-1.));
#10843=DIRECTION('center_axis',(-1.,0.,0.));
#10844=DIRECTION('ref_axis',(0.,-1.17203152359781E-12,-1.));
#10845=DIRECTION('center_axis',(0.,1.,0.));
#10846=DIRECTION('ref_axis',(0.,0.,1.));
#10847=DIRECTION('',(-1.,0.,0.));
#10848=DIRECTION('',(0.,0.,1.));
#10849=DIRECTION('',(1.,0.,0.));
#10850=DIRECTION('',(0.,0.,1.));
#10851=DIRECTION('center_axis',(1.,0.,0.));
#10852=DIRECTION('ref_axis',(0.,0.,-1.));
#10853=DIRECTION('center_axis',(-1.,0.,0.));
#10854=DIRECTION('ref_axis',(0.,0.,-1.));
#10855=DIRECTION('',(0.,-1.,0.));
#10856=DIRECTION('',(0.,0.,-1.));
#10857=DIRECTION('center_axis',(0.,0.,1.));
#10858=DIRECTION('ref_axis',(0.,-1.,0.));
#10859=DIRECTION('',(0.,-1.,0.));
#10860=DIRECTION('',(1.,0.,0.));
#10861=DIRECTION('center_axis',(0.,-1.,0.));
#10862=DIRECTION('ref_axis',(0.,0.,-1.));
#10863=DIRECTION('',(1.,0.,0.));
#10864=DIRECTION('',(0.,0.,-1.));
#10865=DIRECTION('center_axis',(1.,0.,0.));
#10866=DIRECTION('ref_axis',(0.,0.,-1.));
#10867=DIRECTION('center_axis',(1.,0.,0.));
#10868=DIRECTION('ref_axis',(0.,0.,-1.));
#10869=DIRECTION('center_axis',(1.,0.,0.));
#10870=DIRECTION('ref_axis',(0.,0.,-1.));
#10871=DIRECTION('center_axis',(1.,0.,0.));
#10872=DIRECTION('ref_axis',(0.,0.,-1.));
#10873=DIRECTION('',(-1.,0.,0.));
#10874=DIRECTION('center_axis',(-1.,0.,0.));
#10875=DIRECTION('ref_axis',(0.,0.,-1.));
#10876=DIRECTION('center_axis',(1.,0.,0.));
#10877=DIRECTION('ref_axis',(0.,0.,-1.));
#10878=DIRECTION('center_axis',(1.,0.,0.));
#10879=DIRECTION('ref_axis',(0.,0.,-1.));
#10880=DIRECTION('center_axis',(1.,0.,0.));
#10881=DIRECTION('ref_axis',(0.,0.,-1.));
#10882=DIRECTION('center_axis',(-1.,0.,0.));
#10883=DIRECTION('ref_axis',(0.,0.,-1.));
#10884=DIRECTION('center_axis',(1.,0.,0.));
#10885=DIRECTION('ref_axis',(0.,0.,-1.));
#10886=DIRECTION('center_axis',(1.,0.,0.));
#10887=DIRECTION('ref_axis',(0.,0.,-1.));
#10888=DIRECTION('',(-1.,0.,0.));
#10889=DIRECTION('center_axis',(1.,0.,0.));
#10890=DIRECTION('ref_axis',(0.,0.,-1.));
#10891=DIRECTION('center_axis',(1.,0.,0.));
#10892=DIRECTION('ref_axis',(0.,0.,-1.));
#10893=DIRECTION('center_axis',(1.,0.,0.));
#10894=DIRECTION('ref_axis',(0.,0.,-1.));
#14867=CARTESIAN_POINT('',(0.,0.,0.));
#14868=CARTESIAN_POINT('Origin',(4.,0.,4.));
#14869=CARTESIAN_POINT('',(4.12884541125756,8.40637486662632E-6,4.59405635738975));
#14870=CARTESIAN_POINT('',(4.02115458874249,-9.26662433349265E-6,4.59413599269206));
#14871=CARTESIAN_POINT('',(4.,-7.27562663373442E-17,4.5941));
#14872=CARTESIAN_POINT('',(4.,0.254721014554615,3.46322028700965));
#14873=CARTESIAN_POINT('Ctrl Pts',(4.12884541125756,8.40637486662632E-6,
4.59405635738975));
#14874=CARTESIAN_POINT('Ctrl Pts',(4.12564700130467,0.0398130654959074,
4.59407663624518));
#14875=CARTESIAN_POINT('Ctrl Pts',(4.12244859135178,0.079613792300143,4.59013569217808));
#14876=CARTESIAN_POINT('Ctrl Pts',(4.11925018139889,0.118599576779877,4.58219388355888));
#14877=CARTESIAN_POINT('Ctrl Pts',(4.11129754205509,0.215535206692688,4.56244709042845));
#14878=CARTESIAN_POINT('Ctrl Pts',(4.10334490271129,0.30743256945264,4.51796551073728));
#14879=CARTESIAN_POINT('Ctrl Pts',(4.09539226336748,0.383054411795556,4.45418672179759));
#14880=CARTESIAN_POINT('Ctrl Pts',(4.08743962402367,0.458676254138472,4.3904079328579));
#14881=CARTESIAN_POINT('Ctrl Pts',(4.07948698467986,0.518022576064352,4.30733193466969));
#14882=CARTESIAN_POINT('Ctrl Pts',(4.07153434533606,0.553840407547632,4.21511760274296));
#14883=CARTESIAN_POINT('Ctrl Pts',(4.06358170599225,0.589658239030912,4.12290327081622));
#14884=CARTESIAN_POINT('Ctrl Pts',(4.05562906664845,0.601947580071592,4.02155060515096));
#14885=CARTESIAN_POINT('Ctrl Pts',(4.04767642730464,0.589200356533535,3.92344812692479));
#14886=CARTESIAN_POINT('Ctrl Pts',(4.03972378796084,0.576453132995478,3.82534564869861));
#14887=CARTESIAN_POINT('Ctrl Pts',(4.03177114861703,0.538669344878685,3.73049335791153));
#14888=CARTESIAN_POINT('Ctrl Pts',(4.02381850927322,0.480479105222089,3.65049437695417));
#14889=CARTESIAN_POINT('Ctrl Pts',(4.01587900618215,0.422384984811151,3.57062753914914));
#14890=CARTESIAN_POINT('Ctrl Pts',(4.00793950309107,0.343951772361455,3.50556498199611));
#14891=CARTESIAN_POINT('Ctrl Pts',(4.,0.254721014554615,3.46322028700965));
#14892=CARTESIAN_POINT('',(4.,0.254694598474614,4.53673594206822));
#14893=CARTESIAN_POINT('Origin',(4.,0.,4.));
#14894=CARTESIAN_POINT('Ctrl Pts',(3.99999999999998,0.254694598474614,4.53673594206822));
#14895=CARTESIAN_POINT('Ctrl Pts',(4.00705152958082,0.175425736340139,4.5743509952638));
#14896=CARTESIAN_POINT('Ctrl Pts',(4.01410305916165,0.0876996967667308,
4.59405101338575));
#14897=CARTESIAN_POINT('Ctrl Pts',(4.02115458874249,-9.26662433349265E-6,
4.59413599269206));
#14898=CARTESIAN_POINT('Origin',(4.,0.,4.));
#14899=CARTESIAN_POINT('',(4.42884541125756,-2.46302091461148E-6,4.59415045696459));
#14900=CARTESIAN_POINT('',(4.32115458874249,3.58587963140688E-6,4.59404994535016));
#14901=CARTESIAN_POINT('',(4.,-7.27562663373442E-17,4.5941));
#14902=CARTESIAN_POINT('Ctrl Pts',(4.42884541125756,-2.46302091461148E-6,
4.59415045696459));
#14903=CARTESIAN_POINT('Ctrl Pts',(4.42107867343035,0.0966117732708647,
4.59412799973471));
#14904=CARTESIAN_POINT('Ctrl Pts',(4.41331193560314,0.193236775309615,4.57009608476161));
#14905=CARTESIAN_POINT('Ctrl Pts',(4.40554519777592,0.278573173318151,4.52479781884576));
#14906=CARTESIAN_POINT('Ctrl Pts',(4.39759255843212,0.36595214906825,4.47841531183407));
#14907=CARTESIAN_POINT('Ctrl Pts',(4.38963991908831,0.441495654419193,4.40973622444741));
#14908=CARTESIAN_POINT('Ctrl Pts',(4.3816872797445,0.495967466205845,4.32715751007026));
#14909=CARTESIAN_POINT('Ctrl Pts',(4.3737346404007,0.550439277992498,4.24457879569311));
#14910=CARTESIAN_POINT('Ctrl Pts',(4.36578200105689,0.58383939621486,4.14810045432546));
#14911=CARTESIAN_POINT('Ctrl Pts',(4.35782936171309,0.59208420294366,4.04951827803692));
#14912=CARTESIAN_POINT('Ctrl Pts',(4.34987672236928,0.600329009672459,3.95093610174838));
#14913=CARTESIAN_POINT('Ctrl Pts',(4.34192408302547,0.583418504907695,3.85025009053894));
#14914=CARTESIAN_POINT('Ctrl Pts',(4.33397144368167,0.54342022548472,3.75977047903001));
#14915=CARTESIAN_POINT('Ctrl Pts',(4.32601880433786,0.503421946061746,3.66929086752108));
#14916=CARTESIAN_POINT('Ctrl Pts',(4.31806616499406,0.440335891980562,3.58901765571266));
#14917=CARTESIAN_POINT('Ctrl Pts',(4.31011352565025,0.361875197644003,3.52876534000234));
#14918=CARTESIAN_POINT('Ctrl Pts',(4.30216088630644,0.283414503307443,3.46851302429202));
#14919=CARTESIAN_POINT('Ctrl Pts',(4.29420824696263,0.189579168715509,3.4282816046798));
#14920=CARTESIAN_POINT('Ctrl Pts',(4.28625560761883,0.0918418319479975,
3.41298991457491));
#14921=CARTESIAN_POINT('Ctrl Pts',(4.27830296827502,-0.00589550481951406,
3.39769822447003));
#14922=CARTESIAN_POINT('Ctrl Pts',(4.27035032893122,-0.107534843762603,
3.4073462638725));
#14923=CARTESIAN_POINT('Ctrl Pts',(4.26239768958741,-0.200649373295791,
3.44075443909651));
#14924=CARTESIAN_POINT('Ctrl Pts',(4.25444505024361,-0.293763902828979,
3.47416261432052));
#14925=CARTESIAN_POINT('Ctrl Pts',(4.24649241089979,-0.378353622952266,
3.53133092536608));
#14926=CARTESIAN_POINT('Ctrl Pts',(4.23853977155599,-0.444076322467606,
3.60526974769923));
#14927=CARTESIAN_POINT('Ctrl Pts',(4.23058713221218,-0.509799021982947,
3.67920857003239));
#14928=CARTESIAN_POINT('Ctrl Pts',(4.22263449286838,-0.556654700890342,
3.76991790365313));
#14929=CARTESIAN_POINT('Ctrl Pts',(4.21468185352458,-0.578914549750806,
3.86630733464992));
#14930=CARTESIAN_POINT('Ctrl Pts',(4.20672921418077,-0.601174398611269,
3.96269676564671));
#14931=CARTESIAN_POINT('Ctrl Pts',(4.19877657483696,-0.598838417424802,
4.06476629401955));
#14932=CARTESIAN_POINT('Ctrl Pts',(4.19082393549315,-0.5721923335546,4.16003645884502));
#14933=CARTESIAN_POINT('Ctrl Pts',(4.18287129614934,-0.545546249684398,
4.25530662367048));
#14934=CARTESIAN_POINT('Ctrl Pts',(4.17491865680554,-0.494590063130461,
4.34377742494856));
#14935=CARTESIAN_POINT('Ctrl Pts',(4.16696601746173,-0.425553631634784,
4.41463223618795));
#14936=CARTESIAN_POINT('Ctrl Pts',(4.15901337811793,-0.356517200139107,
4.48548704742733));
#14937=CARTESIAN_POINT('Ctrl Pts',(4.15106073877413,-0.269400523701689,
4.53872586862801));
#14938=CARTESIAN_POINT('Ctrl Pts',(4.14310809943032,-0.174855236950146,
4.56783927594351));
#14939=CARTESIAN_POINT('Ctrl Pts',(4.1383538700394,-0.118334381217266,4.5852437891806));
#14940=CARTESIAN_POINT('Ctrl Pts',(4.13359964064848,-0.0591586432141876,
4.59402621418361));
#14941=CARTESIAN_POINT('Ctrl Pts',(4.12884541125756,8.40637486662632E-6,
4.59405635738975));
#14942=CARTESIAN_POINT('Ctrl Pts',(4.02115458874249,-9.26662433349265E-6,
4.59413599269206));
#14943=CARTESIAN_POINT('Ctrl Pts',(4.02205569850546,-0.0112175303500608,
4.59414685213492));
#14944=CARTESIAN_POINT('Ctrl Pts',(4.02295680826843,-0.0224255152200988,
4.5938373961197));
#14945=CARTESIAN_POINT('Ctrl Pts',(4.0238579180314,-0.0336155370699344,
4.59320407706013));
#14946=CARTESIAN_POINT('Ctrl Pts',(4.03181055737521,-0.132371772633995,
4.58761479340425));
#14947=CARTESIAN_POINT('Ctrl Pts',(4.03976319671902,-0.229728915328813,
4.55680066053817));
#14948=CARTESIAN_POINT('Ctrl Pts',(4.04771583606282,-0.31374319278985,4.50455967689729));
#14949=CARTESIAN_POINT('Ctrl Pts',(4.05566847540663,-0.397757470250888,
4.4523186932564));
#14950=CARTESIAN_POINT('Ctrl Pts',(4.06362111475043,-0.468428882478145,
4.37865085884071));
#14951=CARTESIAN_POINT('Ctrl Pts',(4.07157375409424,-0.517135915630147,
4.29254879227412));
#14952=CARTESIAN_POINT('Ctrl Pts',(4.07952639343804,-0.565842948782149,
4.20644672570752));
#14953=CARTESIAN_POINT('Ctrl Pts',(4.08747903278185,-0.592585602858896,
4.10791042699003));
#14954=CARTESIAN_POINT('Ctrl Pts',(4.09543167212566,-0.594084460855775,
4.00899459728238));
#14955=CARTESIAN_POINT('Ctrl Pts',(4.10338431146947,-0.595583318852653,
3.91007876757474));
#14956=CARTESIAN_POINT('Ctrl Pts',(4.11133695081327,-0.571838380769662,
3.81078340687695));
#14957=CARTESIAN_POINT('Ctrl Pts',(4.11928959015708,-0.525757920758293,
3.72324489380985));
#14958=CARTESIAN_POINT('Ctrl Pts',(4.12724222950088,-0.479677460746923,
3.63570638074275));
#14959=CARTESIAN_POINT('Ctrl Pts',(4.13519486884469,-0.411261478807175,
3.55992471530633));
#14960=CARTESIAN_POINT('Ctrl Pts',(4.1431475081885,-0.328872047298013,3.50516726345229));
#14961=CARTESIAN_POINT('Ctrl Pts',(4.1511001475323,-0.246482615788851,3.45040981159825));
#14962=CARTESIAN_POINT('Ctrl Pts',(4.15905278687611,-0.150119734710276,
3.41667657332659));
#14963=CARTESIAN_POINT('Ctrl Pts',(4.16700542621992,-0.0515665150750243,
3.40809082437526));
#14964=CARTESIAN_POINT('Ctrl Pts',(4.17495806556372,0.0469867045602276,
3.39950507542393));
#14965=CARTESIAN_POINT('Ctrl Pts',(4.18291070490753,0.147730262752155,3.41606681579293));
#14966=CARTESIAN_POINT('Ctrl Pts',(4.19086334425134,0.238347648045887,3.45575171487277));
#14967=CARTESIAN_POINT('Ctrl Pts',(4.19881598359514,0.32896503333962,3.49543661395261));
#14968=CARTESIAN_POINT('Ctrl Pts',(4.20676862293895,0.409456245735157,3.55824467174328));
#14969=CARTESIAN_POINT('Ctrl Pts',(4.21472126228276,0.469979735422806,3.63649644709345));
#14970=CARTESIAN_POINT('Ctrl Pts',(4.22267390162656,0.530503225110456,3.71474822244363));
#14971=CARTESIAN_POINT('Ctrl Pts',(4.23062654097037,0.571058992090217,3.80844371535332));
#14972=CARTESIAN_POINT('Ctrl Pts',(4.23857918031417,0.586688754827568,3.90612753493601));
#14973=CARTESIAN_POINT('Ctrl Pts',(4.24653181965798,0.602318517564919,4.0038113545187));
#14974=CARTESIAN_POINT('Ctrl Pts',(4.25448445900178,0.593022276059861,4.10548350077438));
#14975=CARTESIAN_POINT('Ctrl Pts',(4.26243709834559,0.559936509464549,4.19871308474845));
#14976=CARTESIAN_POINT('Ctrl Pts',(4.2703897376894,0.526850742869238,4.29194266872251));
#14977=CARTESIAN_POINT('Ctrl Pts',(4.27834237703321,0.469975451183674,4.37672969041494));
#14978=CARTESIAN_POINT('Ctrl Pts',(4.28629501637701,0.396264473279151,4.44270782630825));
#14979=CARTESIAN_POINT('Ctrl Pts',(4.29424765572082,0.322553495374627,4.50868596220156));
#14980=CARTESIAN_POINT('Ctrl Pts',(4.30220029506462,0.232006831251144,4.55585521229574));
#14981=CARTESIAN_POINT('Ctrl Pts',(4.31015293440843,0.135695012128791,4.57844846968215));
#14982=CARTESIAN_POINT('Ctrl Pts',(4.31382015251978,0.0912825306677821,
4.58886694826517));
#14983=CARTESIAN_POINT('Ctrl Pts',(4.31748737063114,0.0456441298716245,
4.59405951624442));
#14984=CARTESIAN_POINT('Ctrl Pts',(4.32115458874249,3.58587963140688E-6,
4.59404994535016));
#14985=CARTESIAN_POINT('Origin',(4.,0.,4.));
#14986=CARTESIAN_POINT('',(4.72884541125756,-4.67700812217808E-6,4.59405084457266));
#14987=CARTESIAN_POINT('',(4.62115458874249,3.7232086238465E-6,4.59414939806979));
#14988=CARTESIAN_POINT('',(4.,-7.27562663373442E-17,4.5941));
#14989=CARTESIAN_POINT('Ctrl Pts',(4.72884541125756,-4.67700812217808E-6,
4.59405084457266));
#14990=CARTESIAN_POINT('Ctrl Pts',(4.72446298489983,0.0545367878429411,
4.59403588702548));
#14991=CARTESIAN_POINT('Ctrl Pts',(4.7200805585421,0.10908225468116,4.58659074407712));
#14992=CARTESIAN_POINT('Ctrl Pts',(4.71569813218437,0.16154350694756,4.57176871113812));
#14993=CARTESIAN_POINT('Ctrl Pts',(4.70774549284056,0.256743148594298,4.54487167450041));
#14994=CARTESIAN_POINT('Ctrl Pts',(4.69979285349676,0.345079446524661,4.4936824501733));
#14995=CARTESIAN_POINT('Ctrl Pts',(4.69184021415295,0.415752085200636,4.42445961801412));
#14996=CARTESIAN_POINT('Ctrl Pts',(4.68388757480915,0.486424723876611,4.35523678585494));
#14997=CARTESIAN_POINT('Ctrl Pts',(4.67593493546534,0.539433703298198,4.26798034586369));
#14998=CARTESIAN_POINT('Ctrl Pts',(4.66798229612153,0.568297953762936,4.17335858623793));
#14999=CARTESIAN_POINT('Ctrl Pts',(4.66002965677773,0.597162204227674,4.07873682661218));
#15000=CARTESIAN_POINT('Ctrl Pts',(4.65207701743392,0.601881725735563,3.97674974735193));
#15001=CARTESIAN_POINT('Ctrl Pts',(4.64412437809011,0.581879492504365,3.87986665793328));
#15002=CARTESIAN_POINT('Ctrl Pts',(4.63617173874631,0.561877259273167,3.78298356851463));
#15003=CARTESIAN_POINT('Ctrl Pts',(4.6282190994025,0.517153271302883,3.69120446893757));
#15004=CARTESIAN_POINT('Ctrl Pts',(4.6202664600587,0.453175645250056,3.61575060413089));
#15005=CARTESIAN_POINT('Ctrl Pts',(4.61231382071489,0.389198019197228,3.5402967393242));
#15006=CARTESIAN_POINT('Ctrl Pts',(4.60436118137108,0.305966755061857,3.48116810928789));
#15007=CARTESIAN_POINT('Ctrl Pts',(4.59640854202727,0.213658008474022,3.4455939943611));
#15008=CARTESIAN_POINT('Ctrl Pts',(4.58845590268347,0.121349261886187,3.41001987943431));
#15009=CARTESIAN_POINT('Ctrl Pts',(4.58050326333966,0.0199630328458878,
3.39800027961704));
#15010=CARTESIAN_POINT('Ctrl Pts',(4.57255062399586,-0.0781048312986516,
3.41100475468789));
#15011=CARTESIAN_POINT('Ctrl Pts',(4.56459798465205,-0.17617269544319,3.42400922975875));
#15012=CARTESIAN_POINT('Ctrl Pts',(4.55664534530825,-0.270922194691968,
3.46203777971774));
#15013=CARTESIAN_POINT('Ctrl Pts',(4.54869270596444,-0.350768912290741,
3.52044089639904));
#15014=CARTESIAN_POINT('Ctrl Pts',(4.54074006662063,-0.430615629889515,
3.57884401308035));
#15015=CARTESIAN_POINT('Ctrl Pts',(4.53278742727683,-0.495559565838284,
3.65762169648397));
#15016=CARTESIAN_POINT('Ctrl Pts',(4.52483478793302,-0.537660439465301,
3.74714230187364));
#15017=CARTESIAN_POINT('Ctrl Pts',(4.51688214858921,-0.579761313092318,
3.8366629072633));
#15018=CARTESIAN_POINT('Ctrl Pts',(4.50892950924541,-0.599019124397585,
3.936926434639));
#15019=CARTESIAN_POINT('Ctrl Pts',(4.5009768699016,-0.593079343631488,4.03567430223551));
#15020=CARTESIAN_POINT('Ctrl Pts',(4.49302423055779,-0.587139562865391,
4.13442216983203));
#15021=CARTESIAN_POINT('Ctrl Pts',(4.48507159121399,-0.556002190027932,
4.23165437764937));
#15022=CARTESIAN_POINT('Ctrl Pts',(4.47711895187018,-0.503474193090318,
4.31548296397124));
#15023=CARTESIAN_POINT('Ctrl Pts',(4.46916631252638,-0.450946196152703,
4.39931155029312));
#15024=CARTESIAN_POINT('Ctrl Pts',(4.46121367318257,-0.377027575114933,
4.46973651511953));
#15025=CARTESIAN_POINT('Ctrl Pts',(4.45326103383876,-0.290755888038263,
4.51814744739689));
#15026=CARTESIAN_POINT('Ctrl Pts',(4.44530839449495,-0.204484200961595,
4.56655837967425));
#15027=CARTESIAN_POINT('Ctrl Pts',(4.43735575515115,-0.105859447846027,
4.59295527940255));
#15028=CARTESIAN_POINT('Ctrl Pts',(4.42940311580734,-0.00693984821361558,
4.59411076594835));
#15029=CARTESIAN_POINT('Ctrl Pts',(4.42921721429075,-0.0046274959494805,
4.59413777669183));
#15030=CARTESIAN_POINT('Ctrl Pts',(4.42903131277416,-0.00231498256911503,
4.59415099449182));
#15031=CARTESIAN_POINT('Ctrl Pts',(4.42884541125756,-2.46302091461148E-6,
4.59415045696459));
#15032=CARTESIAN_POINT('Ctrl Pts',(4.32115458874249,3.58587963140688E-6,
4.59404994535016));
#15033=CARTESIAN_POINT('Ctrl Pts',(4.32544000997495,-0.0533308355660028,
4.59403876103764));
#15034=CARTESIAN_POINT('Ctrl Pts',(4.3297254312074,-0.106668183692779,4.58692369872924));
#15035=CARTESIAN_POINT('Ctrl Pts',(4.33401085243985,-0.158055593105036,
4.57274269264177));
#15036=CARTESIAN_POINT('Ctrl Pts',(4.34196349178366,-0.253417405095285,
4.54642639353635));
#15037=CARTESIAN_POINT('Ctrl Pts',(4.34991613112746,-0.342064054954561,
4.49577653064689));
#15038=CARTESIAN_POINT('Ctrl Pts',(4.35786877047127,-0.413157291282808,
4.42698573291487));
#15039=CARTESIAN_POINT('Ctrl Pts',(4.36582140981507,-0.484250527611055,
4.35819493518285));
#15040=CARTESIAN_POINT('Ctrl Pts',(4.37377404915888,-0.537790350408272,
4.27126320260829));
#15041=CARTESIAN_POINT('Ctrl Pts',(4.38172668850269,-0.567230782432438,
4.17681912699824));
#15042=CARTESIAN_POINT('Ctrl Pts',(4.3896793278465,-0.596671214456604,4.0823750513882));
#15043=CARTESIAN_POINT('Ctrl Pts',(4.3976319671903,-0.602012255707717,3.98041863274268));
#15044=CARTESIAN_POINT('Ctrl Pts',(4.40558460653411,-0.582600893642323,
3.88341542999892));
#15045=CARTESIAN_POINT('Ctrl Pts',(4.41353724587791,-0.563189531576929,
3.78641222725516));
#15046=CARTESIAN_POINT('Ctrl Pts',(4.42148988522172,-0.519025766195027,
3.69436224041317));
#15047=CARTESIAN_POINT('Ctrl Pts',(4.42944252456553,-0.455509217992651,
3.61851983504546));
#15048=CARTESIAN_POINT('Ctrl Pts',(4.43739516390933,-0.391992669790276,
3.54267742967776));
#15049=CARTESIAN_POINT('Ctrl Pts',(4.44534780325314,-0.309123338767427,
3.48304260578434));
#15050=CARTESIAN_POINT('Ctrl Pts',(4.45330044259694,-0.217033129998519,
3.44690653227429));
#15051=CARTESIAN_POINT('Ctrl Pts',(4.46125308194075,-0.12494292122961,3.41077045876423));
#15052=CARTESIAN_POINT('Ctrl Pts',(4.46920572128456,-0.0236318347146405,
3.39813313563753));
#15053=CARTESIAN_POINT('Ctrl Pts',(4.47715836062837,0.074513469760962,3.41053964803971));
#15054=CARTESIAN_POINT('Ctrl Pts',(4.48511099997217,0.172658774236564,3.42294616044189));
#15055=CARTESIAN_POINT('Ctrl Pts',(4.49306363931598,0.2676382966728,3.46039650837296));
#15056=CARTESIAN_POINT('Ctrl Pts',(4.50101627865978,0.34783949666059,3.51831187658845));
#15057=CARTESIAN_POINT('Ctrl Pts',(4.50896891800359,0.428040696648381,3.57622724480394));
#15058=CARTESIAN_POINT('Ctrl Pts',(4.51692155734739,0.493463574187728,3.65460763330386));
#15059=CARTESIAN_POINT('Ctrl Pts',(4.5248741966912,0.536109291561612,3.74386997215216));
#15060=CARTESIAN_POINT('Ctrl Pts',(4.53282683603501,0.578755008935497,3.83313231100046));
#15061=CARTESIAN_POINT('Ctrl Pts',(4.54077947537881,0.598623566143919,3.93327660019715));
#15062=CARTESIAN_POINT('Ctrl Pts',(4.54873211472262,0.593285761408823,4.03205883640902));
#15063=CARTESIAN_POINT('Ctrl Pts',(4.55668475406643,0.587947956673727,4.1308410726209));
#15064=CARTESIAN_POINT('Ctrl Pts',(4.56463739341024,0.557403789995114,4.22826125584796));
#15065=CARTESIAN_POINT('Ctrl Pts',(4.57259003275404,0.505387701781775,4.31240844187621));
#15066=CARTESIAN_POINT('Ctrl Pts',(4.58054267209785,0.453371613568435,4.39655562790445));
#15067=CARTESIAN_POINT('Ctrl Pts',(4.58849531144165,0.37988360382037,4.46742981673387));
#15068=CARTESIAN_POINT('Ctrl Pts',(4.59644795078546,0.293908582600447,4.51636567348148));
#15069=CARTESIAN_POINT('Ctrl Pts',(4.60440059012926,0.207933561380525,4.56530153022909));
#15070=CARTESIAN_POINT('Ctrl Pts',(4.61235322947307,0.109471528688745,4.59229905489488));
#15071=CARTESIAN_POINT('Ctrl Pts',(4.62030586881688,0.01056080905581,4.59405743239568));
#15072=CARTESIAN_POINT('Ctrl Pts',(4.62058877545875,0.00704216595801619,
4.59411998479525));
#15073=CARTESIAN_POINT('Ctrl Pts',(4.62087168210062,0.00352295504485493,
4.59415059693914));
#15074=CARTESIAN_POINT('Ctrl Pts',(4.62115458874249,3.7232086238465E-6,
4.59414939806979));
#15075=CARTESIAN_POINT('Origin',(4.,0.,4.));
#15076=CARTESIAN_POINT('',(5.02884541125756,1.1583539301252E-5,4.59413174414479));
#15077=CARTESIAN_POINT('',(4.92115458874249,-9.52916733652962E-6,4.59405847898621));
#15078=CARTESIAN_POINT('',(4.,-7.27562663373442E-17,4.5941));
#15079=CARTESIAN_POINT('Ctrl Pts',(5.02884541125756,1.1583539301252E-5,
4.59413174414479));
#15080=CARTESIAN_POINT('Ctrl Pts',(5.02784729636931,0.0124287555737821,
4.59414271605904));
#15081=CARTESIAN_POINT('Ctrl Pts',(5.02684918148107,0.024845254523583,4.59376142828251));
#15082=CARTESIAN_POINT('Ctrl Pts',(5.02585106659282,0.0372368329321061,
4.59298328977014));
#15083=CARTESIAN_POINT('Ctrl Pts',(5.01789842724901,0.135968707532707,4.58678334723719));
#15084=CARTESIAN_POINT('Ctrl Pts',(5.00994578790521,0.233118536601742,4.55538989360237));
#15085=CARTESIAN_POINT('Ctrl Pts',(5.0019931485614,0.316808430381418,4.50264120614281));
#15086=CARTESIAN_POINT('Ctrl Pts',(4.9940405092176,0.400498324161095,4.44989251868324));
#15087=CARTESIAN_POINT('Ctrl Pts',(4.98608786987379,0.470728282651411,4.37578859739892));
#15088=CARTESIAN_POINT('Ctrl Pts',(4.97813523052998,0.518911736914097,4.289389655942));
#15089=CARTESIAN_POINT('Ctrl Pts',(4.97018259118617,0.567095191176782,4.20299071448508));
#15090=CARTESIAN_POINT('Ctrl Pts',(4.96222995184237,0.593232141211837,4.10429675285556));
#15091=CARTESIAN_POINT('Ctrl Pts',(4.95427731249856,0.594126988899363,4.00537445204741));
#15092=CARTESIAN_POINT('Ctrl Pts',(4.94632467315476,0.595021836586889,3.90645215123927));
#15093=CARTESIAN_POINT('Ctrl Pts',(4.93837203381095,0.570674581926886,3.80730151125251));
#15094=CARTESIAN_POINT('Ctrl Pts',(4.93041939446714,0.524062008404491,3.72004504823011));
#15095=CARTESIAN_POINT('Ctrl Pts',(4.92246675512334,0.477449434882097,3.6327885852077));
#15096=CARTESIAN_POINT('Ctrl Pts',(4.91451411577953,0.408571542497308,3.55742629914966));
#15097=CARTESIAN_POINT('Ctrl Pts',(4.90656147643572,0.325849591692228,3.50317225594031));
#15098=CARTESIAN_POINT('Ctrl Pts',(4.89860883709192,0.243127640887147,3.44891821273095));
#15099=CARTESIAN_POINT('Ctrl Pts',(4.89065619774811,0.146561631661773,3.41577241237029));
#15100=CARTESIAN_POINT('Ctrl Pts',(4.88270355840431,0.0479580738465473,
3.40778738038914));
#15101=CARTESIAN_POINT('Ctrl Pts',(4.8747509190605,-0.0506454839686783,
3.39980234840799));
#15102=CARTESIAN_POINT('Ctrl Pts',(4.86679827971669,-0.151286590373755,
3.41697808480634));
#15103=CARTESIAN_POINT('Ctrl Pts',(4.85884564037289,-0.241660499406316,
3.45721462188069));
#15104=CARTESIAN_POINT('Ctrl Pts',(4.85089300102908,-0.332034408438876,
3.49745115895503));
#15105=CARTESIAN_POINT('Ctrl Pts',(4.84294036168527,-0.41214112009892,3.56074849670536));
#15106=CARTESIAN_POINT('Ctrl Pts',(4.83498772234147,-0.472186497854497,
3.63936767349926));
#15107=CARTESIAN_POINT('Ctrl Pts',(4.82703508299766,-0.532231875610076,
3.71798685029316));
#15108=CARTESIAN_POINT('Ctrl Pts',(4.81908244365386,-0.572215919461187,
3.81192786613063));
#15109=CARTESIAN_POINT('Ctrl Pts',(4.81112980431005,-0.587250035475296,
3.9097051523746));
#15110=CARTESIAN_POINT('Ctrl Pts',(4.80317716496624,-0.602284151489406,
4.00748243861856));
#15111=CARTESIAN_POINT('Ctrl Pts',(4.79522452562244,-0.592368339666514,
4.10909599526903));
#15112=CARTESIAN_POINT('Ctrl Pts',(4.78727188627863,-0.558714943052599,
4.20212218107662));
#15113=CARTESIAN_POINT('Ctrl Pts',(4.77931924693482,-0.525061546438685,
4.2951483668842));
#15114=CARTESIAN_POINT('Ctrl Pts',(4.77136660759101,-0.467670565033749,
4.37958718184891));
#15115=CARTESIAN_POINT('Ctrl Pts',(4.76341396824721,-0.393558827964045,
4.44511483080773));
#15116=CARTESIAN_POINT('Ctrl Pts',(4.7554613289034,-0.319447090894342,4.51064247976655));
#15117=CARTESIAN_POINT('Ctrl Pts',(4.7475086895596,-0.228614598159871,4.55725896271948));
#15118=CARTESIAN_POINT('Ctrl Pts',(4.73955605021579,-0.13216685911108,4.5792647797218));
#15119=CARTESIAN_POINT('Ctrl Pts',(4.73598583722972,-0.0888681559330128,
4.58914394690572));
#15120=CARTESIAN_POINT('Ctrl Pts',(4.73241562424364,-0.0444377444908,4.59406302997518));
#15121=CARTESIAN_POINT('Ctrl Pts',(4.72884541125756,-4.67700812217808E-6,
4.59405084457266));
#15122=CARTESIAN_POINT('Ctrl Pts',(4.62115458874249,3.7232086238465E-6,
4.59414939806979));
#15123=CARTESIAN_POINT('Ctrl Pts',(4.62882432144443,-0.0954043143036648,
4.59411689615543));
#15124=CARTESIAN_POINT('Ctrl Pts',(4.63649405414636,-0.190827729806029,
4.57070400848325));
#15125=CARTESIAN_POINT('Ctrl Pts',(4.6441637868483,-0.275369369969159,4.52648596729292));
#15126=CARTESIAN_POINT('Ctrl Pts',(4.65211642619211,-0.363029422787103,
4.48063689435358));
#15127=CARTESIAN_POINT('Ctrl Pts',(4.66006906553591,-0.438990121848901,
4.4124195181391));
#15128=CARTESIAN_POINT('Ctrl Pts',(4.66802170487971,-0.493964237128006,
4.33017434199545));
#15129=CARTESIAN_POINT('Ctrl Pts',(4.67597434422352,-0.548938352407109,
4.24792916585179));
#15130=CARTESIAN_POINT('Ctrl Pts',(4.68392698356733,-0.582925883903521,
4.15165618977896));
#15131=CARTESIAN_POINT('Ctrl Pts',(4.69187962291114,-0.591771392992132,
4.05312609631255));
#15132=CARTESIAN_POINT('Ctrl Pts',(4.69983226225494,-0.600616902080743,
3.95459600284613));
#15133=CARTESIAN_POINT('Ctrl Pts',(4.70778490159875,-0.584320388761555,
3.85380879198612));
#15134=CARTESIAN_POINT('Ctrl Pts',(4.71573754094256,-0.544874323741249,
3.76308707295491));
#15135=CARTESIAN_POINT('Ctrl Pts',(4.72369018028636,-0.505428258720944,
3.6723653539237));
#15136=CARTESIAN_POINT('Ctrl Pts',(4.73164281963017,-0.442832641999522,
3.59170912672127));
#15137=CARTESIAN_POINT('Ctrl Pts',(4.73959545897397,-0.364740640256699,
3.53097971363863));
#15138=CARTESIAN_POINT('Ctrl Pts',(4.74754809831778,-0.286648638513876,
3.47025030055599));
#15139=CARTESIAN_POINT('Ctrl Pts',(4.75550073766158,-0.193060251749651,
3.42944770159313));
#15140=CARTESIAN_POINT('Ctrl Pts',(4.76345337700539,-0.095417934894009,
3.41356059019365));
#15141=CARTESIAN_POINT('Ctrl Pts',(4.7714060163492,0.00222438196163176,
3.39767347879416));
#15142=CARTESIAN_POINT('Ctrl Pts',(4.77935865569301,0.10392062890869,3.40670185495805));
#15143=CARTESIAN_POINT('Ctrl Pts',(4.78731129503681,0.19723705468272,3.43954187673519));
#15144=CARTESIAN_POINT('Ctrl Pts',(4.79526393438062,0.290553480456751,3.47238189851233));
#15145=CARTESIAN_POINT('Ctrl Pts',(4.80321657372443,0.375490085057754,3.52903356590271));
#15146=CARTESIAN_POINT('Ctrl Pts',(4.81116921306823,0.441662211759978,3.60257044098769));
#15147=CARTESIAN_POINT('Ctrl Pts',(4.81912185241204,0.507834338462201,3.67610731607267));
#15148=CARTESIAN_POINT('Ctrl Pts',(4.82707449175584,0.555241987265645,3.76652939885225));
#15149=CARTESIAN_POINT('Ctrl Pts',(4.83502713109965,0.57808892742485,3.86278135818256));
#15150=CARTESIAN_POINT('Ctrl Pts',(4.84297977044346,0.600935867584054,3.95903331751286));
#15151=CARTESIAN_POINT('Ctrl Pts',(4.85093240978726,0.599222099099018,4.0611151533939));
#15152=CARTESIAN_POINT('Ctrl Pts',(4.85888504913107,0.573157153508111,4.15654597106253));
#15153=CARTESIAN_POINT('Ctrl Pts',(4.86683768847488,0.547092207917203,4.25197678873116));
#15154=CARTESIAN_POINT('Ctrl Pts',(4.87479032781868,0.496676085220424,4.34075658818739));
#15155=CARTESIAN_POINT('Ctrl Pts',(4.88274296716249,0.428072843071251,4.41203082979109));
#15156=CARTESIAN_POINT('Ctrl Pts',(4.89069560650629,0.359469600922078,4.48330507139479));
#15157=CARTESIAN_POINT('Ctrl Pts',(4.8986482458501,0.272679239320511,4.53707375514596));
#15158=CARTESIAN_POINT('Ctrl Pts',(4.90660088519391,0.178313062033339,4.56676292714126));
#15159=CARTESIAN_POINT('Ctrl Pts',(4.9114521197101,0.120748216373203,4.58487378690922));
#15160=CARTESIAN_POINT('Ctrl Pts',(4.9163033542263,0.0603642649825261,4.59402420038378));
#15161=CARTESIAN_POINT('Ctrl Pts',(4.92115458874249,-9.52916733652962E-6,
4.59405847898621));
#15162=CARTESIAN_POINT('Origin',(4.,0.,4.));
#15163=CARTESIAN_POINT('',(5.32884541125756,-1.45357002139801E-5,4.59407911932661));
#15164=CARTESIAN_POINT('',(5.22115458874249,1.46139895546772E-5,4.59411444380891));
#15165=CARTESIAN_POINT('',(4.,-7.27562663373442E-17,4.5941));
#15166=CARTESIAN_POINT('Ctrl Pts',(5.32884541125756,-1.45357002139801E-5,
4.59407911932661));
#15167=CARTESIAN_POINT('Ctrl Pts',(5.32327896849499,0.0692531541268509,
4.59401614001471));
#15168=CARTESIAN_POINT('Ctrl Pts',(5.31771252573242,0.138542285837495,4.5819075943171));
#15169=CARTESIAN_POINT('Ctrl Pts',(5.31214608296985,0.203593590158122,4.55818044906639));
#15170=CARTESIAN_POINT('Ctrl Pts',(5.30419344362604,0.296530782575621,4.5242820624512));
#15171=CARTESIAN_POINT('Ctrl Pts',(5.29624080428224,0.380818089806801,4.46666879957728));
#15172=CARTESIAN_POINT('Ctrl Pts',(5.28828816493843,0.446150240572578,4.39238466650784));
#15173=CARTESIAN_POINT('Ctrl Pts',(5.28033552559462,0.511482391338355,4.3181005334384));
#15174=CARTESIAN_POINT('Ctrl Pts',(5.27238288625081,0.557859385638729,4.22714553017344));
#15175=CARTESIAN_POINT('Ctrl Pts',(5.26443024690701,0.579611004278495,4.13064014464439));
#15176=CARTESIAN_POINT('Ctrl Pts',(5.2564776075632,0.601362622918262,4.03413475911534));
#15177=CARTESIAN_POINT('Ctrl Pts',(5.2485249682194,0.598488865897423,3.93207899132219));
#15178=CARTESIAN_POINT('Ctrl Pts',(5.24057232887559,0.571341089151559,3.8369505488493));
#15179=CARTESIAN_POINT('Ctrl Pts',(5.23261968953179,0.544193312405696,3.74182210637642));
#15180=CARTESIAN_POINT('Ctrl Pts',(5.22466705018798,0.492771515934809,3.65362098922379));
#15181=CARTESIAN_POINT('Ctrl Pts',(5.21671441084417,0.423362714708271,3.58313098523844));
#15182=CARTESIAN_POINT('Ctrl Pts',(5.20876177150037,0.353953913481732,3.51264098125308));
#15183=CARTESIAN_POINT('Ctrl Pts',(5.20080913215656,0.266558107499543,3.45986209043499));
#15184=CARTESIAN_POINT('Ctrl Pts',(5.19285649281275,0.171860624350003,3.43124725102074));
#15185=CARTESIAN_POINT('Ctrl Pts',(5.18490385346895,0.0771631412004631,
3.40263241160649));
#15186=CARTESIAN_POINT('Ctrl Pts',(5.17695121412514,-0.0248360191164267,
3.39818162359609));
#15187=CARTESIAN_POINT('Ctrl Pts',(5.16899857478133,-0.121666070051256,
3.41843905644231));
#15188=CARTESIAN_POINT('Ctrl Pts',(5.16104593543753,-0.218496120986084,
3.43869648928852));
#15189=CARTESIAN_POINT('Ctrl Pts',(5.15309329609372,-0.310157062538852,
3.48366214299137));
#15190=CARTESIAN_POINT('Ctrl Pts',(5.14514065674991,-0.385442096207774,
3.54783835396576));
#15191=CARTESIAN_POINT('Ctrl Pts',(5.13718801740611,-0.460727129876697,
3.61201456494015));
#15192=CARTESIAN_POINT('Ctrl Pts',(5.1292353780623,-0.519636255661773,3.6954013331861));
#15193=CARTESIAN_POINT('Ctrl Pts',(5.1212827387185,-0.554967030609594,3.78780349058054));
#15194=CARTESIAN_POINT('Ctrl Pts',(5.11333009937469,-0.590297805557415,
3.88020564797498));
#15195=CARTESIAN_POINT('Ctrl Pts',(5.10537746003088,-0.60205022966798,3.98162319451792));
#15196=CARTESIAN_POINT('Ctrl Pts',(5.09742482068708,-0.588787409028971,
4.07965645386523));
#15197=CARTESIAN_POINT('Ctrl Pts',(5.08947218134327,-0.575524588389962,
4.17768971321255));
#15198=CARTESIAN_POINT('Ctrl Pts',(5.08151954199946,-0.537246523001379,
4.27233868536424));
#15199=CARTESIAN_POINT('Ctrl Pts',(5.07356690265566,-0.47863322769376,4.35203124438164));
#15200=CARTESIAN_POINT('Ctrl Pts',(5.06561426331185,-0.42001993238614,4.43172380339905));
#15201=CARTESIAN_POINT('Ctrl Pts',(5.05766162396805,-0.341071407159484,
4.49645994928216));
#15202=CARTESIAN_POINT('Ctrl Pts',(5.04970898462424,-0.251440184480074,
4.53832480650817));
#15203=CARTESIAN_POINT('Ctrl Pts',(5.04275446016868,-0.1730583412759,4.5749353153996));
#15204=CARTESIAN_POINT('Ctrl Pts',(5.03579993571312,-0.0865070403179845,
4.59405529558476));
#15205=CARTESIAN_POINT('Ctrl Pts',(5.02884541125756,1.1583539301252E-5,
4.59413174414479));
#15206=CARTESIAN_POINT('Ctrl Pts',(4.92115458874249,-9.52916733652962E-6,
4.59405847898621));
#15207=CARTESIAN_POINT('Ctrl Pts',(4.9242559935701,-0.0386066277022544,
4.59408039337166));
#15208=CARTESIAN_POINT('Ctrl Pts',(4.92735739839772,-0.0771995748988638,
4.59037647703175));
#15209=CARTESIAN_POINT('Ctrl Pts',(4.93045880322533,-0.115049119822012,
4.58290605049323));
#15210=CARTESIAN_POINT('Ctrl Pts',(4.93841144256913,-0.212103131417409,
4.56375034161047));
#15211=CARTESIAN_POINT('Ctrl Pts',(4.94636408191294,-0.304269161635426,
4.51982926360553));
#15212=CARTESIAN_POINT('Ctrl Pts',(4.95431672125675,-0.380278658005779,
4.45651276645759));
#15213=CARTESIAN_POINT('Ctrl Pts',(4.96226936060055,-0.456288154376132,
4.39319626930964));
#15214=CARTESIAN_POINT('Ctrl Pts',(4.97022199994436,-0.516141116898821,
4.31048435301868));
#15215=CARTESIAN_POINT('Ctrl Pts',(4.97817463928816,-0.552519705724467,
4.21848967586497));
#15216=CARTESIAN_POINT('Ctrl Pts',(4.98612727863197,-0.588898294550112,
4.12649499871126));
#15217=CARTESIAN_POINT('Ctrl Pts',(4.99407991797578,-0.601802509678713,
4.0252175606948));
#15218=CARTESIAN_POINT('Ctrl Pts',(5.00203255731958,-0.589654635058918,
3.92703990798411));
#15219=CARTESIAN_POINT('Ctrl Pts',(5.00998519666339,-0.577506760439122,
3.82886225527341));
#15220=CARTESIAN_POINT('Ctrl Pts',(5.0179378360072,-0.540306796070929,3.73378438786847));
#15221=CARTESIAN_POINT('Ctrl Pts',(5.025890475351,-0.482602944251693,3.65343086999412));
#15222=CARTESIAN_POINT('Ctrl Pts',(5.03384311469481,-0.424899092432456,
3.57307735211977));
#15223=CARTESIAN_POINT('Ctrl Pts',(5.04179575403862,-0.346691353162178,
3.50744818377599));
#15224=CARTESIAN_POINT('Ctrl Pts',(5.04974839338242,-0.257541687734669,
3.46456742464414));
#15225=CARTESIAN_POINT('Ctrl Pts',(5.05770103272623,-0.16839202230716,3.42168666551229));
#15226=CARTESIAN_POINT('Ctrl Pts',(5.06565367207003,-0.0683004307224215,
3.40155431559236));
#15227=CARTESIAN_POINT('Ctrl Pts',(5.07360631141384,0.0304955267282049,
3.40663182885918));
#15228=CARTESIAN_POINT('Ctrl Pts',(5.08155895075765,0.129291484178831,3.41170934212599));
#15229=CARTESIAN_POINT('Ctrl Pts',(5.08951159010146,0.226791807495345,3.44199671857955));
#15230=CARTESIAN_POINT('Ctrl Pts',(5.09746422944526,0.311075754224562,3.49379091394262));
#15231=CARTESIAN_POINT('Ctrl Pts',(5.10541686878907,0.395359700953779,3.54558510930568));
#15232=CARTESIAN_POINT('Ctrl Pts',(5.11336950813287,0.466427271095698,3.61888612357825));
#15233=CARTESIAN_POINT('Ctrl Pts',(5.12132214747668,0.515589486279599,3.70473190942573));
#15234=CARTESIAN_POINT('Ctrl Pts',(5.12927478682048,0.564751701463499,3.79057769527322));
#15235=CARTESIAN_POINT('Ctrl Pts',(5.13722742616429,0.592008561689381,3.88896825269562));
#15236=CARTESIAN_POINT('Ctrl Pts',(5.1451800655081,0.594027544563649,3.98787399599556));
#15237=CARTESIAN_POINT('Ctrl Pts',(5.1531327048519,0.596046527437917,4.0867797392955));
#15238=CARTESIAN_POINT('Ctrl Pts',(5.16108534419571,0.572827632960568,4.18620066847299));
#15239=CARTESIAN_POINT('Ctrl Pts',(5.16903798353952,0.527209687216453,4.2739812208502));
#15240=CARTESIAN_POINT('Ctrl Pts',(5.17699062288332,0.481591741472338,4.3617617732274));
#15241=CARTESIAN_POINT('Ctrl Pts',(5.18494326222713,0.413574744461461,4.43790194880433));
#15242=CARTESIAN_POINT('Ctrl Pts',(5.19289590157094,0.331474700441294,4.49309257410834));
#15243=CARTESIAN_POINT('Ctrl Pts',(5.20084854091474,0.24937465642113,4.54828319941234));
#15244=CARTESIAN_POINT('Ctrl Pts',(5.20880118025855,0.153191565391677,4.58252427444343));
#15245=CARTESIAN_POINT('Ctrl Pts',(5.21675381960235,0.0546851202186884,
4.59162936142496));
#15246=CARTESIAN_POINT('Ctrl Pts',(5.21822074264906,0.0365148790664279,
4.59330886194775));
#15247=CARTESIAN_POINT('Ctrl Pts',(5.21968766569578,0.018265586889787,4.59413312238171));
#15248=CARTESIAN_POINT('Ctrl Pts',(5.22115458874249,1.46139895546772E-5,
4.59411444380891));
#15249=CARTESIAN_POINT('Origin',(4.,0.,4.));
#15250=CARTESIAN_POINT('',(5.62884541125756,1.52328526200479E-5,4.59408648697874));
#15251=CARTESIAN_POINT('',(5.52115458874249,-1.55733839743342E-5,4.59409663347568));
#15252=CARTESIAN_POINT('',(4.,-7.27562663373442E-17,4.5941));
#15253=CARTESIAN_POINT('Ctrl Pts',(5.62884541125756,1.52328526200479E-5,
4.59408648697874));
#15254=CARTESIAN_POINT('Ctrl Pts',(5.62666327996447,0.0271682673899915,
4.59411287463303));
#15255=CARTESIAN_POINT('Ctrl Pts',(5.62448114867138,0.054317778225707,4.59228554395034));
#15256=CARTESIAN_POINT('Ctrl Pts',(5.62229901737829,0.0812075234320336,
4.58857548522516));
#15257=CARTESIAN_POINT('Ctrl Pts',(5.61434637803449,0.179205497408217,4.57505441109036));
#15258=CARTESIAN_POINT('Ctrl Pts',(5.60639373869068,0.273753285393806,4.53652709601604));
#15259=CARTESIAN_POINT('Ctrl Pts',(5.59844109934688,0.353291132582354,4.47770402899113));
#15260=CARTESIAN_POINT('Ctrl Pts',(5.59048846000307,0.432828979770902,4.41888096196622));
#15261=CARTESIAN_POINT('Ctrl Pts',(5.58253582065927,0.497356886162411,4.33976214299073));
#15262=CARTESIAN_POINT('Ctrl Pts',(5.57458318131546,0.538985436353474,4.25002092526659));
#15263=CARTESIAN_POINT('Ctrl Pts',(5.56663054197165,0.580613986544537,4.16027970754245));
#15264=CARTESIAN_POINT('Ctrl Pts',(5.55867790262784,0.599343180535155,4.05991609106967));
#15265=CARTESIAN_POINT('Ctrl Pts',(5.55072526328404,0.592883119270616,3.96120089488413));
#15266=CARTESIAN_POINT('Ctrl Pts',(5.54277262394023,0.586423058006077,3.86248569869858));
#15267=CARTESIAN_POINT('Ctrl Pts',(5.53481998459642,0.554773741486382,3.76541892280029));
#15268=CARTESIAN_POINT('Ctrl Pts',(5.52686734525262,0.501804729712613,3.68186830256729));
#15269=CARTESIAN_POINT('Ctrl Pts',(5.51891470590881,0.448835717938844,3.5983176823343));
#15270=CARTESIAN_POINT('Ctrl Pts',(5.51096206656501,0.374547010911001,3.52828321776661));
#15271=CARTESIAN_POINT('Ctrl Pts',(5.5030094272212,0.288021414854312,3.48032757600706));
#15272=CARTESIAN_POINT('Ctrl Pts',(5.4950567878774,0.201495818797622,3.4323719342475));
#15273=CARTESIAN_POINT('Ctrl Pts',(5.48710414853359,0.102733333712086,3.40649511529609));
#15274=CARTESIAN_POINT('Ctrl Pts',(5.47915150918978,0.00380901851787326,
3.40586091270526));
#15275=CARTESIAN_POINT('Ctrl Pts',(5.47119886984597,-0.0951152966763399,
3.40522671011442));
#15276=CARTESIAN_POINT('Ctrl Pts',(5.46324623050217,-0.194201441979227,
3.42983512388417));
#15277=CARTESIAN_POINT('Ctrl Pts',(5.45529359115836,-0.281334786601535,
3.47667744027106));
#15278=CARTESIAN_POINT('Ctrl Pts',(5.44734095181456,-0.368468131223842,
3.52351975665794));
#15279=CARTESIAN_POINT('Ctrl Pts',(5.43938831247075,-0.443648675165568,
3.59259597566196));
#15280=CARTESIAN_POINT('Ctrl Pts',(5.43143567312694,-0.497684572991269,
3.67546058871077));
#15281=CARTESIAN_POINT('Ctrl Pts',(5.42348303378314,-0.551720470816969,
3.75832520175959));
#15282=CARTESIAN_POINT('Ctrl Pts',(5.41553039443933,-0.584611722526643,
3.85497820885321));
#15283=CARTESIAN_POINT('Ctrl Pts',(5.40757775509553,-0.592336924628993,
3.95360246348684));
#15284=CARTESIAN_POINT('Ctrl Pts',(5.39962511575172,-0.600062126731343,
4.05222671812048));
#15285=CARTESIAN_POINT('Ctrl Pts',(5.39167247640791,-0.582621279226368,
4.15282222029412));
#15286=CARTESIAN_POINT('Ctrl Pts',(5.3837198370641,-0.542146763261091,4.24308979978386));
#15287=CARTESIAN_POINT('Ctrl Pts',(5.3757671977203,-0.501672247295815,4.3333573792736));
#15288=CARTESIAN_POINT('Ctrl Pts',(5.36781455837649,-0.438164062870237,
4.41329703607943));
#15289=CARTESIAN_POINT('Ctrl Pts',(5.35986191903269,-0.359386950494509,
4.47313505840055));
#15290=CARTESIAN_POINT('Ctrl Pts',(5.35190927968888,-0.28060983811878,4.53297308072167));
#15291=CARTESIAN_POINT('Ctrl Pts',(5.34395664034507,-0.1865637977929,4.57270946855809));
#15292=CARTESIAN_POINT('Ctrl Pts',(5.33600400100126,-0.0887472388280498,
4.58748590729807));
#15293=CARTESIAN_POINT('Ctrl Pts',(5.33361780442003,-0.0593972924141157,
4.59191959101989));
#15294=CARTESIAN_POINT('Ctrl Pts',(5.3312316078388,-0.0297078841644672,
4.59410611700271));
#15295=CARTESIAN_POINT('Ctrl Pts',(5.32884541125756,-1.45357002139801E-5,
4.59407911932661));
#15296=CARTESIAN_POINT('Ctrl Pts',(5.22115458874249,1.46139895546772E-5,
4.59411444380891));
#15297=CARTESIAN_POINT('Ctrl Pts',(5.22764030503958,-0.0806785298274998,
4.59403186011492));
#15298=CARTESIAN_POINT('Ctrl Pts',(5.23412602133668,-0.161404528346198,
4.57747154641029));
#15299=CARTESIAN_POINT('Ctrl Pts',(5.24061173763377,-0.235476461490165,
4.54549665421293));
#15300=CARTESIAN_POINT('Ctrl Pts',(5.24856437697758,-0.32630179870949,4.50628976108741));
#15301=CARTESIAN_POINT('Ctrl Pts',(5.25651701632139,-0.407122673831612,
4.44390687590439));
#15302=CARTESIAN_POINT('Ctrl Pts',(5.26446965566519,-0.468057634114636,
4.36597515601533));
#15303=CARTESIAN_POINT('Ctrl Pts',(5.272422295009,-0.52899259439766,4.28804343612627));
#15304=CARTESIAN_POINT('Ctrl Pts',(5.28037493435281,-0.570041639841584,
4.19456288153117));
#15305=CARTESIAN_POINT('Ctrl Pts',(5.28832757369661,-0.586185965564114,
4.09696276320888));
#15306=CARTESIAN_POINT('Ctrl Pts',(5.29628021304042,-0.602330291286644,
3.99936264488659));
#15307=CARTESIAN_POINT('Ctrl Pts',(5.30423285238423,-0.59356989728778,3.89764296283709));
#15308=CARTESIAN_POINT('Ctrl Pts',(5.31218549172803,-0.560975861048054,
3.80424033358521));
#15309=CARTESIAN_POINT('Ctrl Pts',(5.32013813107184,-0.528381824808328,
3.71083770433334));
#15310=CARTESIAN_POINT('Ctrl Pts',(5.32809077041564,-0.471954146327742,
3.62575212787907));
#15311=CARTESIAN_POINT('Ctrl Pts',(5.33604340975945,-0.398591877830097,
3.55938647478623));
#15312=CARTESIAN_POINT('Ctrl Pts',(5.34399604910326,-0.325229609332449,
3.49302082169338));
#15313=CARTESIAN_POINT('Ctrl Pts',(5.35194868844707,-0.234932750817741,
3.44537509196196));
#15314=CARTESIAN_POINT('Ctrl Pts',(5.35990132779087,-0.138741323057917,
3.42227462497344));
#15315=CARTESIAN_POINT('Ctrl Pts',(5.36785396713468,-0.042549895298095,
3.39917415798493));
#15316=CARTESIAN_POINT('Ctrl Pts',(5.37580660647848,0.059536101706843,3.40061895373932));
#15317=CARTESIAN_POINT('Ctrl Pts',(5.38375924582229,0.155035264439678,3.42643236627792));
#15318=CARTESIAN_POINT('Ctrl Pts',(5.39171188516609,0.250534427172515,3.45224577881651));
#15319=CARTESIAN_POINT('Ctrl Pts',(5.3996645245099,0.339446755633248,3.5024278081393));
#15320=CARTESIAN_POINT('Ctrl Pts',(5.40761716385371,0.41090150670596,3.57084301769608));
#15321=CARTESIAN_POINT('Ctrl Pts',(5.41556980319751,0.482356257778672,3.63925822725286));
#15322=CARTESIAN_POINT('Ctrl Pts',(5.42352244254132,0.536353431463363,3.72590661704362));
#15323=CARTESIAN_POINT('Ctrl Pts',(5.43147508188513,0.566291137850326,3.82019424128906));
#15324=CARTESIAN_POINT('Ctrl Pts',(5.43942772122893,0.596228844237288,3.91448186553449));
#15325=CARTESIAN_POINT('Ctrl Pts',(5.44738036057274,0.602107083326521,4.01640872423458));
#15326=CARTESIAN_POINT('Ctrl Pts',(5.45533299991655,0.583207160329387,4.11351287069736));
#15327=CARTESIAN_POINT('Ctrl Pts',(5.46328563926035,0.564307237332252,4.21061701716013));
#15328=CARTESIAN_POINT('Ctrl Pts',(5.47123827860416,0.520629152248751,4.30289845138559));
#15329=CARTESIAN_POINT('Ctrl Pts',(5.47919091794796,0.457513145863858,4.37907451119169));
#15330=CARTESIAN_POINT('Ctrl Pts',(5.48714355729177,0.394397139478966,4.45525057099779));
#15331=CARTESIAN_POINT('Ctrl Pts',(5.49509619663558,0.311843211792683,4.51532125638452));
#15332=CARTESIAN_POINT('Ctrl Pts',(5.50304883597938,0.219944704826683,4.5519421079172));
#15333=CARTESIAN_POINT('Ctrl Pts',(5.50908408690042,0.150203009669811,4.5797336395568));
#15334=CARTESIAN_POINT('Ctrl Pts',(5.51511933782146,0.0750795109720808,
4.59401975858331));
#15335=CARTESIAN_POINT('Ctrl Pts',(5.52115458874249,-1.55733839743342E-5,
4.59409663347568));
#15336=CARTESIAN_POINT('Origin',(4.,0.,4.));
#15337=CARTESIAN_POINT('',(5.92884541125757,-1.3134308860685E-5,4.59412454375027));
#15338=CARTESIAN_POINT('',(5.82115458874249,1.31105368646138E-5,4.59407040741879));
#15339=CARTESIAN_POINT('',(4.,-7.27562663373442E-17,4.5941));
#15340=CARTESIAN_POINT('Ctrl Pts',(5.92884541125757,-1.3134308860685E-5,
4.59412454375027));
#15341=CARTESIAN_POINT('Ctrl Pts',(5.92209495209015,0.0839697382976411,
4.5940436242297));
#15342=CARTESIAN_POINT('Ctrl Pts',(5.91534449292274,0.16798613900316,4.57606223573506));
#15343=CARTESIAN_POINT('Ctrl Pts',(5.90859403375532,0.244517407380453,4.54150437939301));
#15344=CARTESIAN_POINT('Ctrl Pts',(5.90064139441152,0.334678026211646,4.50079216098422));
#15345=CARTESIAN_POINT('Ctrl Pts',(5.89268875506771,0.41445008323119,4.43707358099086));
#15346=CARTESIAN_POINT('Ctrl Pts',(5.8847361157239,0.474080337065587,4.35813908232779));
#15347=CARTESIAN_POINT('Ctrl Pts',(5.8767834763801,0.533710590899983,4.27920458366471));
#15348=CARTESIAN_POINT('Ctrl Pts',(5.86883083703629,0.573199041549232,4.18505416633191));
#15349=CARTESIAN_POINT('Ctrl Pts',(5.86087819769249,0.587717699183782,4.08719901244189));
#15350=CARTESIAN_POINT('Ctrl Pts',(5.85292555834868,0.602236356818331,3.98934385855186));
#15351=CARTESIAN_POINT('Ctrl Pts',(5.84497291900487,0.591785221438181,3.88778396810461));
#15352=CARTESIAN_POINT('Ctrl Pts',(5.83702027966107,0.557642080814915,3.79493641494568));
#15353=CARTESIAN_POINT('Ctrl Pts',(5.82906764031726,0.523498940191649,3.70208886178675));
#15354=CARTESIAN_POINT('Ctrl Pts',(5.82111500097346,0.465663794325265,3.61795364591614));
#15355=CARTESIAN_POINT('Ctrl Pts',(5.81316236162965,0.391207780605707,3.55281744653948));
#15356=CARTESIAN_POINT('Ctrl Pts',(5.80520972228584,0.31675176688615,3.48768124716281));
#15357=CARTESIAN_POINT('Ctrl Pts',(5.79725708294203,0.225674885313418,3.44154406428009));
#15358=CARTESIAN_POINT('Ctrl Pts',(5.78930444359823,0.129112523455512,3.42004679519738));
#15359=CARTESIAN_POINT('Ctrl Pts',(5.78135180425442,0.0325501615976049,
3.39854952611466));
#15360=CARTESIAN_POINT('Ctrl Pts',(5.77339916491062,-0.0694976805454773,
3.40169217083197));
#15361=CARTESIAN_POINT('Ctrl Pts',(5.76544652556681,-0.164554263536051,
3.42909049911887));
#15362=CARTESIAN_POINT('Ctrl Pts',(5.75749388622301,-0.259610846526622,
3.45648882740576));
#15363=CARTESIAN_POINT('Ctrl Pts',(5.7495412468792,-0.347676170364685,3.50814283926225));
#15364=CARTESIAN_POINT('Ctrl Pts',(5.74158860753539,-0.417983050247216,
3.57773712775495));
#15365=CARTESIAN_POINT('Ctrl Pts',(5.73363596819158,-0.488289930129746,
3.64733141624764));
#15366=CARTESIAN_POINT('Ctrl Pts',(5.72568332884778,-0.540838366056745,
3.73486598137654));
#15367=CARTESIAN_POINT('Ctrl Pts',(5.71773068950397,-0.569203595796233,
3.82963853060694));
#15368=CARTESIAN_POINT('Ctrl Pts',(5.70977805016017,-0.597568825535722,
3.92441107983734));
#15369=CARTESIAN_POINT('Ctrl Pts',(5.70182541081636,-0.6017508490877,4.02642161316923));
#15370=CARTESIAN_POINT('Ctrl Pts',(5.69387277147255,-0.581238357244447,
4.12319795341528));
#15371=CARTESIAN_POINT('Ctrl Pts',(5.68592013212875,-0.560725865401195,
4.21997429366132));
#15372=CARTESIAN_POINT('Ctrl Pts',(5.67796749278494,-0.515518858162713,
4.31151644082153));
#15373=CARTESIAN_POINT('Ctrl Pts',(5.67001485344113,-0.451144507802385,
4.38663212069642));
#15374=CARTESIAN_POINT('Ctrl Pts',(5.66206221409732,-0.386770157442057,
4.46174780057131));
#15375=CARTESIAN_POINT('Ctrl Pts',(5.65410957475352,-0.303228463959881,
4.52043701316089));
#15376=CARTESIAN_POINT('Ctrl Pts',(5.64615693540972,-0.210733537235404,
4.55552420285805));
#15377=CARTESIAN_POINT('Ctrl Pts',(5.640386427359,-0.143618370026196,4.5809837895275));
#15378=CARTESIAN_POINT('Ctrl Pts',(5.63461591930828,-0.07178924788396,4.59401670649762));
#15379=CARTESIAN_POINT('Ctrl Pts',(5.62884541125756,1.52328526200479E-5,
4.59408648697874));
#15380=CARTESIAN_POINT('Ctrl Pts',(5.52115458874249,-1.55733839743342E-5,
4.59409663347568));
#15381=CARTESIAN_POINT('Ctrl Pts',(5.52307197716526,-0.0238731473664388,
4.59412105649149));
#15382=CARTESIAN_POINT('Ctrl Pts',(5.52498936558803,-0.0477278534282068,
4.59271130989713));
#15383=CARTESIAN_POINT('Ctrl Pts',(5.5269067540108,-0.0714062077139717,
4.58984482465595));
#15384=CARTESIAN_POINT('Ctrl Pts',(5.53485939335461,-0.169615527042917,
4.57795567218339));
#15385=CARTESIAN_POINT('Ctrl Pts',(5.54281203269841,-0.264791079455087,
4.54100634955965));
#15386=CARTESIAN_POINT('Ctrl Pts',(5.55076467204222,-0.345296357402727,
4.48351441471562));
#15387=CARTESIAN_POINT('Ctrl Pts',(5.55871731138603,-0.425801635350366,
4.4260224798716));
#15388=CARTESIAN_POINT('Ctrl Pts',(5.56666995072984,-0.491636638833473,
4.34798793280729));
#15389=CARTESIAN_POINT('Ctrl Pts',(5.57462259007364,-0.534752142022197,
4.2589515597096));
#15390=CARTESIAN_POINT('Ctrl Pts',(5.58257522941745,-0.577867645210921,
4.16991518661191));
#15391=CARTESIAN_POINT('Ctrl Pts',(5.59052786876125,-0.598263648105263,
4.06987698748084));
#15392=CARTESIAN_POINT('Ctrl Pts',(5.59848050810506,-0.59344646156208,3.97106799465478));
#15393=CARTESIAN_POINT('Ctrl Pts',(5.60643314744886,-0.588629275018896,
3.87225900182873));
#15394=CARTESIAN_POINT('Ctrl Pts',(5.61438578679267,-0.558598899038186,
3.77467921530768));
#15395=CARTESIAN_POINT('Ctrl Pts',(5.62233842613648,-0.50702695609161,3.69025909300064));
#15396=CARTESIAN_POINT('Ctrl Pts',(5.63029106548029,-0.455455013145033,
3.6058389706936));
#15397=CARTESIAN_POINT('Ctrl Pts',(5.63824370482409,-0.382341503232591,
3.53457851260056));
#15398=CARTESIAN_POINT('Ctrl Pts',(5.6461963441679,-0.296625548722353,3.48519028027742));
#15399=CARTESIAN_POINT('Ctrl Pts',(5.6541489835117,-0.210909594212113,3.43580204795428));
#15400=CARTESIAN_POINT('Ctrl Pts',(5.66210162285551,-0.112591195104077,
3.40828604140104));
#15401=CARTESIAN_POINT('Ctrl Pts',(5.67005426219932,-0.0136911147678568,
3.40600646716786));
#15402=CARTESIAN_POINT('Ctrl Pts',(5.67800690154312,0.0852089655683624,
3.40372689293467));
#15403=CARTESIAN_POINT('Ctrl Pts',(5.68595954088693,0.184690727132768,3.42668375102154));
#15404=CARTESIAN_POINT('Ctrl Pts',(5.69391218023074,0.272591169676606,3.47207025288287));
#15405=CARTESIAN_POINT('Ctrl Pts',(5.70186481957454,0.360491612220445,3.51745675474419));
#15406=CARTESIAN_POINT('Ctrl Pts',(5.70981745891835,0.436810735743714,3.58527290037998));
#15407=CARTESIAN_POINT('Ctrl Pts',(5.71777009826216,0.492217487918224,3.667227242308));
#15408=CARTESIAN_POINT('Ctrl Pts',(5.72572273760596,0.547624240092733,3.74918158423602));
#15409=CARTESIAN_POINT('Ctrl Pts',(5.73367537694977,0.582118620918482,3.84527412245626));
#15410=CARTESIAN_POINT('Ctrl Pts',(5.74162801629357,0.591483222595687,3.94375623549444));
#15411=CARTESIAN_POINT('Ctrl Pts',(5.74958065563738,0.600847824272892,4.04223834853263));
#15412=CARTESIAN_POINT('Ctrl Pts',(5.75753329498119,0.585082646801554,4.14311003638875));
#15413=CARTESIAN_POINT('Ctrl Pts',(5.76548593432499,0.546115197731279,4.23403836123177));
#15414=CARTESIAN_POINT('Ctrl Pts',(5.7734385736688,0.507147748661005,4.32496668607478));
#15415=CARTESIAN_POINT('Ctrl Pts',(5.78139121301261,0.444978027991796,4.4059516479047));
#15416=CARTESIAN_POINT('Ctrl Pts',(5.78934385235641,0.367207131024688,4.46709173242012));
#15417=CARTESIAN_POINT('Ctrl Pts',(5.79729649170022,0.28943623405758,4.52823181693554));
#15418=CARTESIAN_POINT('Ctrl Pts',(5.80524913104403,0.196064160792572,4.56952702413646));
#15419=CARTESIAN_POINT('Ctrl Pts',(5.81320177038783,0.0985069184831505,
4.58592845199323));
#15420=CARTESIAN_POINT('Ctrl Pts',(5.81585270983939,0.0659871057213339,
4.59139571767544));
#15421=CARTESIAN_POINT('Ctrl Pts',(5.81850364929094,0.0330022532417819,
4.59409688335147));
#15422=CARTESIAN_POINT('Ctrl Pts',(5.82115458874249,1.31105368646138E-5,
4.59407040741879));
#15423=CARTESIAN_POINT('Origin',(4.,0.,4.));
#15424=CARTESIAN_POINT('',(6.22884541125756,-1.27841859475647E-5,4.5940334609955));
#15425=CARTESIAN_POINT('',(6.12115458874249,-9.50793186244619E-6,4.59413936148612));
#15426=CARTESIAN_POINT('',(4.,-7.27562663373442E-17,4.5941));
#15427=CARTESIAN_POINT('Ctrl Pts',(6.22884541125756,-1.27841859475647E-5,
4.5940334609955));
#15428=CARTESIAN_POINT('Ctrl Pts',(6.22547926355963,0.0418951881409122,
4.59406590912705));
#15429=CARTESIAN_POINT('Ctrl Pts',(6.2221131158617,0.0838018877146867,4.58971510200585));
#15430=CARTESIAN_POINT('Ctrl Pts',(6.21874696816377,0.124749109322564,4.58093223526196));
#15431=CARTESIAN_POINT('Ctrl Pts',(6.21079432881996,0.22148832423537,4.56018241146135));
#15432=CARTESIAN_POINT('Ctrl Pts',(6.20284168947616,0.31287214740051,4.51469474440412));
#15433=CARTESIAN_POINT('Ctrl Pts',(6.19488905013236,0.387808805213989,4.4501133836823));
#15434=CARTESIAN_POINT('Ctrl Pts',(6.18693641078855,0.462745463027469,4.38553202296047));
#15435=CARTESIAN_POINT('Ctrl Pts',(6.17898377144474,0.521234955489287,4.30185696857405));
#15436=CARTESIAN_POINT('Ctrl Pts',(6.17103113210093,0.556083161424236,4.20927485003939));
#15437=CARTESIAN_POINT('Ctrl Pts',(6.16307849275713,0.590931367359184,4.11669273150472));
#15438=CARTESIAN_POINT('Ctrl Pts',(6.15512585341332,0.602138286767263,4.0152035488218));
#15439=CARTESIAN_POINT('Ctrl Pts',(6.14717321406952,0.588356486924291,3.9172389266648));
#15440=CARTESIAN_POINT('Ctrl Pts',(6.13922057472571,0.574574687081318,3.81927430450779));
#15441=CARTESIAN_POINT('Ctrl Pts',(6.1312679353819,0.535804167987293,3.7248342428767));
#15442=CARTESIAN_POINT('Ctrl Pts',(6.12331529603809,0.476773096629474,3.64545304401991));
#15443=CARTESIAN_POINT('Ctrl Pts',(6.11536265669429,0.417742025271657,3.56607184516312));
#15444=CARTESIAN_POINT('Ctrl Pts',(6.10741001735048,0.338450401650047,3.50174950908064));
#15445=CARTESIAN_POINT('Ctrl Pts',(6.09945737800668,0.248599092144812,3.46035682177302));
#15446=CARTESIAN_POINT('Ctrl Pts',(6.09150473866287,0.158747782639575,3.41896413446539));
#15447=CARTESIAN_POINT('Ctrl Pts',(6.08355209931906,0.0583367872507115,
3.40050109593262));
#15448=CARTESIAN_POINT('Ctrl Pts',(6.07559945997526,-0.0403606640336046,
3.40722161935946));
#15449=CARTESIAN_POINT('Ctrl Pts',(6.06764682063145,-0.139058115317921,
3.4139421427863));
#15450=CARTESIAN_POINT('Ctrl Pts',(6.05969418128764,-0.23604202249769,3.44584622817275));
#15451=CARTESIAN_POINT('Ctrl Pts',(6.05174154194384,-0.319452991027635,
3.49903499090221));
#15452=CARTESIAN_POINT('Ctrl Pts',(6.04378890260003,-0.40286395955758,3.55222375363166));
#15453=CARTESIAN_POINT('Ctrl Pts',(6.03583626325623,-0.472701989437702,
3.62669719370411));
#15454=CARTESIAN_POINT('Ctrl Pts',(6.02788362391242,-0.520429378860104,
3.71334895258148));
#15455=CARTESIAN_POINT('Ctrl Pts',(6.01993098456861,-0.568156768282506,
3.80000071145885));
#15456=CARTESIAN_POINT('Ctrl Pts',(6.0119783452248,-0.593773517247188,3.89883078914114));
#15457=CARTESIAN_POINT('Ctrl Pts',(6.004025705881,-0.594147126960238,3.99775637428654));
#15458=CARTESIAN_POINT('Ctrl Pts',(5.99607306653719,-0.594520736673288,
4.09668195943193));
#15459=CARTESIAN_POINT('Ctrl Pts',(5.98812042719339,-0.569651207134705,
4.19570305204043));
#15460=CARTESIAN_POINT('Ctrl Pts',(5.98016778784958,-0.52257944308796,4.28271270390554));
#15461=CARTESIAN_POINT('Ctrl Pts',(5.97221514850578,-0.475507679041215,
4.36972235577065));
#15462=CARTESIAN_POINT('Ctrl Pts',(5.96426250916196,-0.406233680486307,
4.44472056689237));
#15463=CARTESIAN_POINT('Ctrl Pts',(5.95630986981816,-0.323226996343023,
4.49853792802592));
#15464=CARTESIAN_POINT('Ctrl Pts',(5.94835723047435,-0.240220312199739,
4.55235528915947));
#15465=CARTESIAN_POINT('Ctrl Pts',(5.94040459113055,-0.143480942468078,
4.58499180030486));
#15466=CARTESIAN_POINT('Ctrl Pts',(5.93245195178675,-0.0448366672808267,
4.59245712746544));
#15467=CARTESIAN_POINT('Ctrl Pts',(5.93124977161035,-0.0299248641651563,
4.59358564190382));
#15468=CARTESIAN_POINT('Ctrl Pts',(5.93004759143396,-0.0149695309183627,
4.59413895459864));
#15469=CARTESIAN_POINT('Ctrl Pts',(5.92884541125757,-1.3134308860685E-5,
4.59412454375027));
#15470=CARTESIAN_POINT('Ctrl Pts',(5.82115458874249,1.31105368646138E-5,
4.59407040741879));
#15471=CARTESIAN_POINT('Ctrl Pts',(5.82645628863475,-0.0659629472043463,
4.59401745734129));
#15472=CARTESIAN_POINT('Ctrl Pts',(5.831757988527,-0.131956164688202,4.58305467757793));
#15473=CARTESIAN_POINT('Ctrl Pts',(5.83705968841925,-0.194280919321303,
4.56148970414564));
#15474=CARTESIAN_POINT('Ctrl Pts',(5.84501232776306,-0.287769103462499,
4.52914187992864));
#15475=CARTESIAN_POINT('Ctrl Pts',(5.85296496710686,-0.373003060391055,
4.47293858298203));
#15476=CARTESIAN_POINT('Ctrl Pts',(5.86091760645067,-0.439561779454174,
4.39975142997742));
#15477=CARTESIAN_POINT('Ctrl Pts',(5.86887024579447,-0.506120498517293,
4.32656427697281));
#15478=CARTESIAN_POINT('Ctrl Pts',(5.87682288513828,-0.554003979714975,
4.2363932679102));
#15479=CARTESIAN_POINT('Ctrl Pts',(5.88477552448209,-0.577357812582609,
4.14026304025204));
#15480=CARTESIAN_POINT('Ctrl Pts',(5.8927281638259,-0.600711645450243,4.04413281259387));
#15481=CARTESIAN_POINT('Ctrl Pts',(5.9006808031697,-0.59953582998783,3.94204336634015));
#15482=CARTESIAN_POINT('Ctrl Pts',(5.90863344251351,-0.573974130801472,
3.84647652011691));
#15483=CARTESIAN_POINT('Ctrl Pts',(5.91658608185731,-0.548412431615114,
3.75090967389367));
#15484=CARTESIAN_POINT('Ctrl Pts',(5.92453872120112,-0.498464848704808,
3.66186542770092));
#15485=CARTESIAN_POINT('Ctrl Pts',(5.93249136054493,-0.430238144626613,
3.59023066587279));
#15486=CARTESIAN_POINT('Ctrl Pts',(5.94044399988873,-0.362011440548417,
3.51859590404466));
#15487=CARTESIAN_POINT('Ctrl Pts',(5.94839663923254,-0.275505615302329,
3.46437062658116));
#15488=CARTESIAN_POINT('Ctrl Pts',(5.95634927857635,-0.181297202577209,
3.43418458862315));
#15489=CARTESIAN_POINT('Ctrl Pts',(5.96430191792015,-0.087088789852092,
3.40399855066514));
#15490=CARTESIAN_POINT('Ctrl Pts',(5.97225455726396,0.0148222103520573,
3.39785175221263));
#15491=CARTESIAN_POINT('Ctrl Pts',(5.98020719660777,0.111975824940657,3.41649576758492));
#15492=CARTESIAN_POINT('Ctrl Pts',(5.98815983595157,0.209129439529257,3.43513978295721));
#15493=CARTESIAN_POINT('Ctrl Pts',(5.99611247529537,0.301525668502307,3.47857461215431));
#15494=CARTESIAN_POINT('Ctrl Pts',(6.00406511463918,0.377867748972965,3.54148967172874));
#15495=CARTESIAN_POINT('Ctrl Pts',(6.01201775398299,0.454209829443624,3.60440473130317));
#15496=CARTESIAN_POINT('Ctrl Pts',(6.0199703933268,0.514497761411887,3.68680002125492));
#15497=CARTESIAN_POINT('Ctrl Pts',(6.02792303267061,0.551360647735685,3.77860175380959));
#15498=CARTESIAN_POINT('Ctrl Pts',(6.03587567201441,0.588223534059482,3.87040348636426));
#15499=CARTESIAN_POINT('Ctrl Pts',(6.04382831135821,0.601661374738811,3.97161166152184));
#15500=CARTESIAN_POINT('Ctrl Pts',(6.05178095070202,0.590030977261751,4.06985190192822));
#15501=CARTESIAN_POINT('Ctrl Pts',(6.05973359004583,0.578400579784692,4.16809214233459));
#15502=CARTESIAN_POINT('Ctrl Pts',(6.06768622938964,0.541701944151245,4.26336444798975));
#15503=CARTESIAN_POINT('Ctrl Pts',(6.07563886873345,0.484422419230229,4.3440210474869));
#15504=CARTESIAN_POINT('Ctrl Pts',(6.08359150807725,0.427142894309213,4.42467764698404));
#15505=CARTESIAN_POINT('Ctrl Pts',(6.09154414742105,0.349282480100627,4.49071854032316));
#15506=CARTESIAN_POINT('Ctrl Pts',(6.09949678676486,0.26035984028865,4.53406826097581));
#15507=CARTESIAN_POINT('Ctrl Pts',(6.10671605409073,0.179637418414302,4.5734203814938));
#15508=CARTESIAN_POINT('Ctrl Pts',(6.11393532141662,0.0897989573399868,
4.59407340590587));
#15509=CARTESIAN_POINT('Ctrl Pts',(6.12115458874249,-9.50793186244619E-6,
4.59413936148612));
#15510=CARTESIAN_POINT('Origin',(4.,0.,4.));
#15511=CARTESIAN_POINT('',(6.52884541125757,2.61457539729726E-5,4.59508370962656));
#15512=CARTESIAN_POINT('',(6.42115458874249,-0.000630941829811112,4.59394485456974));
#15513=CARTESIAN_POINT('',(4.,-7.27562663373442E-17,4.5941));
#15514=CARTESIAN_POINT('Ctrl Pts',(6.52884541125757,2.61457539729726E-5,
4.59508370962656));
#15515=CARTESIAN_POINT('Ctrl Pts',(6.5129582963415,0.196771080344787,4.59506033873941));
#15516=CARTESIAN_POINT('Ctrl Pts',(6.49707118142544,0.393450480974957,4.48779253427891));
#15517=CARTESIAN_POINT('Ctrl Pts',(6.48118406650938,0.500111739713094,4.32240987211318));
#15518=CARTESIAN_POINT('Ctrl Pts',(6.46527878782176,0.606894944490356,4.15683812760557));
#15519=CARTESIAN_POINT('Ctrl Pts',(6.44937350913416,0.623454053851315,3.93301856375293));
#15520=CARTESIAN_POINT('Ctrl Pts',(6.43346823044654,0.541809843535619,3.75368369989414));
#15521=CARTESIAN_POINT('Ctrl Pts',(6.41756295175893,0.460165633219924,3.57434883603535));
#15522=CARTESIAN_POINT('Ctrl Pts',(6.40165767307132,0.280318103227576,3.43949867217041));
#15523=CARTESIAN_POINT('Ctrl Pts',(6.3857523943837,0.085604811340831,3.41110814665827));
#15524=CARTESIAN_POINT('Ctrl Pts',(6.36984711569609,-0.109108480545914,
3.38271762114613));
#15525=CARTESIAN_POINT('Ctrl Pts',(6.35394183700848,-0.318687534327053,
3.46078673398678));
#15526=CARTESIAN_POINT('Ctrl Pts',(6.33803655832087,-0.448733343985475,
3.60951691634857));
#15527=CARTESIAN_POINT('Ctrl Pts',(6.33008391897706,-0.513756248814686,
3.68388200752946));
#15528=CARTESIAN_POINT('Ctrl Pts',(6.32213127963325,-0.558895842613217,
3.77591236609064));
#15529=CARTESIAN_POINT('Ctrl Pts',(6.31417864028945,-0.579995970841135,
3.87270290659392));
#15530=CARTESIAN_POINT('Ctrl Pts',(6.30622600094564,-0.601096099069052,
3.9694934470972));
#15531=CARTESIAN_POINT('Ctrl Pts',(6.29827336160184,-0.598156761726356,
4.07104416954258));
#15532=CARTESIAN_POINT('Ctrl Pts',(6.29032072225803,-0.570614590620327,
4.16591643177432));
#15533=CARTESIAN_POINT('Ctrl Pts',(6.28236808291422,-0.543072419514299,
4.26078869400605));
#15534=CARTESIAN_POINT('Ctrl Pts',(6.27441544357042,-0.490927414644939,
4.34898249602413));
#15535=CARTESIAN_POINT('Ctrl Pts',(6.26646280422661,-0.421087730399527,
4.41916768405122));
#15536=CARTESIAN_POINT('Ctrl Pts',(6.2585101648828,-0.351248046154114,4.48935287207832));
#15537=CARTESIAN_POINT('Ctrl Pts',(6.250557525539,-0.263713682532649,4.54152944611444));
#15538=CARTESIAN_POINT('Ctrl Pts',(6.24260488619519,-0.168899197391682,
4.5696117428605));
#15539=CARTESIAN_POINT('Ctrl Pts',(6.23801839454932,-0.114217245248871,
4.58580752565092));
#15540=CARTESIAN_POINT('Ctrl Pts',(6.23343190290344,-0.0571138332845632,
4.59398924930378));
#15541=CARTESIAN_POINT('Ctrl Pts',(6.22884541125756,-1.27841859475647E-5,
4.5940334609955));
#15542=CARTESIAN_POINT('Ctrl Pts',(6.12115458874249,-9.50793186244619E-6,
4.59413936148612));
#15543=CARTESIAN_POINT('Ctrl Pts',(6.12188796076042,-0.00913273504488762,
4.59414606160884));
#15544=CARTESIAN_POINT('Ctrl Pts',(6.12262133277835,-0.0182556526135436,
4.59394031163173));
#15545=CARTESIAN_POINT('Ctrl Pts',(6.12335470479628,-0.0273686726716501,
4.59352013235631));
#15546=CARTESIAN_POINT('Ctrl Pts',(6.13130734414009,-0.126189680404606,
4.58896373511797));
#15547=CARTESIAN_POINT('Ctrl Pts',(6.13925998348389,-0.223846830455152,
4.55919239267511));
#15548=CARTESIAN_POINT('Ctrl Pts',(6.14721262282769,-0.308403173896691,
4.50784224986958));
#15549=CARTESIAN_POINT('Ctrl Pts',(6.1551652621715,-0.392959517338232,4.45649210706404));
#15550=CARTESIAN_POINT('Ctrl Pts',(6.16311790151532,-0.464415054170765,
4.38356316389581));
#15551=CARTESIAN_POINT('Ctrl Pts',(6.17107054085912,-0.514027768136376,
4.29797916579711));
#15552=CARTESIAN_POINT('Ctrl Pts',(6.17902318020293,-0.563640482101988,
4.2123951676984));
#15553=CARTESIAN_POINT('Ctrl Pts',(6.18697581954673,-0.591410373200678,
4.11415611466921));
#15554=CARTESIAN_POINT('Ctrl Pts',(6.19492845889053,-0.593952774873424,
4.0152594949342));
#15555=CARTESIAN_POINT('Ctrl Pts',(6.20288109823434,-0.59649517654617,3.9163628751992));
#15556=CARTESIAN_POINT('Ctrl Pts',(6.21083373757815,-0.573810088792972,
3.81680868875837));
#15557=CARTESIAN_POINT('Ctrl Pts',(6.21878637692196,-0.528651094032059,
3.72879442104321));
#15558=CARTESIAN_POINT('Ctrl Pts',(6.22673901626577,-0.483492099271145,
3.64078015332805));
#15559=CARTESIAN_POINT('Ctrl Pts',(6.23469165560957,-0.415859197502516,
3.56430580433857));
#15560=CARTESIAN_POINT('Ctrl Pts',(6.24264429495337,-0.334059153459168,
3.50867301156809));
#15561=CARTESIAN_POINT('Ctrl Pts',(6.25059693429718,-0.252259109415819,
3.45304021879761));
#15562=CARTESIAN_POINT('Ctrl Pts',(6.25854957364099,-0.156291923097747,
3.41824898224614));
#15563=CARTESIAN_POINT('Ctrl Pts',(6.2665022129848,-0.057819682214149,3.40864436538418));
#15564=CARTESIAN_POINT('Ctrl Pts',(6.2744548523286,0.0406525586694487,3.39903974852221));
#15565=CARTESIAN_POINT('Ctrl Pts',(6.28240749167241,0.141629854118573,3.41462175134974));
#15566=CARTESIAN_POINT('Ctrl Pts',(6.29036013101621,0.232632044389671,3.453312878872));
#15567=CARTESIAN_POINT('Ctrl Pts',(6.29831277036002,0.323634234660771,3.49200400639426));
#15568=CARTESIAN_POINT('Ctrl Pts',(6.30626540970382,0.404661319753841,3.55380425861124));
#15569=CARTESIAN_POINT('Ctrl Pts',(6.31421804904763,0.466059055789261,3.63148218419904));
#15570=CARTESIAN_POINT('Ctrl Pts',(6.32217068839144,0.527456791824679,3.70916010978684));
#15571=CARTESIAN_POINT('Ctrl Pts',(6.33012332773525,0.569225178802449,3.80271570874544));
#15572=CARTESIAN_POINT('Ctrl Pts',(6.33807596707905,0.585790493249255,3.90010619949006));
#15573=CARTESIAN_POINT('Ctrl Pts',(6.34602860642286,0.602355807696062,3.99749669023468));
#15574=CARTESIAN_POINT('Ctrl Pts',(6.35398124576666,0.593718049611903,4.09872207276531));
#15575=CARTESIAN_POINT('Ctrl Pts',(6.36193388511047,0.56173881546021,4.19248215342453));
#15576=CARTESIAN_POINT('Ctrl Pts',(6.36988652445427,0.529759581308516,4.28624223408375));
#15577=CARTESIAN_POINT('Ctrl Pts',(6.37783916379808,0.474438871089287,4.37253701287156));
#15578=CARTESIAN_POINT('Ctrl Pts',(6.38579180314189,0.401374624788453,4.4390182948332));
#15579=CARTESIAN_POINT('Ctrl Pts',(6.39757939834209,0.293077024234899,4.53755846574697));
#15580=CARTESIAN_POINT('Ctrl Pts',(6.40936699354229,0.145797072855576,4.59256860517148));
#15581=CARTESIAN_POINT('Ctrl Pts',(6.42115458874249,-0.000630941829811112,
4.59394485456974));
#15582=CARTESIAN_POINT('Origin',(4.,0.,4.));
#15583=CARTESIAN_POINT('',(6.82884541125756,0.000528213615369061,4.5937871332276));
#15584=CARTESIAN_POINT('',(6.72115458874249,0.000109070110168276,4.59505938903171));
#15585=CARTESIAN_POINT('',(4.,-7.27562663373442E-17,4.5941));
#15586=CARTESIAN_POINT('Ctrl Pts',(6.82884541125756,0.000528213615369061,
4.5937871332276));
#15587=CARTESIAN_POINT('Ctrl Pts',(6.82429524715479,0.0572034606387535,
4.59426930340541));
#15588=CARTESIAN_POINT('Ctrl Pts',(6.81974508305202,0.113754426020979,4.58681959872387));
#15589=CARTESIAN_POINT('Ctrl Pts',(6.81519491894924,0.167823213394864,4.57092612439125));
#15590=CARTESIAN_POINT('Ctrl Pts',(6.79928964026163,0.356822799356826,4.51536985589957));
#15591=CARTESIAN_POINT('Ctrl Pts',(6.78338436157403,0.515493156338912,4.35664088088147));
#15592=CARTESIAN_POINT('Ctrl Pts',(6.76747908288642,0.570983871223461,4.16762126762428));
#15593=CARTESIAN_POINT('Ctrl Pts',(6.7515738041988,0.626474586108011,3.97860165436708));
#15594=CARTESIAN_POINT('Ctrl Pts',(6.73566852551118,0.578785658895023,3.75929140287077));
#15595=CARTESIAN_POINT('Ctrl Pts',(6.71976324682357,0.449805704301045,3.61038767491097));
#15596=CARTESIAN_POINT('Ctrl Pts',(6.70385796813595,0.320825749707067,3.46148394695116));
#15597=CARTESIAN_POINT('Ctrl Pts',(6.68795268944834,0.110554767732096,3.38298674252784));
#15598=CARTESIAN_POINT('Ctrl Pts',(6.67204741076073,-0.0844443642884844,
3.4109402193496));
#15599=CARTESIAN_POINT('Ctrl Pts',(6.65614213207312,-0.279443496309066,
3.43889369617135));
#15600=CARTESIAN_POINT('Ctrl Pts',(6.64023685338551,-0.459170778375258,
3.57329785423817));
#15601=CARTESIAN_POINT('Ctrl Pts',(6.6243315746979,-0.541132009270427,3.75243704050979));
#15602=CARTESIAN_POINT('Ctrl Pts',(6.60842629601029,-0.623093240165596,
3.9315762267814));
#15603=CARTESIAN_POINT('Ctrl Pts',(6.59252101732267,-0.60728841988974,4.15545044125781));
#15604=CARTESIAN_POINT('Ctrl Pts',(6.57661573863506,-0.500919754058047,
4.32127168369798));
#15605=CARTESIAN_POINT('Ctrl Pts',(6.56069229617589,-0.394429615589227,
4.48728229340579));
#15606=CARTESIAN_POINT('Ctrl Pts',(6.54476885371673,-0.197168666623305,
4.59510713395368));
#15607=CARTESIAN_POINT('Ctrl Pts',(6.52884541125757,2.61457539729726E-5,
4.59508370962656));
#15608=CARTESIAN_POINT('Ctrl Pts',(6.42115458874249,-0.000630941829811112,
4.59394485456974));
#15609=CARTESIAN_POINT('Ctrl Pts',(6.4252722722299,-0.0517816819022344,
4.59442561076518));
#15610=CARTESIAN_POINT('Ctrl Pts',(6.42938995571731,-0.102828462800867,
4.58836159088269));
#15611=CARTESIAN_POINT('Ctrl Pts',(6.43350763920472,-0.152073274319339,
4.5753220992581));
#15612=CARTESIAN_POINT('Ctrl Pts',(6.44941291789233,-0.342290043897387,
4.52495476314113));
#15613=CARTESIAN_POINT('Ctrl Pts',(6.46531819657995,-0.5056209461254,4.37051151428857));
#15614=CARTESIAN_POINT('Ctrl Pts',(6.48122347526756,-0.56632363157735,4.18304963962536));
#15615=CARTESIAN_POINT('Ctrl Pts',(6.49712875395518,-0.627026317029301,
3.99558776496215));
#15616=CARTESIAN_POINT('Ctrl Pts',(6.51303403264279,-0.58510078570519,3.77510726448829));
#15617=CARTESIAN_POINT('Ctrl Pts',(6.5289393113304,-0.460166914262479,3.62276494217392));
#15618=CARTESIAN_POINT('Ctrl Pts',(6.54484459001801,-0.335233042819767,
3.47042261985956));
#15619=CARTESIAN_POINT('Ctrl Pts',(6.56074986870563,-0.127290831258456,
3.38621847570468));
#15620=CARTESIAN_POINT('Ctrl Pts',(6.57665514739324,0.068373869747762,3.4088573345089));
#15621=CARTESIAN_POINT('Ctrl Pts',(6.59256042608085,0.26403857075398,3.43149619331313));
#15622=CARTESIAN_POINT('Ctrl Pts',(6.60846570476847,0.447425761205104,3.56097805507645));
#15623=CARTESIAN_POINT('Ctrl Pts',(6.62437098345608,0.534230294511761,3.73782813427527));
#15624=CARTESIAN_POINT('Ctrl Pts',(6.64027626214369,0.621034827818418,3.91467821347409));
#15625=CARTESIAN_POINT('Ctrl Pts',(6.65618154083131,0.611256703980608,4.1388965101084));
#15626=CARTESIAN_POINT('Ctrl Pts',(6.67208681951892,0.509439333868548,4.30754322537844));
#15627=CARTESIAN_POINT('Ctrl Pts',(6.68799209820653,0.40762196375649,4.47618994064847));
#15628=CARTESIAN_POINT('Ctrl Pts',(6.70389737689414,0.213765347370184,4.58926507455422));
#15629=CARTESIAN_POINT('Ctrl Pts',(6.71980265558175,0.016851802420978,4.59484308232941));
#15630=CARTESIAN_POINT('Ctrl Pts',(6.72025329996867,0.0112726493937942,
4.59500112406784));
#15631=CARTESIAN_POINT('Ctrl Pts',(6.72070394435558,0.00569104238866241,
4.59507287148453));
#15632=CARTESIAN_POINT('Ctrl Pts',(6.72115458874249,0.000109070110168276,
4.59505938903171));
#15633=CARTESIAN_POINT('Origin',(4.,0.,4.));
#15634=CARTESIAN_POINT('',(7.12884541125757,-0.000233413975479213,4.59320261234329));
#15635=CARTESIAN_POINT('',(7.02115458874249,0.000491936389841303,4.5936290357477));
#15636=CARTESIAN_POINT('',(4.,-7.27562663373442E-17,4.5941));
#15637=CARTESIAN_POINT('Ctrl Pts',(7.12884541125757,-0.000233413975479213,
4.59320261234329));
#15638=CARTESIAN_POINT('Ctrl Pts',(7.11972691928047,0.113624805666132,4.59280158872514));
#15639=CARTESIAN_POINT('Ctrl Pts',(7.11060842730338,0.227688545642871,4.56127879346404));
#15640=CARTESIAN_POINT('Ctrl Pts',(7.10148993532628,0.322592019514134,4.50005536307953));
#15641=CARTESIAN_POINT('Ctrl Pts',(7.08558465663867,0.488131036726243,4.39326405099382));
#15642=CARTESIAN_POINT('Ctrl Pts',(7.06967937795105,0.595374147168556,4.19610732087965));
#15643=CARTESIAN_POINT('Ctrl Pts',(7.05377409926343,0.595079946532544,3.99911121186167));
#15644=CARTESIAN_POINT('Ctrl Pts',(7.03786882057582,0.594785745896532,3.80211510284369));
#15645=CARTESIAN_POINT('Ctrl Pts',(7.02196354188821,0.486954234182196,3.60527961492189));
#15646=CARTESIAN_POINT('Ctrl Pts',(7.0060582632006,0.321096900356496,3.49898325846904));
#15647=CARTESIAN_POINT('Ctrl Pts',(6.99015298451299,0.155239566530797,3.3926869020162));
#15648=CARTESIAN_POINT('Ctrl Pts',(6.97424770582538,-0.0686435894062663,
3.37692967703231));
#15649=CARTESIAN_POINT('Ctrl Pts',(6.95834242713776,-0.247754555527299,
3.45894666907189));
#15650=CARTESIAN_POINT('Ctrl Pts',(6.94243714845015,-0.426865521648332,
3.54096366111146));
#15651=CARTESIAN_POINT('Ctrl Pts',(6.92653186976253,-0.561204297953336,
3.72075487017451));
#15652=CARTESIAN_POINT('Ctrl Pts',(6.91062659107492,-0.589088840804576,
3.91576771430201));
#15653=CARTESIAN_POINT('Ctrl Pts',(6.89472131238731,-0.616973383655816,
4.11078055842951));
#15654=CARTESIAN_POINT('Ctrl Pts',(6.8788160336997,-0.538403693053295,4.32101503762147));
#15655=CARTESIAN_POINT('Ctrl Pts',(6.86291075501209,-0.389454440281117,
4.44994049623482));
#15656=CARTESIAN_POINT('Ctrl Pts',(6.85155564042725,-0.283116420949728,
4.54198310574898));
#15657=CARTESIAN_POINT('Ctrl Pts',(6.8402005258424,-0.140907108175025,4.59258385846765));
#15658=CARTESIAN_POINT('Ctrl Pts',(6.82884541125756,0.000528213615369061,
4.5937871332276));
#15659=CARTESIAN_POINT('Ctrl Pts',(6.72115458874249,0.000109070110168276,
4.59505938903171));
#15660=CARTESIAN_POINT('Ctrl Pts',(6.73660922304319,-0.191322006690816,
4.59459701474307));
#15661=CARTESIAN_POINT('Ctrl Pts',(6.75206385734389,-0.38318268672033,4.49389457135631));
#15662=CARTESIAN_POINT('Ctrl Pts',(6.76751849164459,-0.49122657597837,4.33588597251985));
#15663=CARTESIAN_POINT('Ctrl Pts',(6.78342377033221,-0.60242093591639,4.17326997329048));
#15664=CARTESIAN_POINT('Ctrl Pts',(6.79932904901982,-0.624839182280325,
3.94995709318712));
#15665=CARTESIAN_POINT('Ctrl Pts',(6.81523432770743,-0.548195780923551,
3.76848141254984));
#15666=CARTESIAN_POINT('Ctrl Pts',(6.83113960639504,-0.471552379566775,
3.58700573191256));
#15667=CARTESIAN_POINT('Ctrl Pts',(6.84704488508266,-0.295847330489284,
3.44736725074137));
#15668=CARTESIAN_POINT('Ctrl Pts',(6.86295016377027,-0.101752734572189,
3.41368297698799));
#15669=CARTESIAN_POINT('Ctrl Pts',(6.87885544245788,0.0923418613449005,
3.37999870323461));
#15670=CARTESIAN_POINT('Ctrl Pts',(6.8947607211455,0.304826004101594,3.45226863689903));
#15671=CARTESIAN_POINT('Ctrl Pts',(6.91066599983311,0.438133727661537,3.59730899203965));
#15672=CARTESIAN_POINT('Ctrl Pts',(6.92657127852072,0.571441451221483,3.74234934718029));
#15673=CARTESIAN_POINT('Ctrl Pts',(6.94247655720833,0.625572755584675,3.96016012379713));
#15674=CARTESIAN_POINT('Ctrl Pts',(6.95838183589594,0.57567402069499,4.15073208753033));
#15675=CARTESIAN_POINT('Ctrl Pts',(6.97428711458356,0.525775285805305,4.34130405126353));
#15676=CARTESIAN_POINT('Ctrl Pts',(6.99019239327118,0.371846511662747,4.5046372021131));
#15677=CARTESIAN_POINT('Ctrl Pts',(7.00609767195879,0.184564651688987,4.56573572985967));
#15678=CARTESIAN_POINT('Ctrl Pts',(7.01111664422002,0.125467135782336,4.58501560681028));
#15679=CARTESIAN_POINT('Ctrl Pts',(7.01613561648126,0.0630485115161635,
4.59411554829291));
#15680=CARTESIAN_POINT('Ctrl Pts',(7.02115458874249,0.000491936389841303,
4.5936290357477));
#15681=CARTESIAN_POINT('Origin',(4.,0.,4.));
#15682=CARTESIAN_POINT('',(7.42884541125756,-0.000438237927964824,4.59464495791636));
#15683=CARTESIAN_POINT('',(7.32115458874249,-0.000317338366111653,4.59328419319629));
#15684=CARTESIAN_POINT('',(4.,-7.27562663373442E-17,4.5941));
#15685=CARTESIAN_POINT('Ctrl Pts',(7.42884541125756,-0.000438237927964824,
4.59464495791636));
#15686=CARTESIAN_POINT('Ctrl Pts',(7.41515859140615,0.169409178821721,4.5932420274804));
#15687=CARTESIAN_POINT('Ctrl Pts',(7.40147177155473,0.340360224580004,4.51673272682389));
#15688=CARTESIAN_POINT('Ctrl Pts',(7.38778495170331,0.450965110664874,4.38826722161738));
#15689=CARTESIAN_POINT('Ctrl Pts',(7.37187967301569,0.579497637321094,4.23897909740477));
#15690=CARTESIAN_POINT('Ctrl Pts',(7.35597439432808,0.626535888751401,4.01952688559808));
#15691=CARTESIAN_POINT('Ctrl Pts',(7.34006911564046,0.570481892017836,3.83067375781486));
#15692=CARTESIAN_POINT('Ctrl Pts',(7.32416383695285,0.51442789528427,3.64182063003164));
#15693=CARTESIAN_POINT('Ctrl Pts',(7.30825855826524,0.355281650386831,3.48356658627189));
#15694=CARTESIAN_POINT('Ctrl Pts',(7.29235327957763,0.166116376105148,3.42857518785077));
#15695=CARTESIAN_POINT('Ctrl Pts',(7.27644800089002,-0.023048898176535,
3.37358378942964));
#15696=CARTESIAN_POINT('Ctrl Pts',(7.2605427222024,-0.242233201842457,3.42185503634715));
#15697=CARTESIAN_POINT('Ctrl Pts',(7.24463744351479,-0.390796368104757,
3.5512248149675));
#15698=CARTESIAN_POINT('Ctrl Pts',(7.22873216482718,-0.539359534367058,
3.68059459358785));
#15699=CARTESIAN_POINT('Ctrl Pts',(7.21282688613957,-0.617301563225728,
3.89106290391106));
#15700=CARTESIAN_POINT('Ctrl Pts',(7.19692160745195,-0.588834786584626,
4.08599160058025));
#15701=CARTESIAN_POINT('Ctrl Pts',(7.18101632876434,-0.560368009943526,
4.28092029724944));
#15702=CARTESIAN_POINT('Ctrl Pts',(7.16511105007672,-0.425492427802657,
4.46030938026461));
#15703=CARTESIAN_POINT('Ctrl Pts',(7.14920577138911,-0.24613717474127,4.54179097474357));
#15704=CARTESIAN_POINT('Ctrl Pts',(7.1424189846786,-0.169606239833077,4.57655919310821));
#15705=CARTESIAN_POINT('Ctrl Pts',(7.13563219796808,-0.0849767524450092,
4.59350108952231));
#15706=CARTESIAN_POINT('Ctrl Pts',(7.12884541125757,-0.000233413975479213,
4.59320261234329));
#15707=CARTESIAN_POINT('Ctrl Pts',(7.02115458874249,0.000491936389841303,
4.5936290357477));
#15708=CARTESIAN_POINT('Ctrl Pts',(7.03204089516887,-0.135195214358064,
4.59257377495492));
#15709=CARTESIAN_POINT('Ctrl Pts',(7.04292720159524,-0.271531381894462,
4.54641716720817));
#15710=CARTESIAN_POINT('Ctrl Pts',(7.05381350802162,-0.376033620593693,
4.46121547122365));
#15711=CARTESIAN_POINT('Ctrl Pts',(7.06971878670923,-0.528715087097646,
4.33673278019746));
#15712=CARTESIAN_POINT('Ctrl Pts',(7.08562406539685,-0.613443074300594,
4.1289034935015));
#15713=CARTESIAN_POINT('Ctrl Pts',(7.10152934408446,-0.591314251018945,
3.93315398851514));
#15714=CARTESIAN_POINT('Ctrl Pts',(7.11743462277207,-0.569185427737295,
3.73740448352876));
#15715=CARTESIAN_POINT('Ctrl Pts',(7.13333990145968,-0.440199793971044,
3.55373476025198));
#15716=CARTESIAN_POINT('Ctrl Pts',(7.14924518014729,-0.263582002606135,
3.46647820559892));
#15717=CARTESIAN_POINT('Ctrl Pts',(7.16515045883491,-0.0869642112412332,
3.37922165094586));
#15718=CARTESIAN_POINT('Ctrl Pts',(7.18105573752253,0.137285737722324,3.38837826491652));
#15719=CARTESIAN_POINT('Ctrl Pts',(7.19696101621014,0.306201705590428,3.48974370695041));
#15720=CARTESIAN_POINT('Ctrl Pts',(7.21286629489775,0.47511767345854,3.59110914898431));
#15721=CARTESIAN_POINT('Ctrl Pts',(7.22877157358536,0.588699660231196,3.78468341908144));
#15722=CARTESIAN_POINT('Ctrl Pts',(7.24467685227297,0.594795648982816,3.98158540759));
#15723=CARTESIAN_POINT('Ctrl Pts',(7.26058213096058,0.600891637734436,4.17848739609855));
#15724=CARTESIAN_POINT('Ctrl Pts',(7.2764874096482,0.499501628465021,4.37871710301853));
#15725=CARTESIAN_POINT('Ctrl Pts',(7.29239268833581,0.337179610128186,4.49033751492072));
#15726=CARTESIAN_POINT('Ctrl Pts',(7.30197998847137,0.239335998647354,4.5576194790522));
#15727=CARTESIAN_POINT('Ctrl Pts',(7.31156728860693,0.119353510611835,4.59270637405629));
#15728=CARTESIAN_POINT('Ctrl Pts',(7.32115458874249,-0.000317338366111653,
4.59328419319629));
#15729=CARTESIAN_POINT('Origin',(4.,0.,4.));
#15730=CARTESIAN_POINT('',(7.72884541125757,0.000455182276646732,4.59460030787683));
#15731=CARTESIAN_POINT('',(7.62115458874249,-0.000367422317862595,4.59479267874092));
#15732=CARTESIAN_POINT('',(4.,-7.27562663373442E-17,4.5941));
#15733=CARTESIAN_POINT('Ctrl Pts',(7.72884541125757,0.000455182276646732,
4.59460030787683));
#15734=CARTESIAN_POINT('Ctrl Pts',(7.72649554221944,0.0296217258780686,
4.59484761241511));
#15735=CARTESIAN_POINT('Ctrl Pts',(7.72414567318131,0.0587549042441869,
4.59288776399295));
#15736=CARTESIAN_POINT('Ctrl Pts',(7.72179580414318,0.0875427725731367,
4.58860617484604));
#15737=CARTESIAN_POINT('Ctrl Pts',(7.70589052545556,0.282395788279217,4.55962589232715));
#15738=CARTESIAN_POINT('Ctrl Pts',(7.68998524676794,0.461428877889185,4.42427810603975));
#15739=CARTESIAN_POINT('Ctrl Pts',(7.67407996808033,0.542437620895056,4.24470879335187));
#15740=CARTESIAN_POINT('Ctrl Pts',(7.65817468939272,0.623446363900926,4.065139480664));
#15741=CARTESIAN_POINT('Ctrl Pts',(7.64226941070511,0.606430760302702,3.84134864157567));
#15742=CARTESIAN_POINT('Ctrl Pts',(7.6263641320175,0.499203655448083,3.67609156159133));
#15743=CARTESIAN_POINT('Ctrl Pts',(7.61045885332988,0.391976550593464,3.51083448160699));
#15744=CARTESIAN_POINT('Ctrl Pts',(7.59455357464227,0.19453794448245,3.40411116072664));
#15745=CARTESIAN_POINT('Ctrl Pts',(7.57864829595466,-0.00245670798462758,
3.40492443279829));
#15746=CARTESIAN_POINT('Ctrl Pts',(7.56274301726704,-0.199451360451705,
3.40573770486994));
#15747=CARTESIAN_POINT('Ctrl Pts',(7.54683773857943,-0.396002059274846,
3.5140875698936));
#15748=CARTESIAN_POINT('Ctrl Pts',(7.53093245989182,-0.50186103876401,3.68022435377194));
#15749=CARTESIAN_POINT('Ctrl Pts',(7.51502718120421,-0.607720018253171,
3.84636113765028));
#15750=CARTESIAN_POINT('Ctrl Pts',(7.4991219025166,-0.622887278408357,4.07028484038331));
#15751=CARTESIAN_POINT('Ctrl Pts',(7.48321662382898,-0.540398655351294,
4.24917917107494));
#15752=CARTESIAN_POINT('Ctrl Pts',(7.46731134514137,-0.45791003229423,4.42807350176658));
#15753=CARTESIAN_POINT('Ctrl Pts',(7.45140606645375,-0.277765526024924,
4.56193846041682));
#15754=CARTESIAN_POINT('Ctrl Pts',(7.43550078776614,-0.0826798719492015,
4.58930892143267));
#15755=CARTESIAN_POINT('Ctrl Pts',(7.43328232892995,-0.0554694406452989,
4.59312653709876));
#15756=CARTESIAN_POINT('Ctrl Pts',(7.43106387009376,-0.0279683367079049,
4.5948723550368));
#15757=CARTESIAN_POINT('Ctrl Pts',(7.42884541125756,-0.000438237927964824,
4.59464495791636));
#15758=CARTESIAN_POINT('Ctrl Pts',(7.32115458874249,-0.000317338366111653,
4.59328419319629));
#15759=CARTESIAN_POINT('Ctrl Pts',(7.32747256729455,-0.0791797758050172,
4.59366497286126));
#15760=CARTESIAN_POINT('Ctrl Pts',(7.3337905458466,-0.157906876560309,4.57905936436794));
#15761=CARTESIAN_POINT('Ctrl Pts',(7.34010852439865,-0.230073660466993,
4.54880513582638));
#15762=CARTESIAN_POINT('Ctrl Pts',(7.35601380308626,-0.411750885321067,
4.47264122794544));
#15763=CARTESIAN_POINT('Ctrl Pts',(7.37191908177388,-0.551851307624962,
4.29730229529918));
#15764=CARTESIAN_POINT('Ctrl Pts',(7.38782436046149,-0.586046744500155,
4.10329655692985));
#15765=CARTESIAN_POINT('Ctrl Pts',(7.4037296391491,-0.620242181375348,3.90929081856053));
#15766=CARTESIAN_POINT('Ctrl Pts',(7.41963491783671,-0.548532632821828,
3.69661827446815));
#15767=CARTESIAN_POINT('Ctrl Pts',(7.43554019652432,-0.403844087697925,
3.56292915991696));
#15768=CARTESIAN_POINT('Ctrl Pts',(7.45144547521194,-0.259155542574025,
3.42924004536577));
#15769=CARTESIAN_POINT('Ctrl Pts',(7.46735075389955,-0.0414880008797467,
3.37453436035576));
#15770=CARTESIAN_POINT('Ctrl Pts',(7.48325603258717,0.149214809903968,3.42393064079835));
#15771=CARTESIAN_POINT('Ctrl Pts',(7.49916131127478,0.339917620687686,3.47332692124094));
#15772=CARTESIAN_POINT('Ctrl Pts',(7.51506658996239,0.50365570056084,3.62682516713614));
#15773=CARTESIAN_POINT('Ctrl Pts',(7.53097186865001,0.56524745100941,3.81394547807041));
#15774=CARTESIAN_POINT('Ctrl Pts',(7.54687714733762,0.626839201457978,4.00106578900469));
#15775=CARTESIAN_POINT('Ctrl Pts',(7.56278242602523,0.58628462248197,4.22180816497804));
#15776=CARTESIAN_POINT('Ctrl Pts',(7.57868770471284,0.462204660718925,4.3748170457164));
#15777=CARTESIAN_POINT('Ctrl Pts',(7.59284333272272,0.351774041004839,4.51099427596058));
#15778=CARTESIAN_POINT('Ctrl Pts',(7.60699896073261,0.175183620117616,4.59352033541115));
#15779=CARTESIAN_POINT('Ctrl Pts',(7.62115458874249,-0.000367422317862596,
4.59479267874092));
#15780=CARTESIAN_POINT('Origin',(4.,0.,4.));
#15781=CARTESIAN_POINT('',(8.02884541125756,0.000208508845897126,4.59318438507865));
#15782=CARTESIAN_POINT('',(7.92115458874249,0.000504499356536197,4.59443266285439));
#15783=CARTESIAN_POINT('',(4.,-7.27562663373442E-17,4.5941));
#15784=CARTESIAN_POINT('Ctrl Pts',(8.02884541125756,0.000208508845897126,
4.59318438507865));
#15785=CARTESIAN_POINT('Ctrl Pts',(8.02192721434511,0.0865993248636432,
4.5934556945658));
#15786=CARTESIAN_POINT('Ctrl Pts',(8.01500901743265,0.17288466952141,4.57582457789876));
#15787=CARTESIAN_POINT('Ctrl Pts',(8.0080908205202,0.250602156771344,4.53974023855861));
#15788=CARTESIAN_POINT('Ctrl Pts',(7.99218554183259,0.42927852421987,4.4567805482338));
#15789=CARTESIAN_POINT('Ctrl Pts',(7.97628026314498,0.562668370741438,4.27628395749428));
#15790=CARTESIAN_POINT('Ctrl Pts',(7.96037498445736,0.589524722071826,4.08112686462655));
#15791=CARTESIAN_POINT('Ctrl Pts',(7.94446970576975,0.616381073402214,3.88596977175883));
#15792=CARTESIAN_POINT('Ctrl Pts',(7.92856442708213,0.536703929541425,3.67615217676291));
#15793=CARTESIAN_POINT('Ctrl Pts',(7.91265914839452,0.387077664089382,3.54801344261061));
#15794=CARTESIAN_POINT('Ctrl Pts',(7.89675386970691,0.237451398637336,3.41987470845831));
#15795=CARTESIAN_POINT('Ctrl Pts',(7.88084859101929,0.0178760115940344,
3.37341483514963));
#15796=CARTESIAN_POINT('Ctrl Pts',(7.86494331233168,-0.170828768780714,
3.42996623095257));
#15797=CARTESIAN_POINT('Ctrl Pts',(7.84903803364407,-0.359533549155462,
3.48651762675552));
#15798=CARTESIAN_POINT('Ctrl Pts',(7.83313275495647,-0.517367722861657,
3.64608029167009));
#15799=CARTESIAN_POINT('Ctrl Pts',(7.81722747626885,-0.571860514742998,
3.83538980050754));
#15800=CARTESIAN_POINT('Ctrl Pts',(7.80132219758124,-0.626353306624339,
4.02469930934499));
#15801=CARTESIAN_POINT('Ctrl Pts',(7.78541691889362,-0.577504716680827,
4.24375566210532));
#15802=CARTESIAN_POINT('Ctrl Pts',(7.769511640206,-0.447743950807975,4.3919774491103));
#15803=CARTESIAN_POINT('Ctrl Pts',(7.75595623055652,-0.337154229471824,
4.51830073342946));
#15804=CARTESIAN_POINT('Ctrl Pts',(7.74240082090705,-0.16779438404434,4.593173711641));
#15805=CARTESIAN_POINT('Ctrl Pts',(7.72884541125757,0.000455182276646732,
4.59460030787683));
#15806=CARTESIAN_POINT('Ctrl Pts',(7.62115458874249,-0.000367422317862596,
4.59479267874092));
#15807=CARTESIAN_POINT('Ctrl Pts',(7.62290423942022,-0.022065717876263,
4.59494994172972));
#15808=CARTESIAN_POINT('Ctrl Pts',(7.62465389009795,-0.043748134618359,
4.59386587358433));
#15809=CARTESIAN_POINT('Ctrl Pts',(7.62640354077568,-0.0652877816099521,
4.59148835294282));
#15810=CARTESIAN_POINT('Ctrl Pts',(7.64230881946329,-0.261094917625702,
4.56987539392751));
#15811=CARTESIAN_POINT('Ctrl Pts',(7.6582140981509,-0.445103845107109,4.44137409039354));
#15812=CARTESIAN_POINT('Ctrl Pts',(7.67411937683852,-0.532825449416136,
4.2649868044631));
#15813=CARTESIAN_POINT('Ctrl Pts',(7.69002465552613,-0.620547053725161,
4.08859951853267));
#15814=CARTESIAN_POINT('Ctrl Pts',(7.70592993421374,-0.611981334861803,
3.86432625020577));
#15815=CARTESIAN_POINT('Ctrl Pts',(7.72183521290136,-0.511061308497056,
3.69514379608856));
#15816=CARTESIAN_POINT('Ctrl Pts',(7.73774049158897,-0.410141282132307,
3.52596134197134));
#15817=CARTESIAN_POINT('Ctrl Pts',(7.75364577027658,-0.216866948266163,
3.4118697020638));
#15818=CARTESIAN_POINT('Ctrl Pts',(7.76955104896419,-0.0199817042712483,
3.40525493058698));
#15819=CARTESIAN_POINT('Ctrl Pts',(7.78545632765181,0.176903539723664,3.39864015911017));
#15820=CARTESIAN_POINT('Ctrl Pts',(7.80136160633942,0.377399693847348,3.49950225606407));
#15821=CARTESIAN_POINT('Ctrl Pts',(7.81726688502703,0.489447406431712,3.66152961365368));
#15822=CARTESIAN_POINT('Ctrl Pts',(7.83317216371464,0.601495119016078,3.82355697124329));
#15823=CARTESIAN_POINT('Ctrl Pts',(7.84907744240226,0.625094390061116,4.04674958946861));
#15824=CARTESIAN_POINT('Ctrl Pts',(7.86498272108987,0.549409432699027,4.22862686054007));
#15825=CARTESIAN_POINT('Ctrl Pts',(7.88088799977748,0.473724475336938,4.41050413161152));
#15826=CARTESIAN_POINT('Ctrl Pts',(7.89679327846509,0.298755289567731,4.55106605552911));
#15827=CARTESIAN_POINT('Ctrl Pts',(7.91269855715271,0.104840323164387,4.58577254351526));
#15828=CARTESIAN_POINT('Ctrl Pts',(7.9155172343493,0.0704753991278659,4.59192310448195));
#15829=CARTESIAN_POINT('Ctrl Pts',(7.91833591154589,0.0355154700816755,
4.59474920414003));
#15830=CARTESIAN_POINT('Ctrl Pts',(7.92115458874249,0.000504499356536197,
4.59443266285439));
#15831=CARTESIAN_POINT('Origin',(4.,0.,4.));
#15832=CARTESIAN_POINT('',(8.32884541125757,-0.000534402448739424,4.5938336238991));
#15833=CARTESIAN_POINT('',(8.2211545887425,0.000116005647334215,4.59313666129657));
#15834=CARTESIAN_POINT('',(4.,-7.27562663373442E-17,4.5941));
#15835=CARTESIAN_POINT('Ctrl Pts',(8.32884541125757,-0.000534402448739424,
4.5938336238991));
#15836=CARTESIAN_POINT('Ctrl Pts',(8.31735888647079,0.142509087977489,4.59259298046846));
#15837=CARTESIAN_POINT('Ctrl Pts',(8.30587236168401,0.286359812054371,4.54070236535691));
#15838=CARTESIAN_POINT('Ctrl Pts',(8.29438583689723,0.393155811111917,4.44670960845581));
#15839=CARTESIAN_POINT('Ctrl Pts',(8.27848055820962,0.541035187969857,4.31655875596735));
#15840=CARTESIAN_POINT('Ctrl Pts',(8.262575279522,0.617867056310918,4.10568264439756));
#15841=CARTESIAN_POINT('Ctrl Pts',(8.24667000083439,0.588373472681163,3.91090666274675));
#15842=CARTESIAN_POINT('Ctrl Pts',(8.23076472214677,0.558879889051408,3.71613068109593));
#15843=CARTESIAN_POINT('Ctrl Pts',(8.21485944345917,0.423060853450833,3.53745482936408));
#15844=CARTESIAN_POINT('Ctrl Pts',(8.19895416477155,0.243278720997716,3.45691949951456));
#15845=CARTESIAN_POINT('Ctrl Pts',(8.18304888608394,0.0634965885445972,
3.37638416966503));
#15846=CARTESIAN_POINT('Ctrl Pts',(8.16714360739632,-0.160248640761069,
3.39398936169784));
#15847=CARTESIAN_POINT('Ctrl Pts',(8.15123832870871,-0.325222623502191,
3.50165151624576));
#15848=CARTESIAN_POINT('Ctrl Pts',(8.1353330500211,-0.490196606243315,3.60931367079368));
#15849=CARTESIAN_POINT('Ctrl Pts',(8.11942777133349,-0.59639934241989,3.80703278785672));
#15850=CARTESIAN_POINT('Ctrl Pts',(8.10352249264588,-0.595067028646789,
4.00402461368555));
#15851=CARTESIAN_POINT('Ctrl Pts',(8.08761721395827,-0.593734714873688,
4.20101643951437));
#15852=CARTESIAN_POINT('Ctrl Pts',(8.07171193527065,-0.484867351150922,
4.39728097410898));
#15853=CARTESIAN_POINT('Ctrl Pts',(8.05580665658303,-0.3184522251018,4.50270184645125));
#15854=CARTESIAN_POINT('Ctrl Pts',(8.04681957480788,-0.224421408301879,
4.56226861162124));
#15855=CARTESIAN_POINT('Ctrl Pts',(8.03783249303272,-0.112017456676448,
4.59283194056482));
#15856=CARTESIAN_POINT('Ctrl Pts',(8.02884541125756,0.000208508845897126,
4.59318438507865));
#15857=CARTESIAN_POINT('Ctrl Pts',(7.92115458874249,0.000504499356536197,
4.59443266285439));
#15858=CARTESIAN_POINT('Ctrl Pts',(7.93424119023351,-0.162045019349314,
4.59296301969496));
#15859=CARTESIAN_POINT('Ctrl Pts',(7.94732779172453,-0.325694779556815,
4.52375140444135));
#15860=CARTESIAN_POINT('Ctrl Pts',(7.96041439321555,-0.436005268305889,
4.40499428651169));
#15861=CARTESIAN_POINT('Ctrl Pts',(7.97631967190316,-0.570075146335334,
4.26065848946726));
#15862=CARTESIAN_POINT('Ctrl Pts',(7.99222495059077,-0.625354155356748,
4.04313584332371));
#15863=CARTESIAN_POINT('Ctrl Pts',(8.00813022927838,-0.576460513088508,
3.85230354456612));
#15864=CARTESIAN_POINT('Ctrl Pts',(8.024035507966,-0.527566870820267,3.66147124580852));
#15865=CARTESIAN_POINT('Ctrl Pts',(8.03994078665361,-0.374500577262366,
3.49732929443689));
#15866=CARTESIAN_POINT('Ctrl Pts',(8.05584606534123,-0.187543198716277,
3.43524473024767));
#15867=CARTESIAN_POINT('Ctrl Pts',(8.07175134402884,-0.000585820170193818,
3.37316016605846));
#15868=CARTESIAN_POINT('Ctrl Pts',(8.08765662271645,0.220262643364076,3.41313298905166));
#15869=CARTESIAN_POINT('Ctrl Pts',(8.10356190140406,0.37359792075985,3.53680937001953));
#15870=CARTESIAN_POINT('Ctrl Pts',(8.11946718009167,0.526933198155627,3.66048575098741));
#15871=CARTESIAN_POINT('Ctrl Pts',(8.13537245877928,0.612755289412907,3.86786568992997));
#15872=CARTESIAN_POINT('Ctrl Pts',(8.1512777374669,0.591658321059451,4.06372909240644));
#15873=CARTESIAN_POINT('Ctrl Pts',(8.16718301615451,0.570561352705995,4.2595924948829));
#15874=CARTESIAN_POINT('Ctrl Pts',(8.18308829484212,0.44254532474181,4.44393936089328));
#15875=CARTESIAN_POINT('Ctrl Pts',(8.19899357352974,0.266389781296621,4.53212540863836));
#15876=CARTESIAN_POINT('Ctrl Pts',(8.20638057860065,0.184576572093718,4.57308230066594));
#15877=CARTESIAN_POINT('Ctrl Pts',(8.21376758367158,0.0923795717789203,
4.59329710918813));
#15878=CARTESIAN_POINT('Ctrl Pts',(8.2211545887425,0.000116005647334215,
4.59313666129657));
#15879=CARTESIAN_POINT('Origin',(4.,0.,4.));
#15880=CARTESIAN_POINT('',(8.62884541125757,3.48566139269993E-5,4.59507810043999));
#15881=CARTESIAN_POINT('',(8.5211545887425,-0.000547905086566465,4.594005652201));
#15882=CARTESIAN_POINT('',(4.,-7.27562663373442E-17,4.5941));
#15883=CARTESIAN_POINT('Ctrl Pts',(8.62884541125757,3.48566139269993E-5,
4.59507810043999));
#15884=CARTESIAN_POINT('Ctrl Pts',(8.62869583728408,0.00188744051982823,
4.59507966949126));
#15885=CARTESIAN_POINT('Ctrl Pts',(8.62854626331059,0.00374001065808006,
4.59507176912216));
#15886=CARTESIAN_POINT('Ctrl Pts',(8.6283966893371,0.00559249142073073,
4.59505435897699));
#15887=CARTESIAN_POINT('Ctrl Pts',(8.61249141064948,0.202580123064263,4.59320301275402));
#15888=CARTESIAN_POINT('Ctrl Pts',(8.59658613196187,0.398557131004382,4.48381890612783));
#15889=CARTESIAN_POINT('Ctrl Pts',(8.58068085327426,0.503539164298441,4.31712659320126));
#15890=CARTESIAN_POINT('Ctrl Pts',(8.56477557458664,0.608521197592498,4.15043428027469));
#15891=CARTESIAN_POINT('Ctrl Pts',(8.54887029589904,0.622508256240502,3.92643376104774));
#15892=CARTESIAN_POINT('Ctrl Pts',(8.53296501721142,0.539078074654942,3.74797659726896));
#15893=CARTESIAN_POINT('Ctrl Pts',(8.51705973852381,0.455647893069379,3.56951943349019));
#15894=CARTESIAN_POINT('Ctrl Pts',(8.50115445983619,0.274800471250253,3.43660562515959));
#15895=CARTESIAN_POINT('Ctrl Pts',(8.48524918114857,0.0795732942734406,
3.41026356994308));
#15896=CARTESIAN_POINT('Ctrl Pts',(8.46934390246096,-0.115653882703369,
3.38392151472657));
#15897=CARTESIAN_POINT('Ctrl Pts',(8.45343862377335,-0.32526081483786,3.46415121262414));
#15898=CARTESIAN_POINT('Ctrl Pts',(8.43753334508574,-0.453004866631874,
3.61411458059983));
#15899=CARTESIAN_POINT('Ctrl Pts',(8.42162806639813,-0.580748918425883,
3.76407794857552));
#15900=CARTESIAN_POINT('Ctrl Pts',(8.40572278771052,-0.626630089879422,
3.98377498662932));
#15901=CARTESIAN_POINT('Ctrl Pts',(8.3898175090229,-0.569581688133314,4.17233010950212));
#15902=CARTESIAN_POINT('Ctrl Pts',(8.37391223033529,-0.512533286387202,
4.36088523237493));
#15903=CARTESIAN_POINT('Ctrl Pts',(8.35800695164768,-0.352555311441432,
4.51829844006673));
#15904=CARTESIAN_POINT('Ctrl Pts',(8.34210167296007,-0.163102881281137,
4.57229224720906));
#15905=CARTESIAN_POINT('Ctrl Pts',(8.33768291905923,-0.110469810133188,
4.58729263485501));
#15906=CARTESIAN_POINT('Ctrl Pts',(8.3332641651584,-0.0555618361628184,
4.59431088730997));
#15907=CARTESIAN_POINT('Ctrl Pts',(8.32884541125757,-0.000534402448739424,
4.5938336238991));
#15908=CARTESIAN_POINT('Ctrl Pts',(8.2211545887425,0.000116005647334215,
4.59313666129657));
#15909=CARTESIAN_POINT('Ctrl Pts',(8.22967286235919,-0.106277085140544,
4.59295164192424));
#15910=CARTESIAN_POINT('Ctrl Pts',(8.23819113597589,-0.212758691085218,
4.56567285125378));
#15911=CARTESIAN_POINT('Ctrl Pts',(8.24670940959258,-0.303508593564514,
4.51186277431583));
#15912=CARTESIAN_POINT('Ctrl Pts',(8.26261468828019,-0.472956366054245,
4.41138886276846));
#15913=CARTESIAN_POINT('Ctrl Pts',(8.2785199669678,-0.587556852107514,4.21841581019395));
#15914=CARTESIAN_POINT('Ctrl Pts',(8.29442524565541,-0.594690356875377,
4.02154867831793));
#15915=CARTESIAN_POINT('Ctrl Pts',(8.31033052434302,-0.60182386164324,3.82468154644191));
#15916=CARTESIAN_POINT('Ctrl Pts',(8.32623580303064,-0.501490385125681,
3.62392033526436));
#15917=CARTESIAN_POINT('Ctrl Pts',(8.34214108171825,-0.339758814980244,
3.51144609945163));
#15918=CARTESIAN_POINT('Ctrl Pts',(8.35804636040587,-0.178027244834812,
3.3989718636389));
#15919=CARTESIAN_POINT('Ctrl Pts',(8.37395163909348,0.0451024189384938,
3.37478460319097));
#15920=CARTESIAN_POINT('Ctrl Pts',(8.38985691778109,0.227178474572579,3.44999008482693));
#15921=CARTESIAN_POINT('Ctrl Pts',(8.4057621964687,0.40925453020667,3.5251955664629));
#15922=CARTESIAN_POINT('Ctrl Pts',(8.42166747515631,0.550276977701535,3.69979379018275));
#15923=CARTESIAN_POINT('Ctrl Pts',(8.43757275384392,0.585494275335268,3.89361663829603));
#15924=CARTESIAN_POINT('Ctrl Pts',(8.45347803253154,0.620711572969,4.0874394864093));
#15925=CARTESIAN_POINT('Ctrl Pts',(8.46938331121915,0.550123720741606,4.30048695891599));
#15926=CARTESIAN_POINT('Ctrl Pts',(8.48528858990677,0.406141674070155,4.4349366697363));
#15927=CARTESIAN_POINT('Ctrl Pts',(8.49724392285201,0.297916389879728,4.53599689564107));
#15928=CARTESIAN_POINT('Ctrl Pts',(8.50919925579725,0.148224117540273,4.59265016978245));
#15929=CARTESIAN_POINT('Ctrl Pts',(8.5211545887425,-0.000547905086566465,
4.594005652201));
#15930=CARTESIAN_POINT('Origin',(4.,0.,4.));
#15931=CARTESIAN_POINT('',(8.92884541125757,0.000516595407308196,4.59372894893997));
#15932=CARTESIAN_POINT('',(8.82115458874249,0.000142235148737217,4.59503945166131));
#15933=CARTESIAN_POINT('',(4.,-7.27562663373442E-17,4.5941));
#15934=CARTESIAN_POINT('Ctrl Pts',(8.92884541125757,0.000516595407308196,
4.59372894893997));
#15935=CARTESIAN_POINT('Ctrl Pts',(8.92412750940976,0.0592956068199462,
4.59421507565108));
#15936=CARTESIAN_POINT('Ctrl Pts',(8.91940960756194,0.117944888069788,4.58619493689145));
#15937=CARTESIAN_POINT('Ctrl Pts',(8.91469170571413,0.17383025386194,4.56912565303288));
#15938=CARTESIAN_POINT('Ctrl Pts',(8.89878642702651,0.362234410233906,4.51158064138869));
#15939=CARTESIAN_POINT('Ctrl Pts',(8.8828811483389,0.519225559109383,4.35118846702123));
#15940=CARTESIAN_POINT('Ctrl Pts',(8.86697586965128,0.572720006672535,4.16159443076672));
#15941=CARTESIAN_POINT('Ctrl Pts',(8.85107059096367,0.626214454235688,3.97200039451221));
#15942=CARTESIAN_POINT('Ctrl Pts',(8.83516531227606,0.576212200486512,3.75320449637065));
#15943=CARTESIAN_POINT('Ctrl Pts',(8.81926003358845,0.445672164925724,3.60566855627755));
#15944=CARTESIAN_POINT('Ctrl Pts',(8.80335475490084,0.315132129364936,3.45813261618446));
#15945=CARTESIAN_POINT('Ctrl Pts',(8.78744947621322,0.104054311992536,3.38185663413984));
#15946=CARTESIAN_POINT('Ctrl Pts',(8.77154419752561,-0.0906432834200916,
3.41186331412789));
#15947=CARTESIAN_POINT('Ctrl Pts',(8.755638918838,-0.285340878832719,3.44186999411594));
#15948=CARTESIAN_POINT('Ctrl Pts',(8.73973364015038,-0.463658252285575,
3.57815933613666));
#15949=CARTESIAN_POINT('Ctrl Pts',(8.72382836146277,-0.543719609875046,
3.75815304026071));
#15950=CARTESIAN_POINT('Ctrl Pts',(8.70792308277515,-0.623780967464517,
3.93814674438476));
#15951=CARTESIAN_POINT('Ctrl Pts',(8.69201780408754,-0.605586309190603,
4.16184481061213));
#15952=CARTESIAN_POINT('Ctrl Pts',(8.67611252539993,-0.497489852380174,
4.32653455081593));
#15953=CARTESIAN_POINT('Ctrl Pts',(8.66035682068581,-0.390409939629295,
4.48967554111606));
#15954=CARTESIAN_POINT('Ctrl Pts',(8.64460111597169,-0.195111159088962,
4.59491282095998));
#15955=CARTESIAN_POINT('Ctrl Pts',(8.62884541125757,3.48566139269993E-5,
4.59507810043999));
#15956=CARTESIAN_POINT('Ctrl Pts',(8.5211545887425,-0.000547905086566465,
4.594005652201));
#15957=CARTESIAN_POINT('Ctrl Pts',(8.52510453448487,-0.0497009834700827,
4.59445349267793));
#15958=CARTESIAN_POINT('Ctrl Pts',(8.52905448022724,-0.0987536084630192,
4.58886509038946));
#15959=CARTESIAN_POINT('Ctrl Pts',(8.53300442596961,-0.146177075786514,
4.57684766499685));
#15960=CARTESIAN_POINT('Ctrl Pts',(8.54890970465722,-0.337137537856201,
4.52845700030318));
#15961=CARTESIAN_POINT('Ctrl Pts',(8.56481498334483,-0.501682220880061,
4.37582372178193));
#15962=CARTESIAN_POINT('Ctrl Pts',(8.58072026203244,-0.564259167724997,
4.18903057354857));
#15963=CARTESIAN_POINT('Ctrl Pts',(8.59662554072005,-0.626836114569933,
4.00223742531521));
#15964=CARTESIAN_POINT('Ctrl Pts',(8.61253081940767,-0.587445325235947,
3.78128440736974));
#15965=CARTESIAN_POINT('Ctrl Pts',(8.62843609809528,-0.464173383698336,
3.62762379780141));
#15966=CARTESIAN_POINT('Ctrl Pts',(8.6443413767829,-0.340901442160722,3.47396318823307));
#15967=CARTESIAN_POINT('Ctrl Pts',(8.66024665547051,-0.133748348419481,
3.38759498704188));
#15968=CARTESIAN_POINT('Ctrl Pts',(8.67615193415812,0.0621699608040676,
3.40817581827756));
#15969=CARTESIAN_POINT('Ctrl Pts',(8.69205721284573,0.25808827002761,3.42875664951325));
#15970=CARTESIAN_POINT('Ctrl Pts',(8.70796249153334,0.44277179473346,3.55628651317581));
#15971=CARTESIAN_POINT('Ctrl Pts',(8.72386777022095,0.531421673692279,3.73220909121499));
#15972=CARTESIAN_POINT('Ctrl Pts',(8.73977304890857,0.620071552651101,3.90813166925417));
#15973=CARTESIAN_POINT('Ctrl Pts',(8.75567832759618,0.612687785862888,4.13244696166997));
#15974=CARTESIAN_POINT('Ctrl Pts',(8.7715836062838,0.512660686655375,4.30215887618246));
#15975=CARTESIAN_POINT('Ctrl Pts',(8.78748888497141,0.412633587447865,4.47187079069495));
#15976=CARTESIAN_POINT('Ctrl Pts',(8.80339416365902,0.21996315582106,4.58697932730413));
#15977=CARTESIAN_POINT('Ctrl Pts',(8.81929944234663,0.0231155027642346,
4.59463151583965));
#15978=CARTESIAN_POINT('Ctrl Pts',(8.81991782447859,0.0154622529370322,
4.59492902566351));
#15979=CARTESIAN_POINT('Ctrl Pts',(8.82053620661054,0.00780268890311657,
4.59506410656044));
#15980=CARTESIAN_POINT('Ctrl Pts',(8.82115458874249,0.000142235148737217,
4.59503945166131));
#15981=CARTESIAN_POINT('Origin',(4.,0.,4.));
#15982=CARTESIAN_POINT('',(9.22884541125756,-0.000264402795292107,4.59322887297718));
#15983=CARTESIAN_POINT('',(9.12115458874249,0.000475196148639644,4.59357609051269));
#15984=CARTESIAN_POINT('',(4.,-7.27562663373442E-17,4.5941));
#15985=CARTESIAN_POINT('Ctrl Pts',(9.22884541125756,-0.000264402795292107,
4.59322887297718));
#15986=CARTESIAN_POINT('Ctrl Pts',(9.21955918153543,0.115675446261185,4.59276508993807));
#15987=CARTESIAN_POINT('Ctrl Pts',(9.21027295181329,0.231857423975292,4.55999255403315));
#15988=CARTESIAN_POINT('Ctrl Pts',(9.20098672209116,0.327844211240712,4.49662776730038));
#15989=CARTESIAN_POINT('Ctrl Pts',(9.18508144340355,0.492248565587605,4.38809775866155));
#15990=CARTESIAN_POINT('Ctrl Pts',(9.16917616471593,0.597407924103304,4.18982173958679));
#15991=CARTESIAN_POINT('Ctrl Pts',(9.15327088602831,0.595037558282966,3.99283966966863));
#15992=CARTESIAN_POINT('Ctrl Pts',(9.1373656073407,0.592667192462628,3.79585759975047));
#15993=CARTESIAN_POINT('Ctrl Pts',(9.12146032865309,0.482767102306254,3.60016947898891));
#15994=CARTESIAN_POINT('Ctrl Pts',(9.10555504996548,0.315798759724268,3.49562701355602));
#15995=CARTESIAN_POINT('Ctrl Pts',(9.08964977127787,0.148830417142278,3.39108454812312));
#15996=CARTESIAN_POINT('Ctrl Pts',(9.07374449259025,-0.0752061778653251,
3.37768773801888));
#15997=CARTESIAN_POINT('Ctrl Pts',(9.05783921390264,-0.253442899077741,
3.46158783167087));
#15998=CARTESIAN_POINT('Ctrl Pts',(9.04193393521502,-0.431679620290152,
3.54548792532286));
#15999=CARTESIAN_POINT('Ctrl Pts',(9.02602865652741,-0.56411646770738,3.72668492273107));
#16000=CARTESIAN_POINT('Ctrl Pts',(9.0101233778398,-0.589944043936388,3.92198082849844));
#16001=CARTESIAN_POINT('Ctrl Pts',(8.99421809915219,-0.615771620165397,
4.11727673426582));
#16002=CARTESIAN_POINT('Ctrl Pts',(8.97831282046457,-0.534989925206181,
4.32667154839236));
#16003=CARTESIAN_POINT('Ctrl Pts',(8.96240754177696,-0.384690495792338,
4.45402003099517));
#16004=CARTESIAN_POINT('Ctrl Pts',(8.95122016493716,-0.278973620993485,
4.54359378149875));
#16005=CARTESIAN_POINT('Ctrl Pts',(8.94003278809737,-0.138863784294423,
4.59257621560968));
#16006=CARTESIAN_POINT('Ctrl Pts',(8.92884541125757,0.000516595407308196,
4.59372894893997));
#16007=CARTESIAN_POINT('Ctrl Pts',(8.82115458874249,0.000142235148737217,
4.59503945166131));
#16008=CARTESIAN_POINT('Ctrl Pts',(8.83644148529816,-0.189230254871984,
4.59442996300828));
#16009=CARTESIAN_POINT('Ctrl Pts',(8.85172838185382,-0.379146468724227,
4.49620311855542));
#16010=CARTESIAN_POINT('Ctrl Pts',(8.86701527840948,-0.487657002993039,
4.34104488491935));
#16011=CARTESIAN_POINT('Ctrl Pts',(8.88292055709709,-0.600556981206626,
4.17961022500168));
#16012=CARTESIAN_POINT('Ctrl Pts',(8.89882583578469,-0.62533206314696,3.95654506470448));
#16013=CARTESIAN_POINT('Ctrl Pts',(8.91473111447231,-0.550606579334316,
3.77427148852754));
#16014=CARTESIAN_POINT('Ctrl Pts',(8.93063639315992,-0.47588109552167,3.5919979123506));
#16015=CARTESIAN_POINT('Ctrl Pts',(8.94654167184753,-0.301655045956043,
3.45051592029392));
#16016=CARTESIAN_POINT('Ctrl Pts',(8.96244695053515,-0.107925661701669,
3.41478805750048));
#16017=CARTESIAN_POINT('Ctrl Pts',(8.97835222922276,0.0858037225526985,
3.37906019470703));
#16018=CARTESIAN_POINT('Ctrl Pts',(8.99425750791037,0.299036441495806,3.4490864611768));
#16019=CARTESIAN_POINT('Ctrl Pts',(9.01016278659798,0.433865051721373,3.5927137579139));
#16020=CARTESIAN_POINT('Ctrl Pts',(9.0260680652856,0.568693661946943,3.736341054651));
#16021=CARTESIAN_POINT('Ctrl Pts',(9.04197334397321,0.625118163454969,3.95356938165542));
#16022=CARTESIAN_POINT('Ctrl Pts',(9.05787862266082,0.577230812276762,4.14465668133936));
#16023=CARTESIAN_POINT('Ctrl Pts',(9.07378390134844,0.529343461098555,4.3357439810233));
#16024=CARTESIAN_POINT('Ctrl Pts',(9.08968918003605,0.377144257234124,4.50069025338676));
#16025=CARTESIAN_POINT('Ctrl Pts',(9.10559445872366,0.190516636080703,4.56375914846174));
#16026=CARTESIAN_POINT('Ctrl Pts',(9.11078116872994,0.129657384941762,4.58432590969837));
#16027=CARTESIAN_POINT('Ctrl Pts',(9.11596787873622,0.0651369761893139,
4.59405891310139));
#16028=CARTESIAN_POINT('Ctrl Pts',(9.12115458874249,0.000475196148639644,
4.59357609051269));
#16029=CARTESIAN_POINT('Origin',(4.,0.,4.));
#16030=CARTESIAN_POINT('',(9.52884541125756,-0.000414715089906426,4.59470005288553));
#16031=CARTESIAN_POINT('',(9.4211545887425,-0.000345133784900094,4.59331940772745));
#16032=CARTESIAN_POINT('',(4.,-7.27562663373442E-17,4.5941));
#16033=CARTESIAN_POINT('Ctrl Pts',(9.52884541125756,-0.000414715089906426,
4.59470005288553));
#16034=CARTESIAN_POINT('Ctrl Pts',(9.5149908536611,0.17147269131647,4.59333531965569));
#16035=CARTESIAN_POINT('Ctrl Pts',(9.50113629606464,0.344448366351018,4.51470554290992));
#16036=CARTESIAN_POINT('Ctrl Pts',(9.48728173846818,0.455032043431697,4.38349290156166));
#16037=CARTESIAN_POINT('Ctrl Pts',(9.47137645978057,0.581984072756561,4.23285845412795));
#16038=CARTESIAN_POINT('Ctrl Pts',(9.45547118109296,0.626706888961734,4.01292269047354));
#16039=CARTESIAN_POINT('Ctrl Pts',(9.43956590240535,0.56866566691212,3.82467080855373));
#16040=CARTESIAN_POINT('Ctrl Pts',(9.42366062371773,0.510624444862503,3.63641892663391));
#16041=CARTESIAN_POINT('Ctrl Pts',(9.40775534503012,0.349819184558098,3.47985092644869));
#16042=CARTESIAN_POINT('Ctrl Pts',(9.39185006634251,0.160084858421151,3.42685620983728));
#16043=CARTESIAN_POINT('Ctrl Pts',(9.37594478765489,-0.0296494677157886,
3.37386149322587));
#16044=CARTESIAN_POINT('Ctrl Pts',(9.36003950896728,-0.248312859685263,
3.42444006018826));
#16045=CARTESIAN_POINT('Ctrl Pts',(9.34413423027966,-0.395504338780113,
3.55536837257802));
#16046=CARTESIAN_POINT('Ctrl Pts',(9.32822895159205,-0.542695817874971,
3.6862966849678));
#16047=CARTESIAN_POINT('Ctrl Pts',(9.31232367290444,-0.618415384095196,
3.89757474278496));
#16048=CARTESIAN_POINT('Ctrl Pts',(9.29641839421683,-0.587895816063128,
4.09219260031737));
#16049=CARTESIAN_POINT('Ctrl Pts',(9.28051311552922,-0.55737624803106,4.28681045784976));
#16050=CARTESIAN_POINT('Ctrl Pts',(9.26460783684159,-0.42061754574671,4.4647681150974));
#16051=CARTESIAN_POINT('Ctrl Pts',(9.24870255815398,-0.240413519515492,
4.54435494461976));
#16052=CARTESIAN_POINT('Ctrl Pts',(9.24208350918851,-0.165420852186184,
4.57747534017911));
#16053=CARTESIAN_POINT('Ctrl Pts',(9.23546446022304,-0.0829041350566004,
4.59355944875842));
#16054=CARTESIAN_POINT('Ctrl Pts',(9.22884541125756,-0.000264402795292107,
4.59322887297718));
#16055=CARTESIAN_POINT('Ctrl Pts',(9.12115458874249,0.000475196148639644,
4.59357609051269));
#16056=CARTESIAN_POINT('Ctrl Pts',(9.13187315742383,-0.133151270259641,
4.59257831599443));
#16057=CARTESIAN_POINT('Ctrl Pts',(9.14259172610516,-0.267381477949042,
4.54795275857003));
#16058=CARTESIAN_POINT('Ctrl Pts',(9.1533102947865,-0.371151898503526,4.46515291500219));
#16059=CARTESIAN_POINT('Ctrl Pts',(9.16921557347411,-0.525136773491911,
4.34228626868117));
#16060=CARTESIAN_POINT('Ctrl Pts',(9.18512085216173,-0.612050485026272,
4.13536145825263));
#16061=CARTESIAN_POINT('Ctrl Pts',(9.20102613084934,-0.591985933785934,
3.93938960239856));
#16062=CARTESIAN_POINT('Ctrl Pts',(9.21693140953695,-0.571921382545595,
3.74341774654449));
#16063=CARTESIAN_POINT('Ctrl Pts',(9.23283668822456,-0.444878568530549,
3.55839884526489));
#16064=CARTESIAN_POINT('Ctrl Pts',(9.24874196691217,-0.269190177198291,
3.46928575052316));
#16065=CARTESIAN_POINT('Ctrl Pts',(9.26464724559978,-0.0935017858660342,
3.38017265578144));
#16066=CARTESIAN_POINT('Ctrl Pts',(9.28055252428739,0.130832182783434,3.38696536757758));
#16067=CARTESIAN_POINT('Ctrl Pts',(9.29645780297501,0.300807061133818,3.48654496003073));
#16068=CARTESIAN_POINT('Ctrl Pts',(9.31236308166262,0.470781939484206,3.58612455248389));
#16069=CARTESIAN_POINT('Ctrl Pts',(9.32826836035024,0.586397727535503,3.77849102559406));
#16070=CARTESIAN_POINT('Ctrl Pts',(9.34417363903785,0.594568546715174,3.97531783326339));
#16071=CARTESIAN_POINT('Ctrl Pts',(9.36007891772546,0.602739365894845,4.17214464093271));
#16072=CARTESIAN_POINT('Ctrl Pts',(9.37598419641307,0.503465216202894,4.37343178316119));
#16073=CARTESIAN_POINT('Ctrl Pts',(9.39188947510069,0.342328587234952,4.48675671999422));
#16074=CARTESIAN_POINT('Ctrl Pts',(9.40164451298129,0.243500144778355,4.55626125828842));
#16075=CARTESIAN_POINT('Ctrl Pts',(9.41139955086189,0.121401365174849,4.59267772446372));
#16076=CARTESIAN_POINT('Ctrl Pts',(9.4211545887425,-0.000345133784900094,
4.59331940772745));
#16077=CARTESIAN_POINT('Origin',(4.,0.,4.));
#16078=CARTESIAN_POINT('',(9.82884541125756,0.000474857175501747,4.59454166667424));
#16079=CARTESIAN_POINT('',(9.7211545887425,-0.000338423355870402,4.59484023865297));
#16080=CARTESIAN_POINT('',(4.,-7.27562663373442E-17,4.5941));
#16081=CARTESIAN_POINT('Ctrl Pts',(9.82884541125756,0.000474857175501747,
4.59454166667424));
#16082=CARTESIAN_POINT('Ctrl Pts',(9.82632780447438,0.0317313679687054,
4.59481419231428));
#16083=CARTESIAN_POINT('Ctrl Pts',(9.82381019769121,0.0629485386443197,
4.59256288124703));
#16084=CARTESIAN_POINT('Ctrl Pts',(9.82129259090804,0.093741277189286,4.58765086492638));
#16085=CARTESIAN_POINT('Ctrl Pts',(9.80538731222043,0.288278045752977,4.55661862072519));
#16086=CARTESIAN_POINT('Ctrl Pts',(9.78948203353282,0.465874751366426,4.41939150759219));
#16087=CARTESIAN_POINT('Ctrl Pts',(9.77357675484521,0.54498650030893,4.23897841027765));
#16088=CARTESIAN_POINT('Ctrl Pts',(9.7576714761576,0.624098249251433,4.05856531296313));
#16089=CARTESIAN_POINT('Ctrl Pts',(9.74176619746998,0.604725041522997,3.83496623146707));
#16090=CARTESIAN_POINT('Ctrl Pts',(9.72586091878237,0.495762234499694,3.67084840431546));
#16091=CARTESIAN_POINT('Ctrl Pts',(9.70995564009475,0.386799427476386,3.50673057716384));
#16092=CARTESIAN_POINT('Ctrl Pts',(9.69405036140714,0.188247021158209,3.40209400435668));
#16093=CARTESIAN_POINT('Ctrl Pts',(9.67814508271953,-0.00872811953311764,
3.40498337331868));
#16094=CARTESIAN_POINT('Ctrl Pts',(9.66223980403192,-0.205703260224436,
3.40787274228067));
#16095=CARTESIAN_POINT('Ctrl Pts',(9.6463345253443,-0.4011011352889,3.51828805301183));
#16096=CARTESIAN_POINT('Ctrl Pts',(9.63042924665669,-0.505203307099277,
3.68553126611098));
#16097=CARTESIAN_POINT('Ctrl Pts',(9.61452396796908,-0.609305478909656,
3.85277447921013));
#16098=CARTESIAN_POINT('Ctrl Pts',(9.59861868928147,-0.622111947465945,
4.07684559467727));
#16099=CARTESIAN_POINT('Ctrl Pts',(9.58271341059386,-0.537742524204099,
4.25486063595701));
#16100=CARTESIAN_POINT('Ctrl Pts',(9.56680813190624,-0.453373100942255,
4.43287567723675));
#16101=CARTESIAN_POINT('Ctrl Pts',(9.55090285321863,-0.271827785862281,
4.5648346443291));
#16102=CARTESIAN_POINT('Ctrl Pts',(9.53499757453102,-0.0764645071000137,
4.59014756226876));
#16103=CARTESIAN_POINT('Ctrl Pts',(9.53294685343987,-0.0512756623106346,
4.5934112419387));
#16104=CARTESIAN_POINT('Ctrl Pts',(9.53089613234871,-0.025857110284879,
4.59490205769144));
#16105=CARTESIAN_POINT('Ctrl Pts',(9.52884541125756,-0.000414715089906426,
4.59470005288553));
#16106=CARTESIAN_POINT('Ctrl Pts',(9.4211545887425,-0.000345133784900094,
4.59331940772745));
#16107=CARTESIAN_POINT('Ctrl Pts',(9.42730482954951,-0.0771024252662454,
4.59372396859559));
#16108=CARTESIAN_POINT('Ctrl Pts',(9.43345507035652,-0.153719688677923,
4.57990840728947));
#16109=CARTESIAN_POINT('Ctrl Pts',(9.43960531116353,-0.224276981305518,
4.55119942103951));
#16110=CARTESIAN_POINT('Ctrl Pts',(9.45551058985114,-0.406746812634079,
4.47695445381419));
#16111=CARTESIAN_POINT('Ctrl Pts',(9.47141586853875,-0.548687367047265,
4.30310178792596));
#16112=CARTESIAN_POINT('Ctrl Pts',(9.48732114722636,-0.58492554696818,4.10946721245096));
#16113=CARTESIAN_POINT('Ctrl Pts',(9.50322642591398,-0.621163726889096,
3.91583263697596));
#16114=CARTESIAN_POINT('Ctrl Pts',(9.5191317046016,-0.55169953231774,3.70241615191419));
#16115=CARTESIAN_POINT('Ctrl Pts',(9.53503698328921,-0.408427982613559,
3.56720957829912));
#16116=CARTESIAN_POINT('Ctrl Pts',(9.55094226197682,-0.265156432909381,
3.43200300468405));
#16117=CARTESIAN_POINT('Ctrl Pts',(9.56684754066442,-0.0480775280723801,
3.37500634251568));
#16118=CARTESIAN_POINT('Ctrl Pts',(9.58275281935204,0.14313528264739,3.42239004773181));
#16119=CARTESIAN_POINT('Ctrl Pts',(9.59865809803965,0.334348093367161,3.46977375294793));
#16120=CARTESIAN_POINT('Ctrl Pts',(9.61456337672728,0.499694809969701,3.62153782554855));
#16121=CARTESIAN_POINT('Ctrl Pts',(9.63046865541489,0.563255215433827,3.80799862400389));
#16122=CARTESIAN_POINT('Ctrl Pts',(9.6463739341025,0.626815620897955,3.99445942245922));
#16123=CARTESIAN_POINT('Ctrl Pts',(9.6622792127901,0.588589715223662,4.21561694676927));
#16124=CARTESIAN_POINT('Ctrl Pts',(9.67818449147771,0.466129217091882,4.36992501817411));
#16125=CARTESIAN_POINT('Ctrl Pts',(9.69250785723264,0.355848439261942,4.50888586187125));
#16126=CARTESIAN_POINT('Ctrl Pts',(9.70683122298757,0.177255492135987,4.59363345408847));
#16127=CARTESIAN_POINT('Ctrl Pts',(9.7211545887425,-0.000338423355870402,
4.59484023865297));
#16128=CARTESIAN_POINT('Origin',(4.,0.,4.));
#16129=CARTESIAN_POINT('',(10.1288454112576,0.000175993811045716,4.59316417414361));
#16130=CARTESIAN_POINT('',(10.0211545887425,0.000517772199431355,4.59437035498519));
#16131=CARTESIAN_POINT('',(4.,-7.27562663373442E-17,4.5941));
#16132=CARTESIAN_POINT('Ctrl Pts',(10.1288454112576,0.000175993811045716,
4.59316417414361));
#16133=CARTESIAN_POINT('Ctrl Pts',(10.1217594766001,0.0886689559287146,
4.59339827721605));
#16134=CARTESIAN_POINT('Ctrl Pts',(10.1146735419426,0.177068724884878,4.57486525982572));
#16135=CARTESIAN_POINT('Ctrl Pts',(10.1075876072851,0.256276603526552,4.53706914692868));
#16136=CARTESIAN_POINT('Ctrl Pts',(10.0916823285975,0.434068729046268,4.45223097977176));
#16137=CARTESIAN_POINT('Ctrl Pts',(10.0757770499098,0.565548899719798,4.27033860735548));
#16138=CARTESIAN_POINT('Ctrl Pts',(10.0598717712222,0.590346983641159,4.0749093118617));
#16139=CARTESIAN_POINT('Ctrl Pts',(10.0439664925346,0.61514506756252,3.87948001636793));
#16140=CARTESIAN_POINT('Ctrl Pts',(10.028061213847,0.533261064731712,3.67051379779667));
#16141=CARTESIAN_POINT('Ctrl Pts',(10.0121559351594,0.382292645022166,3.5439591030842));
#16142=CARTESIAN_POINT('Ctrl Pts',(9.99625065647179,0.231324225312614,3.41740440837173));
#16143=CARTESIAN_POINT('Ctrl Pts',(9.98034537778417,0.011271388724311,3.37326123751805));
#16144=CARTESIAN_POINT('Ctrl Pts',(9.96444009909655,-0.17682691184915,3.43179826703564));
#16145=CARTESIAN_POINT('Ctrl Pts',(9.94853482040894,-0.364925212422603,
3.49033529655323));
#16146=CARTESIAN_POINT('Ctrl Pts',(9.93262954172133,-0.521068976981223,
3.65155252644206));
#16147=CARTESIAN_POINT('Ctrl Pts',(9.91672426303372,-0.573563594737602,
3.84142582527571));
#16148=CARTESIAN_POINT('Ctrl Pts',(9.90081898434611,-0.626058212493981,
4.03129912410937));
#16149=CARTESIAN_POINT('Ctrl Pts',(9.8849137056585,-0.574903683448118,4.24982849188785));
#16150=CARTESIAN_POINT('Ctrl Pts',(9.86900842697089,-0.443588003168223,
4.39667448814241));
#16151=CARTESIAN_POINT('Ctrl Pts',(9.85562075506645,-0.333057953489513,
4.52027659892262));
#16152=CARTESIAN_POINT('Ctrl Pts',(9.842233083162,-0.165735336637852,4.59309247934331));
#16153=CARTESIAN_POINT('Ctrl Pts',(9.82884541125756,0.000474857175501747,
4.59454166667424));
#16154=CARTESIAN_POINT('Ctrl Pts',(9.7211545887425,-0.000338423355870402,
4.59484023865297));
#16155=CARTESIAN_POINT('Ctrl Pts',(9.72273650167518,-0.0199523965301825,
4.59497351934566));
#16156=CARTESIAN_POINT('Ctrl Pts',(9.72431841460787,-0.0395541838993478,
4.59408780127083));
#16157=CARTESIAN_POINT('Ctrl Pts',(9.72590032754056,-0.0590504136254521,
4.592143576127));
#16158=CARTESIAN_POINT('Ctrl Pts',(9.74180560622817,-0.255074455621757,
4.57259544417541));
#16159=CARTESIAN_POINT('Ctrl Pts',(9.75771088491579,-0.4404274490251,4.4460405617726));
#16160=CARTESIAN_POINT('Ctrl Pts',(9.7736161636034,-0.530003140903138,4.2705875768224));
#16161=CARTESIAN_POINT('Ctrl Pts',(9.78952144229101,-0.619578832781174,
4.0951345918722));
#16162=CARTESIAN_POINT('Ctrl Pts',(9.80542672097862,-0.61337722313391,3.87078350437461));
#16163=CARTESIAN_POINT('Ctrl Pts',(9.82133199966623,-0.514245828742901,
3.70054684219675));
#16164=CARTESIAN_POINT('Ctrl Pts',(9.83723727835384,-0.41511443435189,3.53031018001889));
#16165=CARTESIAN_POINT('Ctrl Pts',(9.85314255704146,-0.223053255217129,
3.41418794316076));
#16166=CARTESIAN_POINT('Ctrl Pts',(9.86904783572907,-0.0262486593588972,
3.40549855006092));
#16167=CARTESIAN_POINT('Ctrl Pts',(9.88495311441669,0.170555936499329,3.39680915696108));
#16168=CARTESIAN_POINT('Ctrl Pts',(9.9008583931043,0.372103949081026,3.49555260761951));
#16169=CARTESIAN_POINT('Ctrl Pts',(9.91676367179191,0.485853057801912,3.65639008698476));
#16170=CARTESIAN_POINT('Ctrl Pts',(9.93266895047952,0.5996021665228,3.81722756635002));
#16171=CARTESIAN_POINT('Ctrl Pts',(9.94857422916713,0.625552371382872,4.04015907442209));
#16172=CARTESIAN_POINT('Ctrl Pts',(9.96447950785475,0.551788436173011,4.22282389414861));
#16173=CARTESIAN_POINT('Ctrl Pts',(9.98038478654236,0.478024500963153,4.40548871387512));
#16174=CARTESIAN_POINT('Ctrl Pts',(9.99629006522997,0.304546425683368,4.54788684525607));
#16175=CARTESIAN_POINT('Ctrl Pts',(10.0121953439176,0.111008003250015,4.58463509072946));
#16176=CARTESIAN_POINT('Ctrl Pts',(10.0151817588592,0.0746687445744621,
4.59153503329043));
#16177=CARTESIAN_POINT('Ctrl Pts',(10.0181681738009,0.0376222632219309,
4.59471031472953));
#16178=CARTESIAN_POINT('Ctrl Pts',(10.0211545887425,0.000517772199431355,
4.59437035498519));
#16179=CARTESIAN_POINT('Origin',(4.,0.,4.));
#16180=CARTESIAN_POINT('',(10.4288454112576,-0.000541293539476018,4.59389423388278));
#16181=CARTESIAN_POINT('',(10.3211545887425,8.19078234495683E-5,4.59312629593825));
#16182=CARTESIAN_POINT('',(4.,-7.27562663373442E-17,4.5941));
#16183=CARTESIAN_POINT('Ctrl Pts',(10.4288454112576,-0.000541293539476018,
4.59389423388278));
#16184=CARTESIAN_POINT('Ctrl Pts',(10.4171911487257,0.144553461780974,4.59260897165526));
#16185=CARTESIAN_POINT('Ctrl Pts',(10.4055368861939,0.290497422953868,4.53904330389552));
#16186=CARTESIAN_POINT('Ctrl Pts',(10.3938826236621,0.397841883685798,4.4425412994096));
#16187=CARTESIAN_POINT('Ctrl Pts',(10.3779773449745,0.544341377656434,4.31083916286766));
#16188=CARTESIAN_POINT('Ctrl Pts',(10.3620720662869,0.618946539098701,4.09916502578488));
#16189=CARTESIAN_POINT('Ctrl Pts',(10.3461667875993,0.587401834162399,3.90471069671543));
#16190=CARTESIAN_POINT('Ctrl Pts',(10.3302615089117,0.555857129226098,3.710256367646));
#16191=CARTESIAN_POINT('Ctrl Pts',(10.314356230224,0.418162557911234,3.5330218465899));
#16192=CARTESIAN_POINT('Ctrl Pts',(10.2984509515364,0.237541641988682,3.45438572744188));
#16193=CARTESIAN_POINT('Ctrl Pts',(10.2825456728488,0.0569207260661262,
3.37574960829385));
#16194=CARTESIAN_POINT('Ctrl Pts',(10.2666403941612,-0.16662653446412,3.3957118910539));
#16195=CARTESIAN_POINT('Ctrl Pts',(10.2507351154736,-0.330456695071223,
3.50510674001315));
#16196=CARTESIAN_POINT('Ctrl Pts',(10.234829836786,-0.494286855678321,3.61450158897239));
#16197=CARTESIAN_POINT('Ctrl Pts',(10.2189245580984,-0.59839991636228,3.81332900413083));
#16198=CARTESIAN_POINT('Ctrl Pts',(10.2030192794108,-0.594991564317383,
4.01029584814195));
#16199=CARTESIAN_POINT('Ctrl Pts',(10.1871140007231,-0.591583212272486,
4.20726269215308));
#16200=CARTESIAN_POINT('Ctrl Pts',(10.1712087220355,-0.480653447498727,
4.40236896501689));
#16201=CARTESIAN_POINT('Ctrl Pts',(10.1553034433479,-0.313136524928893,
4.50603012050002));
#16202=CARTESIAN_POINT('Ctrl Pts',(10.1464840993178,-0.220249792163878,
4.56350936438632));
#16203=CARTESIAN_POINT('Ctrl Pts',(10.1376647552877,-0.109964716607974,
4.59287280319057));
#16204=CARTESIAN_POINT('Ctrl Pts',(10.1288454112576,0.000175993811045716,
4.59316417414361));
#16205=CARTESIAN_POINT('Ctrl Pts',(10.0211545887425,0.000517772199431355,
4.59437035498519));
#16206=CARTESIAN_POINT('Ctrl Pts',(10.0340734524885,-0.159991692577292,
4.59289973094197));
#16207=CARTESIAN_POINT('Ctrl Pts',(10.0469923162344,-0.321586704601994,
4.52564765365589));
#16208=CARTESIAN_POINT('Ctrl Pts',(10.0599111799804,-0.431712787135162,
4.40956688772629));
#16209=CARTESIAN_POINT('Ctrl Pts',(10.075816458668,-0.567296385500051,4.2666520796839));
#16210=CARTESIAN_POINT('Ctrl Pts',(10.0917217373556,-0.624864812642908,
4.04972410403331));
#16211=CARTESIAN_POINT('Ctrl Pts',(10.1076270160433,-0.577985082339038,
3.85838710972745));
#16212=CARTESIAN_POINT('Ctrl Pts',(10.1235322947309,-0.531105352035168,
3.6670501154216));
#16213=CARTESIAN_POINT('Ctrl Pts',(10.1394375734185,-0.379777464284567,
3.50130410246047));
#16214=CARTESIAN_POINT('Ctrl Pts',(10.1553428521061,-0.193484782987353,
3.43725262786029));
#16215=CARTESIAN_POINT('Ctrl Pts',(10.1712481307937,-0.00719210169012799,
3.37320115326011));
#16216=CARTESIAN_POINT('Ctrl Pts',(10.1871534094813,0.214065373153706,3.41084421702088));
#16217=CARTESIAN_POINT('Ctrl Pts',(10.2030586881689,0.368695569727689,3.53289771681035));
#16218=CARTESIAN_POINT('Ctrl Pts',(10.2189639668565,0.523325766301663,3.65495121659981));
#16219=CARTESIAN_POINT('Ctrl Pts',(10.2348692455442,0.611328684605784,3.86141515241798));
#16220=CARTESIAN_POINT('Ctrl Pts',(10.2507745242318,0.592297107651237,4.05749001970593));
#16221=CARTESIAN_POINT('Ctrl Pts',(10.2666798029194,0.573265530696689,4.25356488699388));
#16222=CARTESIAN_POINT('Ctrl Pts',(10.282585081607,0.447199458483466,4.43925068575162));
#16223=CARTESIAN_POINT('Ctrl Pts',(10.2984903602946,0.271983097956201,4.5292883529079));
#16224=CARTESIAN_POINT('Ctrl Pts',(10.3060451031106,0.188758241169316,4.57205474716445));
#16225=CARTESIAN_POINT('Ctrl Pts',(10.3135998459265,0.0944446272328244,
4.59324204311815));
#16226=CARTESIAN_POINT('Ctrl Pts',(10.3211545887425,8.19078234495684E-5,
4.59312629593825));
#16227=CARTESIAN_POINT('Origin',(4.,0.,4.));
#16228=CARTESIAN_POINT('',(10.7288454112576,7.37317986114466E-5,4.59506942345298));
#16229=CARTESIAN_POINT('',(10.6211545887425,-0.000548317120500629,4.59406879148573));
#16230=CARTESIAN_POINT('',(4.,-7.27562663373442E-17,4.5941));
#16231=CARTESIAN_POINT('Ctrl Pts',(10.7288454112576,7.37317986114466E-5,
4.59506942345298));
#16232=CARTESIAN_POINT('Ctrl Pts',(10.728528099539,0.00400402563557926,
4.59507627971693));
#16233=CARTESIAN_POINT('Ctrl Pts',(10.7282107878205,0.00793419209028873,
4.59504072157671));
#16234=CARTESIAN_POINT('Ctrl Pts',(10.727893476102,0.0118635052742893,4.59496237136513));
#16235=CARTESIAN_POINT('Ctrl Pts',(10.7119881974144,0.208820685209451,4.59103505989901));
#16236=CARTESIAN_POINT('Ctrl Pts',(10.6960829187267,0.403634001393415,4.47959161118634));
#16237=CARTESIAN_POINT('Ctrl Pts',(10.6801776400391,0.506853420906232,4.31180214209248));
#16238=CARTESIAN_POINT('Ctrl Pts',(10.6642723613515,0.610072840419052,4.14401267299861));
#16239=CARTESIAN_POINT('Ctrl Pts',(10.6483670826639,0.621698363260717,3.91987718352354));
#16240=CARTESIAN_POINT('Ctrl Pts',(10.6324618039763,0.536392041177647,3.74230920804366));
#16241=CARTESIAN_POINT('Ctrl Pts',(10.6165565252887,0.451085719094577,3.56474123256377));
#16242=CARTESIAN_POINT('Ctrl Pts',(10.6006512466011,0.26884755208677,3.43374077107907));
#16243=CARTESIAN_POINT('Ctrl Pts',(10.5847459679135,0.0733535965831807,
3.40945769333085));
#16244=CARTESIAN_POINT('Ctrl Pts',(10.5688406892258,-0.122140358920403,
3.38517461558263));
#16245=CARTESIAN_POINT('Ctrl Pts',(10.5529354105382,-0.33089010291977,3.46760892157089));
#16246=CARTESIAN_POINT('Ctrl Pts',(10.5370301318506,-0.457046584443773,
3.61891026549369));
#16247=CARTESIAN_POINT('Ctrl Pts',(10.521124853163,-0.583203065967777,3.7702116094165));
#16248=CARTESIAN_POINT('Ctrl Pts',(10.5052195744754,-0.626766285016417,
3.99037999127385));
#16249=CARTESIAN_POINT('Ctrl Pts',(10.4893142957878,-0.567733854410369,
4.17832340467295));
#16250=CARTESIAN_POINT('Ctrl Pts',(10.4734090171002,-0.508701423804317,
4.36626681807206));
#16251=CARTESIAN_POINT('Ctrl Pts',(10.4575037384126,-0.347073343543565,
4.52198526301292));
#16252=CARTESIAN_POINT('Ctrl Pts',(10.4415984597249,-0.157062390163684,
4.57397941748279));
#16253=CARTESIAN_POINT('Ctrl Pts',(10.4373474435692,-0.106278015462724,
4.58787593542499));
#16254=CARTESIAN_POINT('Ctrl Pts',(10.4330964274134,-0.0534661480554494,
4.59436304694399));
#16255=CARTESIAN_POINT('Ctrl Pts',(10.4288454112576,-0.000541293539476018,
4.59389423388278));
#16256=CARTESIAN_POINT('Ctrl Pts',(10.3211545887425,8.19078234495684E-5,
4.59312629593825));
#16257=CARTESIAN_POINT('Ctrl Pts',(10.3295051246142,-0.104220686264852,
4.59299835631127));
#16258=CARTESIAN_POINT('Ctrl Pts',(10.3378556604858,-0.208583275928277,
4.56684300569277));
#16259=CARTESIAN_POINT('Ctrl Pts',(10.3462061963575,-0.298097175589899,
4.5150330474864));
#16260=CARTESIAN_POINT('Ctrl Pts',(10.3621114750451,-0.468594439767441,
4.41635053935381));
#16261=CARTESIAN_POINT('Ctrl Pts',(10.3780167537327,-0.585222319281217,
4.22459598753381));
#16262=CARTESIAN_POINT('Ctrl Pts',(10.3939220324203,-0.594430225977177,
4.02781496975607));
#16263=CARTESIAN_POINT('Ctrl Pts',(10.4098273111079,-0.603638132673137,
3.83103395197833));
#16264=CARTESIAN_POINT('Ctrl Pts',(10.4257325897955,-0.505426066551287,
3.62922646824286));
#16265=CARTESIAN_POINT('Ctrl Pts',(10.4416378684831,-0.344888853364916,
3.51505397731042));
#16266=CARTESIAN_POINT('Ctrl Pts',(10.4575431471707,-0.184351640178541,
3.40088148637798));
#16267=CARTESIAN_POINT('Ctrl Pts',(10.4734484258584,0.0385107200723601,
3.37434398824859));
#16268=CARTESIAN_POINT('Ctrl Pts',(10.489353704546,0.221369260089487,3.4476263793543));
#16269=CARTESIAN_POINT('Ctrl Pts',(10.5052589832336,0.40422780010661,3.52090877046001));
#16270=CARTESIAN_POINT('Ctrl Pts',(10.5211642619212,0.54708251988996,3.69401105080081));
#16271=CARTESIAN_POINT('Ctrl Pts',(10.5370695406088,0.584340575799814,3.88745197659776));
#16272=CARTESIAN_POINT('Ctrl Pts',(10.5529748192964,0.621598631709669,4.08089290239472));
#16273=CARTESIAN_POINT('Ctrl Pts',(10.568880097984,0.55326002374602,4.29467247364782));
#16274=CARTESIAN_POINT('Ctrl Pts',(10.5847853766716,0.4107029495177,4.43063215550545));
#16275=CARTESIAN_POINT('Ctrl Pts',(10.5969084473619,0.302045344566967,4.53426120008624));
#16276=CARTESIAN_POINT('Ctrl Pts',(10.6090315180522,0.150270129189204,4.59268036842864));
#16277=CARTESIAN_POINT('Ctrl Pts',(10.6211545887425,-0.000548317120500629,
4.59406879148573));
#16278=CARTESIAN_POINT('Origin',(4.,0.,4.));
#16279=CARTESIAN_POINT('',(11.0288454112576,0.000503618959454472,4.59367252935801));
#16280=CARTESIAN_POINT('',(10.9211545887425,0.000179316795020235,4.59501533910171));
#16281=CARTESIAN_POINT('',(4.,-7.27562663373442E-17,4.5941));
#16282=CARTESIAN_POINT('Ctrl Pts',(11.0288454112576,0.000503618959454472,
4.59367252935801));
#16283=CARTESIAN_POINT('Ctrl Pts',(11.0239597716647,0.0613870506829751,
4.59415995979602));
#16284=CARTESIAN_POINT('Ctrl Pts',(11.0190741320719,0.122135879976345,4.58554712933309));
#16285=CARTESIAN_POINT('Ctrl Pts',(11.014188492479,0.179818659528701,4.56726203449827));
#16286=CARTESIAN_POINT('Ctrl Pts',(10.9982832137914,0.36760588100072,4.50773461262244));
#16287=CARTESIAN_POINT('Ctrl Pts',(10.9823779351038,0.52289792528528,4.34569680405454));
#16288=CARTESIAN_POINT('Ctrl Pts',(10.9664726564162,0.574391255511512,4.15554951523459));
#16289=CARTESIAN_POINT('Ctrl Pts',(10.9505673777285,0.625884585737745,3.96540222641464));
#16290=CARTESIAN_POINT('Ctrl Pts',(10.9346620990409,0.573579201905647,3.74714545734266));
#16291=CARTESIAN_POINT('Ctrl Pts',(10.9187568203533,0.441491523412615,3.60099348269406));
#16292=CARTESIAN_POINT('Ctrl Pts',(10.9028515416657,0.309403844919578,3.45484150804546));
#16293=CARTESIAN_POINT('Ctrl Pts',(10.8869462629781,0.0975338717655902,
3.38079432782024));
#16294=CARTESIAN_POINT('Ctrl Pts',(10.8710409842905,-0.0968366678563846,
3.41285127449999));
#16295=CARTESIAN_POINT('Ctrl Pts',(10.8551357056029,-0.291207207478354,
3.44490822117975));
#16296=CARTESIAN_POINT('Ctrl Pts',(10.8392304269153,-0.468078313568319,
3.58306929476445));
#16297=CARTESIAN_POINT('Ctrl Pts',(10.8233251482276,-0.546238257009186,
3.76389677537701));
#16298=CARTESIAN_POINT('Ctrl Pts',(10.80741986954,-0.624398200450053,3.94472425598957));
#16299=CARTESIAN_POINT('Ctrl Pts',(10.7915145908524,-0.603846981241821,
4.16821814362997));
#16300=CARTESIAN_POINT('Ctrl Pts',(10.7756093121648,-0.494020849794526,
4.33175950034039));
#16301=CARTESIAN_POINT('Ctrl Pts',(10.7600213451957,-0.386385759396791,
4.49203819249975));
#16302=CARTESIAN_POINT('Ctrl Pts',(10.7444333782267,-0.193002309618558,
4.59473260886404));
#16303=CARTESIAN_POINT('Ctrl Pts',(10.7288454112576,7.37317986114466E-5,
4.59506942345298));
#16304=CARTESIAN_POINT('Ctrl Pts',(10.6211545887425,-0.000548317120500629,
4.59406879148573));
#16305=CARTESIAN_POINT('Ctrl Pts',(10.6249367967398,-0.0476013079303647,
4.5945019577127));
#16306=CARTESIAN_POINT('Ctrl Pts',(10.6287190047372,-0.0945611723716044,
4.58938408097059));
#16307=CARTESIAN_POINT('Ctrl Pts',(10.6325012127345,-0.140089514783682,
4.57835619988505));
#16308=CARTESIAN_POINT('Ctrl Pts',(10.6484064914221,-0.331549364363767,
4.53198076994489));
#16309=CARTESIAN_POINT('Ctrl Pts',(10.6643117701097,-0.497693523030948,
4.38109011760241));
#16310=CARTESIAN_POINT('Ctrl Pts',(10.6802170487973,-0.562235622104956,
4.19496684675621));
#16311=CARTESIAN_POINT('Ctrl Pts',(10.6961223274849,-0.626777721178965,
4.00884357591002));
#16312=CARTESIAN_POINT('Ctrl Pts',(10.7120276061725,-0.589717760659791,
3.78748768656011));
#16313=CARTESIAN_POINT('Ctrl Pts',(10.7279328848602,-0.468072106540212,
3.63253643830059));
#16314=CARTESIAN_POINT('Ctrl Pts',(10.7438381635478,-0.346426452420629,
3.47758519004106));
#16315=CARTESIAN_POINT('Ctrl Pts',(10.7597434422354,-0.140195104700642,
3.38903858287192));
#16316=CARTESIAN_POINT('Ctrl Pts',(10.775648720923,0.0559292266755373,3.40755347270721));
#16317=CARTESIAN_POINT('Ctrl Pts',(10.7915539996106,0.252053558051711,3.4260683625425));
#16318=CARTESIAN_POINT('Ctrl Pts',(10.8074592782982,0.438070873084069,3.55164474938222));
#16319=CARTESIAN_POINT('Ctrl Pts',(10.8233645569858,0.528569890453362,3.72662326908837));
#16320=CARTESIAN_POINT('Ctrl Pts',(10.8392698356734,0.619068907822657,3.90160178879453));
#16321=CARTESIAN_POINT('Ctrl Pts',(10.8551751143611,0.614049627528876,4.12598244136713));
#16322=CARTESIAN_POINT('Ctrl Pts',(10.8710803930487,0.515816690734684,4.29673912390739));
#16323=CARTESIAN_POINT('Ctrl Pts',(10.8869856717363,0.417583753940498,4.46749580644764));
#16324=CARTESIAN_POINT('Ctrl Pts',(10.9028909504239,0.226137160645921,4.58462851895556));
#16325=CARTESIAN_POINT('Ctrl Pts',(10.9187962291115,0.0293810870543861,
4.59435487532392));
#16326=CARTESIAN_POINT('Ctrl Pts',(10.9195823489885,0.0196563998352688,
4.59483560139116));
#16327=CARTESIAN_POINT('Ctrl Pts',(10.9203684688655,0.00991874240631306,
4.5950539509358));
#16328=CARTESIAN_POINT('Ctrl Pts',(10.9211545887425,0.000179316795020235,
4.59501533910171));
#16329=CARTESIAN_POINT('Origin',(4.,0.,4.));
#16330=CARTESIAN_POINT('',(11.3288454112576,-0.000294350894641693,4.59325842069974));
#16331=CARTESIAN_POINT('',(11.2211545887425,0.000456638431143918,4.59352536526061));
#16332=CARTESIAN_POINT('',(4.,-7.27562663373442E-17,4.5941));
#16333=CARTESIAN_POINT('Ctrl Pts',(11.3288454112576,-0.000294350894641693,
4.59325842069974));
#16334=CARTESIAN_POINT('Ctrl Pts',(11.3193914437904,0.117725031793324,4.59273125875086));
#16335=CARTESIAN_POINT('Ctrl Pts',(11.3099374763232,0.236024696118704,4.55868066117597));
#16336=CARTESIAN_POINT('Ctrl Pts',(11.300483508856,0.333060002447629,4.49314500997921));
#16337=CARTESIAN_POINT('Ctrl Pts',(11.2845782301684,0.496311419914153,4.38288835848583));
#16338=CARTESIAN_POINT('Ctrl Pts',(11.2686729514808,0.599375291650127,4.18351506848348));
#16339=CARTESIAN_POINT('Ctrl Pts',(11.2527676727932,0.594929048027223,3.98656891995295));
#16340=CARTESIAN_POINT('Ctrl Pts',(11.2368623941056,0.59048280440432,3.78962277142242));
#16341=CARTESIAN_POINT('Ctrl Pts',(11.220957115418,0.478526445422532,3.5951037643637));
#16342=CARTESIAN_POINT('Ctrl Pts',(11.2050518367303,0.310465594643358,3.49232679739763));
#16343=CARTESIAN_POINT('Ctrl Pts',(11.1891465580427,0.142404743864184,3.38954983043155));
#16344=CARTESIAN_POINT('Ctrl Pts',(11.1732412793551,-0.0817605987123653,
3.37851490355812));
#16345=CARTESIAN_POINT('Ctrl Pts',(11.1573360006675,-0.259103191428711,
3.46428878834836));
#16346=CARTESIAN_POINT('Ctrl Pts',(11.1414307219799,-0.436445784145052,
3.5500626731386));
#16347=CARTESIAN_POINT('Ctrl Pts',(11.1255254432923,-0.566965627001181,
3.73264536959251));
#16348=CARTESIAN_POINT('Ctrl Pts',(11.1096201646047,-0.590733529996744,
3.92820262793532));
#16349=CARTESIAN_POINT('Ctrl Pts',(11.0937148859171,-0.614501432992307,
4.12375988627813));
#16350=CARTESIAN_POINT('Ctrl Pts',(11.0778096072294,-0.531517396127296,
4.33229170650985));
#16351=CARTESIAN_POINT('Ctrl Pts',(11.0619043285418,-0.379884178365051,
4.45804909903384));
#16352=CARTESIAN_POINT('Ctrl Pts',(11.0508846894471,-0.274828280424841,
4.54517747360242));
#16353=CARTESIAN_POINT('Ctrl Pts',(11.0398650503523,-0.136819945681758,
4.59257312212411));
#16354=CARTESIAN_POINT('Ctrl Pts',(11.0288454112576,0.000503618959454472,
4.59367252935801));
#16355=CARTESIAN_POINT('Ctrl Pts',(10.9211545887425,0.000179316795020235,
4.59501533910171));
#16356=CARTESIAN_POINT('Ctrl Pts',(10.9362737475531,-0.187135527734918,
4.59427273168419));
#16357=CARTESIAN_POINT('Ctrl Pts',(10.9513929063637,-0.375104412928531,
4.49848156101044));
#16358=CARTESIAN_POINT('Ctrl Pts',(10.9665120651743,-0.484035620954107,
4.34616539940523));
#16359=CARTESIAN_POINT('Ctrl Pts',(10.982417343862,-0.598630701482551,4.1859295668894));
#16360=CARTESIAN_POINT('Ctrl Pts',(10.9983226225496,-0.625755308650954,
3.96313790162893));
#16361=CARTESIAN_POINT('Ctrl Pts',(11.0142279012372,-0.55295497039508,3.7800869107734));
#16362=CARTESIAN_POINT('Ctrl Pts',(11.0301331799248,-0.480154632139201,
3.59703591991786));
#16363=CARTESIAN_POINT('Ctrl Pts',(11.0460384586124,-0.307429348459053,
3.45372560346725));
#16364=CARTESIAN_POINT('Ctrl Pts',(11.0619437373,-0.114087262216405,3.41595799577618));
#16365=CARTESIAN_POINT('Ctrl Pts',(11.0778490159876,0.0792548240262376,
3.37819038808511));
#16366=CARTESIAN_POINT('Ctrl Pts',(11.0937542946752,0.293213712831377,3.4459654891536));
#16367=CARTESIAN_POINT('Ctrl Pts',(11.1096595733629,0.429548534313776,3.58816383989905));
#16368=CARTESIAN_POINT('Ctrl Pts',(11.1255648520505,0.565883355796175,3.7303621906445));
#16369=CARTESIAN_POINT('Ctrl Pts',(11.1414701307381,0.624594109955846,3.94698379106692));
#16370=CARTESIAN_POINT('Ctrl Pts',(11.1573754094257,0.578723302329844,4.13856516675647));
#16371=CARTESIAN_POINT('Ctrl Pts',(11.1732806881133,0.53285249470384,4.33014654244603));
#16372=CARTESIAN_POINT('Ctrl Pts',(11.1891859668009,0.382400125292158,4.49668769340272));
#16373=CARTESIAN_POINT('Ctrl Pts',(11.2050912454885,0.196447557013804,4.56171996888228));
#16374=CARTESIAN_POINT('Ctrl Pts',(11.2104456932399,0.133847376870746,4.58361282144047));
#16375=CARTESIAN_POINT('Ctrl Pts',(11.2158001409912,0.0672239414478651,
4.5940016224088));
#16376=CARTESIAN_POINT('Ctrl Pts',(11.2211545887425,0.000456638431143918,
4.59352536526061));
#16377=CARTESIAN_POINT('Origin',(4.,0.,4.));
#16378=CARTESIAN_POINT('',(11.6288454112576,-0.000389145320547679,4.59475273347735));
#16379=CARTESIAN_POINT('',(11.5211545887425,-0.0003715675665865,4.59335763259963));
#16380=CARTESIAN_POINT('',(4.,-7.27562663373442E-17,4.5941));
#16381=CARTESIAN_POINT('Ctrl Pts',(11.6288454112576,-0.000389145320547679,
4.59475273347735));
#16382=CARTESIAN_POINT('Ctrl Pts',(11.6148231159161,0.173538999407471,4.59343557735163));
#16383=CARTESIAN_POINT('Ctrl Pts',(11.6008008205746,0.348531733704351,4.51264940831536));
#16384=CARTESIAN_POINT('Ctrl Pts',(11.586778525233,0.459048433726307,4.37867598496766));
#16385=CARTESIAN_POINT('Ctrl Pts',(11.5708732465454,0.584405864209301,4.22671194604376));
#16386=CARTESIAN_POINT('Ctrl Pts',(11.5549679678578,0.626808276394098,4.00631705984067));
#16387=CARTESIAN_POINT('Ctrl Pts',(11.5390626891702,0.566786276503563,3.81868733396413));
#16388=CARTESIAN_POINT('Ctrl Pts',(11.5231574104826,0.506764276613028,3.6310576080876));
#16389=CARTESIAN_POINT('Ctrl Pts',(11.507252131795,0.344317864647159,3.47619304253762));
#16390=CARTESIAN_POINT('Ctrl Pts',(11.4913468531074,0.154035560439752,3.4252008940353));
#16391=CARTESIAN_POINT('Ctrl Pts',(11.4754415744198,-0.0362467437676612,
3.37420874553297));
#16392=CARTESIAN_POINT('Ctrl Pts',(11.4595362957322,-0.254364940216614,
3.4270890140783));
#16393=CARTESIAN_POINT('Ctrl Pts',(11.4436310170445,-0.400168380917644,
3.55956131753494));
#16394=CARTESIAN_POINT('Ctrl Pts',(11.4277257383569,-0.545971821618673,
3.69203362099157));
#16395=CARTESIAN_POINT('Ctrl Pts',(11.4118204596693,-0.619460506571779,
3.90409795935952));
#16396=CARTESIAN_POINT('Ctrl Pts',(11.3959151809817,-0.586891540696359,
4.09838336016249));
#16397=CARTESIAN_POINT('Ctrl Pts',(11.3800099022941,-0.554322574820941,
4.29266876096545));
#16398=CARTESIAN_POINT('Ctrl Pts',(11.3641046236065,-0.415695958117004,
4.46917522420345));
#16399=CARTESIAN_POINT('Ctrl Pts',(11.3481993449189,-0.234663168166497,
4.54685844933023));
#16400=CARTESIAN_POINT('Ctrl Pts',(11.3417480336984,-0.161234786808821,
4.57836740127901));
#16401=CARTESIAN_POINT('Ctrl Pts',(11.335296722478,-0.080829826651965,4.59361815176584));
#16402=CARTESIAN_POINT('Ctrl Pts',(11.3288454112576,-0.000294350894641693,
4.59325842069974));
#16403=CARTESIAN_POINT('Ctrl Pts',(11.2211545887425,0.000456638431143918,
4.59352536526061));
#16404=CARTESIAN_POINT('Ctrl Pts',(11.2317054196788,-0.131106980996848,
4.59258691018808));
#16405=CARTESIAN_POINT('Ctrl Pts',(11.2422562506151,-0.263229208150973,
4.54946171071576));
#16406=CARTESIAN_POINT('Ctrl Pts',(11.2528070815514,-0.366229002642205,
4.4690386804108));
#16407=CARTESIAN_POINT('Ctrl Pts',(11.268712360239,-0.521500226874852,4.34780171645731));
#16408=CARTESIAN_POINT('Ctrl Pts',(11.2846176389266,-0.610589908195122,
4.1418043885479));
#16409=CARTESIAN_POINT('Ctrl Pts',(11.3005229176142,-0.592591834014348,
3.94563195463032));
#16410=CARTESIAN_POINT('Ctrl Pts',(11.3164281963018,-0.574593759833574,
3.74945952071274));
#16411=CARTESIAN_POINT('Ctrl Pts',(11.3323334749894,-0.449507930151742,
3.56311198078699));
#16412=CARTESIAN_POINT('Ctrl Pts',(11.3482387536771,-0.274768466013715,
3.47215224147272));
#16413=CARTESIAN_POINT('Ctrl Pts',(11.3641440323647,-0.100029001875688,
3.38119250215845));
#16414=CARTESIAN_POINT('Ctrl Pts',(11.3800493110523,0.12436409671854,3.38562056345565));
#16415=CARTESIAN_POINT('Ctrl Pts',(11.3959545897399,0.295379012183608,3.48340324695247));
#16416=CARTESIAN_POINT('Ctrl Pts',(11.4118598684275,0.466393927648671,3.5811859304493));
#16417=CARTESIAN_POINT('Ctrl Pts',(11.4277651471151,0.584030659984583,3.77232323614575));
#16418=CARTESIAN_POINT('Ctrl Pts',(11.4436704258027,0.594275398502411,3.96905299961855));
#16419=CARTESIAN_POINT('Ctrl Pts',(11.4595757044903,0.60452013702024,4.16578276309136));
#16420=CARTESIAN_POINT('Ctrl Pts',(11.475480983178,0.507372881719984,4.36810498434052));
#16421=CARTESIAN_POINT('Ctrl Pts',(11.4913862618656,0.34743954227408,4.48312185891572));
#16422=CARTESIAN_POINT('Ctrl Pts',(11.5013090374912,0.247662438486696,4.55487707062799));
#16423=CARTESIAN_POINT('Ctrl Pts',(11.5112318131169,0.123448374926332,4.59265218509947));
#16424=CARTESIAN_POINT('Ctrl Pts',(11.5211545887425,-0.0003715675665865,
4.59335763259963));
#16425=CARTESIAN_POINT('Origin',(4.,0.,4.));
#16426=CARTESIAN_POINT('',(11.9288454112576,0.000492284285450728,4.5944814532616));
#16427=CARTESIAN_POINT('',(11.8211545887425,-0.000307672146732893,4.59488449882539));
#16428=CARTESIAN_POINT('',(4.,-7.27562663373442E-17,4.5941));
#16429=CARTESIAN_POINT('Ctrl Pts',(11.9288454112576,0.000492284285450728,
4.5944814532616));
#16430=CARTESIAN_POINT('Ctrl Pts',(11.9261600667293,0.0338400408399785,
4.59477876231094));
#16431=CARTESIAN_POINT('Ctrl Pts',(11.9234747222011,0.0671420792079604,
4.59221542322669));
#16432=CARTESIAN_POINT('Ctrl Pts',(11.9207893776729,0.0999293694653808,
4.5866302815369));
#16433=CARTESIAN_POINT('Ctrl Pts',(11.9048840989853,0.294128282668868,4.55354952256816));
#16434=CARTESIAN_POINT('Ctrl Pts',(11.8889788202977,0.470268877700486,4.41445832512751));
#16435=CARTESIAN_POINT('Ctrl Pts',(11.8730735416101,0.547474845215755,4.2332214826164));
#16436=CARTESIAN_POINT('Ctrl Pts',(11.8571682629225,0.624680812731027,4.05198464010529));
#16437=CARTESIAN_POINT('Ctrl Pts',(11.8412629842349,0.602952152729945,3.82860215252373));
#16438=CARTESIAN_POINT('Ctrl Pts',(11.8253577055472,0.492265746621211,3.66564180763548));
#16439=CARTESIAN_POINT('Ctrl Pts',(11.8094524268596,0.38157934051248,3.50268146274723));
#16440=CARTESIAN_POINT('Ctrl Pts',(11.793547148172,0.181935188296101,3.40014326055229));
#16441=CARTESIAN_POINT('Ctrl Pts',(11.7776418694844,-0.0149985615777061,
3.40510840546499));
#16442=CARTESIAN_POINT('Ctrl Pts',(11.7617365907968,-0.211932311451519,
3.41007355037768));
#16443=CARTESIAN_POINT('Ctrl Pts',(11.7458313121092,-0.406155658982761,
3.52254204239802));
#16444=CARTESIAN_POINT('Ctrl Pts',(11.7299260334216,-0.508489459897291,
3.69087310813977));
#16445=CARTESIAN_POINT('Ctrl Pts',(11.714020754734,-0.610823260811815,3.8592041738815));
#16446=CARTESIAN_POINT('Ctrl Pts',(11.6981154760463,-0.621267515109637,
4.08339781334463));
#16447=CARTESIAN_POINT('Ctrl Pts',(11.6822101973587,-0.53502666307716,4.26051379213839));
#16448=CARTESIAN_POINT('Ctrl Pts',(11.6663049186711,-0.448785811044678,
4.43762977093217));
#16449=CARTESIAN_POINT('Ctrl Pts',(11.6503996399835,-0.265859852681883,
4.56766808905658));
#16450=CARTESIAN_POINT('Ctrl Pts',(11.6344943612959,-0.070240649109886,
4.59092065229643));
#16451=CARTESIAN_POINT('Ctrl Pts',(11.6326113779498,-0.0470818155087989,
4.59367346098309));
#16452=CARTESIAN_POINT('Ctrl Pts',(11.6307283946037,-0.0237450789937817,
4.59492960773286));
#16453=CARTESIAN_POINT('Ctrl Pts',(11.6288454112576,-0.000389145320547679,
4.59475273347735));
#16454=CARTESIAN_POINT('Ctrl Pts',(11.5211545887425,-0.0003715675665865,
4.59335763259963));
#16455=CARTESIAN_POINT('Ctrl Pts',(11.5271370918045,-0.0750233800274846,
4.5937829512795));
#16456=CARTESIAN_POINT('Ctrl Pts',(11.5331195948664,-0.149531931096223,
4.58073359799715));
#16457=CARTESIAN_POINT('Ctrl Pts',(11.5391020979284,-0.218455391669058,
4.55353248138526));
#16458=CARTESIAN_POINT('Ctrl Pts',(11.555007376616,-0.40169756257477,4.48121470137836));
#16459=CARTESIAN_POINT('Ctrl Pts',(11.5709126553036,-0.545462480794654,
4.3088676134633));
#16460=CARTESIAN_POINT('Ctrl Pts',(11.5868179339912,-0.583739378074245,
4.1156257090067));
#16461=CARTESIAN_POINT('Ctrl Pts',(11.6027232126789,-0.622016275353834,
3.92238380455011));
#16462=CARTESIAN_POINT('Ctrl Pts',(11.6186284913665,-0.554805151693135,
3.70824708355197));
#16463=CARTESIAN_POINT('Ctrl Pts',(11.6345337700541,-0.412966511608993,
3.57153806891708));
#16464=CARTESIAN_POINT('Ctrl Pts',(11.6504390487417,-0.271127871524847,
3.43482905428217));
#16465=CARTESIAN_POINT('Ctrl Pts',(11.6663443274293,-0.0546617150172531,
3.37554774601052));
#16466=CARTESIAN_POINT('Ctrl Pts',(11.6822496061169,0.137039856773353,3.42091361287512));
#16467=CARTESIAN_POINT('Ctrl Pts',(11.6981548848045,0.328741428563947,3.46627947973972));
#16468=CARTESIAN_POINT('Ctrl Pts',(11.7140601634921,0.495678415637556,3.61629252174057));
#16469=CARTESIAN_POINT('Ctrl Pts',(11.7299654421798,0.56120041605148,3.80207309651931));
#16470=CARTESIAN_POINT('Ctrl Pts',(11.7458707208674,0.626722416465409,3.98785367129807));
#16471=CARTESIAN_POINT('Ctrl Pts',(11.761775999555,0.590829430219633,4.20940177885472));
#16472=CARTESIAN_POINT('Ctrl Pts',(11.7776812782426,0.470001998091193,4.36499190112672));
#16473=CARTESIAN_POINT('Ctrl Pts',(11.7921723817426,0.359917612963646,4.5067481450567));
#16474=CARTESIAN_POINT('Ctrl Pts',(11.8066634852425,0.179330777996457,4.59375393408315));
#16475=CARTESIAN_POINT('Ctrl Pts',(11.8211545887425,-0.000307672146732893,
4.59488449882539));
#16476=CARTESIAN_POINT('Origin',(4.,0.,4.));
#16477=CARTESIAN_POINT('',(12.2288454112576,0.000142795628640946,4.59314744373127));
#16478=CARTESIAN_POINT('',(12.1211545887425,0.00052868291625318,4.59430727435519));
#16479=CARTESIAN_POINT('',(4.,-7.27562663373442E-17,4.5941));
#16480=CARTESIAN_POINT('Ctrl Pts',(12.2288454112576,0.000142795628640946,
4.59314744373127));
#16481=CARTESIAN_POINT('Ctrl Pts',(12.221591738855,0.0907369315914116,4.59334157666405));
#16482=CARTESIAN_POINT('Ctrl Pts',(12.2143380664525,0.181251971066953,4.57388161006077));
#16483=CARTESIAN_POINT('Ctrl Pts',(12.2070843940499,0.261922584292681,4.53433840020651));
#16484=CARTESIAN_POINT('Ctrl Pts',(12.1911791153623,0.438810719578057,4.44763117963851));
#16485=CARTESIAN_POINT('Ctrl Pts',(12.1752738366747,0.56836661021043,4.26436322928705));
#16486=CARTESIAN_POINT('Ctrl Pts',(12.1593685579871,0.591103672269137,4.06868343852597));
#16487=CARTESIAN_POINT('Ctrl Pts',(12.1434632792995,0.613840734327844,3.87300364776488));
#16488=CARTESIAN_POINT('Ctrl Pts',(12.1275580006119,0.529758967812885,3.66491201659415));
#16489=CARTESIAN_POINT('Ctrl Pts',(12.1116527219243,0.377465162701742,3.53995541841648));
#16490=CARTESIAN_POINT('Ctrl Pts',(12.0957474432367,0.225171357590603,3.41499882023882));
#16491=CARTESIAN_POINT('Ctrl Pts',(12.0798421645491,0.00466551388328543,
3.37317725505421));
#16492=CARTESIAN_POINT('Ctrl Pts',(12.0639368858614,-0.182805413822737,
3.43369341627091));
#16493=CARTESIAN_POINT('Ctrl Pts',(12.0480316071738,-0.37027634152876,3.49420957748762));
#16494=CARTESIAN_POINT('Ctrl Pts',(12.0321263284862,-0.524712353233489,
3.65706346510565));
#16495=CARTESIAN_POINT('Ctrl Pts',(12.0162210497986,-0.575202966010955,
3.84747946371059));
#16496=CARTESIAN_POINT('Ctrl Pts',(12.000315771111,-0.625693578788423,4.03789546231555));
#16497=CARTESIAN_POINT('Ctrl Pts',(11.9844104924234,-0.572238792638624,
4.25587357190742));
#16498=CARTESIAN_POINT('Ctrl Pts',(11.9685052137358,-0.439382783876041,
4.40132746645495));
#16499=CARTESIAN_POINT('Ctrl Pts',(11.9552852795764,-0.328957325572706,
4.52222386487166));
#16500=CARTESIAN_POINT('Ctrl Pts',(11.942065345417,-0.163678510702966,4.59301780268865));
#16501=CARTESIAN_POINT('Ctrl Pts',(11.9288454112576,0.000492284285450728,
4.5944814532616));
#16502=CARTESIAN_POINT('Ctrl Pts',(11.8211545887425,-0.000307672146732893,
4.59488449882539));
#16503=CARTESIAN_POINT('Ctrl Pts',(11.8225687639301,-0.0178384446610953,
4.59499482973335));
#16504=CARTESIAN_POINT('Ctrl Pts',(11.8239829391178,-0.035360185088601,
4.59428731490513));
#16505=CARTESIAN_POINT('Ctrl Pts',(11.8253971143054,-0.0528064866265509,
4.59273302680715));
#16506=CARTESIAN_POINT('Ctrl Pts',(11.8413023929931,-0.249025661204777,
4.57525189322826));
#16507=CARTESIAN_POINT('Ctrl Pts',(11.8572076716807,-0.435702132350142,
4.45065748908313));
#16508=CARTESIAN_POINT('Ctrl Pts',(11.8731129503683,-0.527121962142897,
4.27615829360067));
#16509=CARTESIAN_POINT('Ctrl Pts',(11.8890182290559,-0.618541791935657,
4.10165909811819));
#16510=CARTESIAN_POINT('Ctrl Pts',(11.9049235077435,-0.614704980375792,
3.87725511129838));
#16511=CARTESIAN_POINT('Ctrl Pts',(11.9208287864311,-0.517373229009482,
3.70598315013913));
#16512=CARTESIAN_POINT('Ctrl Pts',(11.9367340651187,-0.420041477643178,
3.53471118897989));
#16513=CARTESIAN_POINT('Ctrl Pts',(11.9526393438063,-0.229214786470442,
3.41657125348121));
#16514=CARTESIAN_POINT('Ctrl Pts',(11.9685446224939,-0.0325126988662629,
3.4058082039356));
#16515=CARTESIAN_POINT('Ctrl Pts',(11.9844499011816,0.164189388737916,3.39504515438998));
#16516=CARTESIAN_POINT('Ctrl Pts',(12.0003551798692,0.366766872773537,3.49165899079743));
#16517=CARTESIAN_POINT('Ctrl Pts',(12.0162604585568,0.482204742918021,3.65128872687397));
#16518=CARTESIAN_POINT('Ctrl Pts',(12.0321657372444,0.597642613062508,3.81091846295053));
#16519=CARTESIAN_POINT('Ctrl Pts',(12.048071015932,0.625940869315854,4.03356409869619));
#16520=CARTESIAN_POINT('Ctrl Pts',(12.0639762946196,0.554106149607013,4.21699617753661));
#16521=CARTESIAN_POINT('Ctrl Pts',(12.0798815733072,0.482271429898174,4.40042825637702));
#16522=CARTESIAN_POINT('Ctrl Pts',(12.0957868519948,0.310303734227154,4.5446467783122));
#16523=CARTESIAN_POINT('Ctrl Pts',(12.1116921306825,0.117163353092859,4.583432699452));
#16524=CARTESIAN_POINT('Ctrl Pts',(12.1148462833691,0.0788619649798074,
4.59112427906975));
#16525=CARTESIAN_POINT('Ctrl Pts',(12.1180004360558,0.0397279339241207,
4.59466958677844));
#16526=CARTESIAN_POINT('Ctrl Pts',(12.1211545887425,0.00052868291625318,
4.59430727435519));
#16527=CARTESIAN_POINT('Origin',(4.,0.,4.));
#16528=CARTESIAN_POINT('',(12.5288454112576,-0.000545899910317726,4.59395595168017));
#16529=CARTESIAN_POINT('',(12.4211545887425,4.74932194801069E-5,4.59311952367199));
#16530=CARTESIAN_POINT('',(4.,-7.27562663373442E-17,4.5941));
#16531=CARTESIAN_POINT('Ctrl Pts',(12.5288454112576,-0.000545899910317726,
4.59395595168017));
#16532=CARTESIAN_POINT('Ctrl Pts',(12.5170234109807,0.14659828900878,4.5926299020853));
#16533=CARTESIAN_POINT('Ctrl Pts',(12.5052014107038,0.29463204299547,4.53735693360054));
#16534=CARTESIAN_POINT('Ctrl Pts',(12.493379410427,0.402483765871145,4.43832383497591));
#16535=CARTESIAN_POINT('Ctrl Pts',(12.4774741317394,0.547587104485886,4.30508504322883));
#16536=CARTESIAN_POINT('Ctrl Pts',(12.4615688530518,0.619957272242066,4.09263639239171));
#16537=CARTESIAN_POINT('Ctrl Pts',(12.4456635743641,0.586364949835353,3.89852531496775));
#16538=CARTESIAN_POINT('Ctrl Pts',(12.4297582956765,0.55277262742864,3.7044142375438));
#16539=CARTESIAN_POINT('Ctrl Pts',(12.4138530169889,0.41321781485904,3.52864073353302));
#16540=CARTESIAN_POINT('Ctrl Pts',(12.3979477383013,0.231778177981285,3.45191255961345));
#16541=CARTESIAN_POINT('Ctrl Pts',(12.3820424596137,0.0503385411035255,
3.37518438569388));
#16542=CARTESIAN_POINT('Ctrl Pts',(12.3661371809261,-0.172985920082391,
3.39750154186552));
#16543=CARTESIAN_POINT('Ctrl Pts',(12.3502319022385,-0.335654061078685,
3.50861693417539));
#16544=CARTESIAN_POINT('Ctrl Pts',(12.3343266235509,-0.498322202074975,
3.61973232648525));
#16545=CARTESIAN_POINT('Ctrl Pts',(12.3184213448632,-0.600334022881645,
3.81964595493332));
#16546=CARTESIAN_POINT('Ctrl Pts',(12.3025160661756,-0.594850011148503,
4.0165659389844));
#16547=CARTESIAN_POINT('Ctrl Pts',(12.286610787488,-0.58936599941536,4.21348592303547));
#16548=CARTESIAN_POINT('Ctrl Pts',(12.2707055088004,-0.476386155142398,
4.40741226268955));
#16549=CARTESIAN_POINT('Ctrl Pts',(12.2548002301128,-0.307786043036728,
4.50930218712431));
#16550=CARTESIAN_POINT('Ctrl Pts',(12.2461486238277,-0.216076754679914,
4.564724762732));
#16551=CARTESIAN_POINT('Ctrl Pts',(12.2374970175426,-0.107910718865932,
4.59291589733543));
#16552=CARTESIAN_POINT('Ctrl Pts',(12.2288454112576,0.000142795628640946,
4.59314744373127));
#16553=CARTESIAN_POINT('Ctrl Pts',(12.1211545887425,0.00052868291625318,
4.59430727435519));
#16554=CARTESIAN_POINT('Ctrl Pts',(12.1339057147434,-0.157940052872902,
4.59284257311225));
#16555=CARTESIAN_POINT('Ctrl Pts',(12.1466568407444,-0.317474678016714,
4.52751565545538));
#16556=CARTESIAN_POINT('Ctrl Pts',(12.1594079667453,-0.427372353356377,
4.41409399619463));
#16557=CARTESIAN_POINT('Ctrl Pts',(12.1753132454329,-0.564454612073754,
4.27261605145303));
#16558=CARTESIAN_POINT('Ctrl Pts',(12.1912185241205,-0.62430606291093,4.0563068416254));
#16559=CARTESIAN_POINT('Ctrl Pts',(12.2071238028081,-0.579445451749542,
3.8644864045766));
#16560=CARTESIAN_POINT('Ctrl Pts',(12.2230290814957,-0.534584840588155,
3.6726659675278));
#16561=CARTESIAN_POINT('Ctrl Pts',(12.2389343601834,-0.38501216742821,3.50533430325784));
#16562=CARTESIAN_POINT('Ctrl Pts',(12.254839638871,-0.199404875886796,3.43932303278057));
#16563=CARTESIAN_POINT('Ctrl Pts',(12.2707449175586,-0.0137975843453769,
3.37331176230329));
#16564=CARTESIAN_POINT('Ctrl Pts',(12.2866501962462,0.207844325577514,3.40862088561871));
#16565=CARTESIAN_POINT('Ctrl Pts',(12.3025554749338,0.363752265741203,3.52903794710619));
#16566=CARTESIAN_POINT('Ctrl Pts',(12.3184607536214,0.519660205904889,3.64945500859368));
#16567=CARTESIAN_POINT('Ctrl Pts',(12.334366032309,0.609834176309377,3.85498000825323));
#16568=CARTESIAN_POINT('Ctrl Pts',(12.3502713109967,0.592870104691008,4.05124456128685));
#16569=CARTESIAN_POINT('Ctrl Pts',(12.3661765896843,0.575906033072638,4.24750911432049));
#16570=CARTESIAN_POINT('Ctrl Pts',(12.3820818683719,0.451803919431404,4.4345132207282));
#16571=CARTESIAN_POINT('Ctrl Pts',(12.3979871470595,0.277546204023914,4.52639250633888));
#16572=CARTESIAN_POINT('Ctrl Pts',(12.4057096276205,0.192938958450368,4.57100260157974));
#16573=CARTESIAN_POINT('Ctrl Pts',(12.4134321081815,0.0965080911524262,
4.59318808505049));
#16574=CARTESIAN_POINT('Ctrl Pts',(12.4211545887425,4.74932194801069E-5,
4.59311952367199));
#16575=CARTESIAN_POINT('Origin',(4.,0.,4.));
#16576=CARTESIAN_POINT('',(12.8288454112576,0.000112157221815526,4.59505491513413));
#16577=CARTESIAN_POINT('',(12.7211545887425,-0.000546355209092884,4.59413239245978));
#16578=CARTESIAN_POINT('',(4.,-7.27562663373442E-17,4.5941));
#16579=CARTESIAN_POINT('Ctrl Pts',(12.8288454112576,0.000112157221815526,
4.59505491513413));
#16580=CARTESIAN_POINT('Ctrl Pts',(12.828360361794,0.00612048155630211,
4.59507046002904));
#16581=CARTESIAN_POINT('Ctrl Pts',(12.8278753123304,0.0121283652366354,
4.59498736156652));
#16582=CARTESIAN_POINT('Ctrl Pts',(12.8273902628668,0.0181332013859869,
4.59480429815638));
#16583=CARTESIAN_POINT('Ctrl Pts',(12.8114849841792,0.215038052543873,4.58880145767424));
#16584=CARTESIAN_POINT('Ctrl Pts',(12.7955797054916,0.408666038032992,4.47531104548453));
#16585=CARTESIAN_POINT('Ctrl Pts',(12.779674426804,0.510111378641258,4.30644305748136));
#16586=CARTESIAN_POINT('Ctrl Pts',(12.7637691481164,0.611556719249521,4.1375750694782));
#16587=CARTESIAN_POINT('Ctrl Pts',(12.7478638694288,0.620819414976937,3.9133295056616));
#16588=CARTESIAN_POINT('Ctrl Pts',(12.7319585907412,0.533646427817818,3.7366704418887));
#16589=CARTESIAN_POINT('Ctrl Pts',(12.7160533120536,0.446473440658691,3.56001137811579));
#16590=CARTESIAN_POINT('Ctrl Pts',(12.700148033366,0.26286477061301,3.43093881438659));
#16591=CARTESIAN_POINT('Ctrl Pts',(12.6842427546783,0.0671257511235207,
3.4087174113557));
#16592=CARTESIAN_POINT('Ctrl Pts',(12.6683374759907,-0.128613268365957,
3.38649600832481));
#16593=CARTESIAN_POINT('Ctrl Pts',(12.6524321973031,-0.336482637299241,
3.47112576599221));
#16594=CARTESIAN_POINT('Ctrl Pts',(12.6365269186155,-0.461037535689932,
3.62374828002683));
#16595=CARTESIAN_POINT('Ctrl Pts',(12.6206216399279,-0.585592434080627,
3.77637079406146));
#16596=CARTESIAN_POINT('Ctrl Pts',(12.6047163612403,-0.626832861928724,
3.9969860644633));
#16597=CARTESIAN_POINT('Ctrl Pts',(12.5888110825527,-0.565822959504995,
4.18429689252621));
#16598=CARTESIAN_POINT('Ctrl Pts',(12.5729058038651,-0.504813057081268,
4.37160772058911));
#16599=CARTESIAN_POINT('Ctrl Pts',(12.5570005251774,-0.341552824385721,
4.52561410631309));
#16600=CARTESIAN_POINT('Ctrl Pts',(12.5410952464898,-0.151004453301302,
4.57560283284656));
#16601=CARTESIAN_POINT('Ctrl Pts',(12.5370119680791,-0.102085973774189,
4.58843617527608));
#16602=CARTESIAN_POINT('Ctrl Pts',(12.5329286896683,-0.0513689988622793,
4.59441396466913));
#16603=CARTESIAN_POINT('Ctrl Pts',(12.5288454112576,-0.000545899910317726,
4.59395595168017));
#16604=CARTESIAN_POINT('Ctrl Pts',(12.4211545887425,4.74932194801069E-5,
4.59311952367199));
#16605=CARTESIAN_POINT('Ctrl Pts',(12.4293373868691,-0.102162877376194,
4.59304687552285));
#16606=CARTESIAN_POINT('Ctrl Pts',(12.4375201849957,-0.204406628577491,
4.5679880979308));
#16607=CARTESIAN_POINT('Ctrl Pts',(12.4457029831223,-0.292652646395614,
4.51814611323009));
#16608=CARTESIAN_POINT('Ctrl Pts',(12.4616082618099,-0.46418046423393,4.42126596969699));
#16609=CARTESIAN_POINT('Ctrl Pts',(12.4775135404976,-0.582822782736806,
4.23075121781716));
#16610=CARTESIAN_POINT('Ctrl Pts',(12.4934188191852,-0.594104068590283,
4.03407817163935));
#16611=CARTESIAN_POINT('Ctrl Pts',(12.5093240978728,-0.605385354443759,
3.83740512546155));
#16612=CARTESIAN_POINT('Ctrl Pts',(12.5252293765604,-0.509305607647849,
3.63457378498577));
#16613=CARTESIAN_POINT('Ctrl Pts',(12.541134655248,-0.34998058313236,3.51871572067214));
#16614=CARTESIAN_POINT('Ctrl Pts',(12.5570399339356,-0.19065555861687,3.4028576563585));
#16615=CARTESIAN_POINT('Ctrl Pts',(12.5729452126232,0.031914743618199,3.37397286820701));
#16616=CARTESIAN_POINT('Ctrl Pts',(12.5888504913108,0.215535456959467,3.44532402892222));
#16617=CARTESIAN_POINT('Ctrl Pts',(12.6047557699985,0.399156170300736,3.51667518963742));
#16618=CARTESIAN_POINT('Ctrl Pts',(12.6206610486861,0.543827294748204,3.68826229921932));
#16619=CARTESIAN_POINT('Ctrl Pts',(12.6365663273737,0.583121970486127,3.88129981619987));
#16620=CARTESIAN_POINT('Ctrl Pts',(12.6524716060613,0.622416646224052,4.07433733318042));
#16621=CARTESIAN_POINT('Ctrl Pts',(12.6683768847489,0.556334873252426,4.28882525755962));
#16622=CARTESIAN_POINT('Ctrl Pts',(12.6842821634365,0.415218606030559,4.42627980869829));
#16623=CARTESIAN_POINT('Ctrl Pts',(12.6965729718718,0.306170972122536,4.53249785050629));
#16624=CARTESIAN_POINT('Ctrl Pts',(12.7088637803072,0.152317016475741,4.59271595401221));
#16625=CARTESIAN_POINT('Ctrl Pts',(12.7211545887425,-0.000546355209092884,
4.59413239245978));
#16626=CARTESIAN_POINT('Origin',(4.,0.,4.));
#16627=CARTESIAN_POINT('',(13.1288454112576,0.000488576923893258,4.59361798633976));
#16628=CARTESIAN_POINT('',(13.0211545887425,0.000215375668158819,4.59498635240753));
#16629=CARTESIAN_POINT('',(4.,-7.27562663373442E-17,4.5941));
#16630=CARTESIAN_POINT('Ctrl Pts',(13.1288454112576,0.000488576923893258,
4.59361798633976));
#16631=CARTESIAN_POINT('Ctrl Pts',(13.1237920339197,0.0634769139372694,
4.59410397103046));
#16632=CARTESIAN_POINT('Ctrl Pts',(13.1187386565818,0.126326538027094,4.58487602541266));
#16633=CARTESIAN_POINT('Ctrl Pts',(13.1136852792439,0.185787091792062,4.56533540718874));
#16634=CARTESIAN_POINT('Ctrl Pts',(13.0977800005563,0.372936519850693,4.50383218710482));
#16635=CARTESIAN_POINT('Ctrl Pts',(13.0818747218686,0.526512210440984,4.34016674272733));
#16636=CARTESIAN_POINT('Ctrl Pts',(13.065969443181,0.575998703695535,4.14948732200047));
#16637=CARTESIAN_POINT('Ctrl Pts',(13.0500641644934,0.625485196950086,3.9588079012736));
#16638=CARTESIAN_POINT('Ctrl Pts',(13.0341588858058,0.570882492868891,3.74111450419737));
#16639=CARTESIAN_POINT('Ctrl Pts',(13.0182536071182,0.437261843116128,3.59636272886105));
#16640=CARTESIAN_POINT('Ctrl Pts',(13.0023483284306,0.303641193363369,3.45161095352474));
#16641=CARTESIAN_POINT('Ctrl Pts',(12.986443049743,0.0910025979390456,3.37980079992835));
#16642=CARTESIAN_POINT('Ctrl Pts',(12.9705377710554,-0.10301929613509,3.41390445256627));
#16643=CARTESIAN_POINT('Ctrl Pts',(12.9546324923678,-0.297041190209231,
3.4480081052042));
#16644=CARTESIAN_POINT('Ctrl Pts',(12.9387272136801,-0.472446382933184,
3.58802556407645));
#16645=CARTESIAN_POINT('Ctrl Pts',(12.9228219349925,-0.54869623058984,3.76966673571907));
#16646=CARTESIAN_POINT('Ctrl Pts',(12.9069166563049,-0.624946078246494,
3.95130790736168));
#16647=CARTESIAN_POINT('Ctrl Pts',(12.8910113776173,-0.602040580835857,
4.17457279177466));
#16648=CARTESIAN_POINT('Ctrl Pts',(12.8751060989297,-0.490496973717212,
4.33694759959386));
#16649=CARTESIAN_POINT('Ctrl Pts',(12.8596858697056,-0.382355015061345,
4.49437060399126));
#16650=CARTESIAN_POINT('Ctrl Pts',(12.8442656404816,-0.190898750836606,
4.59456072668396));
#16651=CARTESIAN_POINT('Ctrl Pts',(12.8288454112576,0.000112157221815526,
4.59505491513413));
#16652=CARTESIAN_POINT('Ctrl Pts',(12.7211545887425,-0.000546355209092884,
4.59413239245978));
#16653=CARTESIAN_POINT('Ctrl Pts',(12.7247690589948,-0.0455002825709059,
4.59454893744622));
#16654=CARTESIAN_POINT('Ctrl Pts',(12.7283835292471,-0.0903685417208244,
4.58988016539195));
#16655=CARTESIAN_POINT('Ctrl Pts',(12.7319979994994,-0.13398639330236,4.5798004937111));
#16656=CARTESIAN_POINT('Ctrl Pts',(12.747903278187,-0.325924363941296,4.53544544968711));
#16657=CARTESIAN_POINT('Ctrl Pts',(12.7638085568746,-0.493649543747071,
4.38631418374101));
#16658=CARTESIAN_POINT('Ctrl Pts',(12.7797138355622,-0.560149626020051,
4.20088146397168));
#16659=CARTESIAN_POINT('Ctrl Pts',(12.7956191142498,-0.626649708293032,
4.01544874420235));
#16660=CARTESIAN_POINT('Ctrl Pts',(12.8115243929374,-0.591924693033219,
3.79371457060979));
#16661=CARTESIAN_POINT('Ctrl Pts',(12.827429671625,-0.471918838153678,3.63748989490844));
#16662=CARTESIAN_POINT('Ctrl Pts',(12.8433349503126,-0.351912983274129,
3.48126521920708));
#16663=CARTESIAN_POINT('Ctrl Pts',(12.8592402290002,-0.146626288774854,
3.39055004139693));
#16664=CARTESIAN_POINT('Ctrl Pts',(12.8751455076879,0.0496822801939141,
3.40699693328572));
#16665=CARTESIAN_POINT('Ctrl Pts',(12.8910507863755,0.245990849162665,3.42344382517451));
#16666=CARTESIAN_POINT('Ctrl Pts',(12.9069560650631,0.433321292600904,3.54705278676224));
#16667=CARTESIAN_POINT('Ctrl Pts',(12.9228613437507,0.525659396179275,3.72106781235173));
#16668=CARTESIAN_POINT('Ctrl Pts',(12.9387666224383,0.617997499757654,3.89508283794124));
#16669=CARTESIAN_POINT('Ctrl Pts',(12.9546719011259,0.615343263476151,4.11950392753251));
#16670=CARTESIAN_POINT('Ctrl Pts',(12.9705771798135,0.518915400343756,4.29128641125856));
#16671=CARTESIAN_POINT('Ctrl Pts',(12.9864824585012,0.422487537211366,4.46306889498459));
#16672=CARTESIAN_POINT('Ctrl Pts',(13.0023877371888,0.232286047228094,4.58221277284539));
#16673=CARTESIAN_POINT('Ctrl Pts',(13.0182930158764,0.0356434078328121,
4.59401221668908));
#16674=CARTESIAN_POINT('Ctrl Pts',(13.0192468734984,0.0238505254767134,
4.59471984273368));
#16675=CARTESIAN_POINT('Ctrl Pts',(13.0202007311205,0.0120344772878951,
4.59504140054066));
#16676=CARTESIAN_POINT('Ctrl Pts',(13.0211545887425,0.000215375668158819,
4.59498635240753));
#16677=CARTESIAN_POINT('Origin',(4.,0.,4.));
#16678=CARTESIAN_POINT('',(13.4288454112576,-0.000323145728561625,4.59329116515504));
#16679=CARTESIAN_POINT('',(13.3211545887425,0.000436239896754628,4.59347700091179));
#16680=CARTESIAN_POINT('',(4.,-7.27562663373442E-17,4.5941));
#16681=CARTESIAN_POINT('Ctrl Pts',(13.4288454112576,-0.000323145728561625,
4.59329116515504));
#16682=CARTESIAN_POINT('Ctrl Pts',(13.4192237060453,0.11977362227264,4.59270025156928));
#16683=CARTESIAN_POINT('Ctrl Pts',(13.4096020008331,0.240190260834984,4.55734300206483));
#16684=CARTESIAN_POINT('Ctrl Pts',(13.3999802956209,0.338238798929947,4.48960747645051));
#16685=CARTESIAN_POINT('Ctrl Pts',(13.3840750169333,0.500319146323361,4.37763642888821));
#16686=CARTESIAN_POINT('Ctrl Pts',(13.3681697382457,0.601276083433826,4.17718801339723));
#16687=CARTESIAN_POINT('Ctrl Pts',(13.3522644595581,0.594754455875995,3.9802996620979));
#16688=CARTESIAN_POINT('Ctrl Pts',(13.3363591808704,0.588232828318166,3.78341131079859));
#16689=CARTESIAN_POINT('Ctrl Pts',(13.3204539021828,0.474232636092054,3.59008302369095));
#16690=CARTESIAN_POINT('Ctrl Pts',(13.3045486234952,0.305097944517489,3.48908297116948));
#16691=CARTESIAN_POINT('Ctrl Pts',(13.2886433448076,0.135963252942929,3.388082918648));
#16692=CARTESIAN_POINT('Ctrl Pts',(13.27273806612,-0.0883059379800925,3.3794111007127));
#16693=CARTESIAN_POINT('Ctrl Pts',(13.2568327874324,-0.264734703826722,
3.46704924928509));
#16694=CARTESIAN_POINT('Ctrl Pts',(13.2409275087448,-0.441163469673367,
3.55468739785749));
#16695=CARTESIAN_POINT('Ctrl Pts',(13.2250222300572,-0.569751810443623,
3.7386355129376));
#16696=CARTESIAN_POINT('Ctrl Pts',(13.2091169513696,-0.591457400179852,
3.9344324022836));
#16697=CARTESIAN_POINT('Ctrl Pts',(13.1932116726819,-0.613162989916079,
4.1302292916296));
#16698=CARTESIAN_POINT('Ctrl Pts',(13.1773063939943,-0.527985828618295,
4.33787495524147));
#16699=CARTESIAN_POINT('Ctrl Pts',(13.1614011153067,-0.375035665205916,
4.46202728915223));
#16700=CARTESIAN_POINT('Ctrl Pts',(13.150549213957,-0.270680367988337,4.54673431669939));
#16701=CARTESIAN_POINT('Ctrl Pts',(13.1396973126073,-0.134776053786733,
4.59257435599745));
#16702=CARTESIAN_POINT('Ctrl Pts',(13.1288454112576,0.000488576923893258,
4.59361798633976));
#16703=CARTESIAN_POINT('Ctrl Pts',(13.0211545887425,0.000215375668158819,
4.59498635240753));
#16704=CARTESIAN_POINT('Ctrl Pts',(13.0361060098081,-0.185045360160338,
4.59412349007018));
#16705=CARTESIAN_POINT('Ctrl Pts',(13.0510574308736,-0.371056311319581,
4.5007301079696));
#16706=CARTESIAN_POINT('Ctrl Pts',(13.0660088519392,-0.480360474535337,
4.35124746348123));
#16707=CARTESIAN_POINT('Ctrl Pts',(13.0819141306268,-0.596637928700896,
4.19222825660313));
#16708=CARTESIAN_POINT('Ctrl Pts',(13.0978194093145,-0.626109048224722,
3.96973483302036));
#16709=CARTESIAN_POINT('Ctrl Pts',(13.1137246880021,-0.555241941841719,
3.78592675992164));
#16710=CARTESIAN_POINT('Ctrl Pts',(13.1296299666897,-0.484374835458714,
3.60211868682292));
#16711=CARTESIAN_POINT('Ctrl Pts',(13.1455352453773,-0.313169503168878,
3.45699596420825));
#16712=CARTESIAN_POINT('Ctrl Pts',(13.1614405240649,-0.120236190459409,
3.4171928066662));
#16713=CARTESIAN_POINT('Ctrl Pts',(13.1773458027525,0.0726971222500488,
3.37738964912416));
#16714=CARTESIAN_POINT('Ctrl Pts',(13.1932510814401,0.287358415379145,3.44290605665475));
#16715=CARTESIAN_POINT('Ctrl Pts',(13.2091563601277,0.425184304693362,3.58365966669054));
#16716=CARTESIAN_POINT('Ctrl Pts',(13.2250616388154,0.563010194007583,3.72441327672633));
#16717=CARTESIAN_POINT('Ctrl Pts',(13.240966917503,0.624000679506934,3.94040408926733));
#16718=CARTESIAN_POINT('Ctrl Pts',(13.2568721961906,0.580151510544767,4.13245826101242));
#16719=CARTESIAN_POINT('Ctrl Pts',(13.2727774748782,0.536302341582597,4.32451243275751));
#16720=CARTESIAN_POINT('Ctrl Pts',(13.2886827535658,0.387613518158899,4.49262996370669));
#16721=CARTESIAN_POINT('Ctrl Pts',(13.3045880322534,0.202356657484476,4.55961839611428));
#16722=CARTESIAN_POINT('Ctrl Pts',(13.3101102177498,0.13803695776657,4.58287624384712));
#16723=CARTESIAN_POINT('Ctrl Pts',(13.3156324032461,0.0693092633201986,
4.59394375907155));
#16724=CARTESIAN_POINT('Ctrl Pts',(13.3211545887425,0.000436239896754628,
4.59347700091179));
#16725=CARTESIAN_POINT('Origin',(4.,0.,4.));
#16726=CARTESIAN_POINT('',(13.7288454112576,-0.000361622974213827,4.59480268714608));
#16727=CARTESIAN_POINT('',(13.6211545887425,-0.000396530615921017,4.59339874939382));
#16728=CARTESIAN_POINT('',(4.,-7.27562663373442E-17,4.5941));
#16729=CARTESIAN_POINT('Ctrl Pts',(13.7288454112576,-0.000361622974213827,
4.59480268714608));
#16730=CARTESIAN_POINT('Ctrl Pts',(13.714655378171,0.175608319374377,4.59354294412002));
#16731=CARTESIAN_POINT('Ctrl Pts',(13.7004653450845,0.352610168065205,4.51056419690263));
#16732=CARTESIAN_POINT('Ctrl Pts',(13.6862753119979,0.463013835099274,4.37381700684221));
#16733=CARTESIAN_POINT('Ctrl Pts',(13.6703700333103,0.586762742631886,4.22054025587244));
#16734=CARTESIAN_POINT('Ctrl Pts',(13.6544647546227,0.626840040937572,3.99971072753873));
#16735=CARTESIAN_POINT('Ctrl Pts',(13.6385594759351,0.564843930165024,3.81272399872504));
#16736=CARTESIAN_POINT('Ctrl Pts',(13.6226541972475,0.502847819392478,3.62573726991136));
#16737=CARTESIAN_POINT('Ctrl Pts',(13.6067489185599,0.338778299541704,3.4725933406177));
#16738=CARTESIAN_POINT('Ctrl Pts',(13.5908436398723,0.147969152919217,3.42360942419035));
#16739=CARTESIAN_POINT('Ctrl Pts',(13.5749383611846,-0.0428399937032757,
3.37462550776301));
#16740=CARTESIAN_POINT('Ctrl Pts',(13.559033082497,-0.260388767097474,3.42980160420198));
#16741=CARTESIAN_POINT('Ctrl Pts',(13.5431278038094,-0.404787974250376,
3.56380318433064));
#16742=CARTESIAN_POINT('Ctrl Pts',(13.5272225251218,-0.549187181403275,
3.6978047644593));
#16743=CARTESIAN_POINT('Ctrl Pts',(13.5113172464342,-0.620436822314871,
3.91063182827765));
#16744=CARTESIAN_POINT('Ctrl Pts',(13.4954119677466,-0.585822076202281,
4.10456319205082));
#16745=CARTESIAN_POINT('Ctrl Pts',(13.479506689059,-0.551207330089691,4.298494555824));
#16746=CARTESIAN_POINT('Ctrl Pts',(13.4636014103714,-0.410728196952908,
4.47353021955202));
#16747=CARTESIAN_POINT('Ctrl Pts',(13.4476961316837,-0.228886751546343,
4.54930121159921));
#16748=CARTESIAN_POINT('Ctrl Pts',(13.4414125582084,-0.15704808052867,4.57923546205676));
#16749=CARTESIAN_POINT('Ctrl Pts',(13.435128984733,-0.0787538239969463,
4.5936770685736));
#16750=CARTESIAN_POINT('Ctrl Pts',(13.4288454112576,-0.000323145728561625,
4.59329116515504));
#16751=CARTESIAN_POINT('Ctrl Pts',(13.3211545887425,0.000436239896754628,
4.59347700091179));
#16752=CARTESIAN_POINT('Ctrl Pts',(13.3315376819337,-0.129062311182503,
4.59259937855127));
#16753=CARTESIAN_POINT('Ctrl Pts',(13.341920775125,-0.259074650003773,4.55094414667863));
#16754=CARTESIAN_POINT('Ctrl Pts',(13.3523038683163,-0.361265427801182,
4.47287234722855));
#16755=CARTESIAN_POINT('Ctrl Pts',(13.3682091470039,-0.517805754487323,
4.35327853206923));
#16756=CARTESIAN_POINT('Ctrl Pts',(13.3841144256915,-0.609061509934468,
4.14823156788458));
#16757=CARTESIAN_POINT('Ctrl Pts',(13.4000197043791,-0.593131911953917,
3.95188034580653));
#16758=CARTESIAN_POINT('Ctrl Pts',(13.4159249830667,-0.577202313973367,
3.75552912372848));
#16759=CARTESIAN_POINT('Ctrl Pts',(13.4318302617543,-0.454087362565127,
3.56787364375704));
#16760=CARTESIAN_POINT('Ctrl Pts',(13.4477355404419,-0.280316234851803,
3.47507736324643));
#16761=CARTESIAN_POINT('Ctrl Pts',(13.4636408191295,-0.106545107138479,
3.38228108273583));
#16762=CARTESIAN_POINT('Ctrl Pts',(13.4795460978172,0.117882196879929,3.38434400168606));
#16763=CARTESIAN_POINT('Ctrl Pts',(13.4954513765048,0.2899181539344,3.48031891499009));
#16764=CARTESIAN_POINT('Ctrl Pts',(13.5113566551924,0.461954110988876,3.57629382829412));
#16765=CARTESIAN_POINT('Ctrl Pts',(13.52726193388,0.581598721079409,3.76618073595195));
#16766=CARTESIAN_POINT('Ctrl Pts',(13.5431672125676,0.593916240998451,3.96279160341967));
#16767=CARTESIAN_POINT('Ctrl Pts',(13.5590724912552,0.606233760917493,4.15940247088739));
#16768=CARTESIAN_POINT('Ctrl Pts',(13.5749777699428,0.511224190665043,4.362737298165));
#16769=CARTESIAN_POINT('Ctrl Pts',(13.5908830486304,0.352511905377589,4.47943333495374));
#16770=CARTESIAN_POINT('Ctrl Pts',(13.6009735620011,0.251822790258117,4.55346680161908));
#16771=CARTESIAN_POINT('Ctrl Pts',(13.6110640753718,0.125494626822297,4.59262991567553));
#16772=CARTESIAN_POINT('Ctrl Pts',(13.6211545887425,-0.000396530615921017,
4.59339874939382));
#16773=CARTESIAN_POINT('Origin',(4.,0.,4.));
#16774=CARTESIAN_POINT('',(14.0288454112576,0.000507412974116619,4.59441995931617));
#16775=CARTESIAN_POINT('',(13.9211545887425,-0.000275297881949146,4.59492513410986));
#16776=CARTESIAN_POINT('',(4.,-7.27562663373442E-17,4.5941));
#16777=CARTESIAN_POINT('Ctrl Pts',(14.0288454112576,0.000507412974116619,
4.59441995931617));
#16778=CARTESIAN_POINT('Ctrl Pts',(14.0259923289843,0.0359476882196221,
4.59474138052009));
#16779=CARTESIAN_POINT('Ctrl Pts',(14.0231392467111,0.0713355155074759,
4.59184535342408));
#16780=CARTESIAN_POINT('Ctrl Pts',(14.0202861644378,0.106106362061302,4.58554453803953));
#16781=CARTESIAN_POINT('Ctrl Pts',(14.0043808857502,0.299945849210873,4.55041893875697));
#16782=CARTESIAN_POINT('Ctrl Pts',(13.9884756070626,0.474610768799237,4.40947910659883));
#16783=CARTESIAN_POINT('Ctrl Pts',(13.972570328375,0.549902379214768,4.22743864981956));
#16784=CARTESIAN_POINT('Ctrl Pts',(13.9566650496873,0.625193989630293,4.04539819304031));
#16785=CARTESIAN_POINT('Ctrl Pts',(13.9407597709997,0.601112290873006,3.82225711163994));
#16786=CARTESIAN_POINT('Ctrl Pts',(13.9248544923121,0.488714580199595,3.66047234987686));
#16787=CARTESIAN_POINT('Ctrl Pts',(13.9089492136245,0.376316869526181,3.49868758811377));
#16788=CARTESIAN_POINT('Ctrl Pts',(13.8930439349369,0.175603146936639,3.39825914598798));
#16789=CARTESIAN_POINT('Ctrl Pts',(13.8771386562493,-0.0212673376532481,
3.40529951534663));
#16790=CARTESIAN_POINT('Ctrl Pts',(13.8612333775617,-0.218137822243141,
3.41233988470529));
#16791=CARTESIAN_POINT('Ctrl Pts',(13.8453280988741,-0.411165068833379,
3.52684906554841));
#16792=CARTESIAN_POINT('Ctrl Pts',(13.8294228201864,-0.511719132099071,
3.69624928651676));
#16793=CARTESIAN_POINT('Ctrl Pts',(13.8135175414988,-0.612273195364761,
3.8656495074851));
#16794=CARTESIAN_POINT('Ctrl Pts',(13.7976122628112,-0.62035407530591,4.08994076857866));
#16795=CARTESIAN_POINT('Ctrl Pts',(13.7817069841236,-0.532251373727382,
4.26613801168402));
#16796=CARTESIAN_POINT('Ctrl Pts',(13.765801705436,-0.44414867214885,4.44233525478938));
#16797=CARTESIAN_POINT('Ctrl Pts',(13.7498964267484,-0.259862389050636,
4.57043847990653));
#16798=CARTESIAN_POINT('Ctrl Pts',(13.7339911480608,-0.0640089891217576,
4.59162810566218));
#16799=CARTESIAN_POINT('Ctrl Pts',(13.7322759024597,-0.0428879079209441,
4.59391322201126));
#16800=CARTESIAN_POINT('Ctrl Pts',(13.7305606568586,-0.0216323041412813,
4.594954960835));
#16801=CARTESIAN_POINT('Ctrl Pts',(13.7288454112576,-0.000361622974213827,
4.59480268714608));
#16802=CARTESIAN_POINT('Ctrl Pts',(13.6211545887425,-0.000396530615921017,
4.59339874939382));
#16803=CARTESIAN_POINT('Ctrl Pts',(13.6269693540594,-0.0729426448807452,
4.59384179797573));
#16804=CARTESIAN_POINT('Ctrl Pts',(13.6327841193764,-0.145343639818557,
4.58153501668255));
#16805=CARTESIAN_POINT('Ctrl Pts',(13.6385988846933,-0.212609537044371,
4.5558040579697));
#16806=CARTESIAN_POINT('Ctrl Pts',(13.6545041633809,-0.396603693856438,
4.48542149789704));
#16807=CARTESIAN_POINT('Ctrl Pts',(13.6704094420685,-0.542177007158105,
4.31459913145184));
#16808=CARTESIAN_POINT('Ctrl Pts',(13.6863147207561,-0.582488370180261,
4.12177136240739));
#16809=CARTESIAN_POINT('Ctrl Pts',(13.7022199994437,-0.622799733202417,
3.92894359336294));
#16810=CARTESIAN_POINT('Ctrl Pts',(13.7181252781313,-0.557849145945042,
3.71411042171923));
#16811=CARTESIAN_POINT('Ctrl Pts',(13.734030556819,-0.417459170243993,3.57591415105311));
#16812=CARTESIAN_POINT('Ctrl Pts',(13.7499358355066,-0.277069194542941,
3.43771788038699));
#16813=CARTESIAN_POINT('Ctrl Pts',(13.7658411141942,-0.0612398303982075,
3.37615851069845));
#16814=CARTESIAN_POINT('Ctrl Pts',(13.7817463928818,0.130929209162332,3.41950150018632));
#16815=CARTESIAN_POINT('Ctrl Pts',(13.7976516715694,0.323098248722867,3.46284448967418));
#16816=CARTESIAN_POINT('Ctrl Pts',(13.813556950257,0.491606963699209,3.61108983833845));
#16817=CARTESIAN_POINT('Ctrl Pts',(13.8294622289446,0.559083281190044,3.79616955381596));
#16818=CARTESIAN_POINT('Ctrl Pts',(13.8453675076322,0.62655959868088,3.98124926929349));
#16819=CARTESIAN_POINT('Ctrl Pts',(13.8612727863198,0.593003518686204,4.20316335158427));
#16820=CARTESIAN_POINT('Ctrl Pts',(13.8771780650075,0.4738225734989,4.36001824251097));
#16821=CARTESIAN_POINT('Ctrl Pts',(13.8918369062525,0.363981395029584,4.50458099992985));
#16822=CARTESIAN_POINT('Ctrl Pts',(13.9064957474975,0.181409709145346,4.59388191268165));
#16823=CARTESIAN_POINT('Ctrl Pts',(13.9211545887425,-0.000275297881949146,
4.59492513410986));
#16824=CARTESIAN_POINT('Origin',(4.,0.,4.));
#16825=CARTESIAN_POINT('',(14.3288454112576,0.000109044058801022,4.5931342436645));
#16826=CARTESIAN_POINT('',(14.2211545887425,0.000537210645871958,4.59424369460725));
#16827=CARTESIAN_POINT('',(4.,-7.27562663373442E-17,4.5941));
#16828=CARTESIAN_POINT('Ctrl Pts',(14.3288454112576,0.000109044058801022,
4.5931342436645));
#16829=CARTESIAN_POINT('Ctrl Pts',(14.32142400111,0.0928032711674493,4.59328573107644));
#16830=CARTESIAN_POINT('Ctrl Pts',(14.3140025909624,0.185434358886594,4.57287353691408));
#16831=CARTESIAN_POINT('Ctrl Pts',(14.3065811808148,0.267539471941071,4.53154830171049));
#16832=CARTESIAN_POINT('Ctrl Pts',(14.2906759021272,0.443503969097433,4.44298165875801));
#16833=CARTESIAN_POINT('Ctrl Pts',(14.2747706234396,0.571121189235106,4.25835848700565));
#16834=CARTESIAN_POINT('Ctrl Pts',(14.258865344752,0.591794703906212,4.06244993615984));
#16835=CARTESIAN_POINT('Ctrl Pts',(14.2429600660644,0.612468218577319,3.86654138531401));
#16836=CARTESIAN_POINT('Ctrl Pts',(14.2270547873768,0.526198027781844,3.65934745537473));
#16837=CARTESIAN_POINT('Ctrl Pts',(14.2111495086891,0.372595753342289,3.53600283331781));
#16838=CARTESIAN_POINT('Ctrl Pts',(14.1952442300015,0.218993478902743,3.4126582112609));
#16839=CARTESIAN_POINT('Ctrl Pts',(14.1793389513139,-0.00194087918087354,
3.37316289708635));
#16840=CARTESIAN_POINT('Ctrl Pts',(14.1634336726263,-0.18876361063844,3.43565146815417));
#16841=CARTESIAN_POINT('Ctrl Pts',(14.1475283939387,-0.375586342096006,
3.49814003922198));
#16842=CARTESIAN_POINT('Ctrl Pts',(14.1316231152511,-0.528297446927522,
3.66261249553216));
#16843=CARTESIAN_POINT('Ctrl Pts',(14.1157178365635,-0.576778446468407,
3.85355004340287));
#16844=CARTESIAN_POINT('Ctrl Pts',(14.0998125578759,-0.625259446009293,
4.04448759127359));
#16845=CARTESIAN_POINT('Ctrl Pts',(14.0839072791882,-0.569510340259543,
4.26189023070484));
#16846=CARTESIAN_POINT('Ctrl Pts',(14.0680020005006,-0.435128760029281,
4.40593586721696));
#16847=CARTESIAN_POINT('Ctrl Pts',(14.0549498040863,-0.324852491748397,
4.52414265738481));
#16848=CARTESIAN_POINT('Ctrl Pts',(14.0418976076719,-0.161623710204441,
4.5929495310973));
#16849=CARTESIAN_POINT('Ctrl Pts',(14.0288454112576,0.000507412974116619,
4.59441995931617));
#16850=CARTESIAN_POINT('Ctrl Pts',(13.9211545887425,-0.000275297881949146,
4.59492513410986));
#16851=CARTESIAN_POINT('Ctrl Pts',(13.9224010261851,-0.015723926578741,
4.59501383895544));
#16852=CARTESIAN_POINT('Ctrl Pts',(13.9236474636277,-0.0311661445373128,
4.59446443570748));
#16853=CARTESIAN_POINT('Ctrl Pts',(13.9248939010703,-0.0465566941337027,
4.59325663951544));
#16854=CARTESIAN_POINT('Ctrl Pts',(13.9407991797579,-0.242949206199084,
4.5778444460306));
#16855=CARTESIAN_POINT('Ctrl Pts',(13.9567044584455,-0.430928419949921,
4.4552243594983));
#16856=CARTESIAN_POINT('Ctrl Pts',(13.9726097371331,-0.524182233176515,
4.28169833602613));
#16857=CARTESIAN_POINT('Ctrl Pts',(13.9885150158207,-0.617436046403107,
4.10817231255396));
#16858=CARTESIAN_POINT('Ctrl Pts',(14.0044202945084,-0.615964459105464,
3.88374035214192));
#16859=CARTESIAN_POINT('Ctrl Pts',(14.020325573196,-0.52044316191294,3.71145211607799));
#16860=CARTESIAN_POINT('Ctrl Pts',(14.0362308518836,-0.424921864720413,
3.53916388001405));
#16861=CARTESIAN_POINT('Ctrl Pts',(14.0521361305712,-0.235350857633014,
3.41901936829824));
#16862=CARTESIAN_POINT('Ctrl Pts',(14.0680414092588,-0.0387731270173405,
3.40618385781531));
#16863=CARTESIAN_POINT('Ctrl Pts',(14.0839466879464,0.157804603598333,3.39334834733239));
#16864=CARTESIAN_POINT('Ctrl Pts',(14.0998519666341,0.361389057742269,3.48782183808236));
#16865=CARTESIAN_POINT('Ctrl Pts',(14.1157572453217,0.478502867019537,3.64622609995664));
#16866=CARTESIAN_POINT('Ctrl Pts',(14.1316625240093,0.595616676296804,3.80463036183091));
#16867=CARTESIAN_POINT('Ctrl Pts',(14.1475678026969,0.626259840707404,4.02696539482948));
#16868=CARTESIAN_POINT('Ctrl Pts',(14.1634730813845,0.556362315559365,4.21114435801894));
#16869=CARTESIAN_POINT('Ctrl Pts',(14.1793783600721,0.486464790411328,4.3953233212084));
#16870=CARTESIAN_POINT('Ctrl Pts',(14.1952836387597,0.316026575704654,4.54134621458875));
#16871=CARTESIAN_POINT('Ctrl Pts',(14.2111889174473,0.123305688986428,4.58216550323889));
#16872=CARTESIAN_POINT('Ctrl Pts',(14.2145108078791,0.0830550475387342,
4.59069079896363));
#16873=CARTESIAN_POINT('Ctrl Pts',(14.2178326983108,0.0418324306113591,
4.59462708830176));
#16874=CARTESIAN_POINT('Ctrl Pts',(14.2211545887425,0.000537210645871958,
4.59424369460725));
#16875=CARTESIAN_POINT('Origin',(4.,0.,4.));
#16876=CARTESIAN_POINT('',(14.6288454112575,-0.000548182068839831,4.59401855345973));
#16877=CARTESIAN_POINT('',(14.5211545887425,1.28950532977596E-5,4.59311636453746));
#16878=CARTESIAN_POINT('',(4.,-7.27562663373442E-17,4.5941));
#16879=CARTESIAN_POINT('Ctrl Pts',(14.6288454112575,-0.000548182068839831,
4.59401855345973));
#16880=CARTESIAN_POINT('Ctrl Pts',(14.6168556732357,0.148643716013534,4.59265593252186));
#16881=CARTESIAN_POINT('Ctrl Pts',(14.6048659352138,0.29876355451001,4.53564313143304));
#16882=CARTESIAN_POINT('Ctrl Pts',(14.5928761971919,0.407080942069735,4.43405768361063));
#16883=CARTESIAN_POINT('Ctrl Pts',(14.5769709185042,0.55077200793829,4.29929703619113));
#16884=CARTESIAN_POINT('Ctrl Pts',(14.5610656398166,0.620899143473568,4.08609746938767));
#16885=CARTESIAN_POINT('Ctrl Pts',(14.545160361129,0.585262934872208,3.89235120454656));
#16886=CARTESIAN_POINT('Ctrl Pts',(14.5292550824414,0.549626726270847,3.69860493970543));
#16887=CARTESIAN_POINT('Ctrl Pts',(14.5133498037538,0.408227173532835,3.52431197682665));
#16888=CARTESIAN_POINT('Ctrl Pts',(14.4974445250662,0.225988969153725,3.44950027073699));
#16889=CARTESIAN_POINT('Ctrl Pts',(14.4815392463786,0.04375076477463,3.37468856464734));
#16890=CARTESIAN_POINT('Ctrl Pts',(14.465633967691,-0.179326091245555,3.39935811534679));
#16891=CARTESIAN_POINT('Ctrl Pts',(14.4497286890033,-0.340814144225853,
3.51218170883678));
#16892=CARTESIAN_POINT('Ctrl Pts',(14.4338234103157,-0.50230219720616,3.62500530232677));
#16893=CARTESIAN_POINT('Ctrl Pts',(14.4179181316281,-0.602201447146573,
3.82598293860731));
#16894=CARTESIAN_POINT('Ctrl Pts',(14.4020128529405,-0.594642384863179,
4.02283418976097));
#16895=CARTESIAN_POINT('Ctrl Pts',(14.3861075742529,-0.587083322579785,
4.21968544091462));
#16896=CARTESIAN_POINT('Ctrl Pts',(14.3702022955653,-0.47206594807259,4.4124103069414));
#16897=CARTESIAN_POINT('Ctrl Pts',(14.3542970168777,-0.302401373731467,
4.51251768287848));
#16898=CARTESIAN_POINT('Ctrl Pts',(14.3458131483376,-0.211902365642262,
4.565914912441));
#16899=CARTESIAN_POINT('Ctrl Pts',(14.3373292797976,-0.10585540495725,4.59296106912451));
#16900=CARTESIAN_POINT('Ctrl Pts',(14.3288454112576,0.000109044058801022,
4.5931342436645));
#16901=CARTESIAN_POINT('Ctrl Pts',(14.2211545887425,0.000537210645871958,
4.59424369460725));
#16902=CARTESIAN_POINT('Ctrl Pts',(14.2337379769984,-0.155889919212927,
4.59279139152499));
#16903=CARTESIAN_POINT('Ctrl Pts',(14.2463213652543,-0.313358837143528,
4.52935553548989));
#16904=CARTESIAN_POINT('Ctrl Pts',(14.2589047535102,-0.422984449084643,
4.4185751090669));
#16905=CARTESIAN_POINT('Ctrl Pts',(14.2748100321978,-0.561550141707708,
4.27854974232482));
#16906=CARTESIAN_POINT('Ctrl Pts',(14.2907153108854,-0.623677968224056,
4.06288332492072));
#16907=CARTESIAN_POINT('Ctrl Pts',(14.306620589573,-0.580841459108965,3.87060075163287));
#16908=CARTESIAN_POINT('Ctrl Pts',(14.3225258682606,-0.538004949993874,
3.67831817834502));
#16909=CARTESIAN_POINT('Ctrl Pts',(14.3384311469482,-0.390204105247342,
3.50941944917344));
#16910=CARTESIAN_POINT('Ctrl Pts',(14.3543364256359,-0.205302819838896,
3.44145571503774));
#16911=CARTESIAN_POINT('Ctrl Pts',(14.3702417043235,-0.0204015344304391,
3.37349198090203));
#16912=CARTESIAN_POINT('Ctrl Pts',(14.3861469830111,0.201600191639931,3.40646324180223));
#16913=CARTESIAN_POINT('Ctrl Pts',(14.4020522616987,0.358768557879186,3.52523048963197));
#16914=CARTESIAN_POINT('Ctrl Pts',(14.4179575403863,0.515936924118427,3.6439977374617));
#16915=CARTESIAN_POINT('Ctrl Pts',(14.4338628190739,0.608271930526566,3.84856097222098));
#16916=CARTESIAN_POINT('Ctrl Pts',(14.4497680977615,0.59337724853295,4.04499341086509));
#16917=CARTESIAN_POINT('Ctrl Pts',(14.4656733764491,0.578482566539332,4.2414258495092));
#16918=CARTESIAN_POINT('Ctrl Pts',(14.4815786551367,0.456358196143958,4.42972749203816));
#16919=CARTESIAN_POINT('Ctrl Pts',(14.4974839338244,0.283078481576349,4.52343819058819));
#16920=CARTESIAN_POINT('Ctrl Pts',(14.5053741521304,0.197118668938093,4.56992576768087));
#16921=CARTESIAN_POINT('Ctrl Pts',(14.5132643704364,0.0985699939877532,
4.59313537862966));
#16922=CARTESIAN_POINT('Ctrl Pts',(14.5211545887425,1.28950532977596E-5,
4.59311636453746));
#16923=CARTESIAN_POINT('Origin',(4.,0.,4.));
#16924=CARTESIAN_POINT('',(14.9288454112575,0.000149915246051877,4.59503491979621));
#16925=CARTESIAN_POINT('',(14.8211545887425,-0.000542004001680995,4.59419620878869));
#16926=CARTESIAN_POINT('',(4.,-7.27562663373442E-17,4.5941));
#16927=CARTESIAN_POINT('Ctrl Pts',(14.9288454112575,0.000149915246051877,
4.59503491979621));
#16928=CARTESIAN_POINT('Ctrl Pts',(14.9281926240489,0.00823674021970066,
4.59506221957623));
#16929=CARTESIAN_POINT('Ctrl Pts',(14.9275398368403,0.0163225255999611,
4.59491168338633));
#16930=CARTESIAN_POINT('Ctrl Pts',(14.9268870496317,0.0244008833477238,
4.59458015690877));
#16931=CARTESIAN_POINT('Ctrl Pts',(14.9109817709441,0.221231534471853,4.58650245417764));
#16932=CARTESIAN_POINT('Ctrl Pts',(14.8950764922565,0.413652681988333,4.47097768448731));
#16933=CARTESIAN_POINT('Ctrl Pts',(14.8791712135689,0.513312675625014,4.30104993462962));
#16934=CARTESIAN_POINT('Ctrl Pts',(14.8632659348813,0.612972669261697,4.13112218477192));
#16935=CARTESIAN_POINT('Ctrl Pts',(14.8473606561937,0.619871509018575,3.90679145474687));
#16936=CARTESIAN_POINT('Ctrl Pts',(14.831455377506,0.530841539545133,3.73106092513143));
#16937=CARTESIAN_POINT('Ctrl Pts',(14.8155500988184,0.441811570071688,3.55533039551599));
#16938=CARTESIAN_POINT('Ctrl Pts',(14.7996448201308,0.256852791367914,3.42820006631018));
#16939=CARTESIAN_POINT('Ctrl Pts',(14.7837395414432,0.0608904496539635,
3.40804280624462));
#16940=CARTESIAN_POINT('Ctrl Pts',(14.7678342627556,-0.135071892059981,
3.38788554617906));
#16941=CARTESIAN_POINT('Ctrl Pts',(14.751928984068,-0.342037796784102,3.47470135525375));
#16942=CARTESIAN_POINT('Ctrl Pts',(14.7360237053804,-0.464977277074429,
3.62862808681558));
#16943=CARTESIAN_POINT('Ctrl Pts',(14.7201184266927,-0.587916757364756,
3.78255481837741));
#16944=CARTESIAN_POINT('Ctrl Pts',(14.7042131480052,-0.62682981322129,4.00359247242638));
#16945=CARTESIAN_POINT('Ctrl Pts',(14.6883078693175,-0.56384921567034,4.19024990955517));
#16946=CARTESIAN_POINT('Ctrl Pts',(14.6724025906299,-0.500868618119389,
4.37690734668397));
#16947=CARTESIAN_POINT('Ctrl Pts',(14.6564973119423,-0.335994367160947,
4.52918456689258));
#16948=CARTESIAN_POINT('Ctrl Pts',(14.6405920332547,-0.144929743580805,
4.57716231297912));
#16949=CARTESIAN_POINT('Ctrl Pts',(14.636676492589,-0.097893704910838,4.5889734116427));
#16950=CARTESIAN_POINT('Ctrl Pts',(14.6327609519233,-0.0492704262804658,
4.59446355048005));
#16951=CARTESIAN_POINT('Ctrl Pts',(14.6288454112575,-0.000548182068839831,
4.59401855345973));
#16952=CARTESIAN_POINT('Ctrl Pts',(14.5211545887425,1.28950532977596E-5,
4.59311636453746));
#16953=CARTESIAN_POINT('Ctrl Pts',(14.5291696491241,-0.100103612291989,
4.59309704959697));
#16954=CARTESIAN_POINT('Ctrl Pts',(14.5371847095056,-0.200228812305367,
4.56910822985942));
#16955=CARTESIAN_POINT('Ctrl Pts',(14.5451997698872,-0.287175610734119,
4.52120162576233));
#16956=CARTESIAN_POINT('Ctrl Pts',(14.5611050485748,-0.459714929737158,
4.42613460781534));
#16957=CARTESIAN_POINT('Ctrl Pts',(14.5770103272624,-0.580358509003398,
4.23688081735026));
#16958=CARTESIAN_POINT('Ctrl Pts',(14.59291560595,-0.593711920942704,4.04033758828107));
#16959=CARTESIAN_POINT('Ctrl Pts',(14.6088208846377,-0.607065332882009,
3.84379435921188));
#16960=CARTESIAN_POINT('Ctrl Pts',(14.6247261633253,-0.513128577494387,
3.63996169153858));
#16961=CARTESIAN_POINT('Ctrl Pts',(14.6406314420129,-0.35503343871745,3.52243092280774));
#16962=CARTESIAN_POINT('Ctrl Pts',(14.6565367207005,-0.196938299940509,
3.40490015407689));
#16963=CARTESIAN_POINT('Ctrl Pts',(14.6724419993881,0.025315222225754,3.37367128428849));
#16964=CARTESIAN_POINT('Ctrl Pts',(14.6883472780757,0.209677713173688,3.44308328926485));
#16965=CARTESIAN_POINT('Ctrl Pts',(14.7042525567633,0.394040204121622,3.51249529424121));
#16966=CARTESIAN_POINT('Ctrl Pts',(14.720157835451,0.540511663851219,3.68254817398232));
#16967=CARTESIAN_POINT('Ctrl Pts',(14.7360631141386,0.581838594751101,3.87516084045512));
#16968=CARTESIAN_POINT('Ctrl Pts',(14.7519683928262,0.623165525650983,4.06777350692792));
#16969=CARTESIAN_POINT('Ctrl Pts',(14.7678736715138,0.559347927721136,4.2829459601324));
#16970=CARTESIAN_POINT('Ctrl Pts',(14.7837789502014,0.419688142031033,4.42188011275284));
#16971=CARTESIAN_POINT('Ctrl Pts',(14.7962374963817,0.310293146587505,4.53070672248707));
#16972=CARTESIAN_POINT('Ctrl Pts',(14.8086960425621,0.154364940471616,4.59275708529138));
#16973=CARTESIAN_POINT('Ctrl Pts',(14.8211545887425,-0.000542004001680995,
4.59419620878869));
#16974=CARTESIAN_POINT('Origin',(4.,0.,4.));
#16975=CARTESIAN_POINT('',(15.2288454112576,0.000471544078774977,4.59356550157774));
#16976=CARTESIAN_POINT('',(15.1211545887425,0.000250233060073018,4.59495282954609));
#16977=CARTESIAN_POINT('',(4.,-7.27562663373442E-17,4.5941));
#16978=CARTESIAN_POINT('Ctrl Pts',(15.2288454112576,0.000471544078774977,
4.59356550157774));
#16979=CARTESIAN_POINT('Ctrl Pts',(15.2236242961746,0.0655651715058866,
4.59404721416646));
#16980=CARTESIAN_POINT('Ctrl Pts',(15.2184031810917,0.130516835945995,4.58418155789741));
#16981=CARTESIAN_POINT('Ctrl Pts',(15.2131820660088,0.191734887706884,4.56334598510492));
#16982=CARTESIAN_POINT('Ctrl Pts',(15.1972767873211,0.378225734681762,4.49987379829874));
#16983=CARTESIAN_POINT('Ctrl Pts',(15.1813715086335,0.530068013118856,4.33459889729257));
#16984=CARTESIAN_POINT('Ctrl Pts',(15.1654662299459,0.577542172676889,4.143408524424));
#16985=CARTESIAN_POINT('Ctrl Pts',(15.1495609512583,0.625016332234921,3.95221815155542));
#16986=CARTESIAN_POINT('Ctrl Pts',(15.1336556725707,0.568122372913892,3.73511230682445));
#16987=CARTESIAN_POINT('Ctrl Pts',(15.1177503938831,0.432983593849097,3.59177680914072));
#16988=CARTESIAN_POINT('Ctrl Pts',(15.1018451151955,0.297844814784303,3.44844131145699));
#16989=CARTESIAN_POINT('Ctrl Pts',(15.0859398365078,0.0844612159757424,
3.37887616082051));
#16990=CARTESIAN_POINT('Ctrl Pts',(15.0700345578202,-0.109190481519281,
3.41502273134472));
#16991=CARTESIAN_POINT('Ctrl Pts',(15.0541292791326,-0.302842179014298,
3.45116930186893));
#16992=CARTESIAN_POINT('Ctrl Pts',(15.038224000445,-0.47676197519578,3.59302759355383));
#16993=CARTESIAN_POINT('Ctrl Pts',(15.0223187217574,-0.551093257596978,
3.77546228038711));
#16994=CARTESIAN_POINT('Ctrl Pts',(15.0064134430698,-0.625424539998176,
3.95789696722038));
#16995=CARTESIAN_POINT('Ctrl Pts',(14.9905081643822,-0.600167308619091,
4.18090804920204));
#16996=CARTESIAN_POINT('Ctrl Pts',(14.9746028856946,-0.486918615563658,
4.34209827230691));
#16997=CARTESIAN_POINT('Ctrl Pts',(14.9593503942156,-0.378317895025423,
4.49667289829699));
#16998=CARTESIAN_POINT('Ctrl Pts',(14.9440979027365,-0.188800216398263,
4.59439705548643));
#16999=CARTESIAN_POINT('Ctrl Pts',(14.9288454112575,0.000149915246051877,
4.59503491979621));
#17000=CARTESIAN_POINT('Ctrl Pts',(14.8211545887425,-0.000542004001680995,
4.59419620878869));
#17001=CARTESIAN_POINT('Ctrl Pts',(14.8246013212497,-0.0433979515083632,
4.5945943510493));
#17002=CARTESIAN_POINT('Ctrl Pts',(14.828048053757,-0.0861757330942537,
4.59035339483295));
#17003=CARTESIAN_POINT('Ctrl Pts',(14.8314947862642,-0.127868389248254,
4.58118038604969));
#17004=CARTESIAN_POINT('Ctrl Pts',(14.8474000649518,-0.320263161387096,
4.5388506546897));
#17005=CARTESIAN_POINT('Ctrl Pts',(14.8633053436395,-0.489550732214419,
4.39149533993331));
#17006=CARTESIAN_POINT('Ctrl Pts',(14.8792106223271,-0.558001411172811,
4.20677376822741));
#17007=CARTESIAN_POINT('Ctrl Pts',(14.8951159010147,-0.6264520901312,4.0220521965215));
#17008=CARTESIAN_POINT('Ctrl Pts',(14.9110211797023,-0.594065877220663,
3.79996436786608));
#17009=CARTESIAN_POINT('Ctrl Pts',(14.9269264583899,-0.475713151262041,
3.64248361741852));
#17010=CARTESIAN_POINT('Ctrl Pts',(14.9428317370775,-0.357360425303418,
3.48500286697096));
#17011=CARTESIAN_POINT('Ctrl Pts',(14.9587370157651,-0.153041186296697,
3.39212919473125));
#17012=CARTESIAN_POINT('Ctrl Pts',(14.9746422944528,0.0434298152403689,
3.40650626183085));
#17013=CARTESIAN_POINT('Ctrl Pts',(14.9905475731404,0.239900816777435,3.42088332893044));
#17014=CARTESIAN_POINT('Ctrl Pts',(15.006452851828,0.428523580844854,3.54251113536931));
#17015=CARTESIAN_POINT('Ctrl Pts',(15.0223581305156,0.522690514153935,3.71554333807889));
#17016=CARTESIAN_POINT('Ctrl Pts',(15.0382634092032,0.616857447463019,3.88857554078846));
#17017=CARTESIAN_POINT('Ctrl Pts',(15.0541686878908,0.616568550013756,4.11301213976874));
#17018=CARTESIAN_POINT('Ctrl Pts',(15.0700739665784,0.521956471292605,4.28580134389743));
#17019=CARTESIAN_POINT('Ctrl Pts',(15.085979245266,0.427344392571456,4.45859054802613));
#17020=CARTESIAN_POINT('Ctrl Pts',(15.1018845239536,0.238409132578427,4.57973235730324));
#17021=CARTESIAN_POINT('Ctrl Pts',(15.1177898026413,0.0419017695106382,
4.59360357799603));
#17022=CARTESIAN_POINT('Ctrl Pts',(15.1189113980083,0.0280446248267054,
4.59458173733358));
#17023=CARTESIAN_POINT('Ctrl Pts',(15.1200329933754,0.0141498265549413,
4.59502647517791));
#17024=CARTESIAN_POINT('Ctrl Pts',(15.1211545887425,0.000250233060073018,
4.59495282954609));
#17025=CARTESIAN_POINT('Origin',(4.,0.,4.));
#17026=CARTESIAN_POINT('',(15.5288454112575,-0.000350670266729247,4.59332700645389));
#17027=CARTESIAN_POINT('',(15.4211545887425,0.000414092275955974,4.59343115273787));
#17028=CARTESIAN_POINT('',(4.,-7.27562663373442E-17,4.5941));
#17029=CARTESIAN_POINT('Ctrl Pts',(15.5288454112575,-0.000350670266729247,
4.59332700645389));
#17030=CARTESIAN_POINT('Ctrl Pts',(15.5190559683003,0.121821298278883,4.59267222728074));
#17031=CARTESIAN_POINT('Ctrl Pts',(15.509266525343,0.244354036528086,4.55597946496206));
#17032=CARTESIAN_POINT('Ctrl Pts',(15.4994770823858,0.343380025451582,4.48601555964668));
#17033=CARTESIAN_POINT('Ctrl Pts',(15.4835718036982,0.504271299656008,4.37234255322809));
#17034=CARTESIAN_POINT('Ctrl Pts',(15.4676665250105,0.603110088323456,4.17084127710728));
#17035=CARTESIAN_POINT('Ctrl Pts',(15.4517612463229,0.594513801222153,3.97403259246294));
#17036=CARTESIAN_POINT('Ctrl Pts',(15.4358559676353,0.58591751412085,3.7772239078186));
#17037=CARTESIAN_POINT('Ctrl Pts',(15.4199506889477,0.469886151250777,3.58510781465072));
#17038=CARTESIAN_POINT('Ctrl Pts',(15.4040454102601,0.299696405559752,3.48589589518039));
#17039=CARTESIAN_POINT('Ctrl Pts',(15.3881401315725,0.129506659868722,3.38668397571006));
#17040=CARTESIAN_POINT('Ctrl Pts',(15.3722348528849,-0.0948414686432761,
3.38037622993726));
#17041=CARTESIAN_POINT('Ctrl Pts',(15.3563295741973,-0.270336810750117,
3.46986890786216));
#17042=CARTESIAN_POINT('Ctrl Pts',(15.3404242955096,-0.445832152856957,
3.55936158578705));
#17043=CARTESIAN_POINT('Ctrl Pts',(15.324519016822,-0.572474708558633,3.74465468740961));
#17044=CARTESIAN_POINT('Ctrl Pts',(15.3086137381344,-0.592115574081638,
3.94066945956945));
#17045=CARTESIAN_POINT('Ctrl Pts',(15.2927084594468,-0.611756439604643,
4.13668423172929));
#17046=CARTESIAN_POINT('Ctrl Pts',(15.2768031807592,-0.524395614948954,
4.3434206744264));
#17047=CARTESIAN_POINT('Ctrl Pts',(15.2608979020716,-0.370145494864779,
4.46595415947185));
#17048=CARTESIAN_POINT('Ctrl Pts',(15.2502137384669,-0.266529987624151,
4.54826443060822));
#17049=CARTESIAN_POINT('Ctrl Pts',(15.2395295748622,-0.13273198696893,4.59257975504152));
#17050=CARTESIAN_POINT('Ctrl Pts',(15.2288454112576,0.000471544078774977,
4.59356550157774));
#17051=CARTESIAN_POINT('Ctrl Pts',(15.1211545887425,0.000250233060073018,
4.59495282954609));
#17052=CARTESIAN_POINT('Ctrl Pts',(15.135938272063,-0.18295950063263,4.59398211075496));
#17053=CARTESIAN_POINT('Ctrl Pts',(15.1507219553836,-0.367002343096231,
4.50294888365168));
#17054=CARTESIAN_POINT('Ctrl Pts',(15.1655056387041,-0.476631971954554,
4.35629051265579));
#17055=CARTESIAN_POINT('Ctrl Pts',(15.1814109173917,-0.594578884209397,
4.19850559451431));
#17056=CARTESIAN_POINT('Ctrl Pts',(15.1973161960793,-0.626393242576541,
3.97633512612291));
#17057=CARTESIAN_POINT('Ctrl Pts',(15.2132214747669,-0.557467239648298,
3.79179038730953));
#17058=CARTESIAN_POINT('Ctrl Pts',(15.2291267534545,-0.488541236720055,
3.60724564849615));
#17059=CARTESIAN_POINT('Ctrl Pts',(15.2450320321422,-0.318874872496425,
3.46032663926078));
#17060=CARTESIAN_POINT('Ctrl Pts',(15.2609373108298,-0.126371763436977,
3.41849235301362));
#17061=CARTESIAN_POINT('Ctrl Pts',(15.2768425895174,0.0661313456224706,
3.37665806676646));
#17062=CARTESIAN_POINT('Ctrl Pts',(15.292747868205,0.281471199517752,3.4399085035075));
#17063=CARTESIAN_POINT('Ctrl Pts',(15.3086531468926,0.420772847618048,3.57920173859056));
#17064=CARTESIAN_POINT('Ctrl Pts',(15.3245584255802,0.560074495718348,3.71849497367363));
#17065=CARTESIAN_POINT('Ctrl Pts',(15.3404637042678,0.623337938023671,3.9338310070987));
#17066=CARTESIAN_POINT('Ctrl Pts',(15.3563689829554,0.581515278282945,4.12633664243329));
#17067=CARTESIAN_POINT('Ctrl Pts',(15.3722742616431,0.53969261854222,4.31884227776789));
#17068=CARTESIAN_POINT('Ctrl Pts',(15.3881795403307,0.392783856755445,4.48851751501199));
#17069=CARTESIAN_POINT('Ctrl Pts',(15.4040848190183,0.208243281137944,4.55745466359042));
#17070=CARTESIAN_POINT('Ctrl Pts',(15.4097747422597,0.142226097106806,4.58211610408423));
#17071=CARTESIAN_POINT('Ctrl Pts',(15.4154646655011,0.0713929250243718,
4.593885435962));
#17072=CARTESIAN_POINT('Ctrl Pts',(15.4211545887425,0.000414092275955974,
4.59343115273787));
#17073=CARTESIAN_POINT('Origin',(4.,0.,4.));
#17074=CARTESIAN_POINT('',(15.8288454112575,-0.000332254705457391,4.59484959654372));
#17075=CARTESIAN_POINT('',(15.7211545887425,-0.000419917270904514,4.59344262983929));
#17076=CARTESIAN_POINT('',(4.,-7.27562663373442E-17,4.5941));
#17077=CARTESIAN_POINT('Ctrl Pts',(15.8288454112575,-0.000332254705457391,
4.59484959654372));
#17078=CARTESIAN_POINT('Ctrl Pts',(15.814487640426,0.177680873019276,4.5936575613883));
#17079=CARTESIAN_POINT('Ctrl Pts',(15.8001298695944,0.356683508224643,4.50844978272675));
#17080=CARTESIAN_POINT('Ctrl Pts',(15.7857720987628,0.466927807092597,4.36891650689757));
#17081=CARTESIAN_POINT('Ctrl Pts',(15.7698668200752,0.589054446233417,4.21434406913608));
#17082=CARTESIAN_POINT('Ctrl Pts',(15.7539615413876,0.626802179063893,3.99310442736787));
#17083=CARTESIAN_POINT('Ctrl Pts',(15.7380562627,0.562838843643149,3.80678146521555));
#17084=CARTESIAN_POINT('Ctrl Pts',(15.7221509840123,0.498875508222402,3.62045850306322));
#17085=CARTESIAN_POINT('Ctrl Pts',(15.7062457053247,0.333201104550436,3.46905222052678));
#17086=CARTESIAN_POINT('Ctrl Pts',(15.6903404266371,0.141886309687413,3.42208197707538));
#17087=CARTESIAN_POINT('Ctrl Pts',(15.6744351479495,-0.0494284851756215,
3.37511173362399));
#17088=CARTESIAN_POINT('Ctrl Pts',(15.6585298692619,-0.266383671229707,
3.43257752925765));
#17089=CARTESIAN_POINT('Ctrl Pts',(15.6426245905743,-0.409362605655794,
3.5680935017987));
#17090=CARTESIAN_POINT('Ctrl Pts',(15.6267193118867,-0.552341540081869,
3.70360947433975));
#17091=CARTESIAN_POINT('Ctrl Pts',(15.6108140331991,-0.621344222879956,
3.9171756237882));
#17092=CARTESIAN_POINT('Ctrl Pts',(15.5949087545115,-0.584687541371933,
4.11073140955597));
#17093=CARTESIAN_POINT('Ctrl Pts',(15.5790034758238,-0.548030859863907,
4.30428719532377));
#17094=CARTESIAN_POINT('Ctrl Pts',(15.5630981971362,-0.405714814049763,
4.47783261741089));
#17095=CARTESIAN_POINT('Ctrl Pts',(15.5471929184486,-0.223084911271984,
4.55168296009627));
#17096=CARTESIAN_POINT('Ctrl Pts',(15.5410770827183,-0.152860773312716,
4.58007960584922));
#17097=CARTESIAN_POINT('Ctrl Pts',(15.5349612469879,-0.0766761255292402,
4.5937360717991));
#17098=CARTESIAN_POINT('Ctrl Pts',(15.5288454112575,-0.000350670266729247,
4.59332700645389));
#17099=CARTESIAN_POINT('Ctrl Pts',(15.4211545887425,0.000414092275955974,
4.59343115273787));
#17100=CARTESIAN_POINT('Ctrl Pts',(15.4313699441887,-0.12701715326484,4.59261555920332));
#17101=CARTESIAN_POINT('Ctrl Pts',(15.4415852996349,-0.254917899718674,
4.55240018390688));
#17102=CARTESIAN_POINT('Ctrl Pts',(15.4518006550811,-0.356261725310785,
4.47665348962993));
#17103=CARTESIAN_POINT('Ctrl Pts',(15.4677059337687,-0.514053766693778,
4.35871610717824));
#17104=CARTESIAN_POINT('Ctrl Pts',(15.4836112124564,-0.607465460011524,
4.15464228236211));
#17105=CARTESIAN_POINT('Ctrl Pts',(15.499516491144,-0.593606107615349,3.95813408188558));
#17106=CARTESIAN_POINT('Ctrl Pts',(15.5154217698316,-0.579746755219174,
3.76162588140906));
#17107=CARTESIAN_POINT('Ctrl Pts',(15.5313270485192,-0.458616357109098,
3.57268330527213));
#17108=CARTESIAN_POINT('Ctrl Pts',(15.5472323272068,-0.285832867492734,
3.47806079093568));
#17109=CARTESIAN_POINT('Ctrl Pts',(15.5631376058944,-0.113049377876356,
3.38343827659922));
#17110=CARTESIAN_POINT('Ctrl Pts',(15.579042884582,0.111387203246309,3.38313582406324));
#17111=CARTESIAN_POINT('Ctrl Pts',(15.5949481632696,0.284425092952457,3.47729230673655));
#17112=CARTESIAN_POINT('Ctrl Pts',(15.6108534419572,0.457462982658595,3.57144878940986));
#17113=CARTESIAN_POINT('Ctrl Pts',(15.6267587206449,0.579102180948212,3.76006420729246));
#17114=CARTESIAN_POINT('Ctrl Pts',(15.6426639993325,0.593491114096805,3.95653434015292));
#17115=CARTESIAN_POINT('Ctrl Pts',(15.6585692780201,0.607880047245398,4.15300447301339));
#17116=CARTESIAN_POINT('Ctrl Pts',(15.6744745567077,0.515018715252963,4.35732932085173));
#17117=CARTESIAN_POINT('Ctrl Pts',(15.6903798353953,0.357545113131455,4.47569155781202));
#17118=CARTESIAN_POINT('Ctrl Pts',(15.700638086511,0.255981111243369,4.55203033647815));
#17119=CARTESIAN_POINT('Ctrl Pts',(15.7108963376268,0.127540214881222,4.59261107697802));
#17120=CARTESIAN_POINT('Ctrl Pts',(15.7211545887425,-0.000419917270904514,
4.59344262983929));
#17121=CARTESIAN_POINT('Origin',(4.,0.,4.));
#17122=CARTESIAN_POINT('',(16.1288454112575,0.000520203518568921,4.59435747030618));
#17123=CARTESIAN_POINT('',(16.0211545887425,-0.00024144267326323,4.59496181546483));
#17124=CARTESIAN_POINT('',(4.,-7.27562663373442E-17,4.5941));
#17125=CARTESIAN_POINT('Ctrl Pts',(16.1288454112575,0.000520203518568921,
4.59435747030618));
#17126=CARTESIAN_POINT('Ctrl Pts',(16.1258245912393,0.0380542554257849,
4.59470210862833));
#17127=CARTESIAN_POINT('Ctrl Pts',(16.122803771221,0.0755288363057283,4.59145263304759));
#17128=CARTESIAN_POINT('Ctrl Pts',(16.1197829512027,0.112271568866026,4.58439375503351));
#17129=CARTESIAN_POINT('Ctrl Pts',(16.1038776725151,0.305730099191281,4.54722721702202));
#17130=CARTESIAN_POINT('Ctrl Pts',(16.0879723938275,0.478899942385972,4.40445440507416));
#17131=CARTESIAN_POINT('Ctrl Pts',(16.0720671151398,0.55226883266698,4.22163055421683));
#17132=CARTESIAN_POINT('Ctrl Pts',(16.0561618364522,0.625637722947984,4.03880670335952));
#17133=CARTESIAN_POINT('Ctrl Pts',(16.0402565577646,0.599205660315318,3.81593181359275));
#17134=CARTESIAN_POINT('Ctrl Pts',(16.024351279077,0.485109129681553,3.65534060523843));
#17135=CARTESIAN_POINT('Ctrl Pts',(16.0084460003894,0.371012599047788,3.4947493968841));
#17136=CARTESIAN_POINT('Ctrl Pts',(15.9925407217018,0.169251600412921,3.39644186994223));
#17137=CARTESIAN_POINT('Ctrl Pts',(15.9766354430142,-0.0275337514538456,
3.40555668173602));
#17138=CARTESIAN_POINT('Ctrl Pts',(15.9607301643265,-0.224319103320618,
3.41467149352982));
#17139=CARTESIAN_POINT('Ctrl Pts',(15.9448248856389,-0.416128808419276,
3.53120864405929));
#17140=CARTESIAN_POINT('Ctrl Pts',(15.9289196069513,-0.514891964967956,
3.70165920408156));
#17141=CARTESIAN_POINT('Ctrl Pts',(15.9130143282637,-0.613655121516638,
3.87210976410384));
#17142=CARTESIAN_POINT('Ctrl Pts',(15.8971090495761,-0.619371729515322,
4.09647373361892));
#17143=CARTESIAN_POINT('Ctrl Pts',(15.8812037708885,-0.52941696442075,4.27173266988224));
#17144=CARTESIAN_POINT('Ctrl Pts',(15.8652984922009,-0.439462199326184,
4.44699160614554));
#17145=CARTESIAN_POINT('Ctrl Pts',(15.8493932135132,-0.25383606113837,4.57314550915708));
#17146=CARTESIAN_POINT('Ctrl Pts',(15.8334879348256,-0.0577702193188812,
4.59226984378546));
#17147=CARTESIAN_POINT('Ctrl Pts',(15.8319404269696,-0.0386939468137543,
4.59413055045147));
#17148=CARTESIAN_POINT('Ctrl Pts',(15.8303929191136,-0.0195188482833839,
4.59497807636063));
#17149=CARTESIAN_POINT('Ctrl Pts',(15.8288454112575,-0.000332254705457391,
4.59484959654372));
#17150=CARTESIAN_POINT('Ctrl Pts',(15.7211545887425,-0.000419917270904514,
4.59344262983929));
#17151=CARTESIAN_POINT('Ctrl Pts',(15.7268016163144,-0.0708602278282204,
4.59390038836772));
#17152=CARTESIAN_POINT('Ctrl Pts',(15.7324486438863,-0.141154849878182,
4.58231274148771));
#17153=CARTESIAN_POINT('Ctrl Pts',(15.7380956714582,-0.206740066761224,
4.55801389847688));
#17154=CARTESIAN_POINT('Ctrl Pts',(15.7540009501458,-0.391465772281827,
4.48957437609924));
#17155=CARTESIAN_POINT('Ctrl Pts',(15.7699062288334,-0.538831311072463,
4.32029570526172));
#17156=CARTESIAN_POINT('Ctrl Pts',(15.785811507521,-0.58117266224226,4.12790349002296));
#17157=CARTESIAN_POINT('Ctrl Pts',(15.8017167862086,-0.62351401341206,3.93551127478418));
#17158=CARTESIAN_POINT('Ctrl Pts',(15.8176220648962,-0.560831176961022,
3.72000551514415));
#17159=CARTESIAN_POINT('Ctrl Pts',(15.8335273435838,-0.421905459495345,
3.58033733863277));
#17160=CARTESIAN_POINT('Ctrl Pts',(15.8494326222715,-0.282979742029676,
3.44066916212139));
#17161=CARTESIAN_POINT('Ctrl Pts',(15.8653379009591,-0.0678111435493865,
3.37683856873865));
#17162=CARTESIAN_POINT('Ctrl Pts',(15.8812431796467,0.124804018556085,3.41815386651619));
#17163=CARTESIAN_POINT('Ctrl Pts',(15.8971484583343,0.317419180661557,3.45946916429373));
#17164=CARTESIAN_POINT('Ctrl Pts',(15.9130537370219,0.487480906392202,3.60593035323155));
#17165=CARTESIAN_POINT('Ctrl Pts',(15.9289590157095,0.556904046010802,3.79028865163133));
#17166=CARTESIAN_POINT('Ctrl Pts',(15.9448642943971,0.6263271856294,3.9746469500311));
#17167=CARTESIAN_POINT('Ctrl Pts',(15.9607695730847,0.595111739135951,4.19690235789283));
#17168=CARTESIAN_POINT('Ctrl Pts',(15.9766748517723,0.477590518943614,4.35500459477727));
#17169=CARTESIAN_POINT('Ctrl Pts',(15.9915014307624,0.368039615220995,4.50238430120742));
#17170=CARTESIAN_POINT('Ctrl Pts',(16.0063280097524,0.18349252241573,4.59401752470064));
#17171=CARTESIAN_POINT('Ctrl Pts',(16.0211545887425,-0.00024144267326323,
4.59496181546483));
#17172=CARTESIAN_POINT('Origin',(4.,0.,4.));
#17173=CARTESIAN_POINT('',(16.4288454112575,7.48704377684928E-5,4.59312461313858));
#17174=CARTESIAN_POINT('',(16.3211545887425,0.000543344619121817,4.59417988242975));
#17175=CARTESIAN_POINT('',(4.,-7.27562663373442E-17,4.5941));
#17176=CARTESIAN_POINT('Ctrl Pts',(16.4288454112575,7.48704377684928E-5,
4.59312461313858));
#17177=CARTESIAN_POINT('Ctrl Pts',(16.4212562633649,0.0948679978941589,
4.5932308806522));
#17178=CARTESIAN_POINT('Ctrl Pts',(16.4136671154723,0.189615837117123,4.57184094704105));
#17179=CARTESIAN_POINT('Ctrl Pts',(16.4060779675797,0.273126642574496,4.52869916135151));
#17180=CARTESIAN_POINT('Ctrl Pts',(16.3901726888921,0.448147956300534,4.43828293357696));
#17181=CARTESIAN_POINT('Ctrl Pts',(16.3742674102045,0.573812330828296,4.25232504748949));
#17182=CARTESIAN_POINT('Ctrl Pts',(16.3583621315169,0.592420001795879,4.05620949715111));
#17183=CARTESIAN_POINT('Ctrl Pts',(16.3424568528292,0.611027672763462,3.86009394681272));
#17184=CARTESIAN_POINT('Ctrl Pts',(16.3265515741416,0.522578640170867,3.6538207322234));
#17185=CARTESIAN_POINT('Ctrl Pts',(16.310646295454,0.367684957814641,3.53210178682255));
#17186=CARTESIAN_POINT('Ctrl Pts',(16.2947410167664,0.212791275458425,3.4103828414217));
#17187=CARTESIAN_POINT('Ctrl Pts',(16.2788357380788,-0.00854705666138705,
3.3732181652093));
#17188=CARTESIAN_POINT('Ctrl Pts',(16.2629304593912,-0.19470084048803,3.43767220519428));
#17189=CARTESIAN_POINT('Ctrl Pts',(16.2470251807036,-0.380854624314662,
3.50212624517926));
#17190=CARTESIAN_POINT('Ctrl Pts',(16.231119902016,-0.531823859848111,3.66819900136163));
#17191=CARTESIAN_POINT('Ctrl Pts',(16.2152146233283,-0.578289861113055,
3.85963689006134));
#17192=CARTESIAN_POINT('Ctrl Pts',(16.1993093446407,-0.624755862378002,
4.05107477876107));
#17193=CARTESIAN_POINT('Ctrl Pts',(16.1834040659531,-0.566718629374431,
4.26787779997815));
#17194=CARTESIAN_POINT('Ctrl Pts',(16.1674987872655,-0.430826404144746,
4.41049917854914));
#17195=CARTESIAN_POINT('Ctrl Pts',(16.1546143285962,-0.320743594918802,
4.52603310245269));
#17196=CARTESIAN_POINT('Ctrl Pts',(16.1417298699269,-0.159570744489656,
4.592887512417));
#17197=CARTESIAN_POINT('Ctrl Pts',(16.1288454112575,0.000520203518568921,
4.59435747030618));
#17198=CARTESIAN_POINT('Ctrl Pts',(16.0211545887425,-0.00024144267326323,
4.59496181546483));
#17199=CARTESIAN_POINT('Ctrl Pts',(16.0222332884401,-0.0136089074611732,
4.59503051682625));
#17200=CARTESIAN_POINT('Ctrl Pts',(16.0233119881376,-0.0269720681925484,
4.59461918253551));
#17201=CARTESIAN_POINT('Ctrl Pts',(16.0243906878352,-0.0403017303441999,
4.59371435609144));
#17202=CARTESIAN_POINT('Ctrl Pts',(16.0402959665228,-0.236845765548457,
4.58037281461397));
#17203=CARTESIAN_POINT('Ctrl Pts',(16.0562012452104,-0.426106842065734,
4.45974066575184));
#17204=CARTESIAN_POINT('Ctrl Pts',(16.072106523898,-0.521184280535122,4.2872070887372));
#17205=CARTESIAN_POINT('Ctrl Pts',(16.0880118025856,-0.616261719004504,
4.11467351172257));
#17206=CARTESIAN_POINT('Ctrl Pts',(16.1039170812732,-0.61715551942601,3.89023850655542));
#17207=CARTESIAN_POINT('Ctrl Pts',(16.1198223599609,-0.523455286459661,
3.71695313254649));
#17208=CARTESIAN_POINT('Ctrl Pts',(16.1357276386485,-0.429755053493313,
3.54366775853756));
#17209=CARTESIAN_POINT('Ctrl Pts',(16.1516329173361,-0.241460787139106,
3.42153201568684));
#17210=CARTESIAN_POINT('Ctrl Pts',(16.1675381960237,-0.045029248433429,
3.40662546997421));
#17211=CARTESIAN_POINT('Ctrl Pts',(16.1834434747113,0.151402290272254,3.39171892426158));
#17212=CARTESIAN_POINT('Ctrl Pts',(16.1993487533989,0.355971101329402,3.48404157568705));
#17213=CARTESIAN_POINT('Ctrl Pts',(16.2152540320865,0.474747841293266,3.64120276856532));
#17214=CARTESIAN_POINT('Ctrl Pts',(16.2311593107741,0.593524581257127,3.79836396144359));
#17215=CARTESIAN_POINT('Ctrl Pts',(16.2470645894618,0.626509250127697,4.02036369577466));
#17216=CARTESIAN_POINT('Ctrl Pts',(16.2629698681494,0.558556683425868,4.20526908558792));
#17217=CARTESIAN_POINT('Ctrl Pts',(16.278875146837,0.490604116724039,4.39017447540119));
#17218=CARTESIAN_POINT('Ctrl Pts',(16.2947804255246,0.32171431444981,4.53798552069667));
#17219=CARTESIAN_POINT('Ctrl Pts',(16.3106857042122,0.129434328669215,4.58083364284428));
#17220=CARTESIAN_POINT('Ctrl Pts',(16.314175332389,0.0872479785030607,4.5902345478711));
#17221=CARTESIAN_POINT('Ctrl Pts',(16.3176649605657,0.0439357035691123,
4.5945828907904));
#17222=CARTESIAN_POINT('Ctrl Pts',(16.3211545887425,0.000543344619121817,
4.59417988242975));
#17223=CARTESIAN_POINT('Origin',(4.,0.,4.));
#17224=CARTESIAN_POINT('',(16.7288454112575,-0.000548108868865471,4.59408180714414));
#17225=CARTESIAN_POINT('',(16.6211545887425,-2.1752937549985E-5,4.5931168278739));
#17226=CARTESIAN_POINT('',(4.,-7.27562663373442E-17,4.5941));
#17227=CARTESIAN_POINT('Ctrl Pts',(16.7288454112575,-0.000548108868865471,
4.59408180714414));
#17228=CARTESIAN_POINT('Ctrl Pts',(16.7166879354906,0.15068989439403,4.59268722311157));
#17229=CARTESIAN_POINT('Ctrl Pts',(16.7045304597237,0.302891836883802,4.53390177381835));
#17230=CARTESIAN_POINT('Ctrl Pts',(16.6923729839567,0.411632901649024,4.42974331917764));
#17231=CARTESIAN_POINT('Ctrl Pts',(16.6764677052691,0.553895734249677,4.29347578465895));
#17232=CARTESIAN_POINT('Ctrl Pts',(16.6605624265815,0.621772048174623,4.07954898308531));
#17233=CARTESIAN_POINT('Ctrl Pts',(16.6446571478939,0.58409591167956,3.88618905124272));
#17234=CARTESIAN_POINT('Ctrl Pts',(16.6287518692063,0.546419775184499,3.69282911940014));
#17235=CARTESIAN_POINT('Ctrl Pts',(16.6128465905187,0.403191188269443,3.52003605728863));
#17236=CARTESIAN_POINT('Ctrl Pts',(16.596941311831,0.220174658543969,3.44714912875817));
#17237=CARTESIAN_POINT('Ctrl Pts',(16.5810360331434,0.0371581288184754,
3.37426220022769));
#17238=CARTESIAN_POINT('Ctrl Pts',(16.5651307544558,-0.185646343717467,
3.40128140527831));
#17239=CARTESIAN_POINT('Ctrl Pts',(16.5492254757682,-0.34593637135519,3.51580066803907));
#17240=CARTESIAN_POINT('Ctrl Pts',(16.5333201970806,-0.506226398992903,
3.63031993079982));
#17241=CARTESIAN_POINT('Ctrl Pts',(16.517414918393,-0.604001981732426,3.83233925127069));
#17242=CARTESIAN_POINT('Ctrl Pts',(16.5015096397054,-0.594368708523554,
4.02909990422408));
#17243=CARTESIAN_POINT('Ctrl Pts',(16.4856043610178,-0.584735435314682,
4.22586055717748));
#17244=CARTESIAN_POINT('Ctrl Pts',(16.4696990823301,-0.467693306157413,
4.4173625426134));
#17245=CARTESIAN_POINT('Ctrl Pts',(16.4537938036425,-0.296983115116624,
4.51567625060054));
#17246=CARTESIAN_POINT('Ctrl Pts',(16.4454776728475,-0.20772669247752,4.56707991793767));
#17247=CARTESIAN_POINT('Ctrl Pts',(16.4371615420525,-0.103798720846626,
4.59300816600183));
#17248=CARTESIAN_POINT('Ctrl Pts',(16.4288454112575,7.48704377684928E-5,
4.59312461313858));
#17249=CARTESIAN_POINT('Ctrl Pts',(16.3211545887425,0.000543344619121817,
4.59417988242975));
#17250=CARTESIAN_POINT('Ctrl Pts',(16.3335702392533,-0.153841115924154,
4.59274603025257));
#17251=CARTESIAN_POINT('Ctrl Pts',(16.3459858897642,-0.309239316255332,
4.53116741914846));
#17252=CARTESIAN_POINT('Ctrl Pts',(16.3584015402751,-0.418549561707542,
4.42300972860235));
#17253=CARTESIAN_POINT('Ctrl Pts',(16.3743068189627,-0.558583297016706,
4.28445249321304));
#17254=CARTESIAN_POINT('Ctrl Pts',(16.3902120976503,-0.622980598348072,
4.06945282343469));
#17255=CARTESIAN_POINT('Ctrl Pts',(16.4061173763379,-0.582172949355422,
3.87672947174358));
#17256=CARTESIAN_POINT('Ctrl Pts',(16.4220226550255,-0.541365300362771,
3.68400612005246));
#17257=CARTESIAN_POINT('Ctrl Pts',(16.4379279337131,-0.395352701046104,
3.5135590864486));
#17258=CARTESIAN_POINT('Ctrl Pts',(16.4538332124007,-0.211177959727979,
3.44365043774355));
#17259=CARTESIAN_POINT('Ctrl Pts',(16.4697384910883,-0.0270032184098532,
3.37374178903851));
#17260=CARTESIAN_POINT('Ctrl Pts',(16.485643769776,0.195333664909731,3.40437152523229));
#17261=CARTESIAN_POINT('Ctrl Pts',(16.5015490484636,0.353744999708243,3.52147576730199));
#17262=CARTESIAN_POINT('Ctrl Pts',(16.5174543271512,0.512156334506764,3.63858000937169));
#17263=CARTESIAN_POINT('Ctrl Pts',(16.5333596058388,0.606642120784206,3.84215875731731));
#17264=CARTESIAN_POINT('Ctrl Pts',(16.5492648845264,0.59381848284593,4.03873726278877));
#17265=CARTESIAN_POINT('Ctrl Pts',(16.565170163214,0.580994844907655,4.23531576826023));
#17266=CARTESIAN_POINT('Ctrl Pts',(16.5810754419016,0.460861782753675,4.42489403125753));
#17267=CARTESIAN_POINT('Ctrl Pts',(16.5969807205892,0.288579316114369,4.52042573380721));
#17268=CARTESIAN_POINT('Ctrl Pts',(16.6050386766403,0.201297315476928,4.56882414767653));
#17269=CARTESIAN_POINT('Ctrl Pts',(16.6130966326914,0.100630370301649,4.59308406930439));
#17270=CARTESIAN_POINT('Ctrl Pts',(16.6211545887425,-2.1752937549985E-5,
4.5931168278739));
#17271=CARTESIAN_POINT('Origin',(4.,0.,4.));
#17272=CARTESIAN_POINT('',(17.0288454112575,0.000186802344652959,4.59500977980842));
#17273=CARTESIAN_POINT('',(16.9211545887425,-0.000535257393875686,4.59425998651214));
#17274=CARTESIAN_POINT('',(4.,-7.27562663373442E-17,4.5941));
#17275=CARTESIAN_POINT('Ctrl Pts',(17.0288454112575,0.000186802344652959,
4.59500977980842));
#17276=CARTESIAN_POINT('Ctrl Pts',(17.0280248863039,0.0103527338555297,
4.59505157132578));
#17277=CARTESIAN_POINT('Ctrl Pts',(17.0272043613502,0.0205166685362397,
4.5948136789481));
#17278=CARTESIAN_POINT('Ctrl Pts',(17.0263838363966,0.0306658549750798,
4.59428997251885));
#17279=CARTESIAN_POINT('Ctrl Pts',(17.010478557709,0.227400443050786,4.58413830477164));
#17280=CARTESIAN_POINT('Ctrl Pts',(16.9945732790214,0.418593379366704,4.46659200952389));
#17281=CARTESIAN_POINT('Ctrl Pts',(16.9786680003338,0.516456956272638,4.29562337257973));
#17282=CARTESIAN_POINT('Ctrl Pts',(16.9627627216462,0.614320533178566,4.12465473563558));
#17283=CARTESIAN_POINT('Ctrl Pts',(16.9468574429585,0.618854750674521,3.90026375699502));
#17284=CARTESIAN_POINT('Ctrl Pts',(16.9309521642709,0.527977687913284,3.72548128085037));
#17285=CARTESIAN_POINT('Ctrl Pts',(16.9150468855833,0.437100625152047,3.55069880470573));
#17286=CARTESIAN_POINT('Ctrl Pts',(16.8991416068957,0.25081228213362,3.42552483105699));
#17287=CARTESIAN_POINT('Ctrl Pts',(16.8832363282081,0.054648384762208,3.40743395292956));
#17288=CARTESIAN_POINT('Ctrl Pts',(16.8673310495205,-0.141515512609204,
3.38934307480212));
#17289=CARTESIAN_POINT('Ctrl Pts',(16.8514257708328,-0.347554964333599,
3.47833529219599));
#17290=CARTESIAN_POINT('Ctrl Pts',(16.8355204921452,-0.468865370989487,
3.63354914383413));
#17291=CARTESIAN_POINT('Ctrl Pts',(16.8196152134576,-0.590175777645383,
3.78876299547228));
#17292=CARTESIAN_POINT('Ctrl Pts',(16.80370993477,-0.62675713923276,4.01019848135471));
#17293=CARTESIAN_POINT('Ctrl Pts',(16.7878046560824,-0.561812842140477,
4.19618179452704));
#17294=CARTESIAN_POINT('Ctrl Pts',(16.7718993773948,-0.496868545048197,
4.38216510769936));
#17295=CARTESIAN_POINT('Ctrl Pts',(16.7559940987072,-0.330398589276266,
4.53269624816158));
#17296=CARTESIAN_POINT('Ctrl Pts',(16.7400888200196,-0.138838935752124,
4.57865768466082));
#17297=CARTESIAN_POINT('Ctrl Pts',(16.7363410170989,-0.0937012275068688,
4.58948769960953));
#17298=CARTESIAN_POINT('Ctrl Pts',(16.7325932141782,-0.0471704703862807,
4.59451171761327));
#17299=CARTESIAN_POINT('Ctrl Pts',(16.7288454112575,-0.000548108868865471,
4.59408180714414));
#17300=CARTESIAN_POINT('Ctrl Pts',(16.6211545887425,-2.1752937549985E-5,
4.5931168278739));
#17301=CARTESIAN_POINT('Ctrl Pts',(16.629001911379,-0.0980428491191961,
4.59314873014073));
#17302=CARTESIAN_POINT('Ctrl Pts',(16.6368492340155,-0.196049888122182,
4.57020350190738));
#17303=CARTESIAN_POINT('Ctrl Pts',(16.6446965566521,-0.281666676968544,
4.52419924569128));
#17304=CARTESIAN_POINT('Ctrl Pts',(16.6606018353397,-0.455198332287519,
4.43095591292362));
#17305=CARTESIAN_POINT('Ctrl Pts',(16.6765071140273,-0.577829771800838,
4.24298410528626));
#17306=CARTESIAN_POINT('Ctrl Pts',(16.6924123927149,-0.593253826592341,
4.0465925244149));
#17307=CARTESIAN_POINT('Ctrl Pts',(16.7083176714025,-0.608677881383846,
3.85020094354353));
#17308=CARTESIAN_POINT('Ctrl Pts',(16.7242229500901,-0.516894551453523,
3.64538958943816));
#17309=CARTESIAN_POINT('Ctrl Pts',(16.7401282287778,-0.360046858872914,
3.52619917105016));
#17310=CARTESIAN_POINT('Ctrl Pts',(16.7560335074654,-0.203199166292313,
3.40700875266216));
#17311=CARTESIAN_POINT('Ctrl Pts',(16.771938786153,0.0187128889385656,3.37343926999153));
#17312=CARTESIAN_POINT('Ctrl Pts',(16.7878440648406,0.203796679382533,3.44090440927292));
#17313=CARTESIAN_POINT('Ctrl Pts',(16.8037493435282,0.388880469826499,3.50836954855431));
#17314=CARTESIAN_POINT('Ctrl Pts',(16.8196546222158,0.537135995483554,3.67686930978772));
#17315=CARTESIAN_POINT('Ctrl Pts',(16.8355599009034,0.58049059114602,3.86903573125179));
#17316=CARTESIAN_POINT('Ctrl Pts',(16.851465179591,0.623845186808487,4.06120215271587));
#17317=CARTESIAN_POINT('Ctrl Pts',(16.8673704582787,0.562298852476364,4.2770352344106));
#17318=CARTESIAN_POINT('Ctrl Pts',(16.8832757369663,0.424111061064287,4.41743355636644));
#17319=CARTESIAN_POINT('Ctrl Pts',(16.8959020208917,0.314411738992559,4.5288876912157));
#17320=CARTESIAN_POINT('Ctrl Pts',(16.9085283048171,0.156414067554279,4.59280392009262));
#17321=CARTESIAN_POINT('Ctrl Pts',(16.9211545887425,-0.000535257393875686,
4.59425998651214));
#17322=CARTESIAN_POINT('Origin',(4.,0.,4.));
#17323=CARTESIAN_POINT('',(17.3288454112575,0.000452601584348983,4.59351524744837));
#17324=CARTESIAN_POINT('',(17.2211545887425,0.000283723793354941,4.5949151055343));
#17325=CARTESIAN_POINT('',(4.,-7.27562663373442E-17,4.5941));
#17326=CARTESIAN_POINT('Ctrl Pts',(17.3288454112575,0.000452601584348983,
4.59351524744837));
#17327=CARTESIAN_POINT('Ctrl Pts',(17.3234565584296,0.0676518012035294,
4.59398979695312));
#17328=CARTESIAN_POINT('Ctrl Pts',(17.3180677056016,0.134706745978521,4.58346365752876));
#17329=CARTESIAN_POINT('Ctrl Pts',(17.3126788527736,0.197661386620268,4.56129398922237));
#17330=CARTESIAN_POINT('Ctrl Pts',(17.296773574086,0.383472937993069,4.49585988588324));
#17331=CARTESIAN_POINT('Ctrl Pts',(17.2808682953984,0.533564938357213,4.32899388620009));
#17332=CARTESIAN_POINT('Ctrl Pts',(17.2649630167108,0.579021491014364,4.13731379770915));
#17333=CARTESIAN_POINT('Ctrl Pts',(17.2490577380232,0.624478043671518,3.94563370921821));
#17334=CARTESIAN_POINT('Ctrl Pts',(17.2331524593355,0.565299148621668,3.72913953191949));
#17335=CARTESIAN_POINT('Ctrl Pts',(17.2172471806479,0.428657250819126,3.58723623291525));
#17336=CARTESIAN_POINT('Ctrl Pts',(17.2013419019603,0.292015353016592,3.44533293391101));
#17337=CARTESIAN_POINT('Ctrl Pts',(17.1854366232727,0.0779104524613767,
3.37802051320125));
#17338=CARTESIAN_POINT('Ctrl Pts',(17.1695313445851,-0.115349538542919,
3.41620598662221));
#17339=CARTESIAN_POINT('Ctrl Pts',(17.1536260658975,-0.308609529547215,
3.45439146004317));
#17340=CARTESIAN_POINT('Ctrl Pts',(17.1377207872099,-0.48102461100059,3.59807482759486));
#17341=CARTESIAN_POINT('Ctrl Pts',(17.1218155085223,-0.553429071780215,
3.78128276563952));
#17342=CARTESIAN_POINT('Ctrl Pts',(17.1059102298347,-0.625833532559839,
3.96449070368418));
#17343=CARTESIAN_POINT('Ctrl Pts',(17.090004951147,-0.598227372665711,4.18722321222181));
#17344=CARTESIAN_POINT('Ctrl Pts',(17.0740996724594,-0.483286172800906,
4.34721094636728));
#17345=CARTESIAN_POINT('Ctrl Pts',(17.0590149187255,-0.374274584390508,
4.4989451987145));
#17346=CARTESIAN_POINT('Ctrl Pts',(17.0439301649915,-0.186706445247169,
4.59424147319602));
#17347=CARTESIAN_POINT('Ctrl Pts',(17.0288454112575,0.000186802344652959,
4.59500977980842));
#17348=CARTESIAN_POINT('Ctrl Pts',(16.9211545887425,-0.000535257393875686,
4.59425998651214));
#17349=CARTESIAN_POINT('Ctrl Pts',(16.9244335835047,-0.0412943609811605,
4.59463812105998));
#17350=CARTESIAN_POINT('Ctrl Pts',(16.9277125782669,-0.0819827620002526,
4.59080381827239));
#17351=CARTESIAN_POINT('Ctrl Pts',(16.9309915730291,-0.121736182180322,
4.58249572362891));
#17352=CARTESIAN_POINT('Ctrl Pts',(16.9468968517167,-0.31456638552074,4.54219600671859));
#17353=CARTESIAN_POINT('Ctrl Pts',(16.9628021304043,-0.485397543709551,
4.39663301068103));
#17354=CARTESIAN_POINT('Ctrl Pts',(16.978707409092,-0.555791216176751,4.21264310503418));
#17355=CARTESIAN_POINT('Ctrl Pts',(16.9946126877796,-0.626184888643955,
4.02865319938731));
#17356=CARTESIAN_POINT('Ctrl Pts',(17.0105179664672,-0.596141075389537,
3.80623638413113));
#17357=CARTESIAN_POINT('Ctrl Pts',(17.0264232451548,-0.479454624411006,
3.64751705115182));
#17358=CARTESIAN_POINT('Ctrl Pts',(17.0423285238424,-0.362768173432475,
3.48879771817251));
#17359=CARTESIAN_POINT('Ctrl Pts',(17.05823380253,-0.159439084729831,3.39377586747005));
#17360=CARTESIAN_POINT('Ctrl Pts',(17.0741390812176,0.0371725263090214,
3.40608151284405));
#17361=CARTESIAN_POINT('Ctrl Pts',(17.0900443599052,0.233784137347885,3.41838715821804));
#17362=CARTESIAN_POINT('Ctrl Pts',(17.1059496385929,0.423678270722955,3.5380202996685));
#17363=CARTESIAN_POINT('Ctrl Pts',(17.1218549172805,0.519663574146654,3.71005045990219));
#17364=CARTESIAN_POINT('Ctrl Pts',(17.1377601959681,0.615648877570348,3.88208062013586));
#17365=CARTESIAN_POINT('Ctrl Pts',(17.1536654746557,0.617725351042682,4.10650779915277));
#17366=CARTESIAN_POINT('Ctrl Pts',(17.1695707533433,0.524939565793509,4.28028453107927));
#17367=CARTESIAN_POINT('Ctrl Pts',(17.1854760320309,0.432153780544336,4.45406126300578));
#17368=CARTESIAN_POINT('Ctrl Pts',(17.2013813107185,0.244505736573655,4.5771875478419));
#17369=CARTESIAN_POINT('Ctrl Pts',(17.2172865894061,0.0481554769387473,
4.59312900463441));
#17370=CARTESIAN_POINT('Ctrl Pts',(17.2185759225182,0.0322386925622284,
4.59442127046022));
#17371=CARTESIAN_POINT('Ctrl Pts',(17.2198652556304,0.0162647237884017,
4.5950091984451));
#17372=CARTESIAN_POINT('Ctrl Pts',(17.2211545887425,0.000283723793354941,
4.5949151055343));
#17373=CARTESIAN_POINT('Origin',(4.,0.,4.));
#17374=CARTESIAN_POINT('',(17.6288454112575,-0.000376811216598938,4.5933658344624));
#17375=CARTESIAN_POINT('',(17.5211545887425,0.000390292690419375,4.59338796628294));
#17376=CARTESIAN_POINT('',(4.,-7.27562663373442E-17,4.5941));
#17377=CARTESIAN_POINT('Ctrl Pts',(17.6288454112575,-0.000376811216598938,
4.5933658344624));
#17378=CARTESIAN_POINT('Ctrl Pts',(17.6188882305552,0.123868145157646,4.5926473455414));
#17379=CARTESIAN_POINT('Ctrl Pts',(17.608931049853,0.248515939035854,4.55458993700248));
#17380=CARTESIAN_POINT('Ctrl Pts',(17.5989738691507,0.348483110949462,4.48236965854082));
#17381=CARTESIAN_POINT('Ctrl Pts',(17.5830685904631,0.508167440925656,4.36700731952407));
#17382=CARTESIAN_POINT('Ctrl Pts',(17.5671633117754,0.604877102606476,4.16447556457896));
#17383=CARTESIAN_POINT('Ctrl Pts',(17.5512580330878,0.594207110796467,3.96776840716434));
#17384=CARTESIAN_POINT('Ctrl Pts',(17.5353527544002,0.583537118986457,3.77106124974973));
#17385=CARTESIAN_POINT('Ctrl Pts',(17.5194474757126,0.465487473685617,3.58017868986561));
#17386=CARTESIAN_POINT('Ctrl Pts',(17.503542197025,0.294261577747463,3.48276592343564));
#17387=CARTESIAN_POINT('Ctrl Pts',(17.4876369183374,0.123035681809298,3.38535315700567));
#17388=CARTESIAN_POINT('Ctrl Pts',(17.4717316396498,-0.101366464766187,
3.38141018402985));
#17389=CARTESIAN_POINT('Ctrl Pts',(17.4558263609621,-0.275908889943427,
3.47274745088526));
#17390=CARTESIAN_POINT('Ctrl Pts',(17.4399210822745,-0.450451315120656,
3.56408471774066));
#17391=CARTESIAN_POINT('Ctrl Pts',(17.4240158035869,-0.575134018899647,
3.75070222442727));
#17392=CARTESIAN_POINT('Ctrl Pts',(17.4081105248993,-0.592707978595278,
3.94691310701022));
#17393=CARTESIAN_POINT('Ctrl Pts',(17.3922052462117,-0.610281938290908,
4.14312398959316));
#17394=CARTESIAN_POINT('Ctrl Pts',(17.3762999675241,-0.520747153903178,
4.34892824807245));
#17395=CARTESIAN_POINT('Ctrl Pts',(17.3603946888365,-0.365214210518585,
4.46982927381454));
#17396=CARTESIAN_POINT('Ctrl Pts',(17.3498782629768,-0.262377240481122,
4.54976793433994));
#17397=CARTESIAN_POINT('Ctrl Pts',(17.3393618371172,-0.130687628661636,
4.59258915708319));
#17398=CARTESIAN_POINT('Ctrl Pts',(17.3288454112575,0.000452601584348983,
4.59351524744837));
#17399=CARTESIAN_POINT('Ctrl Pts',(17.2211545887425,0.000283723793354941,
4.5949151055343));
#17400=CARTESIAN_POINT('Ctrl Pts',(17.235770534318,-0.18087770297476,4.59384846352355));
#17401=CARTESIAN_POINT('Ctrl Pts',(17.2503864798935,-0.362942684182573,
4.50513801271133));
#17402=CARTESIAN_POINT('Ctrl Pts',(17.265002425469,-0.47285052735612,4.36129398677095));
#17403=CARTESIAN_POINT('Ctrl Pts',(17.2809077041566,-0.592453796716944,
4.20476088336606));
#17404=CARTESIAN_POINT('Ctrl Pts',(17.2968129828442,-0.626607860139456,
3.98293804780737));
#17405=CARTESIAN_POINT('Ctrl Pts',(17.3127182615318,-0.559630616639302,
3.79767714163318));
#17406=CARTESIAN_POINT('Ctrl Pts',(17.3286235402194,-0.492653373139145,
3.61241623545897));
#17407=CARTESIAN_POINT('Ctrl Pts',(17.3445288189071,-0.324544822716309,
3.46371725866926));
#17408=CARTESIAN_POINT('Ctrl Pts',(17.3604340975947,-0.132493299638714,
3.41985649047097));
#17409=CARTESIAN_POINT('Ctrl Pts',(17.3763393762823,0.0595582234388708,
3.37599572227269));
#17410=CARTESIAN_POINT('Ctrl Pts',(17.3922446549699,0.275552719171213,3.43697316266583));
#17411=CARTESIAN_POINT('Ctrl Pts',(17.4081499336575,0.416314653091553,3.5747905507646));
#17412=CARTESIAN_POINT('Ctrl Pts',(17.4240552123451,0.557076587011893,3.71260793886338));
#17413=CARTESIAN_POINT('Ctrl Pts',(17.4399604910327,0.622605959120231,3.92726527466781));
#17414=CARTESIAN_POINT('Ctrl Pts',(17.4558657697203,0.582814454063527,4.12020099097945));
#17415=CARTESIAN_POINT('Ctrl Pts',(17.4717710484079,0.543022949006823,4.31313670729109));
#17416=CARTESIAN_POINT('Ctrl Pts',(17.4876763270955,0.397910566785078,4.48435080410994));
#17417=CARTESIAN_POINT('Ctrl Pts',(17.5035816057832,0.214106774115907,4.55522901164789));
#17418=CARTESIAN_POINT('Ctrl Pts',(17.5094392667696,0.146414762764002,4.58133232736073));
#17419=CARTESIAN_POINT('Ctrl Pts',(17.515296927756,0.073474912906076,4.59382676872096));
#17420=CARTESIAN_POINT('Ctrl Pts',(17.5211545887425,0.000390292690419375,
4.59338796628294));
#17421=CARTESIAN_POINT('Origin',(4.,0.,4.));
#17422=CARTESIAN_POINT('',(17.9288454112575,-0.000301159635511528,4.59489313984584));
#17423=CARTESIAN_POINT('',(17.8211545887425,-0.000441626631060947,4.59348913571676));
#17424=CARTESIAN_POINT('',(4.,-7.27562663373442E-17,4.5941));
#17425=CARTESIAN_POINT('Ctrl Pts',(17.9288454112575,-0.000301159635511528,
4.59489313984584));
#17426=CARTESIAN_POINT('Ctrl Pts',(17.9143199026809,0.179756887528332,4.59377956832623));
#17427=CARTESIAN_POINT('Ctrl Pts',(17.8997943941043,0.360751589755073,4.50630604003092));
#17428=CARTESIAN_POINT('Ctrl Pts',(17.8852688855277,0.470789914960854,4.36397502945801));
#17429=CARTESIAN_POINT('Ctrl Pts',(17.8693636068401,0.591280720462369,4.20812407407766));
#17430=CARTESIAN_POINT('Ctrl Pts',(17.8534583281524,0.626694694978596,3.98649889312445));
#17431=CARTESIAN_POINT('Ctrl Pts',(17.8375530494648,0.560771239653389,3.80086039350393));
#17432=CARTESIAN_POINT('Ctrl Pts',(17.8216477707772,0.494847784328189,3.61522189388343));
#17433=CARTESIAN_POINT('Ctrl Pts',(17.8057424920896,0.327586899161578,3.46557007559562));
#17434=CARTESIAN_POINT('Ctrl Pts',(17.789837213402,0.135787706397568,3.42061872235194));
#17435=CARTESIAN_POINT('Ctrl Pts',(17.7739319347144,-0.0560114863664412,
3.37566736910827));
#17436=CARTESIAN_POINT('Ctrl Pts',(17.7580266560268,-0.272348986727849,
3.43541648090873));
#17437=CARTESIAN_POINT('Ctrl Pts',(17.7421213773392,-0.41389176700556,3.57243179339102));
#17438=CARTESIAN_POINT('Ctrl Pts',(17.7262160986515,-0.555434547283271,
3.7094471058733));
#17439=CARTESIAN_POINT('Ctrl Pts',(17.710310819964,-0.622182607477285,3.92372861903742));
#17440=CARTESIAN_POINT('Ctrl Pts',(17.6944055412763,-0.583488062224059,
4.11688732754162));
#17441=CARTESIAN_POINT('Ctrl Pts',(17.6785002625887,-0.544793516970831,
4.31004603604583));
#17442=CARTESIAN_POINT('Ctrl Pts',(17.6625949839011,-0.400656366270352,
4.48208193989012));
#17443=CARTESIAN_POINT('Ctrl Pts',(17.6466897052135,-0.217258291784321,
4.55400343026805));
#17444=CARTESIAN_POINT('Ctrl Pts',(17.6407416072282,-0.148672903323923,
4.58089991415997));
#17445=CARTESIAN_POINT('Ctrl Pts',(17.6347935092429,-0.0745967331795002,
4.59379503652584));
#17446=CARTESIAN_POINT('Ctrl Pts',(17.6288454112575,-0.000376811216598938,
4.5933658344624));
#17447=CARTESIAN_POINT('Ctrl Pts',(17.5211545887425,0.000390292690419375,
4.59338796628294));
#17448=CARTESIAN_POINT('Ctrl Pts',(17.5312022064437,-0.12497140465997,4.59263529057266));
#17449=CARTESIAN_POINT('Ctrl Pts',(17.5412498241448,-0.250759050797478,
4.55382993891589));
#17450=CARTESIAN_POINT('Ctrl Pts',(17.551297441846,-0.351218450958555,4.48038168762358));
#17451=CARTESIAN_POINT('Ctrl Pts',(17.5672027205336,-0.510244680247213,
4.36411383780432));
#17452=CARTESIAN_POINT('Ctrl Pts',(17.5831079992212,-0.605801935707933,
4.16103581990878));
#17453=CARTESIAN_POINT('Ctrl Pts',(17.5990132779088,-0.594014368327242,
3.96439246823218));
#17454=CARTESIAN_POINT('Ctrl Pts',(17.6149185565964,-0.58222680094655,3.76774911655557));
#17455=CARTESIAN_POINT('Ctrl Pts',(17.6308238352841,-0.463094410724447,
3.5775404310979));
#17456=CARTESIAN_POINT('Ctrl Pts',(17.6467291139717,-0.291317751175132,
3.48110219315546));
#17457=CARTESIAN_POINT('Ctrl Pts',(17.6626343926593,-0.119541091625818,
3.38466395521302));
#17458=CARTESIAN_POINT('Ctrl Pts',(17.6785396713469,0.104879837250709,3.38199616478582));
#17459=CARTESIAN_POINT('Ctrl Pts',(17.6944449500345,0.278900439380867,3.47432375837312));
#17460=CARTESIAN_POINT('Ctrl Pts',(17.7103502287221,0.452921041511034,3.56665135196042));
#17461=CARTESIAN_POINT('Ctrl Pts',(17.7262555074097,0.576541316894826,3.75397432956222));
#17462=CARTESIAN_POINT('Ctrl Pts',(17.7421607860974,0.593000065018554,3.95028190484542));
#17463=CARTESIAN_POINT('Ctrl Pts',(17.758066064785,0.60945881314228,4.1465894801286));
#17464=CARTESIAN_POINT('Ctrl Pts',(17.7739713434726,0.518756034005955,4.35188165309317));
#17465=CARTESIAN_POINT('Ctrl Pts',(17.7898766221602,0.362538606470845,4.47189694310939));
#17466=CARTESIAN_POINT('Ctrl Pts',(17.8003026110209,0.260137309937395,4.55056755941266));
#17467=CARTESIAN_POINT('Ctrl Pts',(17.8107285998817,0.129585238016204,4.59259583028147));
#17468=CARTESIAN_POINT('Ctrl Pts',(17.8211545887425,-0.000441626631060947,
4.59348913571676));
#17469=CARTESIAN_POINT('Origin',(4.,0.,4.));
#17470=CARTESIAN_POINT('',(18.2288454112575,0.000530626821107938,4.59429426521737));
#17471=CARTESIAN_POINT('',(18.1211545887425,-0.000206261771334874,4.59499421029555));
#17472=CARTESIAN_POINT('',(4.,-7.27562663373442E-17,4.5941));
#17473=CARTESIAN_POINT('Ctrl Pts',(18.2288454112575,0.000530626821107938,
4.59429426521737));
#17474=CARTESIAN_POINT('Ctrl Pts',(18.2256568534942,0.0401596894680921,
4.59466101186164));
#17475=CARTESIAN_POINT('Ctrl Pts',(18.2224682957309,0.0797220295111884,
4.5910372210354));
#17476=CARTESIAN_POINT('Ctrl Pts',(18.2192797379675,0.118424305077702,4.58317806034235));
#17477=CARTESIAN_POINT('Ctrl Pts',(18.2033744592799,0.311480390123117,4.54397471188459));
#17478=CARTESIAN_POINT('Ctrl Pts',(18.1874691805923,0.483135922039688,4.39938477867344));
#17479=CARTESIAN_POINT('Ctrl Pts',(18.1715639019047,0.554573942717995,4.21579784094385));
#17480=CARTESIAN_POINT('Ctrl Pts',(18.1556586232171,0.626011963396302,4.03221090321426));
#17481=CARTESIAN_POINT('Ctrl Pts',(18.1397533445295,0.597232472836345,3.80962696096622));
#17482=CARTESIAN_POINT('Ctrl Pts',(18.1238480658419,0.481449795543417,3.65024714373002));
#17483=CARTESIAN_POINT('Ctrl Pts',(18.1079427871543,0.365667118250483,3.49086732649381));
#17484=CARTESIAN_POINT('Ctrl Pts',(18.0920375084667,0.16288125422457,3.39469163426944));
#17485=CARTESIAN_POINT('Ctrl Pts',(18.076132229779,-0.0337971069360236,
3.40587987606835));
#17486=CARTESIAN_POINT('Ctrl Pts',(18.0602269510914,-0.230475468096606,
3.41706811786726));
#17487=CARTESIAN_POINT('Ctrl Pts',(18.0443216724038,-0.421046326391869,
3.53562029368944));
#17488=CARTESIAN_POINT('Ctrl Pts',(18.0284163937162,-0.518007606080761,
3.70710225992629));
#17489=CARTESIAN_POINT('Ctrl Pts',(18.0125111150286,-0.614968885769652,
3.87858422616314));
#17490=CARTESIAN_POINT('Ctrl Pts',(17.996605836341,-0.618320586852172,4.10299598281466));
#17491=CARTESIAN_POINT('Ctrl Pts',(17.9807005576534,-0.526523749990007,
4.27729714530494));
#17492=CARTESIAN_POINT('Ctrl Pts',(17.9647952789658,-0.434726913127837,
4.45159830779523));
#17493=CARTESIAN_POINT('Ctrl Pts',(17.9488900002781,-0.247781538320971,
4.57578887612429));
#17494=CARTESIAN_POINT('Ctrl Pts',(17.9329847215905,-0.0515250326741526,
4.59284579538505));
#17495=CARTESIAN_POINT('Ctrl Pts',(17.9316049514795,-0.0344999389365885,
4.59432546938787));
#17496=CARTESIAN_POINT('Ctrl Pts',(17.9302251813685,-0.0174047750035579,
4.59499891739512));
#17497=CARTESIAN_POINT('Ctrl Pts',(17.9288454112575,-0.000301159635511528,
4.59489313984584));
#17498=CARTESIAN_POINT('Ctrl Pts',(17.8211545887425,-0.000441626631060947,
4.59348913571676));
#17499=CARTESIAN_POINT('Ctrl Pts',(17.8266338785693,-0.0687761401428734,
4.59395860479535));
#17500=CARTESIAN_POINT('Ctrl Pts',(17.8321131683962,-0.136965594625977,
4.58306684864343));
#17501=CARTESIAN_POINT('Ctrl Pts',(17.837592458223,-0.200847632772524,4.56016175744822));
#17502=CARTESIAN_POINT('Ctrl Pts',(17.8534977369106,-0.386284368546891,
4.49367287470298));
#17503=CARTESIAN_POINT('Ctrl Pts',(17.8694030155983,-0.535425764161732,
4.32595670214462));
#17504=CARTESIAN_POINT('Ctrl Pts',(17.8853082942859,-0.579792400402821,
4.13402141072584));
#17505=CARTESIAN_POINT('Ctrl Pts',(17.9012135729735,-0.624159036643913,
3.94208611930704));
#17506=CARTESIAN_POINT('Ctrl Pts',(17.9171188516611,-0.563750913511241,
3.72593170902781));
#17507=CARTESIAN_POINT('Ctrl Pts',(17.9330241303487,-0.426304885490399,
3.58480714034942));
#17508=CARTESIAN_POINT('Ctrl Pts',(17.9489294090363,-0.288858857469565,
3.44368257167104));
#17509=CARTESIAN_POINT('Ctrl Pts',(17.9648346877239,-0.0743749245605683,
3.37758784459349));
#17510=CARTESIAN_POINT('Ctrl Pts',(17.9807399664116,0.118664965311668,3.41687086155347));
#17511=CARTESIAN_POINT('Ctrl Pts',(17.9966452450992,0.311704855183904,3.45615387851346));
#17512=CARTESIAN_POINT('Ctrl Pts',(18.0125505237868,0.483300702019379,3.60081463951098));
#17513=CARTESIAN_POINT('Ctrl Pts',(18.0284558024744,0.554662952572844,3.78443104318807));
#17514=CARTESIAN_POINT('Ctrl Pts',(18.044361081162,0.62602520312631,3.96804744686516));
#17515=CARTESIAN_POINT('Ctrl Pts',(18.0602663598496,0.597153857397765,4.19061949322182));
#17516=CARTESIAN_POINT('Ctrl Pts',(18.0761716385372,0.481305415899848,4.34995151481781));
#17517=CARTESIAN_POINT('Ctrl Pts',(18.0911659552723,0.372092100044007,4.50015792394613));
#17518=CARTESIAN_POINT('Ctrl Pts',(18.1061602720074,0.185579460002099,4.59416090236354));
#17519=CARTESIAN_POINT('Ctrl Pts',(18.1211545887425,-0.000206261771334874,
4.59499421029555));
#17520=CARTESIAN_POINT('Origin',(4.,0.,4.));
#17521=CARTESIAN_POINT('',(18.5288454112575,4.04073003155148E-5,4.59311858068669));
#17522=CARTESIAN_POINT('',(18.4211545887425,0.000547083855738422,4.59411609730493));
#17523=CARTESIAN_POINT('',(4.,-7.27562663373442E-17,4.5941));
#17524=CARTESIAN_POINT('Ctrl Pts',(18.5288454112575,4.04073003155148E-5,
4.59311858068669));
#17525=CARTESIAN_POINT('Ctrl Pts',(18.5210885256199,0.0969311390001333,
4.59317716754242));
#17526=CARTESIAN_POINT('Ctrl Pts',(18.5133316399822,0.193796352446061,4.57078374547556));
#17527=CARTESIAN_POINT('Ctrl Pts',(18.5055747543446,0.27868347559656,4.52579129559858));
#17528=CARTESIAN_POINT('Ctrl Pts',(18.489669475657,0.452742165355285,4.43353552600749));
#17529=CARTESIAN_POINT('Ctrl Pts',(18.4737641969693,0.576439736070726,4.24626358090446));
#17530=CARTESIAN_POINT('Ctrl Pts',(18.4578589182817,0.592979496483005,4.04996281465819));
#17531=CARTESIAN_POINT('Ctrl Pts',(18.4419536395941,0.609519256895283,3.85366204841193));
#17532=CARTESIAN_POINT('Ctrl Pts',(18.4260483609065,0.518901207004412,3.64833246102244));
#17533=CARTESIAN_POINT('Ctrl Pts',(18.4101430822189,0.362733321586741,3.52825271224048));
#17534=CARTESIAN_POINT('Ctrl Pts',(18.3942378035313,0.206565436169079,3.40817296345854));
#17535=CARTESIAN_POINT('Ctrl Pts',(18.3783325248437,-0.015152284775374,
3.37334305328413));
#17536=CARTESIAN_POINT('Ctrl Pts',(18.3624272461561,-0.200616443892158,
3.43975540293737));
#17537=CARTESIAN_POINT('Ctrl Pts',(18.3465219674685,-0.386080603008964,
3.50616775259061));
#17538=CARTESIAN_POINT('Ctrl Pts',(18.3306166887808,-0.535291200298091,
3.67382236207151));
#17539=CARTESIAN_POINT('Ctrl Pts',(18.3147114100932,-0.579737042064157,
3.86573932758804));
#17540=CARTESIAN_POINT('Ctrl Pts',(18.2988061314056,-0.624182883830224,
4.05765629310458));
#17541=CARTESIAN_POINT('Ctrl Pts',(18.282900852718,-0.563863970073232,4.27383561465674));
#17542=CARTESIAN_POINT('Ctrl Pts',(18.2669955740304,-0.426476194107598,
4.41501689358062));
#17543=CARTESIAN_POINT('Ctrl Pts',(18.2542788531061,-0.316630774880643,
4.52789532589669));
#17544=CARTESIAN_POINT('Ctrl Pts',(18.2415621321818,-0.157519428275204,
4.5928315930404));
#17545=CARTESIAN_POINT('Ctrl Pts',(18.2288454112575,0.000530626821107938,
4.59429426521737));
#17546=CARTESIAN_POINT('Ctrl Pts',(18.1211545887425,-0.000206261771334874,
4.59499421029555));
#17547=CARTESIAN_POINT('Ctrl Pts',(18.122065550695,-0.0114934532352288,
4.59504483693191));
#17548=CARTESIAN_POINT('Ctrl Pts',(18.1229765126475,-0.0227779616248223,
4.59475157188293));
#17549=CARTESIAN_POINT('Ctrl Pts',(18.1238874746001,-0.0340422900297544,
4.59410612569417));
#17550=CARTESIAN_POINT('Ctrl Pts',(18.1397927532877,-0.230716017194119,
4.58283671813918));
#17551=CARTESIAN_POINT('Ctrl Pts',(18.1556980319753,-0.421237934255556,
4.46420590619388));
#17552=CARTESIAN_POINT('Ctrl Pts',(18.1716033106629,-0.518128437217054,
4.29268393984778));
#17553=CARTESIAN_POINT('Ctrl Pts',(18.1875085893505,-0.615018940178556,
4.12116197350168));
#17554=CARTESIAN_POINT('Ctrl Pts',(18.2034138680381,-0.618278029040109,
3.89674885275477));
#17555=CARTESIAN_POINT('Ctrl Pts',(18.2193191467258,-0.526409268077163,
3.72248558851787));
#17556=CARTESIAN_POINT('Ctrl Pts',(18.2352244254134,-0.434540507114227,
3.54822232428098));
#17557=CARTESIAN_POINT('Ctrl Pts',(18.251129704101,-0.24754389632682,3.42410891655409));
#17558=CARTESIAN_POINT('Ctrl Pts',(18.2670349827886,-0.0512803682143169,
3.40713299136011));
#17559=CARTESIAN_POINT('Ctrl Pts',(18.2829402614762,0.144983159898198,3.39015706616613));
#17560=CARTESIAN_POINT('Ctrl Pts',(18.2988455401638,0.35051360533581,3.48031862350507));
#17561=CARTESIAN_POINT('Ctrl Pts',(18.3147508188514,0.470940082829639,3.63621929066782));
#17562=CARTESIAN_POINT('Ctrl Pts',(18.330656097539,0.591366560323475,3.79211995783059));
#17563=CARTESIAN_POINT('Ctrl Pts',(18.3465613762266,0.62668906987352,4.01375973481717));
#17564=CARTESIAN_POINT('Ctrl Pts',(18.3624666549143,0.560689009466533,4.199371012841));
#17565=CARTESIAN_POINT('Ctrl Pts',(18.3783719336019,0.49468894905955,4.38498229086483));
#17566=CARTESIAN_POINT('Ctrl Pts',(18.3942772122895,0.327366318695548,4.53456506992591));
#17567=CARTESIAN_POINT('Ctrl Pts',(18.4101824909771,0.135548591400956,4.57943726620491));
#17568=CARTESIAN_POINT('Ctrl Pts',(18.4138398568989,0.0914407431336166,
4.58975547846199));
#17569=CARTESIAN_POINT('Ctrl Pts',(18.4174972228207,0.0460377050408626,
4.59453706917327));
#17570=CARTESIAN_POINT('Ctrl Pts',(18.4211545887425,0.000547083855738422,
4.59411609730493));
#17571=CARTESIAN_POINT('Origin',(4.,0.,4.));
#17572=CARTESIAN_POINT('',(18.8288454112575,-0.000545657836941327,4.59414547262434));
#17573=CARTESIAN_POINT('',(18.7211545887425,-5.63168744233308E-5,4.59312091231189));
#17574=CARTESIAN_POINT('',(4.,-7.27562663373442E-17,4.5941));
#17575=CARTESIAN_POINT('Ctrl Pts',(18.8288454112575,-0.000545657836941327,
4.59414547262434));
#17576=CARTESIAN_POINT('Ctrl Pts',(18.8165201977456,0.15273698101805,4.59272393327212));
#17577=CARTESIAN_POINT('Ctrl Pts',(18.8041949842336,0.307016766534516,4.53213273669464));
#17578=CARTESIAN_POINT('Ctrl Pts',(18.7918697707216,0.416139138999065,4.42538122089617));
#17579=CARTESIAN_POINT('Ctrl Pts',(18.775964492034,0.556957936451544,4.28762193522949));
#17580=CARTESIAN_POINT('Ctrl Pts',(18.7600592133464,0.622575889387102,4.0729916608594));
#17581=CARTESIAN_POINT('Ctrl Pts',(18.7441539346588,0.582864009884755,3.88003953951897));
#17582=CARTESIAN_POINT('Ctrl Pts',(18.7282486559712,0.543152130382401,3.6870874181785));
#17583=CARTESIAN_POINT('Ctrl Pts',(18.7123433772835,0.3981104184421,3.51581344986768));
#17584=CARTESIAN_POINT('Ctrl Pts',(18.6964380985959,0.214335891977863,3.44485939483061));
#17585=CARTESIAN_POINT('Ctrl Pts',(18.6805328199083,0.0305613655136472,
3.37390533979354));
#17586=CARTESIAN_POINT('Ctrl Pts',(18.6646275412207,-0.191945975474496,
3.40327119803019));
#17587=CARTESIAN_POINT('Ctrl Pts',(18.6487222625331,-0.351020173514001,
3.51947340980541));
#17588=CARTESIAN_POINT('Ctrl Pts',(18.6328169838455,-0.510094371553506,
3.63567562158063));
#17589=CARTESIAN_POINT('Ctrl Pts',(18.6169117051579,-0.605735426644373,
3.83871418689441));
#17590=CARTESIAN_POINT('Ctrl Pts',(18.6010064264702,-0.594029012528289,
4.03536238640794));
#17591=CARTESIAN_POINT('Ctrl Pts',(18.5851011477826,-0.582322598412206,
4.23201058592146));
#17592=CARTESIAN_POINT('Ctrl Pts',(18.569195869095,-0.463268715089173,4.42226841963472));
#17593=CARTESIAN_POINT('Ctrl Pts',(18.5532905904074,-0.29153186902666,4.51877753945177));
#17594=CARTESIAN_POINT('Ctrl Pts',(18.5451421973574,-0.203549800283198,
4.56821988225003));
#17595=CARTESIAN_POINT('Ctrl Pts',(18.5369938043075,-0.101740616897797,
4.59305703682098));
#17596=CARTESIAN_POINT('Ctrl Pts',(18.5288454112575,4.04073003155148E-5,
4.59311858068669));
#17597=CARTESIAN_POINT('Ctrl Pts',(18.4211545887425,0.000547083855738422,
4.59411609730493));
#17598=CARTESIAN_POINT('Ctrl Pts',(18.4334025015083,-0.151793472668411,
4.59270633223614));
#17599=CARTESIAN_POINT('Ctrl Pts',(18.4456504142741,-0.305116246576315,
4.53295143150856));
#17600=CARTESIAN_POINT('Ctrl Pts',(18.4578983270399,-0.414068183831284,
4.42739736222451));
#17601=CARTESIAN_POINT('Ctrl Pts',(18.4738036057275,-0.555554407543751,
4.29032364846819));
#17602=CARTESIAN_POINT('Ctrl Pts',(18.4897088844152,-0.622214030743504,
4.07601460745865));
#17603=CARTESIAN_POINT('Ctrl Pts',(18.5056141631028,-0.583439774593308,
3.88287188415962));
#17604=CARTESIAN_POINT('Ctrl Pts',(18.5215194417904,-0.54466551844311,3.68972916086059));
#17605=CARTESIAN_POINT('Ctrl Pts',(18.537424720478,-0.400457382942952,3.51775275527208));
#17606=CARTESIAN_POINT('Ctrl Pts',(18.5533299991656,-0.217029642971419,
3.44590695711865));
#17607=CARTESIAN_POINT('Ctrl Pts',(18.5692352778532,-0.0336019029998957,
3.37406115896522));
#17608=CARTESIAN_POINT('Ctrl Pts',(18.5851405565408,0.189045441442997,3.40234596824686));
#17609=CARTESIAN_POINT('Ctrl Pts',(18.6010458352284,0.348682149221421,3.51777419717301));
#17610=CARTESIAN_POINT('Ctrl Pts',(18.6169511139161,0.508318856999844,3.63320242609916));
#17611=CARTESIAN_POINT('Ctrl Pts',(18.6328563926037,0.604944928113798,3.83577407466982));
#17612=CARTESIAN_POINT('Ctrl Pts',(18.6487616712913,0.594193758619731,4.03247681196108));
#17613=CARTESIAN_POINT('Ctrl Pts',(18.6646669499789,0.583442589125664,4.22917954925235));
#17614=CARTESIAN_POINT('Ctrl Pts',(18.6805722286665,0.465314179023576,4.42001337526422));
#17615=CARTESIAN_POINT('Ctrl Pts',(18.6964775073541,0.294048096631404,4.51735547060535));
#17616=CARTESIAN_POINT('Ctrl Pts',(18.7047032011502,0.205474838715737,4.56769764225005));
#17617=CARTESIAN_POINT('Ctrl Pts',(18.7129288949463,0.102689258835563,4.59303430424318));
#17618=CARTESIAN_POINT('Ctrl Pts',(18.7211545887425,-5.63168744233308E-5,
4.59312091231189));
#17619=CARTESIAN_POINT('Origin',(4.,0.,4.));
#17620=CARTESIAN_POINT('',(19.1288454112575,0.000222628893785728,4.59497983522242));
#17621=CARTESIAN_POINT('',(19.0211545887425,-0.000526118841417405,4.59432346427954));
#17622=CARTESIAN_POINT('',(4.,-7.27562663373442E-17,4.5941));
#17623=CARTESIAN_POINT('Ctrl Pts',(19.1288454112575,0.000222628893785728,
4.59497983522242));
#17624=CARTESIAN_POINT('Ctrl Pts',(19.1278571485589,0.012468395078646,4.59503853204781));
#17625=CARTESIAN_POINT('Ctrl Pts',(19.1268688858602,0.0247107891953784,
4.59469333777414));
#17626=CARTESIAN_POINT('Ctrl Pts',(19.1258806231615,0.0369274203756033,
4.59393377720877));
#17627=CARTESIAN_POINT('Ctrl Pts',(19.1099753444739,0.233544093050454,4.58170927203582));
#17628=CARTESIAN_POINT('Ctrl Pts',(19.0940700657862,0.423487581379576,4.46215450773496));
#17629=CARTESIAN_POINT('Ctrl Pts',(19.0781647870986,0.519543871337238,4.29016397409385));
#17630=CARTESIAN_POINT('Ctrl Pts',(19.062259508411,0.615600161294901,4.11817344045274));
#17631=CARTESIAN_POINT('Ctrl Pts',(19.0463542297234,0.617769252881104,3.89374713747137));
#17632=CARTESIAN_POINT('Ctrl Pts',(19.0304489510358,0.525055191022736,3.71993212880311));
#17633=CARTESIAN_POINT('Ctrl Pts',(19.0145436723482,0.432341129164367,3.54611712013485));
#17634=CARTESIAN_POINT('Ctrl Pts',(18.9986383936606,0.244743913861428,3.42291340577968));
#17635=CARTESIAN_POINT('Ctrl Pts',(18.982733114973,0.0484002497885746,3.40689091904056));
#17636=CARTESIAN_POINT('Ctrl Pts',(18.9668278362853,-0.147943414284278,
3.39086843230144));
#17637=CARTESIAN_POINT('Ctrl Pts',(18.9509225575977,-0.353033527127044,
3.48202717317836));
#17638=CARTESIAN_POINT('Ctrl Pts',(18.9350172789101,-0.472701385564812,
3.63851090447403));
#17639=CARTESIAN_POINT('Ctrl Pts',(18.9191120002225,-0.592369244002587,
3.79499463576972));
#17640=CARTESIAN_POINT('Ctrl Pts',(18.9032067215349,-0.626614848035354,
4.01680335748416));
#17641=CARTESIAN_POINT('Ctrl Pts',(18.8873014428473,-0.559714065105754,
4.20209188855652));
#17642=CARTESIAN_POINT('Ctrl Pts',(18.8713961641597,-0.492813282176159,
4.38738041962887));
#17643=CARTESIAN_POINT('Ctrl Pts',(18.8554908854721,-0.324766112284209,
4.53614876005914));
#17644=CARTESIAN_POINT('Ctrl Pts',(18.8395856067844,-0.132732706353525,
4.58008878179264));
#17645=CARTESIAN_POINT('Ctrl Pts',(18.8360055416088,-0.0895085590353085,
4.5899790920924));
#17646=CARTESIAN_POINT('Ctrl Pts',(18.8324254764332,-0.0450691735440342,
4.59455838259347));
#17647=CARTESIAN_POINT('Ctrl Pts',(18.8288454112575,-0.000545657836941327,
4.59414547262434));
#17648=CARTESIAN_POINT('Ctrl Pts',(18.7211545887425,-5.63168744233308E-5,
4.59312091231189));
#17649=CARTESIAN_POINT('Ctrl Pts',(18.728834173634,-0.0959805501911411,
4.59320177041728));
#17650=CARTESIAN_POINT('Ctrl Pts',(18.7365137585255,-0.191869914813978,
4.57127401300463));
#17651=CARTESIAN_POINT('Ctrl Pts',(18.744193343417,-0.276126457005151,4.5271386400555));
#17652=CARTESIAN_POINT('Ctrl Pts',(18.7600986221046,-0.450631173567243,
4.43572934949413));
#17653=CARTESIAN_POINT('Ctrl Pts',(18.7760039007922,-0.575236852009173,
4.249060403701));
#17654=CARTESIAN_POINT('Ctrl Pts',(18.7919091794798,-0.592729836422094,
4.05284228527226));
#17655=CARTESIAN_POINT('Ctrl Pts',(18.8078144581674,-0.610222820835014,
3.85662416684351));
#17656=CARTESIAN_POINT('Ctrl Pts',(18.823719736855,-0.520603111218926,3.65085687577915));
#17657=CARTESIAN_POINT('Ctrl Pts',(18.8396250155426,-0.365020286731977,
3.53002004684018));
#17658=CARTESIAN_POINT('Ctrl Pts',(18.8555302942302,-0.209437462245028,
3.40918321790122));
#17659=CARTESIAN_POINT('Ctrl Pts',(18.8714355729179,0.0121084771127808,
3.37327685108765));
#17660=CARTESIAN_POINT('Ctrl Pts',(18.8873408516055,0.197893008823487,3.43878763096633));
#17661=CARTESIAN_POINT('Ctrl Pts',(18.9032461302931,0.383677540534204,3.50429841084501));
#17662=CARTESIAN_POINT('Ctrl Pts',(18.9191514089807,0.533700664597814,3.67122633741595));
#17663=CARTESIAN_POINT('Ctrl Pts',(18.9350566876683,0.579078109400399,3.86292516893752));
#17664=CARTESIAN_POINT('Ctrl Pts',(18.9509619663559,0.624455554202981,4.05462400045908));
#17665=CARTESIAN_POINT('Ctrl Pts',(18.9668672450435,0.56518731974455,4.27109373693126));
#17666=CARTESIAN_POINT('Ctrl Pts',(18.9827725237311,0.428486871854059,4.41294063344238));
#17667=CARTESIAN_POINT('Ctrl Pts',(18.9955665454016,0.318526617336051,4.52704063153052));
#17668=CARTESIAN_POINT('Ctrl Pts',(19.008360567072,0.158464569423419,4.5928566151945));
#17669=CARTESIAN_POINT('Ctrl Pts',(19.0211545887425,-0.000526118841417405,
4.59432346427954));
#17670=CARTESIAN_POINT('Origin',(4.,0.,4.));
#17671=CARTESIAN_POINT('',(19.4288454112575,0.000431836873498515,4.59346738712276));
#17672=CARTESIAN_POINT('',(19.3211545887425,0.000315695961457875,4.59487351203822));
#17673=CARTESIAN_POINT('',(4.,-7.27562663373442E-17,4.5941));
#17674=CARTESIAN_POINT('Ctrl Pts',(19.4288454112575,0.000431836873498515,
4.59346738712276));
#17675=CARTESIAN_POINT('Ctrl Pts',(19.4232888206845,0.0697367837969298,
4.59393182999066));
#17676=CARTESIAN_POINT('Ctrl Pts',(19.4177322301115,0.13889623855249,4.58272225272434));
#17677=CARTESIAN_POINT('Ctrl Pts',(19.4121756395385,0.203565929825556,4.55917964700716));
#17678=CARTESIAN_POINT('Ctrl Pts',(19.3962703608509,0.38867754617092,4.49179089484985));
#17679=CARTESIAN_POINT('Ctrl Pts',(19.3803650821633,0.537002597765565,4.32335233206236));
#17680=CARTESIAN_POINT('Ctrl Pts',(19.3644598034757,0.580436494614329,4.13120381907284));
#17681=CARTESIAN_POINT('Ctrl Pts',(19.3485545247881,0.623870391463095,3.93905530608331));
#17682=CARTESIAN_POINT('Ctrl Pts',(19.3326492461004,0.562413133565966,3.72319684289176));
#17683=CARTESIAN_POINT('Ctrl Pts',(19.3167439674128,0.424283294458304,3.58274150440131));
#17684=CARTESIAN_POINT('Ctrl Pts',(19.3008386887252,0.286153455350651,3.44228616591086));
#17685=CARTESIAN_POINT('Ctrl Pts',(19.2849334100376,0.071351035032473,3.37723395212151));
#17686=CARTESIAN_POINT('Ctrl Pts',(19.26902813135,-0.12149578302492,3.4174540870367));
#17687=CARTESIAN_POINT('Ctrl Pts',(19.2531228526624,-0.314342601082313,
3.45767422195189));
#17688=CARTESIAN_POINT('Ctrl Pts',(19.2372175739748,-0.485233816878921,
3.60316670557164));
#17689=CARTESIAN_POINT('Ctrl Pts',(19.2213122952871,-0.555703413721375,
3.78712754492824));
#17690=CARTESIAN_POINT('Ctrl Pts',(19.2054070165995,-0.626173010563829,
3.97108838428485));
#17691=CARTESIAN_POINT('Ctrl Pts',(19.1895017379119,-0.59622098845213,4.19351757937831));
#17692=CARTESIAN_POINT('Ctrl Pts',(19.1735964592243,-0.479600048885993,
4.35228505390253));
#17693=CARTESIAN_POINT('Ctrl Pts',(19.1586794432354,-0.370225264934164,
4.50118762911129));
#17694=CARTESIAN_POINT('Ctrl Pts',(19.1437624272465,-0.184617181632464,
4.59409385471947));
#17695=CARTESIAN_POINT('Ctrl Pts',(19.1288454112575,0.000222628893785728,
4.59497983522242));
#17696=CARTESIAN_POINT('Ctrl Pts',(19.0211545887425,-0.000526118841417405,
4.59432346427954));
#17697=CARTESIAN_POINT('Ctrl Pts',(19.0242658457596,-0.0391895592568775,
4.59468017342281));
#17698=CARTESIAN_POINT('Ctrl Pts',(19.0273771027768,-0.0777896429211806,
4.59123148246997));
#17699=CARTESIAN_POINT('Ctrl Pts',(19.030488359794,-0.115590453236054,4.58374636034569));
#17700=CARTESIAN_POINT('Ctrl Pts',(19.0463936384816,-0.308834669113126,
4.5454811341878));
#17701=CARTESIAN_POINT('Ctrl Pts',(19.0622989171692,-0.481190439544719,
4.40172662532195));
#17702=CARTESIAN_POINT('Ctrl Pts',(19.0782041958568,-0.553519286527586,
4.21848882245705));
#17703=CARTESIAN_POINT('Ctrl Pts',(19.0941094745444,-0.625848133510457,
4.03525101959215));
#17704=CARTESIAN_POINT('Ctrl Pts',(19.1100147532321,-0.598150057044591,
3.81252992272818));
#17705=CARTESIAN_POINT('Ctrl Pts',(19.1259200319197,-0.483142842019737,
3.65258963701249));
#17706=CARTESIAN_POINT('Ctrl Pts',(19.1418253106073,-0.36813562699489,3.49264935129682));
#17707=CARTESIAN_POINT('Ctrl Pts',(19.1577305892949,-0.165819273411065,
3.39548987672941));
#17708=CARTESIAN_POINT('Ctrl Pts',(19.1736358679825,0.0309111084379188,
3.40572273351557));
#17709=CARTESIAN_POINT('Ctrl Pts',(19.1895411466701,0.227641490286902,3.41595559030173));
#17710=CARTESIAN_POINT('Ctrl Pts',(19.2054464253577,0.418785900401045,3.53358077844144));
#17711=CARTESIAN_POINT('Ctrl Pts',(19.2213517040453,0.516578912360374,3.70458978792342));
#17712=CARTESIAN_POINT('Ctrl Pts',(19.237256982733,0.614371924319703,3.87559879740541));
#17713=CARTESIAN_POINT('Ctrl Pts',(19.2531622614206,0.618813538124218,4.09999162822965));
#17714=CARTESIAN_POINT('Ctrl Pts',(19.2690675401082,0.527864352527146,4.27473658562515));
#17715=CARTESIAN_POINT('Ctrl Pts',(19.2849728187958,0.436915166930073,4.44948154302064));
#17716=CARTESIAN_POINT('Ctrl Pts',(19.3008780974834,0.250575181931413,4.5745786269874));
#17717=CARTESIAN_POINT('Ctrl Pts',(19.316783376171,0.0544038354309166,4.59258854924263));
#17718=CARTESIAN_POINT('Ctrl Pts',(19.3182404470282,0.0364327229714708,
4.59423842494573));
#17719=CARTESIAN_POINT('Ctrl Pts',(19.3196975178853,0.0183791031991185,
4.59498959766064));
#17720=CARTESIAN_POINT('Ctrl Pts',(19.3211545887425,0.000315695961457875,
4.59487351203822));
#17721=CARTESIAN_POINT('Origin',(4.,0.,4.));
#17722=CARTESIAN_POINT('',(19.7288454112575,-0.000401422265437046,4.59340756962635));
#17723=CARTESIAN_POINT('',(19.6211545887425,0.000364945106097663,4.59334757974602));
#17724=CARTESIAN_POINT('',(4.,-7.27562663373442E-17,4.5941));
#17725=CARTESIAN_POINT('Ctrl Pts',(19.7288454112575,-0.000401422265437046,
4.59340756962635));
#17726=CARTESIAN_POINT('Ctrl Pts',(19.7187204928102,0.125914276337785,4.59262579220321));
#17727=CARTESIAN_POINT('Ctrl Pts',(19.7085955743629,0.252675872983383,4.55317429478549));
#17728=CARTESIAN_POINT('Ctrl Pts',(19.6984706559155,0.353547469597214,4.47867015725961));
#17729=CARTESIAN_POINT('Ctrl Pts',(19.6825653772279,0.512007102052776,4.36163128164859));
#17730=CARTESIAN_POINT('Ctrl Pts',(19.6666600985403,0.606576931433326,4.15809158444534));
#17731=CARTESIAN_POINT('Ctrl Pts',(19.6507548198527,0.593834428727047,3.9615078130365));
#17732=CARTESIAN_POINT('Ctrl Pts',(19.6348495411651,0.581091926020768,3.76492404162769));
#17733=CARTESIAN_POINT('Ctrl Pts',(19.6189442624775,0.46103709122769,3.57529619601327));
#17734=CARTESIAN_POINT('Ctrl Pts',(19.6030389837899,0.288794059426421,3.47969339775167));
#17735=CARTESIAN_POINT('Ctrl Pts',(19.5871337051022,0.116551027625133,3.38409059949006));
#17736=CARTESIAN_POINT('Ctrl Pts',(19.5712284264146,-0.107880201184358,
3.38251284858128));
#17737=CARTESIAN_POINT('Ctrl Pts',(19.555323147727,-0.281450319664219,3.47568456171554));
#17738=CARTESIAN_POINT('Ctrl Pts',(19.5394178690394,-0.45502043814407,3.5688562748498));
#17739=CARTESIAN_POINT('Ctrl Pts',(19.5235125903518,-0.577729446294298,
3.75677745202708));
#17740=CARTESIAN_POINT('Ctrl Pts',(19.5076073116642,-0.593234549413986,
3.95316264945144));
#17741=CARTESIAN_POINT('Ctrl Pts',(19.4917020329766,-0.608739652533674,
4.1495478468758));
#17742=CARTESIAN_POINT('Ctrl Pts',(19.475796754289,-0.517040850622822,4.35439706454724));
#17743=CARTESIAN_POINT('Ctrl Pts',(19.4598914756013,-0.360242359119356,
4.47365220261941));
#17744=CARTESIAN_POINT('Ctrl Pts',(19.4495427874867,-0.258222223711561,
4.55124494740629));
#17745=CARTESIAN_POINT('Ctrl Pts',(19.4391940993721,-0.128642866595325,
4.59260240088276));
#17746=CARTESIAN_POINT('Ctrl Pts',(19.4288454112575,0.000431836873498515,
4.59346738712276));
#17747=CARTESIAN_POINT('Ctrl Pts',(19.3211545887425,0.000315695961457875,
4.59487351203822));
#17748=CARTESIAN_POINT('Ctrl Pts',(19.3356027965729,-0.178799726336078,
4.59372241551416));
#17749=CARTESIAN_POINT('Ctrl Pts',(19.3500510044034,-0.35887750705714,4.50729762043595));
#17750=CARTESIAN_POINT('Ctrl Pts',(19.3644992122339,-0.469016560662847,
4.36625733020606));
#17751=CARTESIAN_POINT('Ctrl Pts',(19.3804044909215,-0.590262902253753,
4.21099342837053));
#17752=CARTESIAN_POINT('Ctrl Pts',(19.3963097696091,-0.626752877433238,
3.98954286415574));
#17753=CARTESIAN_POINT('Ctrl Pts',(19.4122150482967,-0.561731832709929,
3.80358636875254));
#17754=CARTESIAN_POINT('Ctrl Pts',(19.4281203269843,-0.49671078798662,3.61762987334934));
#17755=CARTESIAN_POINT('Ctrl Pts',(19.4440256056719,-0.330178723360516,
3.46716744675772));
#17756=CARTESIAN_POINT('Ctrl Pts',(19.4599308843595,-0.138600118749324,
3.42128506802099));
#17757=CARTESIAN_POINT('Ctrl Pts',(19.4758361630471,0.0529784858618673,
3.37540268928427));
#17758=CARTESIAN_POINT('Ctrl Pts',(19.4917414417347,0.269603630458146,3.43410035840244));
#17759=CARTESIAN_POINT('Ctrl Pts',(19.5076467204224,0.411810215621333,3.57042659223364));
#17760=CARTESIAN_POINT('Ctrl Pts',(19.52355199911,0.554016800784528,3.70675282606484));
#17761=CARTESIAN_POINT('Ctrl Pts',(19.5394572777976,0.621804826514621,3.92070762460909));
#17762=CARTESIAN_POINT('Ctrl Pts',(19.5553625564852,0.584048894878601,4.11405198996909));
#17763=CARTESIAN_POINT('Ctrl Pts',(19.5712678351728,0.546292963242583,4.30739635532907));
#17764=CARTESIAN_POINT('Ctrl Pts',(19.5871731138604,0.402993074240464,4.4801302875048));
#17765=CARTESIAN_POINT('Ctrl Pts',(19.6030783925481,0.219946482677819,4.55294168410437));
#17766=CARTESIAN_POINT('Ctrl Pts',(19.6091037912795,0.150602919307179,4.5805248346624));
#17767=CARTESIAN_POINT('Ctrl Pts',(19.615129190011,0.0755552166468998,4.59376787586841));
#17768=CARTESIAN_POINT('Ctrl Pts',(19.6211545887425,0.000364945106097663,
4.59334757974602));
#17769=CARTESIAN_POINT('Origin',(4.,0.,4.));
#17770=CARTESIAN_POINT('',(20.0288454112575,-0.000266600559035268,4.5949350414008));
#17771=CARTESIAN_POINT('',(19.9211545887425,-0.000461335262921832,4.59353843444423));
#17772=CARTESIAN_POINT('',(4.,-7.27562663373442E-17,4.5941));
#17773=CARTESIAN_POINT('Ctrl Pts',(20.0288454112575,-0.000266600559035268,
4.5949350414008));
#17774=CARTESIAN_POINT('Ctrl Pts',(20.0141521649359,0.181839152323842,4.59391190659116));
#17775=CARTESIAN_POINT('Ctrl Pts',(19.9994589186142,0.364814066967773,4.50413264800542));
#17776=CARTESIAN_POINT('Ctrl Pts',(19.9847656722925,0.474598868642052,4.35899217880197));
#17777=CARTESIAN_POINT('Ctrl Pts',(19.9688603936049,0.593439717564554,4.20187920587587));
#17778=CARTESIAN_POINT('Ctrl Pts',(19.9529551149173,0.626517665065843,3.97989492921597));
#17779=CARTESIAN_POINT('Ctrl Pts',(19.9370498362297,0.558641803885684,3.79496194153783));
#17780=CARTESIAN_POINT('Ctrl Pts',(19.9211445575421,0.490765942705524,3.61002895385969));
#17781=CARTESIAN_POINT('Ctrl Pts',(19.9052392788545,0.321936272843916,3.46214725516331));
#17782=CARTESIAN_POINT('Ctrl Pts',(19.8893340001669,0.129673778938228,3.41921955761011));
#17783=CARTESIAN_POINT('Ctrl Pts',(19.8734287214793,-0.0625887149674591,
3.37629186005692));
#17784=CARTESIAN_POINT('Ctrl Pts',(19.8575234427916,-0.278284032917226,
3.43831816364691));
#17785=CARTESIAN_POINT('Ctrl Pts',(19.841618164104,-0.418374827314372,3.57681771754473));
#17786=CARTESIAN_POINT('Ctrl Pts',(19.8257128854164,-0.558465621711518,
3.71531727144255));
#17787=CARTESIAN_POINT('Ctrl Pts',(19.8098076067288,-0.622951892556044,
3.9302900756482));
#17788=CARTESIAN_POINT('Ctrl Pts',(19.7939023280412,-0.58222383973146,4.12303018792675));
#17789=CARTESIAN_POINT('Ctrl Pts',(19.7779970493536,-0.541495786906873,
4.3157703002053));
#17790=CARTESIAN_POINT('Ctrl Pts',(19.762091770666,-0.395553410413165,4.48627772055676));
#17791=CARTESIAN_POINT('Ctrl Pts',(19.7461864919784,-0.211407504401025,
4.55626240372308));
#17792=CARTESIAN_POINT('Ctrl Pts',(19.7404061317381,-0.144484459893097,
4.58169651826758));
#17793=CARTESIAN_POINT('Ctrl Pts',(19.7346257714978,-0.0725156072563085,
4.59385388977766));
#17794=CARTESIAN_POINT('Ctrl Pts',(19.7288454112575,-0.000401422265437046,
4.59340756962635));
#17795=CARTESIAN_POINT('Ctrl Pts',(19.6211545887425,0.000364945106097663,
4.59334757974602));
#17796=CARTESIAN_POINT('Ctrl Pts',(19.6310344686986,-0.122924963130536,
4.59265841784648));
#17797=CARTESIAN_POINT('Ctrl Pts',(19.6409143486547,-0.246598186964828,
4.55523353708024));
#17798=CARTESIAN_POINT('Ctrl Pts',(19.6507942286109,-0.346136160298313,
4.48405653351353));
#17799=CARTESIAN_POINT('Ctrl Pts',(19.6666995072985,-0.506378917588675,
4.36947112529969));
#17800=CARTESIAN_POINT('Ctrl Pts',(19.6826047859861,-0.60407113804621,4.16741144784858));
#17801=CARTESIAN_POINT('Ctrl Pts',(19.6985100646737,-0.5943566574826,3.97065479758251));
#17802=CARTESIAN_POINT('Ctrl Pts',(19.7144153433613,-0.584642176918989,
3.77389814731645));
#17803=CARTESIAN_POINT('Ctrl Pts',(19.7303206220489,-0.467520995334232,
3.58244452423543));
#17804=CARTESIAN_POINT('Ctrl Pts',(19.7462259007365,-0.296770260159971,
3.48420125495101));
#17805=CARTESIAN_POINT('Ctrl Pts',(19.7621311794242,-0.12601952498572,3.38595798566659));
#17806=CARTESIAN_POINT('Ctrl Pts',(19.7780364581118,0.098360763778029,3.38092507017875));
#17807=CARTESIAN_POINT('Ctrl Pts',(19.7939417367994,0.27334477570878,3.47141355644931));
#17808=CARTESIAN_POINT('Ctrl Pts',(19.809847015487,0.448328787639532,3.56190204271987));
#17809=CARTESIAN_POINT('Ctrl Pts',(19.8257522941746,0.573916522737285,3.74791193074883));
#17810=CARTESIAN_POINT('Ctrl Pts',(19.8416575728622,0.592443207149574,3.9440350735258));
#17811=CARTESIAN_POINT('Ctrl Pts',(19.8575628515498,0.610969891561863,4.14015821630277));
#17812=CARTESIAN_POINT('Ctrl Pts',(19.8734681302375,0.522435525288687,4.34639461382776));
#17813=CARTESIAN_POINT('Ctrl Pts',(19.8893734089251,0.367491719635661,4.46804975837363));
#17814=CARTESIAN_POINT('Ctrl Pts',(19.8999671355309,0.264291244586565,4.54907828775811));
#17815=CARTESIAN_POINT('Ctrl Pts',(19.9105608621367,0.131629953687138,4.59258455010229));
#17816=CARTESIAN_POINT('Ctrl Pts',(19.9211545887425,-0.000461335262921832,
4.59353843444423));
#17817=CARTESIAN_POINT('Origin',(4.,0.,4.));
#17818=CARTESIAN_POINT('',(20.3288454112575,0.000547175593784699,4.59423670486774));
#17819=CARTESIAN_POINT('',(20.2211545887425,-0.000159442692484791,4.59503650419094));
#17820=CARTESIAN_POINT('',(4.,-7.27562663373442E-17,4.5941));
#17821=CARTESIAN_POINT('Ctrl Pts',(20.3288454112575,0.000547175593784699,
4.59423670486774));
#17822=CARTESIAN_POINT('Ctrl Pts',(20.3254891157492,0.0422991098545892,
4.59465405164581));
#17823=CARTESIAN_POINT('Ctrl Pts',(20.3221328202408,0.0839734681026259,
4.59066114403672));
#17824=CARTESIAN_POINT('Ctrl Pts',(20.3187765247324,0.124636177719752,4.58197547152207));
#17825=CARTESIAN_POINT('Ctrl Pts',(20.3028712460448,0.317334266145104,4.54081460186972));
#17826=CARTESIAN_POINT('Ctrl Pts',(20.2869659673572,0.48731321493246,4.39426577643889));
#17827=CARTESIAN_POINT('Ctrl Pts',(20.2710606886696,0.556778600406793,4.20989870881916));
#17828=CARTESIAN_POINT('Ctrl Pts',(20.255155409982,0.626243985881127,4.02553164119943));
#17829=CARTESIAN_POINT('Ctrl Pts',(20.2392501312944,0.595195808042437,3.80334633139079));
#17830=CARTESIAN_POINT('Ctrl Pts',(20.2233448526068,0.477757630702126,3.64521515909767));
#17831=CARTESIAN_POINT('Ctrl Pts',(20.2074395739191,0.360319453361808,3.48708398680455));
#17832=CARTESIAN_POINT('Ctrl Pts',(20.1915342952315,0.156491276519859,3.39300695202695));
#17833=CARTESIAN_POINT('Ctrl Pts',(20.1756290165439,-0.04006765138094,3.40625706061923));
#17834=CARTESIAN_POINT('Ctrl Pts',(20.1597237378563,-0.236626579281727,
3.4195071692115));
#17835=CARTESIAN_POINT('Ctrl Pts',(20.1438184591687,-0.425916258241364,
3.54008442117362));
#17836=CARTESIAN_POINT('Ctrl Pts',(20.1279131804811,-0.521059912873915,
3.71258420787224));
#17837=CARTESIAN_POINT('Ctrl Pts',(20.1120079017935,-0.616203567506467,
3.88508399457085));
#17838=CARTESIAN_POINT('Ctrl Pts',(20.0961026231058,-0.617201197811932,
4.10950631600596));
#17839=CARTESIAN_POINT('Ctrl Pts',(20.0801973444182,-0.523575121773085,
4.28282745216878));
#17840=CARTESIAN_POINT('Ctrl Pts',(20.0642920657306,-0.429949045734243,
4.45614858833159));
#17841=CARTESIAN_POINT('Ctrl Pts',(20.048386787043,-0.241699263351099,4.57836853922213));
#17842=CARTESIAN_POINT('Ctrl Pts',(20.0324815083554,-0.0452724969876719,
4.59335768007126));
#17843=CARTESIAN_POINT('Ctrl Pts',(20.0312694759895,-0.030304158296608,
4.59449989984645));
#17844=CARTESIAN_POINT('Ctrl Pts',(20.0300574436235,-0.0152883365109376,
4.5950194388496));
#17845=CARTESIAN_POINT('Ctrl Pts',(20.0288454112575,-0.000266600559035268,
4.5949350414008));
#17846=CARTESIAN_POINT('Ctrl Pts',(19.9211545887425,-0.000461335262921832,
4.59353843444423));
#17847=CARTESIAN_POINT('Ctrl Pts',(19.9264661408243,-0.0666901315043342,
4.5940166992278));
#17848=CARTESIAN_POINT('Ctrl Pts',(19.9317776929061,-0.132775635823809,
4.58379778651276));
#17849=CARTESIAN_POINT('Ctrl Pts',(19.9370892449879,-0.194932679790098,
4.56224768701753));
#17850=CARTESIAN_POINT('Ctrl Pts',(19.9529945236755,-0.381060028529917,
4.49771657954882));
#17851=CARTESIAN_POINT('Ctrl Pts',(19.9688998023631,-0.531961480976676,
4.33158047304464));
#17852=CARTESIAN_POINT('Ctrl Pts',(19.9848050810507,-0.578348134104426,
4.14012389605102));
#17853=CARTESIAN_POINT('Ctrl Pts',(20.0007103597384,-0.624734787232175,
3.94866731905739));
#17854=CARTESIAN_POINT('Ctrl Pts',(20.016615638426,-0.566606641040915,3.73189027157431));
#17855=CARTESIAN_POINT('Ctrl Pts',(20.0325209171136,-0.430656211588969,
3.58932409618151));
#17856=CARTESIAN_POINT('Ctrl Pts',(20.0484261958012,-0.294705782137024,
3.44675792078871));
#17857=CARTESIAN_POINT('Ctrl Pts',(20.0643314744888,-0.080933069424392,
3.37840261748619));
#17858=CARTESIAN_POINT('Ctrl Pts',(20.0802367531764,0.112511319004002,3.41565067076361));
#17859=CARTESIAN_POINT('Ctrl Pts',(20.096142031864,0.305955707432406,3.45289872404102));
#17860=CARTESIAN_POINT('Ctrl Pts',(20.1120473105516,0.479071771576571,3.59575013389837));
#17861=CARTESIAN_POINT('Ctrl Pts',(20.1279525892393,0.552362916535151,3.77860107435498));
#17862=CARTESIAN_POINT('Ctrl Pts',(20.1438578679269,0.625654061493722,3.96145201481158));
#17863=CARTESIAN_POINT('Ctrl Pts',(20.1597631466145,0.599120287266732,4.18430248586742));
#17864=CARTESIAN_POINT('Ctrl Pts',(20.1756684253021,0.484961816589866,4.3448525870839));
#17865=CARTESIAN_POINT('Ctrl Pts',(20.1908304797822,0.376137759761604,4.49790047950022));
#17866=CARTESIAN_POINT('Ctrl Pts',(20.2059925342623,0.187686755696174,4.59433432972249));
#17867=CARTESIAN_POINT('Ctrl Pts',(20.2211545887425,-0.000159442692484791,
4.59503650419094));
#17868=CARTESIAN_POINT('Origin',(4.,0.,4.));
#17869=CARTESIAN_POINT('',(20.6288454112575,1.84392275237588E-6,4.59415158619139));
#17870=CARTESIAN_POINT('',(20.5211545887425,0.00014515264107467,4.59408556636595));
#17871=CARTESIAN_POINT('',(4.,-7.27562663373442E-17,4.5941));
#17872=CARTESIAN_POINT('Ctrl Pts',(20.6288454112575,1.84392275237588E-6,
4.59415158619139));
#17873=CARTESIAN_POINT('Ctrl Pts',(20.6209207878748,0.0985777406598016,
4.59414764832452));
#17874=CARTESIAN_POINT('Ctrl Pts',(20.6129961644921,0.197149291092008,4.56908802213256));
#17875=CARTESIAN_POINT('Ctrl Pts',(20.6050715411094,0.283761277174982,4.52200793915563));
#17876=CARTESIAN_POINT('Ctrl Pts',(20.5971189017656,0.370679463050262,4.47476141372331));
#17877=CARTESIAN_POINT('Ctrl Pts',(20.5891662624218,0.445553373684486,4.40533845822152));
#17878=CARTESIAN_POINT('Ctrl Pts',(20.581213623078,0.499196468040806,4.3222224876916));
#17879=CARTESIAN_POINT('Ctrl Pts',(20.5732609837342,0.552839562397126,4.23910651716169));
#17880=CARTESIAN_POINT('Ctrl Pts',(20.5653083443904,0.585251840475543,4.14229753160364));
#17881=CARTESIAN_POINT('Ctrl Pts',(20.5573557050466,0.592531230276538,4.04364021904617));
#17882=CARTESIAN_POINT('Ctrl Pts',(20.5494030657028,0.599810620077534,3.9449829064887));
#17883=CARTESIAN_POINT('Ctrl Pts',(20.541450426359,0.581957121601108,3.84447726693182));
#17884=CARTESIAN_POINT('Ctrl Pts',(20.5334977870152,0.541038843355354,3.75439549632807));
#17885=CARTESIAN_POINT('Ctrl Pts',(20.5255451476714,0.5001205651096,3.66431372572433));
#17886=CARTESIAN_POINT('Ctrl Pts',(20.5175925083276,0.436137507094518,3.58465582407373));
#17887=CARTESIAN_POINT('Ctrl Pts',(20.5096398689838,0.357128912623608,3.5251911792601));
#17888=CARTESIAN_POINT('Ctrl Pts',(20.50168722964,0.278120318152698,3.46572653444646));
#17889=CARTESIAN_POINT('Ctrl Pts',(20.4937345902962,0.184086187225959,3.42645514646979));
#17890=CARTESIAN_POINT('Ctrl Pts',(20.4857819509524,0.0861162623359374,
3.4121221101222));
#17891=CARTESIAN_POINT('Ctrl Pts',(20.4778293116085,-0.0118536625540841,
3.39778907377461));
#17892=CARTESIAN_POINT('Ctrl Pts',(20.4698766722647,-0.113759381407388,
3.4083943890561));
#17893=CARTESIAN_POINT('Ctrl Pts',(20.4619240329209,-0.206384677702653,
3.44274365129583));
#17894=CARTESIAN_POINT('Ctrl Pts',(20.4539713935771,-0.299009973997917,
3.47709291353557));
#17895=CARTESIAN_POINT('Ctrl Pts',(20.4460187542333,-0.382354847735142,
3.53518612273354));
#17896=CARTESIAN_POINT('Ctrl Pts',(20.4380661148895,-0.447563842371028,
3.60976099223211));
#17897=CARTESIAN_POINT('Ctrl Pts',(20.4301134755457,-0.512772837006921,
3.68433586173069));
#17898=CARTESIAN_POINT('Ctrl Pts',(20.4221608362019,-0.559845952541473,
3.77539239152987));
#17899=CARTESIAN_POINT('Ctrl Pts',(20.4142081968581,-0.580888308445953,
3.87190852591559));
#17900=CARTESIAN_POINT('Ctrl Pts',(20.3983029181705,-0.622973020254908,
4.06494079468701));
#17901=CARTESIAN_POINT('Ctrl Pts',(20.3823976394829,-0.5609346935436,4.27981148180459));
#17902=CARTESIAN_POINT('Ctrl Pts',(20.3664923607953,-0.422206916156273,
4.41936036842645));
#17903=CARTESIAN_POINT('Ctrl Pts',(20.353943377616,-0.312753156865475,4.52946196836027));
#17904=CARTESIAN_POINT('Ctrl Pts',(20.3413943944368,-0.155560747392339,
4.59267627084609));
#17905=CARTESIAN_POINT('Ctrl Pts',(20.3288454112575,0.000547175593784699,
4.59423670486774));
#17906=CARTESIAN_POINT('Ctrl Pts',(20.2211545887425,-0.000159442692484791,
4.59503650419094));
#17907=CARTESIAN_POINT('Ctrl Pts',(20.22189781295,-0.00936741923094289,
4.59507092387091));
#17908=CARTESIAN_POINT('Ctrl Pts',(20.2226410371574,-0.0185739425223631,
4.59487531632137));
#17909=CARTESIAN_POINT('Ctrl Pts',(20.2233842613649,-0.0277695625699301,
4.59444507412072));
#17910=CARTESIAN_POINT('Ctrl Pts',(20.2392895400526,-0.224559303926058,
4.58523772856393));
#17911=CARTESIAN_POINT('Ctrl Pts',(20.2551948187402,-0.416355619511548,
4.46857330607325));
#17912=CARTESIAN_POINT('Ctrl Pts',(20.2711000974278,-0.51503297954037,4.29810345018796));
#17913=CARTESIAN_POINT('Ctrl Pts',(20.2870053761154,-0.613710339569191,
4.12763359430267));
#17914=CARTESIAN_POINT('Ctrl Pts',(20.302910654803,-0.619268744041345,3.90335830502277));
#17915=CARTESIAN_POINT('Ctrl Pts',(20.3188159334906,-0.529271009537506,
3.72809546473432));
#17916=CARTESIAN_POINT('Ctrl Pts',(20.3347212121782,-0.439273275033663,
3.55283262444587));
#17917=CARTESIAN_POINT('Ctrl Pts',(20.3506264908658,-0.253719401553817,
3.42658223314887));
#17918=CARTESIAN_POINT('Ctrl Pts',(20.3665317695535,-0.0575887485100287,
3.40762076142476));
#17919=CARTESIAN_POINT('Ctrl Pts',(20.3824370482411,0.138541904533748,3.38865928970065));
#17920=CARTESIAN_POINT('Ctrl Pts',(20.3983423269287,0.345249337141466,3.47698673754941));
#17921=CARTESIAN_POINT('Ctrl Pts',(20.4142476056163,0.467192899405167,3.63141813202173));
#17922=CARTESIAN_POINT('Ctrl Pts',(20.4301528843039,0.589136461668875,3.78584952649406));
#17923=CARTESIAN_POINT('Ctrl Pts',(20.4460581629915,0.626316153588557,4.00638486758996));
#17924=CARTESIAN_POINT('Ctrl Pts',(20.4619634416791,0.562534942182983,4.19337293359078));
#17925=CARTESIAN_POINT('Ctrl Pts',(20.4699160810229,0.530644336480201,4.28686696659118));
#17926=CARTESIAN_POINT('Ctrl Pts',(20.4778687203667,0.473513504946115,4.3719741808178));
#17927=CARTESIAN_POINT('Ctrl Pts',(20.4858213597105,0.400240502138227,4.43864269813793));
#17928=CARTESIAN_POINT('Ctrl Pts',(20.4937739990544,0.326967499330329,4.50531121545807));
#17929=CARTESIAN_POINT('Ctrl Pts',(20.5017266383982,0.237552325248626,4.55354103587171));
#17930=CARTESIAN_POINT('Ctrl Pts',(20.509679277742,0.141619450488441,4.57712494713439));
#17931=CARTESIAN_POINT('Ctrl Pts',(20.5135043814088,0.0954771353210092,
4.58846846487098));
#17932=CARTESIAN_POINT('Ctrl Pts',(20.5173294850756,0.0478269697500401,
4.59411022582368));
#17933=CARTESIAN_POINT('Ctrl Pts',(20.5211545887425,0.00014515264107467,
4.59408556636595));
#17934=CARTESIAN_POINT('Origin',(4.,0.,4.));
#17935=CARTESIAN_POINT('',(20.9288454112575,-6.4040329070536E-6,4.59405282094147));
#17936=CARTESIAN_POINT('',(20.8211545887425,5.65245430726296E-6,4.59414685459231));
#17937=CARTESIAN_POINT('',(4.,-7.27562663373442E-17,4.5941));
#17938=CARTESIAN_POINT('Ctrl Pts',(20.9288454112575,-6.4040329070536E-6,
4.59405282094147));
#17939=CARTESIAN_POINT('Ctrl Pts',(20.9243050993443,0.0564994875152707,
4.59403151438501));
#17940=CARTESIAN_POINT('Ctrl Pts',(20.9197647874311,0.113011285737041,4.58603249222448));
#17941=CARTESIAN_POINT('Ctrl Pts',(20.9152244755179,0.167207550221224,4.57013805289591));
#17942=CARTESIAN_POINT('Ctrl Pts',(20.9072718361741,0.262135685878584,4.5422979516059));
#17943=CARTESIAN_POINT('Ctrl Pts',(20.8993191968303,0.349959832061366,4.49023494241839));
#17944=CARTESIAN_POINT('Ctrl Pts',(20.8913665574865,0.419942299057043,4.42031443844746));
#17945=CARTESIAN_POINT('Ctrl Pts',(20.8834139181427,0.489924766052721,4.35039393447653));
#17946=CARTESIAN_POINT('Ctrl Pts',(20.8754612787989,0.542065553861293,4.26261593572219));
#17947=CARTESIAN_POINT('Ctrl Pts',(20.8675086394551,0.569989725359365,4.16771249585991));
#17948=CARTESIAN_POINT('Ctrl Pts',(20.8595560001113,0.597913896857441,4.07280905599763));
#17949=CARTESIAN_POINT('Ctrl Pts',(20.8516033607674,0.601621452045013,3.97078017502742));
#17950=CARTESIAN_POINT('Ctrl Pts',(20.8436507214236,0.580659121393648,3.87410027737825));
#17951=CARTESIAN_POINT('Ctrl Pts',(20.8356980820798,0.559696790742287,3.77742037972911));
#17952=CARTESIAN_POINT('Ctrl Pts',(20.827745442736,0.514064574252002,3.686089465401));
#17953=CARTESIAN_POINT('Ctrl Pts',(20.8197928033922,0.44934157601673,3.61127397478397));
#17954=CARTESIAN_POINT('Ctrl Pts',(20.8118401640484,0.384618577781443,3.53645848416692));
#17955=CARTESIAN_POINT('Ctrl Pts',(20.8038875247046,0.300804797801161,3.47815841726095));
#17956=CARTESIAN_POINT('Ctrl Pts',(20.7959348853608,0.208147717693743,3.44350176598286));
#17957=CARTESIAN_POINT('Ctrl Pts',(20.787982246017,0.115490637586335,3.40884511470477));
#17958=CARTESIAN_POINT('Ctrl Pts',(20.7800296066732,0.0139902573517945,
3.39783187905454));
#17959=CARTESIAN_POINT('Ctrl Pts',(20.7720769673294,-0.0839438183138644,
3.41180854931868));
#17960=CARTESIAN_POINT('Ctrl Pts',(20.7641243279856,-0.181877893979523,
3.42578521958283));
#17961=CARTESIAN_POINT('Ctrl Pts',(20.7561716886418,-0.2762456650763,3.46475179576135));
#17962=CARTESIAN_POINT('Ctrl Pts',(20.748219049298,-0.355509010203556,3.52394413563581));
#17963=CARTESIAN_POINT('Ctrl Pts',(20.7402664099542,-0.434772355330821,
3.58313647551028));
#17964=CARTESIAN_POINT('Ctrl Pts',(20.7323137706103,-0.498931274488562,
3.66255457908069));
#17965=CARTESIAN_POINT('Ctrl Pts',(20.7243611312665,-0.54014217617541,3.75248840252759));
#17966=CARTESIAN_POINT('Ctrl Pts',(20.7164084919227,-0.581353077862249,
3.84242222597448));
#17967=CARTESIAN_POINT('Ctrl Pts',(20.7084558525789,-0.599615962078206,
3.94287176929784));
#17968=CARTESIAN_POINT('Ctrl Pts',(20.7005032132351,-0.592696601504336,
4.0415558946729));
#17969=CARTESIAN_POINT('Ctrl Pts',(20.6925505738913,-0.585777240930466,
4.14024002004797));
#17970=CARTESIAN_POINT('Ctrl Pts',(20.6845979345475,-0.553675635566762,
4.23715872747472));
#17971=CARTESIAN_POINT('Ctrl Pts',(20.6766452952037,-0.50031917594212,4.32046203197985));
#17972=CARTESIAN_POINT('Ctrl Pts',(20.6686926558599,-0.446962716317479,
4.40376533648498));
#17973=CARTESIAN_POINT('Ctrl Pts',(20.6607400165161,-0.3723514024319,4.47345323806848));
#17974=CARTESIAN_POINT('Ctrl Pts',(20.6527873771723,-0.285602702553558,
4.52100610813718));
#17975=CARTESIAN_POINT('Ctrl Pts',(20.6448347378285,-0.198854002675205,
4.56855897820588));
#17976=CARTESIAN_POINT('Ctrl Pts',(20.6368820984847,-0.099967916804087,
4.59397681675976));
#17977=CARTESIAN_POINT('Ctrl Pts',(20.6289294591409,-0.00104364331035449,
4.59415068835528));
#17978=CARTESIAN_POINT('Ctrl Pts',(20.6289014431798,-0.000695147863829354,
4.59415130087895));
#17979=CARTESIAN_POINT('Ctrl Pts',(20.6288734272186,-0.000346651943377611,
4.59415160011295));
#17980=CARTESIAN_POINT('Ctrl Pts',(20.6288454112575,1.84392275237588E-6,
4.59415158619139));
#17981=CARTESIAN_POINT('Ctrl Pts',(20.5211545887425,0.00014515264107467,
4.59408556636595));
#17982=CARTESIAN_POINT('Ctrl Pts',(20.5252821244194,-0.0513066296901884,
4.59405895720698));
#17983=CARTESIAN_POINT('Ctrl Pts',(20.5294096600964,-0.102795266482965,
4.58743447362686));
#17984=CARTESIAN_POINT('Ctrl Pts',(20.5335371957734,-0.152465997634008,
4.57425651377355));
#17985=CARTESIAN_POINT('Ctrl Pts',(20.5414898351172,-0.248167995557571,
4.5488661670383));
#17986=CARTESIAN_POINT('Ctrl Pts',(20.549442474461,-0.33712141596603,4.49914747145609));
#17987=CARTESIAN_POINT('Ctrl Pts',(20.5573951138048,-0.408848640915227,
4.43107686705031));
#17988=CARTESIAN_POINT('Ctrl Pts',(20.5653477531486,-0.480575865864423,
4.36300626264453));
#17989=CARTESIAN_POINT('Ctrl Pts',(20.5733003924924,-0.535076895354358,
4.27658374941519));
#17990=CARTESIAN_POINT('Ctrl Pts',(20.5812530318362,-0.565476628275392,
4.18243021985824));
#17991=CARTESIAN_POINT('Ctrl Pts',(20.58920567118,-0.595876361196427,4.08827669030129));
#17992=CARTESIAN_POINT('Ctrl Pts',(20.5971583105238,-0.602174797548561,
3.98639214441672));
#17993=CARTESIAN_POINT('Ctrl Pts',(20.6051109498677,-0.58371402745925,3.88920441471463));
#17994=CARTESIAN_POINT('Ctrl Pts',(20.6130635892115,-0.565253257369939,
3.79201668501254));
#17995=CARTESIAN_POINT('Ctrl Pts',(20.6210162285553,-0.522033280839182,
3.69952577149293));
#17996=CARTESIAN_POINT('Ctrl Pts',(20.6289688678991,-0.459278917219465,
3.62305528060961));
#17997=CARTESIAN_POINT('Ctrl Pts',(20.6369215072429,-0.396524553599749,
3.54658478972629));
#17998=CARTESIAN_POINT('Ctrl Pts',(20.6448741465867,-0.314235802891072,
3.48613472147926));
#17999=CARTESIAN_POINT('Ctrl Pts',(20.6528267859305,-0.222505051509483,
3.44908779917463));
#18000=CARTESIAN_POINT('Ctrl Pts',(20.6607794252743,-0.130774300127894,
3.41204087687));
#18001=CARTESIAN_POINT('Ctrl Pts',(20.6687320646181,-0.029601548073392,
3.39839710050778));
#18002=CARTESIAN_POINT('Ctrl Pts',(20.6766847039619,0.0686601223983595,
3.40982890848785));
#18003=CARTESIAN_POINT('Ctrl Pts',(20.6846373433057,0.1669217928701,3.42126071646792));
#18004=CARTESIAN_POINT('Ctrl Pts',(20.6925899826495,0.262272381759091,3.45776810879028));
#18005=CARTESIAN_POINT('Ctrl Pts',(20.7005426219933,0.343045155251024,3.51488528173127));
#18006=CARTESIAN_POINT('Ctrl Pts',(20.7084952613371,0.423817928742975,3.57200245467228));
#18007=CARTESIAN_POINT('Ctrl Pts',(20.7164479006809,0.490012886837861,3.64972940823193));
#18008=CARTESIAN_POINT('Ctrl Pts',(20.7244005400247,0.533541468465666,3.73856417004634));
#18009=CARTESIAN_POINT('Ctrl Pts',(20.7323531793686,0.577070050093471,3.82739893186076));
#18010=CARTESIAN_POINT('Ctrl Pts',(20.7403058187123,0.597932255254196,3.92734150192994));
#18011=CARTESIAN_POINT('Ctrl Pts',(20.7482584580562,0.593574919799613,4.02617190099588));
#18012=CARTESIAN_POINT('Ctrl Pts',(20.7562110974,0.589217584345031,4.1250023000618));
#18013=CARTESIAN_POINT('Ctrl Pts',(20.7641637367438,0.559640708275147,4.22272052812447));
#18014=CARTESIAN_POINT('Ctrl Pts',(20.7721163760876,0.508461778515953,4.30737953925928));
#18015=CARTESIAN_POINT('Ctrl Pts',(20.7800690154314,0.457282848756759,4.39203855039408));
#18016=CARTESIAN_POINT('Ctrl Pts',(20.7880216547752,0.384501865308254,4.46363834460102));
#18017=CARTESIAN_POINT('Ctrl Pts',(20.795974294119,0.299016600344635,4.51342469267633));
#18018=CARTESIAN_POINT('Ctrl Pts',(20.8039269334628,0.213531335381016,4.56321104075164));
#18019=CARTESIAN_POINT('Ctrl Pts',(20.8118795728066,0.115341788902283,4.59118394269532));
#18020=CARTESIAN_POINT('Ctrl Pts',(20.8198322121504,0.0164533379892873,
4.59392342516246));
#18021=CARTESIAN_POINT('Ctrl Pts',(20.8202730043478,0.0109722321971217,
4.59407526688998));
#18022=CARTESIAN_POINT('Ctrl Pts',(20.8207137965451,0.00548897925183007,
4.59414958726715));
#18023=CARTESIAN_POINT('Ctrl Pts',(20.8211545887425,5.65245430726296E-6,
4.59414685459231));
#18024=CARTESIAN_POINT('Origin',(4.,0.,4.));
#18025=CARTESIAN_POINT('',(21.2288454112575,1.28243205298473E-5,4.59412621697841));
#18026=CARTESIAN_POINT('',(21.1211545887425,-1.09306879613159E-5,4.5940621922514));
#18027=CARTESIAN_POINT('',(4.,-7.27562663373442E-17,4.5941));
#18028=CARTESIAN_POINT('Ctrl Pts',(21.2288454112575,1.28243205298473E-5,
4.59412621697841));
#18029=CARTESIAN_POINT('Ctrl Pts',(21.2276894108138,0.0143945780386088,
4.59413985249388));
#18030=CARTESIAN_POINT('Ctrl Pts',(21.2265334103701,0.028775363636007,4.59362827285675));
#18031=CARTESIAN_POINT('Ctrl Pts',(21.2253774099263,0.043117441953227,4.59258471957415));
#18032=CARTESIAN_POINT('Ctrl Pts',(21.2174247705826,0.141782954511012,4.58540565408365));
#18033=CARTESIAN_POINT('Ctrl Pts',(21.2094721312387,0.238616577754522,4.55305001116024));
#18034=CARTESIAN_POINT('Ctrl Pts',(21.2015194918949,0.321779082392626,4.49947370882601));
#18035=CARTESIAN_POINT('Ctrl Pts',(21.1935668525511,0.404941587030731,4.44589740649178));
#18036=CARTESIAN_POINT('Ctrl Pts',(21.1856142132073,0.474432973063433,4.37110044474674));
#18037=CARTESIAN_POINT('Ctrl Pts',(21.1776615738635,0.521756972098598,4.28422777087894));
#18038=CARTESIAN_POINT('Ctrl Pts',(21.1697089345197,0.569080971133768,4.19735509701114));
#18039=CARTESIAN_POINT('Ctrl Pts',(21.1617562951759,0.594237583171398,4.09840671102057));
#18040=CARTESIAN_POINT('Ctrl Pts',(21.1538036558321,0.594151069756079,3.9994804007435));
#18041=CARTESIAN_POINT('Ctrl Pts',(21.1458510164883,0.59406455634076,3.90055409046644));
#18042=CARTESIAN_POINT('Ctrl Pts',(21.1378983771445,0.568734917472505,3.80164985590287));
#18043=CARTESIAN_POINT('Ctrl Pts',(21.1299457378007,0.521259046500119,3.71486008677882));
#18044=CARTESIAN_POINT('Ctrl Pts',(21.1219930984569,0.473783175527722,3.62807031765475));
#18045=CARTESIAN_POINT('Ctrl Pts',(21.114040459113,0.40416107245118,3.5533950139702));
#18046=CARTESIAN_POINT('Ctrl Pts',(21.1060878197692,0.320904987578411,3.49996424865404));
#18047=CARTESIAN_POINT('Ctrl Pts',(21.0981351804254,0.237648902705652,3.44653348333788));
#18048=CARTESIAN_POINT('Ctrl Pts',(21.0901825410817,0.140758836036697,3.41434725639011));
#18049=CARTESIAN_POINT('Ctrl Pts',(21.0822299017378,0.042080917889342,3.40734077242984));
#18050=CARTESIAN_POINT('Ctrl Pts',(21.074277262394,-0.056597000258024,3.40033428846957));
#18051=CARTESIAN_POINT('Ctrl Pts',(21.0663246230502,-0.157062769883762,
3.41850754749682));
#18052=CARTESIAN_POINT('Ctrl Pts',(21.0583719837064,-0.247033082431791,
3.45963862106718));
#18053=CARTESIAN_POINT('Ctrl Pts',(21.0504193443626,-0.337003394979799,
3.50076969463752));
#18054=CARTESIAN_POINT('Ctrl Pts',(21.0424667050188,-0.416478250450111,
3.56485858275095));
#18055=CARTESIAN_POINT('Ctrl Pts',(21.034514065675,-0.475740765152555,3.644069545988));
#18056=CARTESIAN_POINT('Ctrl Pts',(21.0265614263312,-0.535003279855012,
3.72328050922507));
#18057=CARTESIAN_POINT('Ctrl Pts',(21.0186087869874,-0.574053453789596,
3.81761354758578));
#18058=CARTESIAN_POINT('Ctrl Pts',(21.0106561476436,-0.588116871685884,
3.91553516229212));
#18059=CARTESIAN_POINT('Ctrl Pts',(21.0027035082998,-0.60218028958217,4.01345677699845));
#18060=CARTESIAN_POINT('Ctrl Pts',(20.994750868956,-0.591256951440166,4.11496696805043));
#18061=CARTESIAN_POINT('Ctrl Pts',(20.9867982296121,-0.556682383467722,
4.20765473214191));
#18062=CARTESIAN_POINT('Ctrl Pts',(20.9788455902683,-0.522107815495282,
4.30034249623339));
#18063=CARTESIAN_POINT('Ctrl Pts',(20.9708929509246,-0.463882017692404,
4.38420783336438));
#18064=CARTESIAN_POINT('Ctrl Pts',(20.9629403115808,-0.389123888092725,
4.4489970636758));
#18065=CARTESIAN_POINT('Ctrl Pts',(20.9549876722369,-0.314365758493028,
4.51378629398723));
#18066=CARTESIAN_POINT('Ctrl Pts',(20.9470350328931,-0.223075297096518,
4.5594994174791));
#18067=CARTESIAN_POINT('Ctrl Pts',(20.9390823935493,-0.12641400383229,4.58054738252877));
#18068=CARTESIAN_POINT('Ctrl Pts',(20.9356700661187,-0.0849384674446181,
4.58957866703598));
#18069=CARTESIAN_POINT('Ctrl Pts',(20.9322577386881,-0.0424741039190781,
4.59406883414683));
#18070=CARTESIAN_POINT('Ctrl Pts',(20.9288454112575,-6.4040329070536E-6,
4.59405282094147));
#18071=CARTESIAN_POINT('Ctrl Pts',(20.8211545887425,5.65245430726296E-6,
4.59414685459231));
#18072=CARTESIAN_POINT('Ctrl Pts',(20.8286664358889,-0.0934395423672534,
4.59410028517524));
#18073=CARTESIAN_POINT('Ctrl Pts',(20.8361782830354,-0.18690618531264,4.57167601133058));
#18074=CARTESIAN_POINT('Ctrl Pts',(20.8436901301818,-0.270133012248912,
4.529191754035));
#18075=CARTESIAN_POINT('Ctrl Pts',(20.8516427695256,-0.358243556226857,
4.4842145374498));
#18076=CARTESIAN_POINT('Ctrl Pts',(20.8595954088694,-0.434877288835492,
4.41675404128879));
#18077=CARTESIAN_POINT('Ctrl Pts',(20.8675480482133,-0.490664589397756,
4.33505825661903));
#18078=CARTESIAN_POINT('Ctrl Pts',(20.8755006875571,-0.546451889960021,
4.25336247194927));
#18079=CARTESIAN_POINT('Ctrl Pts',(20.8834533269009,-0.581392758475918,
4.15743139877076));
#18080=CARTESIAN_POINT('Ctrl Pts',(20.8914059662447,-0.591215252505097,
4.05899390323763));
#18081=CARTESIAN_POINT('Ctrl Pts',(20.8993586055885,-0.601037746534278,
3.96055640770449));
#18082=CARTESIAN_POINT('Ctrl Pts',(20.9073112449323,-0.585741866076735,
3.85961248981672));
#18083=CARTESIAN_POINT('Ctrl Pts',(20.9152638842761,-0.547197711916726,
3.76850392583047));
#18084=CARTESIAN_POINT('Ctrl Pts',(20.9232165236199,-0.508653557756717,
3.67739536184422));
#18085=CARTESIAN_POINT('Ctrl Pts',(20.9311691629637,-0.446861129894262,
3.59612215175949));
#18086=CARTESIAN_POINT('Ctrl Pts',(20.9391218023075,-0.369375409551539,
3.53462104847409));
#18087=CARTESIAN_POINT('Ctrl Pts',(20.9470744416513,-0.291889689208826,
3.4731199451887));
#18088=CARTESIAN_POINT('Ctrl Pts',(20.9550270809951,-0.198710676385865,
3.43139094870266));
#18089=CARTESIAN_POINT('Ctrl Pts',(20.9629797203389,-0.101230766359376,
3.41453599926792));
#18090=CARTESIAN_POINT('Ctrl Pts',(20.9709323596827,-0.00375085633288601,
3.39768104983318));
#18091=CARTESIAN_POINT('Ctrl Pts',(20.9788849990265,0.0980299508971346,
3.40570014744973));
#18092=CARTESIAN_POINT('Ctrl Pts',(20.9868376383704,0.191667561123074,3.43761284710704));
#18093=CARTESIAN_POINT('Ctrl Pts',(20.9947902777142,0.285305171349014,3.46952554676435));
#18094=CARTESIAN_POINT('Ctrl Pts',(21.002742917058,0.37079958457088,3.52533184846243));
#18095=CARTESIAN_POINT('Ctrl Pts',(21.0106955564018,0.437697946637459,3.59820867233944));
#18096=CARTESIAN_POINT('Ctrl Pts',(21.0186481957456,0.504596308704037,3.67108549621644));
#18097=CARTESIAN_POINT('Ctrl Pts',(21.0266008350894,0.552898619615334,3.76103284227238));
#18098=CARTESIAN_POINT('Ctrl Pts',(21.0345534744332,0.576699262792956,3.8570534220826));
#18099=CARTESIAN_POINT('Ctrl Pts',(21.042506113777,0.600499905970578,3.95307400189282));
#18100=CARTESIAN_POINT('Ctrl Pts',(21.0504587531208,0.599798881414527,4.05516781545734));
#18101=CARTESIAN_POINT('Ctrl Pts',(21.0584113924646,0.574681899562831,4.15085250374278));
#18102=CARTESIAN_POINT('Ctrl Pts',(21.0663640318084,0.549564917711138,4.24653719202821));
#18103=CARTESIAN_POINT('Ctrl Pts',(21.0743166711522,0.500031978563804,4.33581275503458));
#18104=CARTESIAN_POINT('Ctrl Pts',(21.082269310496,0.432139158218639,4.40776403918836));
#18105=CARTESIAN_POINT('Ctrl Pts',(21.0902219498398,0.364246337873458,4.47971532334216));
#18106=CARTESIAN_POINT('Ctrl Pts',(21.0981745891836,0.277993636330433,4.53434232864337));
#18107=CARTESIAN_POINT('Ctrl Pts',(21.1061272285274,0.183926621270441,4.56496615973523));
#18108=CARTESIAN_POINT('Ctrl Pts',(21.1111363485991,0.124676735433976,4.5842551580617));
#18109=CARTESIAN_POINT('Ctrl Pts',(21.1161454686708,0.0623266393968894,
4.59402126159141));
#18110=CARTESIAN_POINT('Ctrl Pts',(21.1211545887425,-1.09306879613159E-5,
4.5940621922514));
#18111=CARTESIAN_POINT('Origin',(4.,0.,4.));
#18112=CARTESIAN_POINT('',(21.5288454112575,-1.51073027558624E-5,4.59408477831653));
#18113=CARTESIAN_POINT('',(21.4211545887425,1.51733402061755E-5,4.59410821609125));
#18114=CARTESIAN_POINT('',(4.,-7.27562663373442E-17,4.5941));
#18115=CARTESIAN_POINT('Ctrl Pts',(21.5288454112575,-1.51073027558624E-5,
4.59408477831653));
#18116=CARTESIAN_POINT('Ctrl Pts',(21.5231210829395,0.0712153309254728,
4.59401644885886));
#18117=CARTESIAN_POINT('Ctrl Pts',(21.5173967546214,0.142469702059594,4.58119587380047));
#18118=CARTESIAN_POINT('Ctrl Pts',(21.5116724263034,0.209120766622247,4.55613331912479));
#18119=CARTESIAN_POINT('Ctrl Pts',(21.5037197869596,0.301717111362981,4.52131465616629));
#18120=CARTESIAN_POINT('Ctrl Pts',(21.4957671476158,0.385428743083265,4.46286809139133));
#18121=CARTESIAN_POINT('Ctrl Pts',(21.4878145082719,0.450020774675764,4.38793951336988));
#18122=CARTESIAN_POINT('Ctrl Pts',(21.4798618689281,0.514612806268249,4.31301093534845));
#18123=CARTESIAN_POINT('Ctrl Pts',(21.4719092295843,0.560085237732952,4.22160034408054));
#18124=CARTESIAN_POINT('Ctrl Pts',(21.4639565902405,0.58087844500124,4.1248839293359));
#18125=CARTESIAN_POINT('Ctrl Pts',(21.4560039508967,0.601671652269532,4.02816751459124));
#18126=CARTESIAN_POINT('Ctrl Pts',(21.4480513115529,0.597785635341394,3.92614527636987));
#18127=CARTESIAN_POINT('Ctrl Pts',(21.4400986722091,0.569695512712777,3.83129082280931));
#18128=CARTESIAN_POINT('Ctrl Pts',(21.4321460328653,0.541605390084162,3.73643636924876));
#18129=CARTESIAN_POINT('Ctrl Pts',(21.4241933935215,0.489311161755075,3.64874970034904));
#18130=CARTESIAN_POINT('Ctrl Pts',(21.4162407541777,0.419206509371839,3.57895170565158));
#18131=CARTESIAN_POINT('Ctrl Pts',(21.4082881148339,0.349101856988603,3.50915371095413));
#18132=CARTESIAN_POINT('Ctrl Pts',(21.4003354754901,0.261186780551223,3.45724439045894));
#18133=CARTESIAN_POINT('Ctrl Pts',(21.3923828361463,0.16621009553345,3.42957036558731));
#18134=CARTESIAN_POINT('Ctrl Pts',(21.3844301968025,0.0712334105156764,
3.40189634071567));
#18135=CARTESIAN_POINT('Ctrl Pts',(21.3764775574587,-0.0308048830825163,
3.3984576114676));
#18136=CARTESIAN_POINT('Ctrl Pts',(21.3685249181149,-0.127429214135013,
3.41967460932821));
#18137=CARTESIAN_POINT('Ctrl Pts',(21.360572278771,-0.22405354518751,3.44089160718882));
#18138=CARTESIAN_POINT('Ctrl Pts',(21.3526196394272,-0.315263913694308,
3.4867643321581));
#18139=CARTESIAN_POINT('Ctrl Pts',(21.3446670000834,-0.389908609845283,
3.5516842188346));
#18140=CARTESIAN_POINT('Ctrl Pts',(21.3367143607396,-0.464553305996249,
3.6166041055111));
#18141=CARTESIAN_POINT('Ctrl Pts',(21.3287617213958,-0.522632329791381,
3.70057115389483));
#18142=CARTESIAN_POINT('Ctrl Pts',(21.320809082052,-0.557044729551177,3.79331924871262));
#18143=CARTESIAN_POINT('Ctrl Pts',(21.3128564427082,-0.591457129310977,
3.88606734353042));
#18144=CARTESIAN_POINT('Ctrl Pts',(21.3049038033644,-0.602202905035458,
3.9875964847823));
#18145=CARTESIAN_POINT('Ctrl Pts',(21.2969511640206,-0.587968239287942,
4.08549335215105));
#18146=CARTESIAN_POINT('Ctrl Pts',(21.2889985246768,-0.573733573540424,
4.18339021951981));
#18147=CARTESIAN_POINT('Ctrl Pts',(21.281045885333,-0.534518466320906,4.27765481300544));
#18148=CARTESIAN_POINT('Ctrl Pts',(21.2730932459892,-0.47511749858569,4.35676200219639));
#18149=CARTESIAN_POINT('Ctrl Pts',(21.2651406066454,-0.415716530850488,
4.43586919138732));
#18150=CARTESIAN_POINT('Ctrl Pts',(21.2571879673016,-0.336129702599601,
4.49981897628356));
#18151=CARTESIAN_POINT('Ctrl Pts',(21.2492353279577,-0.246087587538132,
4.54079262470289));
#18152=CARTESIAN_POINT('Ctrl Pts',(21.2424386890577,-0.169134048541188,
4.57581031891556));
#18153=CARTESIAN_POINT('Ctrl Pts',(21.2356420501576,-0.0845438791841879,
4.59404604774026));
#18154=CARTESIAN_POINT('Ctrl Pts',(21.2288454112575,1.28243205298473E-5,
4.59412621697841));
#18155=CARTESIAN_POINT('Ctrl Pts',(21.1211545887425,-1.09306879613159E-5,
4.5940621922514));
#18156=CARTESIAN_POINT('Ctrl Pts',(21.1240981080146,-0.0366424819978743,
4.5940862444172));
#18157=CARTESIAN_POINT('Ctrl Pts',(21.1270416272867,-0.0732697079540161,
4.59075208378119));
#18158=CARTESIAN_POINT('Ctrl Pts',(21.1299851465589,-0.109260984540888,
4.58401866488291));
#18159=CARTESIAN_POINT('Ctrl Pts',(21.1379377859027,-0.20650024671525,4.56582668205621));
#18160=CARTESIAN_POINT('Ctrl Pts',(21.1458904252465,-0.299097442487026,
4.52282205952027));
#18161=CARTESIAN_POINT('Ctrl Pts',(21.1538430645903,-0.375731303474415,
4.46026269810429));
#18162=CARTESIAN_POINT('Ctrl Pts',(21.1617957039341,-0.452365164461805,
4.3977033366883));
#18163=CARTESIAN_POINT('Ctrl Pts',(21.1697483432779,-0.513035690664809,
4.31558923639226));
#18164=CARTESIAN_POINT('Ctrl Pts',(21.1777009826217,-0.550325083965727,
4.22395996434209));
#18165=CARTESIAN_POINT('Ctrl Pts',(21.1856536219655,-0.587614477266646,
4.13233069229192));
#18166=CARTESIAN_POINT('Ctrl Pts',(21.1936062613093,-0.601522737665479,
4.03118624848761));
#18167=CARTESIAN_POINT('Ctrl Pts',(21.2015589006531,-0.590349390887683,
3.93289291874755));
#18168=CARTESIAN_POINT('Ctrl Pts',(21.2095115399969,-0.579176044109886,
3.83459958900749));
#18169=CARTESIAN_POINT('Ctrl Pts',(21.2174641793407,-0.542921090155459,
3.73915737333167));
#18170=CARTESIAN_POINT('Ctrl Pts',(21.2254168186845,-0.486017190935348,
3.65823538248142));
#18171=CARTESIAN_POINT('Ctrl Pts',(21.2333694580283,-0.429113291715238,
3.57731339163117));
#18172=CARTESIAN_POINT('Ctrl Pts',(21.2413220973721,-0.351560447229444,
3.51091162560648));
#18173=CARTESIAN_POINT('Ctrl Pts',(21.249274736716,-0.262840548960938,3.46714860467879));
#18174=CARTESIAN_POINT('Ctrl Pts',(21.2572273760598,-0.174120650692433,
3.4233855837511));
#18175=CARTESIAN_POINT('Ctrl Pts',(21.2651800154036,-0.0742336986412151,
3.40226130792041));
#18176=CARTESIAN_POINT('Ctrl Pts',(21.2731326547474,0.0246077668693877,
3.40635850761334));
#18177=CARTESIAN_POINT('Ctrl Pts',(21.2810852940912,0.123449232380002,3.41045570730627));
#18178=CARTESIAN_POINT('Ctrl Pts',(21.289037933435,0.221245211350001,3.43977438252282));
#18179=CARTESIAN_POINT('Ctrl Pts',(21.2969905727788,0.306038813396919,3.49072992590572));
#18180=CARTESIAN_POINT('Ctrl Pts',(21.3049432121226,0.390832415443818,3.54168546928862));
#18181=CARTESIAN_POINT('Ctrl Pts',(21.3128958514664,0.462623640567642,3.61427788083785));
#18182=CARTESIAN_POINT('Ctrl Pts',(21.3208484908102,0.512635033719562,3.69963174955258));
#18183=CARTESIAN_POINT('Ctrl Pts',(21.328801130154,0.562646426871494,3.78498561826733));
#18184=CARTESIAN_POINT('Ctrl Pts',(21.3367537694978,0.590877988051513,3.88310094414759));
#18185=CARTESIAN_POINT('Ctrl Pts',(21.3447064088416,0.59387802439953,3.98198179230066));
#18186=CARTESIAN_POINT('Ctrl Pts',(21.3526590481854,0.596878060747546,4.08086264045372));
#18187=CARTESIAN_POINT('Ctrl Pts',(21.3606116875293,0.574646572263566,4.1805090108796));
#18188=CARTESIAN_POINT('Ctrl Pts',(21.3685643268731,0.529901661201384,4.26873777763737));
#18189=CARTESIAN_POINT('Ctrl Pts',(21.3765169662169,0.485156750139203,4.35696654439514));
#18190=CARTESIAN_POINT('Ctrl Pts',(21.3844696055607,0.417898416498819,4.4337777074848));
#18191=CARTESIAN_POINT('Ctrl Pts',(21.3924222449045,0.336349907607971,4.48978005607163));
#18192=CARTESIAN_POINT('Ctrl Pts',(21.4003748842483,0.254801398717122,4.54578240465847));
#18193=CARTESIAN_POINT('Ctrl Pts',(21.4083275235921,0.158962714575808,4.58097593874246));
#18194=CARTESIAN_POINT('Ctrl Pts',(21.4162801629359,0.0605514396169286,
4.59105776945554));
#18195=CARTESIAN_POINT('Ctrl Pts',(21.4179049715381,0.0404449719157324,
4.59311759444699));
#18196=CARTESIAN_POINT('Ctrl Pts',(21.4195297801403,0.0202311170044278,
4.59412918598148));
#18197=CARTESIAN_POINT('Ctrl Pts',(21.4211545887425,1.51733402061755E-5,
4.59410821609125));
#18198=CARTESIAN_POINT('Origin',(4.,0.,4.));
#18199=CARTESIAN_POINT('',(21.8288454112575,1.47252919898561E-5,4.59408074293421));
#18200=CARTESIAN_POINT('',(21.7211545887425,-1.54601956517634E-5,4.59410286710644));
#18201=CARTESIAN_POINT('',(4.,-7.27562663373442E-17,4.5941));
#18202=CARTESIAN_POINT('Ctrl Pts',(21.8288454112575,1.47252919898561E-5,
4.59408074293421));
#18203=CARTESIAN_POINT('Ctrl Pts',(21.826505394409,0.0291331941223908,4.59410767674242));
#18204=CARTESIAN_POINT('Ctrl Pts',(21.8241653775604,0.0582478076928112,
4.59200528777341));
#18205=CARTESIAN_POINT('Ctrl Pts',(21.8218253607118,0.0870422430987805,
4.58774093918134));
#18206=CARTESIAN_POINT('Ctrl Pts',(21.813872721368,0.184901264939656,4.57324838268129));
#18207=CARTESIAN_POINT('Ctrl Pts',(21.8059200820242,0.279062206656402,4.53378504179028));
#18208=CARTESIAN_POINT('Ctrl Pts',(21.7979674426804,0.358012610677869,4.47417584741217));
#18209=CARTESIAN_POINT('Ctrl Pts',(21.7900148033366,0.436963014699336,4.41456665303406));
#18210=CARTESIAN_POINT('Ctrl Pts',(21.7820621639928,0.500702881025523,4.33481160516884));
#18211=CARTESIAN_POINT('Ctrl Pts',(21.774109524649,0.541439142878506,4.24466184465998));
#18212=CARTESIAN_POINT('Ctrl Pts',(21.7661568853052,0.58217540473149,4.15451208415111));
#18213=CARTESIAN_POINT('Ctrl Pts',(21.7582042459614,0.599908062111268,4.0539676109986));
#18214=CARTESIAN_POINT('Ctrl Pts',(21.7502516066176,0.59246905613922,3.95532135643358));
#18215=CARTESIAN_POINT('Ctrl Pts',(21.7422989672738,0.585030050167171,3.85667510186855));
#18216=CARTESIAN_POINT('Ctrl Pts',(21.73434632793,0.552419380843296,3.759927065891));
#18217=CARTESIAN_POINT('Ctrl Pts',(21.7263936885861,0.498624146640836,3.67690601358098));
#18218=CARTESIAN_POINT('Ctrl Pts',(21.7184410492423,0.444828912438376,3.59388496127097));
#18219=CARTESIAN_POINT('Ctrl Pts',(21.7104884098985,0.369849113357332,3.52459089262848));
#18220=CARTESIAN_POINT('Ctrl Pts',(21.7025357705547,0.28285205103972,3.47749595131133));
#18221=CARTESIAN_POINT('Ctrl Pts',(21.6945831312109,0.195854988722108,3.43040100999418));
#18222=CARTESIAN_POINT('Ctrl Pts',(21.6866304918671,0.0968406631679286,
3.40550519600236));
#18223=CARTESIAN_POINT('Ctrl Pts',(21.6786778525233,-0.00208507577578169,
3.40585236167057));
#18224=CARTESIAN_POINT('Ctrl Pts',(21.6707252131795,-0.101010814719503,
3.40619952733877));
#18225=CARTESIAN_POINT('Ctrl Pts',(21.6627725738357,-0.199847967052756,
3.431789672667));
#18226=CARTESIAN_POINT('Ctrl Pts',(21.6548199344919,-0.28651234476781,3.47949405385809));
#18227=CARTESIAN_POINT('Ctrl Pts',(21.6468672951481,-0.373176722482865,
3.52719843504918));
#18228=CARTESIAN_POINT('Ctrl Pts',(21.6389146558043,-0.44766832557972,3.59701705210314));
#18229=CARTESIAN_POINT('Ctrl Pts',(21.6309620164605,-0.500879541024521,
3.68041362817464));
#18230=CARTESIAN_POINT('Ctrl Pts',(21.6230093771167,-0.55409075646931,3.76381020424612));
#18231=CARTESIAN_POINT('Ctrl Pts',(21.6150567377728,-0.586021584262053,
3.86078473933514));
#18232=CARTESIAN_POINT('Ctrl Pts',(21.607104098429,-0.592768045815946,3.95948077576042));
#18233=CARTESIAN_POINT('Ctrl Pts',(21.5991514590852,-0.599514507369841,
4.05817681218572));
#18234=CARTESIAN_POINT('Ctrl Pts',(21.5911988197414,-0.581076602684875,
4.15859434994728));
#18235=CARTESIAN_POINT('Ctrl Pts',(21.5832461803976,-0.539708616728004,
4.24845597739434));
#18236=CARTESIAN_POINT('Ctrl Pts',(21.5752935410538,-0.498340630771147,
4.33831760484137));
#18237=CARTESIAN_POINT('Ctrl Pts',(21.56734090171,-0.434042563542403,4.41762332197391));
#18238=CARTESIAN_POINT('Ctrl Pts',(21.5593882623662,-0.354675729482573,
4.47667692475034));
#18239=CARTESIAN_POINT('Ctrl Pts',(21.5514356230224,-0.275308895422716,
4.53573052752678));
#18240=CARTESIAN_POINT('Ctrl Pts',(21.5434829836786,-0.180873294531764,
4.57453201594709));
#18241=CARTESIAN_POINT('Ctrl Pts',(21.5355303443348,-0.0829149652056982,
4.58833737958621));
#18242=CARTESIAN_POINT('Ctrl Pts',(21.533302033309,-0.055467269432644,4.59220561033096));
#18243=CARTESIAN_POINT('Ctrl Pts',(21.5310737222833,-0.0277430016607059,
4.5941113769453));
#18244=CARTESIAN_POINT('Ctrl Pts',(21.5288454112575,-1.51073027558624E-5,
4.59408477831653));
#18245=CARTESIAN_POINT('Ctrl Pts',(21.4211545887425,1.51733402061755E-5,
4.59410821609125));
#18246=CARTESIAN_POINT('Ctrl Pts',(21.4274824194841,-0.0787159889745399,
4.59402654867773));
#18247=CARTESIAN_POINT('Ctrl Pts',(21.4338102502257,-0.15747883181342,4.57828382012605));
#18248=CARTESIAN_POINT('Ctrl Pts',(21.4401380809673,-0.230053504748576,
4.54780575811717));
#18249=CARTESIAN_POINT('Ctrl Pts',(21.4480907203111,-0.321263308378747,
4.50950178872359));
#18250=CARTESIAN_POINT('Ctrl Pts',(21.4560433596549,-0.402699049862651,
4.44792372259427));
#18251=CARTESIAN_POINT('Ctrl Pts',(21.4639959989987,-0.464404100671371,
4.37060031698995));
#18252=CARTESIAN_POINT('Ctrl Pts',(21.4719486383425,-0.526109151480106,
4.2932769113856));
#18253=CARTESIAN_POINT('Ctrl Pts',(21.4799012776864,-0.568083511613643,
4.20020816630624));
#18254=CARTESIAN_POINT('Ctrl Pts',(21.4878539170302,-0.585195243866348,
4.10277300340868));
#18255=CARTESIAN_POINT('Ctrl Pts',(21.495806556374,-0.602306976119048,4.00533784051114));
#18256=CARTESIAN_POINT('Ctrl Pts',(21.5037591957178,-0.594556080490919,
3.90353625979537));
#18257=CARTESIAN_POINT('Ctrl Pts',(21.5117118350616,-0.562890209537588,
3.80981489101362));
#18258=CARTESIAN_POINT('Ctrl Pts',(21.5196644744054,-0.53122433858425,3.71609352223184));
#18259=CARTESIAN_POINT('Ctrl Pts',(21.5276171137492,-0.47564349230572,3.63045236538409));
#18260=CARTESIAN_POINT('Ctrl Pts',(21.535569753093,-0.402943186155437,3.56336221830407));
#18261=CARTESIAN_POINT('Ctrl Pts',(21.5435223924368,-0.330242880005154,
3.49627207122406));
#18262=CARTESIAN_POINT('Ctrl Pts',(21.5514750317806,-0.24042311398314,3.44773293391182));
#18263=CARTESIAN_POINT('Ctrl Pts',(21.5594276711244,-0.144465577806233,
3.42367937699355));
#18264=CARTESIAN_POINT('Ctrl Pts',(21.5673803104682,-0.0485080416293372,
3.39962582007528));
#18265=CARTESIAN_POINT('Ctrl Pts',(21.575332949812,0.0535872647024426,3.40005784355098));
#18266=CARTESIAN_POINT('Ctrl Pts',(21.5832855891558,0.149337799479898,3.42492262666669));
#18267=CARTESIAN_POINT('Ctrl Pts',(21.5912382284996,0.245088334257342,3.44978740978241));
#18268=CARTESIAN_POINT('Ctrl Pts',(21.5991908678434,0.33449409748049,3.49908495253815));
#18269=CARTESIAN_POINT('Ctrl Pts',(21.6071435071872,0.406624016913212,3.56678795891296));
#18270=CARTESIAN_POINT('Ctrl Pts',(21.6150961465311,0.478753936345942,3.63449096528778));
#18271=CARTESIAN_POINT('Ctrl Pts',(21.6230487858749,0.533608011988269,3.72059943528167));
#18272=CARTESIAN_POINT('Ctrl Pts',(21.6310014252187,0.564479585995414,3.81458543566408));
#18273=CARTESIAN_POINT('Ctrl Pts',(21.6389540645625,0.595351160002559,3.90857143604649));
#18274=CARTESIAN_POINT('Ctrl Pts',(21.6469067039063,0.602240232374519,4.0104349668174));
#18275=CARTESIAN_POINT('Ctrl Pts',(21.6548593432501,0.584304520186539,4.10772182398666));
#18276=CARTESIAN_POINT('Ctrl Pts',(21.6628119825939,0.566368807998562,4.2050086811559));
#18277=CARTESIAN_POINT('Ctrl Pts',(21.6707646219377,0.523608311250652,4.29771886472347));
#18278=CARTESIAN_POINT('Ctrl Pts',(21.6787172612815,0.461251083056512,4.37451729206089));
#18279=CARTESIAN_POINT('Ctrl Pts',(21.6866699006253,0.398893854862358,4.45131571939834));
#18280=CARTESIAN_POINT('Ctrl Pts',(21.6946225399691,0.316939895221968,4.51220239050563));
#18281=CARTESIAN_POINT('Ctrl Pts',(21.7025751793129,0.225409191891896,4.54973308058009));
#18282=CARTESIAN_POINT('Ctrl Pts',(21.7087683157894,0.15412944274098,4.5789601931952));
#18283=CARTESIAN_POINT('Ctrl Pts',(21.7149614522659,0.0770418275534371,
4.59402294959611));
#18284=CARTESIAN_POINT('Ctrl Pts',(21.7211545887425,-1.54601956517634E-5,
4.59410286710644));
#18285=CARTESIAN_POINT('Origin',(4.,0.,4.));
#18286=CARTESIAN_POINT('',(22.1288454112575,-1.19684274697274E-5,4.59413016891312));
#18287=CARTESIAN_POINT('',(22.0211545887425,1.20066176157995E-5,4.59406577061205));
#18288=CARTESIAN_POINT('',(4.,-7.27562663373442E-17,4.5941));
#18289=CARTESIAN_POINT('Ctrl Pts',(22.1288454112575,-1.19684274697274E-5,
4.59413016891312));
#18290=CARTESIAN_POINT('Ctrl Pts',(22.1219370665346,0.0859328098890183,
4.59405244111828));
#18291=CARTESIAN_POINT('Ctrl Pts',(22.1150287218117,0.171910584533005,4.57519344187135));
#18292=CARTESIAN_POINT('Ctrl Pts',(22.1081203770888,0.24987714748571,4.53905210772026));
#18293=CARTESIAN_POINT('Ctrl Pts',(22.100167737745,0.339629466009183,4.49744749656716));
#18294=CARTESIAN_POINT('Ctrl Pts',(22.0922150984012,0.418765494330909,4.4329406966096));
#18295=CARTESIAN_POINT('Ctrl Pts',(22.0842624590574,0.477609775176754,4.35341854270704));
#18296=CARTESIAN_POINT('Ctrl Pts',(22.0763098197136,0.536454056022584,4.2738963888045));
#18297=CARTESIAN_POINT('Ctrl Pts',(22.0683571803698,0.575006589392542,4.17935888095698));
#18298=CARTESIAN_POINT('Ctrl Pts',(22.060404541026,0.588553803007579,4.081364517074));
#18299=CARTESIAN_POINT('Ctrl Pts',(22.0524519016822,0.60210101662262,3.983370153191));
#18300=CARTESIAN_POINT('Ctrl Pts',(22.0444992623384,0.590642910482727,3.88191893327255));
#18301=CARTESIAN_POINT('Ctrl Pts',(22.0365466229946,0.55558039411957,3.78941465069146));
#18302=CARTESIAN_POINT('Ctrl Pts',(22.0285939836508,0.520517877756421,3.69691036811039));
#18303=CARTESIAN_POINT('Ctrl Pts',(22.020641344307,0.461850951170019,3.61335302286667));
#18304=CARTESIAN_POINT('Ctrl Pts',(22.0126887049632,0.386752445163155,3.5489586384446));
#18305=CARTESIAN_POINT('Ctrl Pts',(22.0047360656194,0.311653939156274,3.48456425402251));
#18306=CARTESIAN_POINT('Ctrl Pts',(21.9967834262756,0.220123853728924,3.43933283042207));
#18307=CARTESIAN_POINT('Ctrl Pts',(21.9888307869318,0.123352988439278,3.41879452521803));
#18308=CARTESIAN_POINT('Ctrl Pts',(21.980878147588,0.0265821231496428,3.398256220014));
#18309=CARTESIAN_POINT('Ctrl Pts',(21.9729255082441,-0.075429522002288,
3.40241103320635));
#18310=CARTESIAN_POINT('Ctrl Pts',(21.9649728689003,-0.170209634025949,
3.43075098229493));
#18311=CARTESIAN_POINT('Ctrl Pts',(21.9570202295565,-0.26498974604961,3.4590909313835));
#18312=CARTESIAN_POINT('Ctrl Pts',(21.9490675902127,-0.352538324945002,
3.5116160163683));
#18313=CARTESIAN_POINT('Ctrl Pts',(21.9411149508689,-0.422151364554475,
3.58190433023263));
#18314=CARTESIAN_POINT('Ctrl Pts',(21.9331623115251,-0.491764404163956,
3.65219264409696));
#18315=CARTESIAN_POINT('Ctrl Pts',(21.9252096721813,-0.543441904487514,
3.74024418684083));
#18316=CARTESIAN_POINT('Ctrl Pts',(21.9172570328375,-0.570865587277161,
3.83529345812586));
#18317=CARTESIAN_POINT('Ctrl Pts',(21.9093043934937,-0.598289270066803,
3.93034272941087));
#18318=CARTESIAN_POINT('Ctrl Pts',(21.9013517541499,-0.601459135322544,
4.03238972923704));
#18319=CARTESIAN_POINT('Ctrl Pts',(21.8933991148061,-0.579987623844179,
4.12895782202339));
#18320=CARTESIAN_POINT('Ctrl Pts',(21.8854464754623,-0.558516112365809,
4.22552591480976));
#18321=CARTESIAN_POINT('Ctrl Pts',(21.8774938361185,-0.512403224153321,
4.31661510055631));
#18322=CARTESIAN_POINT('Ctrl Pts',(21.8695411967747,-0.447286887835617,
4.39108848569571));
#18323=CARTESIAN_POINT('Ctrl Pts',(21.8615885574308,-0.38217055151792,4.46556187083511));
#18324=CARTESIAN_POINT('Ctrl Pts',(21.853635918087,-0.298050767095013,4.52341945536736));
#18325=CARTESIAN_POINT('Ctrl Pts',(21.8456832787432,-0.205212323901057,
4.55758736157894));
#18326=CARTESIAN_POINT('Ctrl Pts',(21.840070656248,-0.139691040693493,4.58170156451555));
#18327=CARTESIAN_POINT('Ctrl Pts',(21.8344580337528,-0.0698270680627233,
4.59401614113532));
#18328=CARTESIAN_POINT('Ctrl Pts',(21.8288454112575,1.47252919898561E-5,
4.59408074293421));
#18329=CARTESIAN_POINT('Ctrl Pts',(21.7211545887425,-1.54601956517634E-5,
4.59410286710644));
#18330=CARTESIAN_POINT('Ctrl Pts',(21.7229140916097,-0.0219078436841643,
4.59412557209431));
#18331=CARTESIAN_POINT('Ctrl Pts',(21.724673594477,-0.0437977792686499,
4.59293892497318));
#18332=CARTESIAN_POINT('Ctrl Pts',(21.7264330973443,-0.0655513867134097,
4.59052415646896));
#18333=CARTESIAN_POINT('Ctrl Pts',(21.7343857366881,-0.163873814968881,
4.57960983324176));
#18334=CARTESIAN_POINT('Ctrl Pts',(21.742338376032,-0.259411224460086,4.54360647774573));
#18335=CARTESIAN_POINT('Ctrl Pts',(21.7502910153758,-0.340482865683332,
4.48691599054611));
#18336=CARTESIAN_POINT('Ctrl Pts',(21.7582436547196,-0.421554506906578,
4.4302255033465));
#18337=CARTESIAN_POINT('Ctrl Pts',(21.7661962940634,-0.488160379861865,
4.3528478844433));
#18338=CARTESIAN_POINT('Ctrl Pts',(21.7741489334072,-0.532157009426634,
4.26424360160945));
#18339=CARTESIAN_POINT('Ctrl Pts',(21.782101572751,-0.576153638991403,4.1756393187756));
#18340=CARTESIAN_POINT('Ctrl Pts',(21.7900542120948,-0.597541025165654,
4.0758083720111));
#18341=CARTESIAN_POINT('Ctrl Pts',(21.7980068514386,-0.593704268699233,
3.9769564542281));
#18342=CARTESIAN_POINT('Ctrl Pts',(21.8059594907824,-0.589867512232813,
3.87810453644509));
#18343=CARTESIAN_POINT('Ctrl Pts',(21.8139121301262,-0.560806613125721,
3.78023164764359));
#18344=CARTESIAN_POINT('Ctrl Pts',(21.82186476947,-0.510074662095298,3.69530408148155));
#18345=CARTESIAN_POINT('Ctrl Pts',(21.8298174088138,-0.459342711064876,
3.61037651531951));
#18346=CARTESIAN_POINT('Ctrl Pts',(21.8377700481576,-0.386939708111122,
3.53839427179695));
#18347=CARTESIAN_POINT('Ctrl Pts',(21.8457226875014,-0.301717906454235,
3.48815816056295));
#18348=CARTESIAN_POINT('Ctrl Pts',(21.8536753268452,-0.216496104797349,
3.43792204932895));
#18349=CARTESIAN_POINT('Ctrl Pts',(21.8616279661891,-0.118455504437329,
3.40943207038352));
#18350=CARTESIAN_POINT('Ctrl Pts',(21.8695806055329,-0.0195829040543552,
3.40617151167847));
#18351=CARTESIAN_POINT('Ctrl Pts',(21.8775332448767,0.0792896963286298,
3.40291095297342));
#18352=CARTESIAN_POINT('Ctrl Pts',(21.8854858842205,0.178994296734569,3.42487981450875));
#18353=CARTESIAN_POINT('Ctrl Pts',(21.8934385235643,0.267340651814441,3.46939210375187));
#18354=CARTESIAN_POINT('Ctrl Pts',(21.9013911629081,0.355687006894294,3.51390439299499));
#18355=CARTESIAN_POINT('Ctrl Pts',(21.9093438022519,0.432675116648084,3.58096010994589));
#18356=CARTESIAN_POINT('Ctrl Pts',(21.9172964415957,0.488892136101412,3.66236077992681));
#18357=CARTESIAN_POINT('Ctrl Pts',(21.9252490809395,0.545109155554752,3.74376144990775));
#18358=CARTESIAN_POINT('Ctrl Pts',(21.9332017202833,0.580555084707621,3.8395070729187));
#18359=CARTESIAN_POINT('Ctrl Pts',(21.9411543596271,0.590896175957217,3.93789144251738));
#18360=CARTESIAN_POINT('Ctrl Pts',(21.9491069989709,0.601237267206812,4.03627581211605));
#18361=CARTESIAN_POINT('Ctrl Pts',(21.9570596383147,0.58647352055314,4.13729892830245));
#18362=CARTESIAN_POINT('Ctrl Pts',(21.9650122776585,0.548410005102802,4.22860933921557));
#18363=CARTESIAN_POINT('Ctrl Pts',(21.9729649170023,0.510346489652465,4.31991975012869));
#18364=CARTESIAN_POINT('Ctrl Pts',(21.9809175563462,0.448983205405461,4.40151745576853));
#18365=CARTESIAN_POINT('Ctrl Pts',(21.98887019569,0.371822649612145,4.46342602528218));
#18366=CARTESIAN_POINT('Ctrl Pts',(21.9968228350338,0.29466209381883,4.52533459479583));
#18367=CARTESIAN_POINT('Ctrl Pts',(22.0047754743776,0.201704266479203,4.5675540281833));
#18368=CARTESIAN_POINT('Ctrl Pts',(22.0127281137214,0.104314528045707,4.58492242469582));
#18369=CARTESIAN_POINT('Ctrl Pts',(22.0155369387284,0.069917050565085,4.59105683924014));
#18370=CARTESIAN_POINT('Ctrl Pts',(22.0183457637354,0.0349667096964542,
4.59409118517947));
#18371=CARTESIAN_POINT('Ctrl Pts',(22.0211545887425,1.20066176157995E-5,
4.59406577061205));
#18372=CARTESIAN_POINT('Origin',(4.,0.,4.));
#18373=CARTESIAN_POINT('',(22.4288454112575,5.18920962550018E-6,4.59405135764298));
#18374=CARTESIAN_POINT('',(22.3211545887424,-7.30827440488969E-6,4.59414400810326));
#18375=CARTESIAN_POINT('',(4.,-7.27562663373442E-17,4.5941));
#18376=CARTESIAN_POINT('Ctrl Pts',(22.4288454112575,5.18920962550018E-6,
4.59405135764298));
#18377=CARTESIAN_POINT('Ctrl Pts',(22.4253213780041,0.0438634191921666,
4.5940647188338));
#18378=CARTESIAN_POINT('Ctrl Pts',(22.4217973447507,0.0877187745911938,
4.589273164082));
#18379=CARTESIAN_POINT('Ctrl Pts',(22.4182733114973,0.130485535360993,4.57964583089408));
#18380=CARTESIAN_POINT('Ctrl Pts',(22.4103206721535,0.226996720088313,4.55791995512033));
#18381=CARTESIAN_POINT('Ctrl Pts',(22.4023680328097,0.317964089339764,4.51156722320365));
#18382=CARTESIAN_POINT('Ctrl Pts',(22.3944153934659,0.392265646131591,4.44625488916104));
#18383=CARTESIAN_POINT('Ctrl Pts',(22.3864627541221,0.4665672029234,4.38094255511845));
#18384=CARTESIAN_POINT('Ctrl Pts',(22.3785101147783,0.524202947255594,4.29667061894994));
#18385=CARTESIAN_POINT('Ctrl Pts',(22.3705574754345,0.558126122886914,4.20374247196213));
#18386=CARTESIAN_POINT('Ctrl Pts',(22.3626048360906,0.592049298518242,4.11081432497429));
#18387=CARTESIAN_POINT('Ctrl Pts',(22.3546521967468,0.602259905448686,4.00922996716717));
#18388=CARTESIAN_POINT('Ctrl Pts',(22.346699557403,0.587509558716917,3.91140947017845));
#18389=CARTESIAN_POINT('Ctrl Pts',(22.3387469180592,0.572759211985149,3.81358897318973));
#18390=CARTESIAN_POINT('Ctrl Pts',(22.3307942787154,0.533047911591167,3.71953233701942));
#18391=CARTESIAN_POINT('Ctrl Pts',(22.3228416393716,0.473230904440663,3.6407392662825));
#18392=CARTESIAN_POINT('Ctrl Pts',(22.3148890000278,0.413413897290173,3.5619461955456));
#18393=CARTESIAN_POINT('Ctrl Pts',(22.306936360684,0.333491183383171,3.49841669024209));
#18394=CARTESIAN_POINT('Ctrl Pts',(22.2989837213402,0.243234403245124,3.45791809774646));
#18395=CARTESIAN_POINT('Ctrl Pts',(22.2910310819964,0.152977623107077,3.41741950525082));
#18396=CARTESIAN_POINT('Ctrl Pts',(22.2830784426526,0.0523867767379842,
3.39995182556307));
#18397=CARTESIAN_POINT('Ctrl Pts',(22.2751258033088,-0.0462395349927855,
3.40765072037886));
#18398=CARTESIAN_POINT('Ctrl Pts',(22.267173163965,-0.144865846723578,3.41534961519466));
#18399=CARTESIAN_POINT('Ctrl Pts',(22.2592205246212,-0.241527623816046,
3.448215084514));
#18400=CARTESIAN_POINT('Ctrl Pts',(22.2512678852774,-0.324406647450603,
3.50222887712101));
#18401=CARTESIAN_POINT('Ctrl Pts',(22.2433152459336,-0.40728567108515,3.55624266972802));
#18402=CARTESIAN_POINT('Ctrl Pts',(22.2353626065897,-0.476381941261788,
3.63140478562268));
#18403=CARTESIAN_POINT('Ctrl Pts',(22.2274099672459,-0.523247497912515,
3.71852563243507));
#18404=CARTESIAN_POINT('Ctrl Pts',(22.2194573279021,-0.570113054563243,
3.80564647924745));
#18405=CARTESIAN_POINT('Ctrl Pts',(22.2115046885583,-0.59474789768806,3.90472605697756));
#18406=CARTESIAN_POINT('Ctrl Pts',(22.2035520492145,-0.594140082177443,
4.00365053781872));
#18407=CARTESIAN_POINT('Ctrl Pts',(22.1955994098707,-0.593532266666827,
4.10257501865988));
#18408=CARTESIAN_POINT('Ctrl Pts',(22.1876467705269,-0.567681792520777,
4.2013444026121));
#18409=CARTESIAN_POINT('Ctrl Pts',(22.1796941311831,-0.519749232289404,
4.2878827872712));
#18410=CARTESIAN_POINT('Ctrl Pts',(22.1717414918393,-0.471816672058032,
4.37442117193029));
#18411=CARTESIAN_POINT('Ctrl Pts',(22.1637888524955,-0.401802025741336,
4.44872855729627));
#18412=CARTESIAN_POINT('Ctrl Pts',(22.1558362131517,-0.318265537426909,
4.50171985346399));
#18413=CARTESIAN_POINT('Ctrl Pts',(22.1478835738079,-0.234729049112483,
4.55471114963171));
#18414=CARTESIAN_POINT('Ctrl Pts',(22.1399309344641,-0.137670718800326,
4.58638635660118));
#18415=CARTESIAN_POINT('Ctrl Pts',(22.1319782951203,-0.0389572492816432,
4.5928727489116));
#18416=CARTESIAN_POINT('Ctrl Pts',(22.1309340004994,-0.0259947671705595,
4.5937245044491));
#18417=CARTESIAN_POINT('Ctrl Pts',(22.1298897058784,-0.0130037447923657,
4.5941419185755));
#18418=CARTESIAN_POINT('Ctrl Pts',(22.1288454112575,-1.19684274697274E-5,
4.59413016891312));
#18419=CARTESIAN_POINT('Ctrl Pts',(22.0211545887425,1.20066176157995E-5,
4.59406577061205));
#18420=CARTESIAN_POINT('Ctrl Pts',(22.0262984030792,-0.064000704172389,
4.59401922879619));
#18421=CARTESIAN_POINT('Ctrl Pts',(22.031442217416,-0.128028044405449,4.5837112392356));
#18422=CARTESIAN_POINT('Ctrl Pts',(22.0365860317528,-0.188701337098646,
4.56338935830438));
#18423=CARTESIAN_POINT('Ctrl Pts',(22.0445386710966,-0.282505814282095,
4.53197053576284));
#18424=CARTESIAN_POINT('Ctrl Pts',(22.0524913104404,-0.368293119121642,
4.4766155310422));
#18425=CARTESIAN_POINT('Ctrl Pts',(22.0604439497842,-0.435574585201076,
4.40409224738955));
#18426=CARTESIAN_POINT('Ctrl Pts',(22.068396589128,-0.502856051280518,4.33156896373689));
#18427=CARTESIAN_POINT('Ctrl Pts',(22.0763492284718,-0.551631678599843,
4.24187740115222));
#18428=CARTESIAN_POINT('Ctrl Pts',(22.0843018678156,-0.575937982408454,
4.14598357473613));
#18429=CARTESIAN_POINT('Ctrl Pts',(22.0922545071594,-0.600244286217068,
4.05008974832002));
#18430=CARTESIAN_POINT('Ctrl Pts',(22.1002071465032,-0.600081266514962,
3.94799365807249));
#18431=CARTESIAN_POINT('Ctrl Pts',(22.1081597858471,-0.575468854681199,
3.85217794154701));
#18432=CARTESIAN_POINT('Ctrl Pts',(22.1161124251909,-0.550856442847438,
3.75636222502155));
#18433=CARTESIAN_POINT('Ctrl Pts',(22.1240650645347,-0.501794638882025,
3.66682688221814));
#18434=CARTESIAN_POINT('Ctrl Pts',(22.1320177038785,-0.434281916527717,
3.5945188282416));
#18435=CARTESIAN_POINT('Ctrl Pts',(22.1399703432223,-0.366769194173409,
3.52221077426505));
#18436=CARTESIAN_POINT('Ctrl Pts',(22.1479229825661,-0.280805553430205,
3.46713000911538));
#18437=CARTESIAN_POINT('Ctrl Pts',(22.1558756219099,-0.186901220180937,
3.43601090651668));
#18438=CARTESIAN_POINT('Ctrl Pts',(22.1638282612537,-0.0929968869316588,
3.40489180391798));
#18439=CARTESIAN_POINT('Ctrl Pts',(22.1717809005975,0.00884813882368474,
3.39773436387026));
#18440=CARTESIAN_POINT('Ctrl Pts',(22.1797335399413,0.106181915586414,3.41541368090248));
#18441=CARTESIAN_POINT('Ctrl Pts',(22.1876861792851,0.203515692349121,3.4330929979347));
#18442=CARTESIAN_POINT('Ctrl Pts',(22.1956388186289,0.296338220119215,3.47560907204686));
#18443=CARTESIAN_POINT('Ctrl Pts',(22.2035914579727,0.373300680656879,3.53776373412001));
#18444=CARTESIAN_POINT('Ctrl Pts',(22.2115440973165,0.450263141194552,3.59991839619317));
#18445=CARTESIAN_POINT('Ctrl Pts',(22.2194967366603,0.511365534499791,3.68171164622733));
#18446=CARTESIAN_POINT('Ctrl Pts',(22.2274493760041,0.549137260797828,3.7731431454068));
#18447=CARTESIAN_POINT('Ctrl Pts',(22.2354020153479,0.586908987095865,3.86457464458628));
#18448=CARTESIAN_POINT('Ctrl Pts',(22.2433546546918,0.6013500463867,3.96564439291107));
#18449=CARTESIAN_POINT('Ctrl Pts',(22.2513072940356,0.590694822479903,4.06399523710107));
#18450=CARTESIAN_POINT('Ctrl Pts',(22.2592599333794,0.580039598573106,4.16234608129106));
#18451=CARTESIAN_POINT('Ctrl Pts',(22.2672125727232,0.544288091468676,4.25797802134625));
#18452=CARTESIAN_POINT('Ctrl Pts',(22.275165212067,0.487811409852587,4.33919875012361));
#18453=CARTESIAN_POINT('Ctrl Pts',(22.2831178514108,0.431334728236497,4.42041947890096));
#18454=CARTESIAN_POINT('Ctrl Pts',(22.2910704907546,0.354132872108749,4.48722899640046));
#18455=CARTESIAN_POINT('Ctrl Pts',(22.2990231300984,0.265644819817582,4.53145892916239));
#18456=CARTESIAN_POINT('Ctrl Pts',(22.3064002829798,0.183560135512932,4.57248819778762));
#18457=CARTESIAN_POINT('Ctrl Pts',(22.3137774358611,0.0917635873240076,
4.59408754951618));
#18458=CARTESIAN_POINT('Ctrl Pts',(22.3211545887424,-7.30827440488969E-6,
4.59414400810326));
#18459=CARTESIAN_POINT('Origin',(4.,0.,4.));
#18460=CARTESIAN_POINT('',(22.7288454112575,-7.11440487624268E-7,4.59414971000239));
#18461=CARTESIAN_POINT('',(22.6211545887425,-1.51245797256638E-7,4.59404869726453));
#18462=CARTESIAN_POINT('',(4.,-7.27562663373442E-17,4.5941));
#18463=CARTESIAN_POINT('Ctrl Pts',(22.7288454112575,-7.11440487624268E-7,
4.59414971000239));
#18464=CARTESIAN_POINT('Ctrl Pts',(22.7287056894736,0.0017373052546791,
4.59414999869406));
#18465=CARTESIAN_POINT('Ctrl Pts',(22.7285659676897,0.0034753215591825,
4.59414251282321));
#18466=CARTESIAN_POINT('Ctrl Pts',(22.7284262459057,0.00521327185949689,
4.59412723628209));
#18467=CARTESIAN_POINT('Ctrl Pts',(22.7204736065619,0.104133365400505,4.59325773105135));
#18468=CARTESIAN_POINT('Ctrl Pts',(22.7125209672181,0.202839630323109,4.56714939948764));
#18469=CARTESIAN_POINT('Ctrl Pts',(22.7045683278743,0.289252680684759,4.51898953373575));
#18470=CARTESIAN_POINT('Ctrl Pts',(22.6966156885305,0.375665731046408,4.47082966798385));
#18471=CARTESIAN_POINT('Ctrl Pts',(22.6886630491867,0.449785566847107,4.40061826804377));
#18472=CARTESIAN_POINT('Ctrl Pts',(22.6807104098429,0.502555912967013,4.31694216252228));
#18473=CARTESIAN_POINT('Ctrl Pts',(22.6727577704991,0.555326259086918,4.23326605700079));
#18474=CARTESIAN_POINT('Ctrl Pts',(22.6648051311553,0.586747115526033,4.13612524589788));
#18475=CARTESIAN_POINT('Ctrl Pts',(22.6568524918115,0.592973744123511,4.03739517928057));
#18476=CARTESIAN_POINT('Ctrl Pts',(22.6488998524677,0.59920037272099,3.93866511266326));
#18477=CARTESIAN_POINT('Ctrl Pts',(22.6409472131239,0.580232773476834,3.83834579053153));
#18478=CARTESIAN_POINT('Ctrl Pts',(22.6329945737801,0.538391640361539,3.74870332422701));
#18479=CARTESIAN_POINT('Ctrl Pts',(22.6250419344363,0.496550507246239,3.65906085792248));
#18480=CARTESIAN_POINT('Ctrl Pts',(22.6170892950925,0.431835840259791,3.58009524744515));
#18481=CARTESIAN_POINT('Ctrl Pts',(22.6091366557487,0.35215901686313,3.52146073929621));
#18482=CARTESIAN_POINT('Ctrl Pts',(22.6011840164048,0.272482193466486,3.46282623114728));
#18483=CARTESIAN_POINT('Ctrl Pts',(22.593231377061,0.17784321365963,3.42452282532672));
#18484=CARTESIAN_POINT('Ctrl Pts',(22.5852787377172,0.0798134434713266,
3.41123383340666));
#18485=CARTESIAN_POINT('Ctrl Pts',(22.5773260983734,-0.0182163267169884,
3.3979448414866));
#18486=CARTESIAN_POINT('Ctrl Pts',(22.5693734590296,-0.119636887286728,
3.40967026346704));
#18487=CARTESIAN_POINT('Ctrl Pts',(22.5614208196858,-0.212048437952692,
3.44497640167274));
#18488=CARTESIAN_POINT('Ctrl Pts',(22.553468180342,-0.304459988618666,3.48028253987845));
#18489=CARTESIAN_POINT('Ctrl Pts',(22.5455155409982,-0.387862529380837,
3.53916939430943));
#18490=CARTESIAN_POINT('Ctrl Pts',(22.5375629016544,-0.452058834188948,
3.61443730067171));
#18491=CARTESIAN_POINT('Ctrl Pts',(22.5296102623106,-0.516255138997059,
3.689705207034));
#18492=CARTESIAN_POINT('Ctrl Pts',(22.5216576229668,-0.561245207851117,
3.7813541653276));
#18493=CARTESIAN_POINT('Ctrl Pts',(22.513704983623,-0.581528460676763,3.87817881267738));
#18494=CARTESIAN_POINT('Ctrl Pts',(22.5057523442792,-0.601811713502406,
3.97500346002715));
#18495=CARTESIAN_POINT('Ctrl Pts',(22.4977997049354,-0.597388150299644,
4.07700379643311));
#18496=CARTESIAN_POINT('Ctrl Pts',(22.4898470655916,-0.568798575589296,
4.17170890717095));
#18497=CARTESIAN_POINT('Ctrl Pts',(22.4818944262477,-0.540209000878948,
4.26641401790879));
#18498=CARTESIAN_POINT('Ctrl Pts',(22.4739417869039,-0.487453414661012,
4.35382390297851));
#18499=CARTESIAN_POINT('Ctrl Pts',(22.4659891475601,-0.416981925106977,
4.42325150516024));
#18500=CARTESIAN_POINT('Ctrl Pts',(22.4580365082163,-0.346510435552941,
4.49267910734197));
#18501=CARTESIAN_POINT('Ctrl Pts',(22.4500838688725,-0.258323042662803,
4.54412442663572));
#18502=CARTESIAN_POINT('Ctrl Pts',(22.4421312295287,-0.163201846116148,
4.57129757646718));
#18503=CARTESIAN_POINT('Ctrl Pts',(22.4377026234383,-0.11023146834083,4.58642955613285));
#18504=CARTESIAN_POINT('Ctrl Pts',(22.4332740173479,-0.0551108697057404,
4.59403456681078));
#18505=CARTESIAN_POINT('Ctrl Pts',(22.4288454112575,5.18920962550018E-6,
4.59405135764298));
#18506=CARTESIAN_POINT('Ctrl Pts',(22.3211545887424,-7.30827440488969E-6,
4.59414400810326));
#18507=CARTESIAN_POINT('Ctrl Pts',(22.3217300752049,-0.00716629073194701,
4.59414841239758));
#18508=CARTESIAN_POINT('Ctrl Pts',(22.3223055616673,-0.0143251170819474,
4.59402171850555));
#18509=CARTESIAN_POINT('Ctrl Pts',(22.3228810481298,-0.0214791647150919,
4.59376292335171));
#18510=CARTESIAN_POINT('Ctrl Pts',(22.3308336874736,-0.120340848501978,
4.59018663675477));
#18511=CARTESIAN_POINT('Ctrl Pts',(22.3387863268174,-0.218289967621164,
4.56138371553656));
#18512=CARTESIAN_POINT('Ctrl Pts',(22.3467389661612,-0.303350908332583,
4.51087570903952));
#18513=CARTESIAN_POINT('Ctrl Pts',(22.3546916055051,-0.388411849044011,
4.46036770254246));
#18514=CARTESIAN_POINT('Ctrl Pts',(22.3626442448489,-0.460584611347669,
4.38815461076656));
#18515=CARTESIAN_POINT('Ctrl Pts',(22.3705968841927,-0.511045091866278,
4.3030654678256));
#18516=CARTESIAN_POINT('Ctrl Pts',(22.3785495235365,-0.561505572384874,
4.21797632488466));
#18517=CARTESIAN_POINT('Ctrl Pts',(22.3865021628803,-0.590253771118432,
4.12001113077866));
#18518=CARTESIAN_POINT('Ctrl Pts',(22.3944548022241,-0.593774829630164,
4.02114746451658));
#18519=CARTESIAN_POINT('Ctrl Pts',(22.4024074415679,-0.597295888141896,
3.92228379825449));
#18520=CARTESIAN_POINT('Ctrl Pts',(22.4103600809117,-0.575589806431797,
3.82252165983632));
#18521=CARTESIAN_POINT('Ctrl Pts',(22.4183127202555,-0.531310447862662,
3.73405832985033));
#18522=CARTESIAN_POINT('Ctrl Pts',(22.4262653595993,-0.487031089293526,
3.64559499986435));
#18523=CARTESIAN_POINT('Ctrl Pts',(22.4342179989431,-0.420178453865353,
3.56843047831055));
#18524=CARTESIAN_POINT('Ctrl Pts',(22.4421706382869,-0.338926188203527,
3.51199917808983));
#18525=CARTESIAN_POINT('Ctrl Pts',(22.4501232776307,-0.257673922541701,
3.45556787786912));
#18526=CARTESIAN_POINT('Ctrl Pts',(22.4580759169745,-0.162022026646223,
3.41986979898149));
#18527=CARTESIAN_POINT('Ctrl Pts',(22.4660285563183,-0.0636652448434586,
3.40926951931498));
#18528=CARTESIAN_POINT('Ctrl Pts',(22.4739811956621,0.0346915369593057,
3.39866923964846));
#18529=CARTESIAN_POINT('Ctrl Pts',(22.4819338350059,0.135753204669356,3.41316675920307));
#18530=CARTESIAN_POINT('Ctrl Pts',(22.4898864743497,0.227163587879617,3.45098955584192));
#18531=CARTESIAN_POINT('Ctrl Pts',(22.4978391136936,0.318573971089878,3.48881235248077));
#18532=CARTESIAN_POINT('Ctrl Pts',(22.5057917530374,0.40033306980035,3.54996042620388));
#18533=CARTESIAN_POINT('Ctrl Pts',(22.5137443923812,0.462444730281743,3.62695759769032));
#18534=CARTESIAN_POINT('Ctrl Pts',(22.521697031725,0.524556390763143,3.70395476917678));
#18535=CARTESIAN_POINT('Ctrl Pts',(22.5296496710688,0.567020613015458,3.79680103842659));
#18536=CARTESIAN_POINT('Ctrl Pts',(22.5376023104126,0.584645549343987,3.89414467407578));
#18537=CARTESIAN_POINT('Ctrl Pts',(22.5455549497564,0.602270485672515,3.99148830972497));
#18538=CARTESIAN_POINT('Ctrl Pts',(22.5535075891002,0.595056136077256,4.09332931177355));
#18539=CARTESIAN_POINT('Ctrl Pts',(22.561460228444,0.563884587368514,4.18721625032571));
#18540=CARTESIAN_POINT('Ctrl Pts',(22.5694128677878,0.532713038659782,4.28110318887784));
#18541=CARTESIAN_POINT('Ctrl Pts',(22.5773655071316,0.477584290837583,4.36703606393356));
#18542=CARTESIAN_POINT('Ctrl Pts',(22.5853181464754,0.405238519368296,4.43450837402952));
#18543=CARTESIAN_POINT('Ctrl Pts',(22.5932707858192,0.332892747898984,4.5019806841255));
#18544=CARTESIAN_POINT('Ctrl Pts',(22.601223425163,0.24332995278257,4.55099242926169));
#18545=CARTESIAN_POINT('Ctrl Pts',(22.6091760645068,0.14750052788588,4.57555132613148));
#18546=CARTESIAN_POINT('Ctrl Pts',(22.6131689059187,0.0993867282199646,
4.58788179608141));
#18547=CARTESIAN_POINT('Ctrl Pts',(22.6171617473306,0.0496932250345643,
4.5940481472271));
#18548=CARTESIAN_POINT('Ctrl Pts',(22.6211545887425,-1.51173456864708E-7,
4.59404872180247));
#18549=CARTESIAN_POINT('Origin',(3.42660065607856,0.,4.));
#18550=CARTESIAN_POINT('',(22.7766006560786,-4.98014040841517E-7,4.41590979742004));
#18551=CARTESIAN_POINT('',(22.8,4.87367679877478E-13,4.415875));
#18552=CARTESIAN_POINT('',(3.42660065607856,4.87367679877478E-13,4.415875));
#18553=CARTESIAN_POINT('',(22.8,-0.195748955928421,4.36692555359082));
#18554=CARTESIAN_POINT('Ctrl Pts',(22.7766006560786,-4.98014040834069E-7,
4.41590979742004));
#18555=CARTESIAN_POINT('Ctrl Pts',(22.7844004373857,-0.0679170312443507,
4.41589851620688));
#18556=CARTESIAN_POINT('Ctrl Pts',(22.7922002186928,-0.135834416676695,
4.39892762624317));
#18557=CARTESIAN_POINT('Ctrl Pts',(22.8,-0.195762566582618,4.36695865185838));
#18558=CARTESIAN_POINT('Origin',(22.8,0.,4.));
#18559=CARTESIAN_POINT('Origin',(3.42660065607856,0.,4.));
#18560=CARTESIAN_POINT('',(22.4766006560785,3.63249072247605E-6,4.41584094994071));
#18561=CARTESIAN_POINT('',(22.5733993439214,-1.05822049303872E-7,4.41583910483016));
#18562=CARTESIAN_POINT('',(3.42660065607856,4.87367679877478E-13,4.415875));
#18563=CARTESIAN_POINT('Ctrl Pts',(22.4766006560785,3.63249072248342E-6,
4.41584094994071));
#18564=CARTESIAN_POINT('Ctrl Pts',(22.4810292621689,-0.0385780726118879,
4.41582919621688));
#18565=CARTESIAN_POINT('Ctrl Pts',(22.4934105076031,-0.146451497349971,
4.40094585736882));
#18566=CARTESIAN_POINT('Ctrl Pts',(22.5137443923812,-0.304292138366774,
4.30886736509782));
#18567=CARTESIAN_POINT('Ctrl Pts',(22.5376023104126,-0.415080201412036,
4.12530439950267));
#18568=CARTESIAN_POINT('Ctrl Pts',(22.561460228444,-0.424369795825249,3.91110111771763));
#18569=CARTESIAN_POINT('Ctrl Pts',(22.5853181464754,-0.329889515310188,
3.71863599132299));
#18570=CARTESIAN_POINT('Ctrl Pts',(22.6091760645068,-0.154742073939436,
3.59497211022641));
#18571=CARTESIAN_POINT('Ctrl Pts',(22.6330339825383,0.0582436639512456,
3.57034842802071));
#18572=CARTESIAN_POINT('Ctrl Pts',(22.6568919005697,0.256987911016647,3.65078654733876));
#18573=CARTESIAN_POINT('Ctrl Pts',(22.6807498186011,0.39289034562191,3.81661632308649));
#18574=CARTESIAN_POINT('Ctrl Pts',(22.7046077366325,0.432722782933869,4.02728943245291));
#18575=CARTESIAN_POINT('Ctrl Pts',(22.7284656546639,0.366738191089385,4.2312875884069));
#18576=CARTESIAN_POINT('Ctrl Pts',(22.7523235726953,0.211084664509997,4.37873330099785));
#18577=CARTESIAN_POINT('Ctrl Pts',(22.7683685731669,0.0716802821347026,
4.41560650088387));
#18578=CARTESIAN_POINT('Ctrl Pts',(22.7764609342946,0.00121612829983627,
4.41590999950663));
#18579=CARTESIAN_POINT('Ctrl Pts',(22.7766006560786,-4.98014040834069E-7,
4.41590979742004));
#18580=CARTESIAN_POINT('',(22.8,0.415641328671541,4.01393920819689));
#18581=CARTESIAN_POINT('Origin',(22.8,0.,4.));
#18582=CARTESIAN_POINT('Ctrl Pts',(22.5733993439214,-1.0582204931428E-7,
4.41583910483016));
#18583=CARTESIAN_POINT('Ctrl Pts',(22.5773591418533,-0.034498011376554,
4.41583950370926));
#18584=CARTESIAN_POINT('Ctrl Pts',(22.5892715791291,-0.138279341065089,
4.40307041914735));
#18585=CARTESIAN_POINT('Ctrl Pts',(22.6091366557487,-0.295063722636797,
4.31769517074077));
#18586=CARTESIAN_POINT('Ctrl Pts',(22.6329945737801,-0.411209141905604,
4.13747522778479));
#18587=CARTESIAN_POINT('Ctrl Pts',(22.6568524918115,-0.426804986482714,
3.92363755172126));
#18588=CARTESIAN_POINT('Ctrl Pts',(22.6807104098429,-0.33803111495158,3.72847502015617));
#18589=CARTESIAN_POINT('Ctrl Pts',(22.7045683278743,-0.16660749730952,3.59970312177549));
#18590=CARTESIAN_POINT('Ctrl Pts',(22.7284262459057,0.0455714674079685,
3.56882345794434));
#18591=CARTESIAN_POINT('Ctrl Pts',(22.7522841639372,0.246577802732478,3.64336153500176));
#18592=CARTESIAN_POINT('Ctrl Pts',(22.7761420819686,0.387346815298129,3.80514019809748));
#18593=CARTESIAN_POINT('Ctrl Pts',(22.7920473606562,0.417963038852713,3.94471011778788));
#18594=CARTESIAN_POINT('Ctrl Pts',(22.8,0.415641328671541,4.01393920819689));
#18595=CARTESIAN_POINT('Origin',(3.42660065607856,0.,4.));
#18596=CARTESIAN_POINT('',(22.1766006560786,-8.37799962078257E-6,4.41589611849309));
#18597=CARTESIAN_POINT('',(22.2733993439214,-5.11585294796223E-6,4.41590580604266));
#18598=CARTESIAN_POINT('',(3.42660065607856,4.87367679877478E-13,4.415875));
#18599=CARTESIAN_POINT('Ctrl Pts',(22.1766006560786,-8.37799962077716E-6,
4.41589611849309));
#18600=CARTESIAN_POINT('Ctrl Pts',(22.1776449506995,-0.0091027307950905,
4.41590434335565));
#18601=CARTESIAN_POINT('Ctrl Pts',(22.1866418846642,-0.0874489573854402,
4.4133870032437));
#18602=CARTESIAN_POINT('Ctrl Pts',(22.2035914579727,-0.232253957950086,
4.36612956178204));
#18603=CARTESIAN_POINT('Ctrl Pts',(22.2274493760041,-0.379286482964224,
4.21008217638027));
#18604=CARTESIAN_POINT('Ctrl Pts',(22.2513072940356,-0.433573131350875,
4.00266397632408));
#18605=CARTESIAN_POINT('Ctrl Pts',(22.275165212067,-0.381839338801546,3.79459436150246));
#18606=CARTESIAN_POINT('Ctrl Pts',(22.2990231300984,-0.236735426869051,
3.63675202040985));
#18607=CARTESIAN_POINT('Ctrl Pts',(22.3228810481298,-0.0337432544318164,
3.56773370504276));
#18608=CARTESIAN_POINT('Ctrl Pts',(22.3467389661613,0.177500062688638,3.60441627341574));
#18609=CARTESIAN_POINT('Ctrl Pts',(22.3705968841926,0.345339779804043,3.73782983856348));
#18610=CARTESIAN_POINT('Ctrl Pts',(22.3944548022241,0.428734513273282,3.93535114928888));
#18611=CARTESIAN_POINT('Ctrl Pts',(22.4183127202555,0.407291980919218,4.1486808655136));
#18612=CARTESIAN_POINT('Ctrl Pts',(22.4421706382869,0.286255462618544,4.32565405918856));
#18613=CARTESIAN_POINT('Ctrl Pts',(22.4615999502279,0.130682174689606,4.40492695636159));
#18614=CARTESIAN_POINT('Ctrl Pts',(22.4730766228251,0.0307047625933256,
4.41585030288671));
#18615=CARTESIAN_POINT('Ctrl Pts',(22.4766006560785,3.63249072248342E-6,
4.41584094994071));
#18616=CARTESIAN_POINT('Ctrl Pts',(22.2733993439214,-5.11585294797612E-6,
4.41590580604266));
#18617=CARTESIAN_POINT('Ctrl Pts',(22.2739748303838,-0.0050164638240448,
4.41590888908576));
#18618=CARTESIAN_POINT('Ctrl Pts',(22.2825029561901,-0.0792779396689182,
4.41459464077989));
#18619=CARTESIAN_POINT('Ctrl Pts',(22.2989837213402,-0.221370022215225,
4.37281103827166));
#18620=CARTESIAN_POINT('Ctrl Pts',(22.3228416393716,-0.372934645290675,
4.22116172228637));
#18621=CARTESIAN_POINT('Ctrl Pts',(22.346699557403,-0.43330658847365,4.01543234121164));
#18622=CARTESIAN_POINT('Ctrl Pts',(22.3705574754345,-0.387723268841402,
3.80592933171158));
#18623=CARTESIAN_POINT('Ctrl Pts',(22.3944153934659,-0.247331046528593,
3.64388188817752));
#18624=CARTESIAN_POINT('Ctrl Pts',(22.4182733114973,-0.0464596501027702,
3.56891502119853));
#18625=CARTESIAN_POINT('Ctrl Pts',(22.4421312295287,0.165772403721094,3.59936017830047));
#18626=CARTESIAN_POINT('Ctrl Pts',(22.4659891475602,0.337468575289321,3.7277726770023));
#18627=CARTESIAN_POINT('Ctrl Pts',(22.4898470655915,0.426644514167594,3.92275218663495));
#18628=CARTESIAN_POINT('Ctrl Pts',(22.513704983623,0.411494197867752,4.13662086224655));
#18629=CARTESIAN_POINT('Ctrl Pts',(22.5375629016544,0.295722435535401,4.31708206952049));
#18630=CARTESIAN_POINT('Ctrl Pts',(22.5574610217539,0.138855410360913,4.40292493148274));
#18631=CARTESIAN_POINT('Ctrl Pts',(22.5694065025095,0.0347856757474044,
4.41583870262252));
#18632=CARTESIAN_POINT('Ctrl Pts',(22.5733993439214,-1.0582204931428E-7,
4.41583910483016));
#18633=CARTESIAN_POINT('Origin',(3.42660065607856,0.,4.));
#18634=CARTESIAN_POINT('',(21.8766006560786,1.03078286340212E-5,4.41586151989188));
#18635=CARTESIAN_POINT('',(21.9733993439214,8.40473402259622E-6,4.41585103914036));
#18636=CARTESIAN_POINT('',(3.42660065607856,4.87367679877478E-13,4.415875));
#18637=CARTESIAN_POINT('Ctrl Pts',(21.8766006560786,1.03078286340201E-5,
4.41586151989188));
#18638=CARTESIAN_POINT('Ctrl Pts',(21.8822132785738,-0.0488795353146484,
4.415816298089));
#18639=CARTESIAN_POINT('Ctrl Pts',(21.8957785404128,-0.167079919178725,
4.39498170153279));
#18640=CARTESIAN_POINT('Ctrl Pts',(21.9172964415957,-0.326407159500644,
4.28539643168872));
#18641=CARTESIAN_POINT('Ctrl Pts',(21.9411543596271,-0.423245389017799,
4.09410684177624));
#18642=CARTESIAN_POINT('Ctrl Pts',(21.9650122776585,-0.416588591947193,
3.87980556563057));
#18643=CARTESIAN_POINT('Ctrl Pts',(21.98887019569,-0.30806453650007,3.69489510271888));
#18644=CARTESIAN_POINT('Ctrl Pts',(22.0127281137213,-0.12421031036921,3.58459109808296));
#18645=CARTESIAN_POINT('Ctrl Pts',(22.0365860317528,0.0900167200678817,
3.57586588547707));
#18646=CARTESIAN_POINT('Ctrl Pts',(22.0604439497842,0.282232210442068,3.67085301705332));
#18647=CARTESIAN_POINT('Ctrl Pts',(22.0843018678157,0.405434237512275,3.8463255517439));
#18648=CARTESIAN_POINT('Ctrl Pts',(22.108159785847,0.429496549703537,4.05937567504088));
#18649=CARTESIAN_POINT('Ctrl Pts',(22.1320177038785,0.348535256241736,4.25790682842971));
#18650=CARTESIAN_POINT('Ctrl Pts',(22.1548313272889,0.18962186617866,4.38744320371645));
#18651=CARTESIAN_POINT('Ctrl Pts',(22.1696923113557,0.0601536901409818,
4.41584170838249));
#18652=CARTESIAN_POINT('Ctrl Pts',(22.1766006560786,-8.37799962077716E-6,
4.41589611849309));
#18653=CARTESIAN_POINT('Ctrl Pts',(21.9733993439214,8.40473402260317E-6,
4.41585103914036));
#18654=CARTESIAN_POINT('Ctrl Pts',(21.9785431582582,-0.044801031555974,
4.41581845947763));
#18655=CARTESIAN_POINT('Ctrl Pts',(21.9916396119388,-0.158914563981884,
4.39744691543598));
#18656=CARTESIAN_POINT('Ctrl Pts',(22.0126887049632,-0.317860118355158,
4.29488591379237));
#18657=CARTESIAN_POINT('Ctrl Pts',(22.0365466229946,-0.420290167226249,
4.10653136780738));
#18658=CARTESIAN_POINT('Ctrl Pts',(22.060404541026,-0.419947821735935,3.89212700053744));
#18659=CARTESIAN_POINT('Ctrl Pts',(22.0842624590574,-0.316916794682727,
3.70410052003731));
#18660=CARTESIAN_POINT('Ctrl Pts',(22.1081203770888,-0.136390978688423,
3.58842952252864));
#18661=CARTESIAN_POINT('Ctrl Pts',(22.1319782951203,0.0774861468089536,
3.57339871771534));
#18662=CARTESIAN_POINT('Ctrl Pts',(22.1558362131517,0.27241579873489,3.66268354680831));
#18663=CARTESIAN_POINT('Ctrl Pts',(22.1796941311831,0.400732367405962,3.83445143701846));
#18664=CARTESIAN_POINT('Ctrl Pts',(22.2035520492145,0.431058956528623,4.04670046033727));
#18665=CARTESIAN_POINT('Ctrl Pts',(22.227409967246,0.355979888945518,4.24752994899471));
#18666=CARTESIAN_POINT('Ctrl Pts',(22.2506923988149,0.197764744804664,4.38444734931837));
#18667=CARTESIAN_POINT('Ctrl Pts',(22.26602219104,0.064235283418036,4.41586628455644));
#18668=CARTESIAN_POINT('Ctrl Pts',(22.2733993439214,-5.11585294797612E-6,
4.41590580604266));
#18669=CARTESIAN_POINT('Origin',(3.42660065607856,0.,4.));
#18670=CARTESIAN_POINT('',(21.5766006560785,-1.05752387382048E-5,4.41586434469346));
#18671=CARTESIAN_POINT('',(21.6733993439214,-1.08222664516599E-5,4.41587700699864));
#18672=CARTESIAN_POINT('',(3.42660065607856,4.87367679877478E-13,4.415875));
#18673=CARTESIAN_POINT('Ctrl Pts',(21.5766006560785,-1.05752387381843E-5,
4.41586434469346));
#18674=CARTESIAN_POINT('Ctrl Pts',(21.5788289671043,-0.0194203346498642,
4.41588296395747));
#18675=CARTESIAN_POINT('Ctrl Pts',(21.5890099174739,-0.10809016089515,4.40978779866957));
#18676=CARTESIAN_POINT('Ctrl Pts',(21.6071435071872,-0.258824259222961,
4.34785450957493));
#18677=CARTESIAN_POINT('Ctrl Pts',(21.6310014252187,-0.39385182381868,4.18131050126406));
#18678=CARTESIAN_POINT('Ctrl Pts',(21.6548593432501,-0.432571889182456,
3.97043113659525));
#18679=CARTESIAN_POINT('Ctrl Pts',(21.6787172612815,-0.365516344619441,
3.76678216446856));
#18680=CARTESIAN_POINT('Ctrl Pts',(21.702575179313,-0.209082097331647,3.62016130585559));
#18681=CARTESIAN_POINT('Ctrl Pts',(21.7264330973443,-0.00152158196427748,
3.56642135455923));
#18682=CARTESIAN_POINT('Ctrl Pts',(21.7502910153758,0.206411001640417,3.61870319251831));
#18683=CARTESIAN_POINT('Ctrl Pts',(21.7741489334072,0.363870472821225,3.76422248622317));
#18684=CARTESIAN_POINT('Ctrl Pts',(21.7980068514386,0.432353701764573,3.96739580449697));
#18685=CARTESIAN_POINT('Ctrl Pts',(21.82186476947,0.395114673548107,4.17854173669174));
#18686=CARTESIAN_POINT('Ctrl Pts',(21.8457226875014,0.261259344941517,4.3460293508861));
#18687=CARTESIAN_POINT('Ctrl Pts',(21.8639679830376,0.110037800305057,4.4094070875278));
#18688=CARTESIAN_POINT('Ctrl Pts',(21.87426063923,0.0203934810735595,4.41588037378429));
#18689=CARTESIAN_POINT('Ctrl Pts',(21.8766006560786,1.03078286340201E-5,
4.41586151989188));
#18690=CARTESIAN_POINT('Ctrl Pts',(21.6733993439214,-1.0822266451653E-5,
4.41587700699864));
#18691=CARTESIAN_POINT('Ctrl Pts',(21.6751588467887,-0.0153356749568721,
4.41589290068126));
#18692=CARTESIAN_POINT('Ctrl Pts',(21.6848709889998,-0.0999166717736498,
4.41130778913604));
#18693=CARTESIAN_POINT('Ctrl Pts',(21.7025357705547,-0.248467031045983,
4.35532645760922));
#18694=CARTESIAN_POINT('Ctrl Pts',(21.7263936885861,-0.388341045935521,
4.1928315042612));
#18695=CARTESIAN_POINT('Ctrl Pts',(21.7502516066176,-0.433255096896122,
3.98318399549658));
#18696=CARTESIAN_POINT('Ctrl Pts',(21.774109524649,-0.372226475033738,3.77764845789182));
#18697=CARTESIAN_POINT('Ctrl Pts',(21.7979674426804,-0.220178340780001,
3.62648392906691));
#18698=CARTESIAN_POINT('Ctrl Pts',(21.8218253607118,-0.0142906046679706,
3.56665425395863));
#18699=CARTESIAN_POINT('Ctrl Pts',(21.8456832787432,0.195091573553633,3.61278941785858));
#18700=CARTESIAN_POINT('Ctrl Pts',(21.8695411967747,0.356768547853618,3.75360811649661));
#18701=CARTESIAN_POINT('Ctrl Pts',(21.8933991148061,0.431205894023261,3.95467634223136));
#18702=CARTESIAN_POINT('Ctrl Pts',(21.9172570328375,0.400201653291494,4.16682743688221));
#18703=CARTESIAN_POINT('Ctrl Pts',(21.941114950869,0.271337207055788,4.33818467892719));
#18704=CARTESIAN_POINT('Ctrl Pts',(21.9598290545635,0.118211900824938,4.40773087908456));
#18705=CARTESIAN_POINT('Ctrl Pts',(21.9705905189143,0.0244769910710258,
4.41586882955141));
#18706=CARTESIAN_POINT('Ctrl Pts',(21.9733993439214,8.40473402260317E-6,
4.41585103914036));
#18707=CARTESIAN_POINT('Origin',(3.42660065607856,0.,4.));
#18708=CARTESIAN_POINT('',(21.2766006560785,8.9771325895615E-6,4.41589335210553));
#18709=CARTESIAN_POINT('',(21.3733993439214,1.06214664634743E-5,4.41588075133303));
#18710=CARTESIAN_POINT('',(3.42660065607856,4.87367679877478E-13,4.415875));
#18711=CARTESIAN_POINT('Ctrl Pts',(21.2766006560785,8.97713258955941E-6,
4.41589335210553));
#18712=CARTESIAN_POINT('Ctrl Pts',(21.2833972949786,-0.0591814269577189,
4.41583723296416));
#18713=CARTESIAN_POINT('Ctrl Pts',(21.2981465732225,-0.187680420990878,
4.38813575385326));
#18714=CARTESIAN_POINT('Ctrl Pts',(21.3208484908102,-0.346716519889314,
4.26034671465164));
#18715=CARTESIAN_POINT('Ctrl Pts',(21.3447064088417,-0.429069235164158,
4.0623886883135));
#18716=CARTESIAN_POINT('Ctrl Pts',(21.368564326873,-0.406502834830527,3.8491749282489));
#18717=CARTESIAN_POINT('Ctrl Pts',(21.3924222449045,-0.284535418465691,
3.67284200661995));
#18718=CARTESIAN_POINT('Ctrl Pts',(21.4162801629359,-0.0929913416969399,
3.5765081259772));
#18719=CARTESIAN_POINT('Ctrl Pts',(21.4401380809674,0.121291651150069,3.58372954422009));
#18720=CARTESIAN_POINT('Ctrl Pts',(21.4639959989987,0.305915531372611,3.69274042788069));
#18721=CARTESIAN_POINT('Ctrl Pts',(21.4878539170302,0.415734731202803,3.87688464650718));
#18722=CARTESIAN_POINT('Ctrl Pts',(21.5117118350615,0.423895464867194,4.09113392265755));
#18723=CARTESIAN_POINT('Ctrl Pts',(21.535569753093,0.328402210690932,4.28309847227994));
#18724=CARTESIAN_POINT('Ctrl Pts',(21.5571993600986,0.169024930905334,4.39437398220882));
#18725=CARTESIAN_POINT('Ctrl Pts',(21.5708763277605,0.0498513310028489,
4.41581651349798));
#18726=CARTESIAN_POINT('Ctrl Pts',(21.5766006560785,-1.05752387381843E-5,
4.41586434469346));
#18727=CARTESIAN_POINT('Ctrl Pts',(21.3733993439214,1.06214664634605E-5,
4.41588075133303));
#18728=CARTESIAN_POINT('Ctrl Pts',(21.379727174663,-0.0551018547626871,
4.41582358345633));
#18729=CARTESIAN_POINT('Ctrl Pts',(21.3940076447484,-0.1795281855266,4.39095386216025));
#18730=CARTESIAN_POINT('Ctrl Pts',(21.4162407541777,-0.338898428465248,
4.27044521104599));
#18731=CARTESIAN_POINT('Ctrl Pts',(21.4400986722091,-0.427045644525908,
4.07499849655415));
#18732=CARTESIAN_POINT('Ctrl Pts',(21.4639565902406,-0.410768568010174,
3.86121260673678));
#18733=CARTESIAN_POINT('Ctrl Pts',(21.4878145082719,-0.294047387504818,
3.68136401506497));
#18734=CARTESIAN_POINT('Ctrl Pts',(21.5116724263034,-0.105423611064507,
3.57943060117972));
#18735=CARTESIAN_POINT('Ctrl Pts',(21.5355303443348,0.108979109962582,3.58033786138646));
#18736=CARTESIAN_POINT('Ctrl Pts',(21.5593882623662,0.296733470072461,3.68386394585134));
#18737=CARTESIAN_POINT('Ctrl Pts',(21.5832461803976,0.411928413892185,3.86469390692879));
#18738=CARTESIAN_POINT('Ctrl Pts',(21.6071040984291,0.426395639810567,4.07860989342611));
#18739=CARTESIAN_POINT('Ctrl Pts',(21.6309620164605,0.33659751701124,4.27330361969026));
#18740=CARTESIAN_POINT('Ctrl Pts',(21.6530604316246,0.177184770587036,4.39173732935402));
#18741=CARTESIAN_POINT('Ctrl Pts',(21.6672062074449,0.0539299276789421,
4.41582106406873));
#18742=CARTESIAN_POINT('Ctrl Pts',(21.6733993439214,-1.0822266451653E-5,
4.41587700699864));
#18743=CARTESIAN_POINT('Origin',(3.42660065607856,0.,4.));
#18744=CARTESIAN_POINT('',(20.9766006560786,-4.48287659654576E-6,4.41584197426197));
#18745=CARTESIAN_POINT('',(21.0733993439214,-7.65157297119567E-6,4.41584853425778));
#18746=CARTESIAN_POINT('',(3.42660065607856,4.87367679877478E-13,4.415875));
#18747=CARTESIAN_POINT('Ctrl Pts',(20.9766006560786,-4.48287659652116E-6,
4.41584197426197));
#18748=CARTESIAN_POINT('Ctrl Pts',(20.9800129835092,-0.0297322302090305,
4.41585318364051));
#18749=CARTESIAN_POINT('Ctrl Pts',(20.9913779502836,-0.128734546054536,
4.40538471300776));
#18750=CARTESIAN_POINT('Ctrl Pts',(21.0106955564018,-0.28396276796243,4.32765515869354));
#18751=CARTESIAN_POINT('Ctrl Pts',(21.0345534744332,-0.40623841344949,4.15153583326342));
#18752=CARTESIAN_POINT('Ctrl Pts',(21.0584113924646,-0.429177699343215,
3.93836186909709));
#18753=CARTESIAN_POINT('Ctrl Pts',(21.082269310496,-0.347171348131155,3.74026010679315));
#18754=CARTESIAN_POINT('Ctrl Pts',(21.1061272285274,-0.180272145040548,
3.605671823621));
#18755=CARTESIAN_POINT('Ctrl Pts',(21.1299851465589,0.0307085077608185,
3.56750752082027));
#18756=CARTESIAN_POINT('Ctrl Pts',(21.1538430645903,0.234180094072738,3.63509941005724));
#18757=CARTESIAN_POINT('Ctrl Pts',(21.1777009826217,0.380388268371489,3.79191943321731));
#18758=CARTESIAN_POINT('Ctrl Pts',(21.2015589006531,0.433581149524578,3.99962082296209));
#18759=CARTESIAN_POINT('Ctrl Pts',(21.2254168186846,0.380751629084578,4.2074149318183));
#18760=CARTESIAN_POINT('Ctrl Pts',(21.2492747367159,0.234817963878357,4.36449043997717));
#18761=CARTESIAN_POINT('Ctrl Pts',(21.2663360158473,0.0893960873046664,
4.41308118928586));
#18762=CARTESIAN_POINT('Ctrl Pts',(21.2754446556348,0.0100763257733538,
4.41590289708112));
#18763=CARTESIAN_POINT('Ctrl Pts',(21.2766006560785,8.97713258955941E-6,
4.41589335210553));
#18764=CARTESIAN_POINT('Ctrl Pts',(21.0733993439214,-7.65157297121996E-6,
4.41584853425778));
#18765=CARTESIAN_POINT('Ctrl Pts',(21.0763428631935,-0.0256500457845501,
4.41586537097631));
#18766=CARTESIAN_POINT('Ctrl Pts',(21.0872390218095,-0.120560449820324,
4.40722571769055));
#18767=CARTESIAN_POINT('Ctrl Pts',(21.1060878197692,-0.274189543318984,
4.33587624407661));
#18768=CARTESIAN_POINT('Ctrl Pts',(21.1299457378007,-0.401599180171465,
4.16343456021562));
#18769=CARTESIAN_POINT('Ctrl Pts',(21.1538036558321,-0.430806878168669,
3.95102867450389));
#18770=CARTESIAN_POINT('Ctrl Pts',(21.1776615738635,-0.354670559489406,
3.75059761183336));
#18771=CARTESIAN_POINT('Ctrl Pts',(21.2015194918949,-0.191807627993766,
3.61115222665144));
#18772=CARTESIAN_POINT('Ctrl Pts',(21.2253774099264,0.0179574932869785,
3.56679071405539));
#18773=CARTESIAN_POINT('Ctrl Pts',(21.2492353279577,0.223331518303719,3.62836067225603));
#18774=CARTESIAN_POINT('Ctrl Pts',(21.2730932459892,0.374094903668402,3.78080656934254));
#18775=CARTESIAN_POINT('Ctrl Pts',(21.2969511640206,0.433381894944723,3.98685123093373));
#18776=CARTESIAN_POINT('Ctrl Pts',(21.320809082052,0.386695207821707,4.19611112472705));
#18777=CARTESIAN_POINT('Ctrl Pts',(21.3446670000834,0.245451009020076,4.35741650656472));
#18778=CARTESIAN_POINT('Ctrl Pts',(21.3621970873732,0.0975684711839555,
4.41172139589413));
#18779=CARTESIAN_POINT('Ctrl Pts',(21.3717745353192,0.014161952170494,4.41589543043265));
#18780=CARTESIAN_POINT('Ctrl Pts',(21.3733993439214,1.06214664634605E-5,
4.41588075133303));
#18781=CARTESIAN_POINT('Origin',(3.42660065607856,0.,4.));
#18782=CARTESIAN_POINT('',(20.6766006560786,1.29204965968245E-6,4.41591114679826));
#18783=CARTESIAN_POINT('',(20.7733993439214,3.9567662055099E-6,4.41590779860895));
#18784=CARTESIAN_POINT('',(3.42660065607856,4.87367679877478E-13,4.415875));
#18785=CARTESIAN_POINT('Ctrl Pts',(20.6766006560786,1.29076178055295E-6,
4.41591111076812));
#18786=CARTESIAN_POINT('Ctrl Pts',(20.6766286720397,-0.000242659277546582,
4.41591112051333));
#18787=CARTESIAN_POINT('Ctrl Pts',(20.6846093273446,-0.0697345275278937,
4.41585145172406));
#18788=CARTESIAN_POINT('Ctrl Pts',(20.7005426219933,-0.208420567790133,
4.38020336888205));
#18789=CARTESIAN_POINT('Ctrl Pts',(20.7244005400248,-0.365106210756856,
4.23385701605743));
#18790=CARTESIAN_POINT('Ctrl Pts',(20.7482584580562,-0.432520392530856,
4.03032528343114));
#18791=CARTESIAN_POINT('Ctrl Pts',(20.7721163760876,-0.394167874571092,
3.81937870627435));
#18792=CARTESIAN_POINT('Ctrl Pts',(20.795974294119,-0.259432524437891,3.65259868360638));
#18793=CARTESIAN_POINT('Ctrl Pts',(20.8198322121504,-0.0612578225112809,
3.57076788979259));
#18794=CARTESIAN_POINT('Ctrl Pts',(20.8436901301819,0.151895538690754,3.5938959627232));
#18795=CARTESIAN_POINT('Ctrl Pts',(20.8675480482132,0.327906592802717,3.71632757520176));
#18796=CARTESIAN_POINT('Ctrl Pts',(20.8914059662447,0.423735399567132,3.90812480123879));
#18797=CARTESIAN_POINT('Ctrl Pts',(20.9152638842761,0.415949440063929,4.12238802732943));
#18798=CARTESIAN_POINT('Ctrl Pts',(20.9391218023075,0.30645246920106,4.30672404095661));
#18799=CARTESIAN_POINT('Ctrl Pts',(20.9595673929083,0.148398440326279,4.40042000858165));
#18800=CARTESIAN_POINT('Ctrl Pts',(20.9720603441653,0.0395501167658222,
4.4158270594931));
#18801=CARTESIAN_POINT('Ctrl Pts',(20.9766006560786,-4.48287659652116E-6,
4.41584197426197));
#18802=CARTESIAN_POINT('Ctrl Pts',(20.7733993439214,3.95676620551077E-6,
4.41590779860895));
#18803=CARTESIAN_POINT('Ctrl Pts',(20.7809111910678,-0.0654084660523611,
4.41587519962517));
#18804=CARTESIAN_POINT('Ctrl Pts',(20.7963756775582,-0.200102595337945,
4.3835597345012));
#18805=CARTESIAN_POINT('Ctrl Pts',(20.8197928033922,-0.358062019934396,
4.24450842127602));
#18806=CARTESIAN_POINT('Ctrl Pts',(20.8436507214237,-0.431438726014498,
4.04305074550709));
#18807=CARTESIAN_POINT('Ctrl Pts',(20.867508639455,-0.399316990859146,3.83106596928302));
#18808=CARTESIAN_POINT('Ctrl Pts',(20.8913665574865,-0.269551332195825,
3.66039017609669));
#18809=CARTESIAN_POINT('Ctrl Pts',(20.9152244755179,-0.0738730526583281,
3.57275822989076));
#18810=CARTESIAN_POINT('Ctrl Pts',(20.9390823935493,0.139869212314499,3.58959853735383));
#18811=CARTESIAN_POINT('Ctrl Pts',(20.9629403115807,0.319409638666883,3.70679317993256));
#18812=CARTESIAN_POINT('Ctrl Pts',(20.9867982296122,0.420845711130686,3.8956848776653));
#18813=CARTESIAN_POINT('Ctrl Pts',(21.0106561476436,0.419373541863394,4.11008446384341));
#18814=CARTESIAN_POINT('Ctrl Pts',(21.034514065675,0.315353119032788,4.29756540021079));
#18815=CARTESIAN_POINT('Ctrl Pts',(21.0554284644342,0.156567902793621,4.39812991232556));
#18816=CARTESIAN_POINT('Ctrl Pts',(21.0683902238497,0.0436291721249729,
4.41581988245125));
#18817=CARTESIAN_POINT('Ctrl Pts',(21.0733993439214,-7.65157297121996E-6,
4.41584853425778));
#18818=CARTESIAN_POINT('Origin',(3.42660065607856,0.,4.));
#18819=CARTESIAN_POINT('',(20.3766006560786,0.000383027521040961,4.41597069455794));
#18820=CARTESIAN_POINT('',(20.4733993439214,0.000101608071013781,4.41586489633469));
#18821=CARTESIAN_POINT('',(3.42660065607856,4.87367679877478E-13,4.415875));
#18822=CARTESIAN_POINT('Ctrl Pts',(20.3766006560786,0.000383027521040954,
4.41597069455794));
#18823=CARTESIAN_POINT('Ctrl Pts',(20.3891496392578,-0.108893832387875,
4.41487837761012));
#18824=CARTESIAN_POINT('Ctrl Pts',(20.4176039011246,-0.35839559572325,4.31454223548297));
#18825=CARTESIAN_POINT('Ctrl Pts',(20.4540108023354,-0.457800032585507,
3.97025345815189));
#18826=CARTESIAN_POINT('Ctrl Pts',(20.4858213597105,-0.325993724402262,
3.71529210935379));
#18827=CARTESIAN_POINT('Ctrl Pts',(20.509679277742,-0.15096738523986,3.59329490328468));
#18828=CARTESIAN_POINT('Ctrl Pts',(20.5335371957734,0.0630371972956549,
3.57102347342756));
#18829=CARTESIAN_POINT('Ctrl Pts',(20.5573951138048,0.260511246441404,3.65349437971329));
#18830=CARTESIAN_POINT('Ctrl Pts',(20.5812530318362,0.394877283734959,3.82077798440408));
#18831=CARTESIAN_POINT('Ctrl Pts',(20.6051109498677,0.432370081305563,4.03184236506754));
#18832=CARTESIAN_POINT('Ctrl Pts',(20.6289688678991,0.364303478986858,4.23514367899931));
#18833=CARTESIAN_POINT('Ctrl Pts',(20.6527987699694,0.207251017164088,4.38076243960928));
#18834=CARTESIAN_POINT('Ctrl Pts',(20.6686760326959,0.0690052481014253,
4.41590835422812));
#18835=CARTESIAN_POINT('Ctrl Pts',(20.6766006560786,1.29076178055295E-6,
4.41591111076812));
#18836=CARTESIAN_POINT('Ctrl Pts',(20.4733993439214,0.000101608071013788,
4.4158648963347));
#18837=CARTESIAN_POINT('Ctrl Pts',(20.4775268795984,-0.0359150725839473,
4.41584626969953));
#18838=CARTESIAN_POINT('Ctrl Pts',(20.4896070546192,-0.141401612166324,
4.40227446254147));
#18839=CARTESIAN_POINT('Ctrl Pts',(20.5096398689838,-0.298255971346869,
4.31460392554555));
#18840=CARTESIAN_POINT('Ctrl Pts',(20.5334977870152,-0.412709509332759,
4.13311446574462));
#18841=CARTESIAN_POINT('Ctrl Pts',(20.5573557050466,-0.425936384696969,
3.91915434697803));
#18842=CARTESIAN_POINT('Ctrl Pts',(20.581213623078,-0.335173342752607,3.72492109335083));
#18843=CARTESIAN_POINT('Ctrl Pts',(20.6050715411095,-0.162364888615448,
3.59797442377207));
#18844=CARTESIAN_POINT('Ctrl Pts',(20.6289294591408,0.0501004451364318,
3.56932214892951));
#18845=CARTESIAN_POINT('Ctrl Pts',(20.6527873771723,0.250339089241223,3.64598859455508));
#18846=CARTESIAN_POINT('Ctrl Pts',(20.6766452952037,0.389350172549011,3.80921715950176));
#18847=CARTESIAN_POINT('Ctrl Pts',(20.7005032132352,0.433161330121289,4.01909908002448));
#18848=CARTESIAN_POINT('Ctrl Pts',(20.7243611312665,0.371049143609512,4.22430982617278));
#18849=CARTESIAN_POINT('Ctrl Pts',(20.748219049298,0.218207240773441,4.37467120177868));
#18850=CARTESIAN_POINT('Ctrl Pts',(20.7645651201829,0.0769305199015265,
4.41491906931248));
#18851=CARTESIAN_POINT('Ctrl Pts',(20.772958551724,0.00384233167249433,
4.41590971150433));
#18852=CARTESIAN_POINT('Ctrl Pts',(20.7733993439214,3.95676620551077E-6,
4.41590779860895));
#18853=CARTESIAN_POINT('Origin',(3.42660065607856,0.,4.));
#18854=CARTESIAN_POINT('',(20.0766006560786,-0.000186622634748148,4.41645953600834));
#18855=CARTESIAN_POINT('',(20.1733993439214,-0.000111611226006447,4.41653056081536));
#18856=CARTESIAN_POINT('',(3.42660065607856,4.87367679877478E-13,4.415875));
#18857=CARTESIAN_POINT('Ctrl Pts',(20.0766006560786,-0.000186622634748109,
4.41645953600834));
#18858=CARTESIAN_POINT('Ctrl Pts',(20.0778126884445,-0.0107019642254321,
4.4165186149328));
#18859=CARTESIAN_POINT('Ctrl Pts',(20.0949299994981,-0.159149739060163,
4.41138240526969));
#18860=CARTESIAN_POINT('Ctrl Pts',(20.1279525892393,-0.432744382500041,
4.23375285658289));
#18861=CARTESIAN_POINT('Ctrl Pts',(20.1756684253021,-0.430649333670284,
3.76246031529274));
#18862=CARTESIAN_POINT('Ctrl Pts',(20.223384261365,-0.033136228617316,3.50924504180455));
#18863=CARTESIAN_POINT('Ctrl Pts',(20.2711000974278,0.394908089060633,3.70680919012016));
#18864=CARTESIAN_POINT('Ctrl Pts',(20.3188159334906,0.460110046434968,4.17340395051402));
#18865=CARTESIAN_POINT('Ctrl Pts',(20.3539827863742,0.197028357007358,4.40022211154544));
#18866=CARTESIAN_POINT('Ctrl Pts',(20.3732443605702,0.0296097328916507,
4.416262840815));
#18867=CARTESIAN_POINT('Ctrl Pts',(20.3766006560786,0.000383027521040954,
4.41597069455794));
#18868=CARTESIAN_POINT('Ctrl Pts',(20.1733993439214,-0.000111611226006447,
4.41653056081536));
#18869=CARTESIAN_POINT('Ctrl Pts',(20.1741425681289,-0.00655727229825777,
4.41655465488103));
#18870=CARTESIAN_POINT('Ctrl Pts',(20.190791071024,-0.150919726673813,4.41348743992374));
#18871=CARTESIAN_POINT('Ctrl Pts',(20.2233448526067,-0.425711472830213,
4.24633918020534));
#18872=CARTESIAN_POINT('Ctrl Pts',(20.2710606886696,-0.437384262562023,
3.77535541015343));
#18873=CARTESIAN_POINT('Ctrl Pts',(20.3187765247324,-0.0477164433392854,
3.51022640082505));
#18874=CARTESIAN_POINT('Ctrl Pts',(20.3664923607953,0.386374384143037,3.69571627142296));
#18875=CARTESIAN_POINT('Ctrl Pts',(20.4062555575143,0.45143962727185,4.08165775845481));
#18876=CARTESIAN_POINT('Ctrl Pts',(20.4380661148895,0.291471375703242,4.31996082336987));
#18877=CARTESIAN_POINT('Ctrl Pts',(20.4577964972439,0.136183087716603,4.40372206768731));
#18878=CARTESIAN_POINT('Ctrl Pts',(20.4695742402546,0.0334792813416625,
4.41588215816259));
#18879=CARTESIAN_POINT('Ctrl Pts',(20.4733993439214,0.000101608071013788,
4.4158648963347));
#18880=CARTESIAN_POINT('Origin',(3.42660065607856,0.,4.));
#18881=CARTESIAN_POINT('',(19.7766006560786,-0.000280998963924209,4.41539029291088));
#18882=CARTESIAN_POINT('',(19.8733993439214,-0.000322938566065189,4.41548189938477));
#18883=CARTESIAN_POINT('',(3.42660065607856,4.87367679877478E-13,4.415875));
#18884=CARTESIAN_POINT('Ctrl Pts',(19.7766006560786,-0.000280998963924181,
4.41539029291088));
#18885=CARTESIAN_POINT('Ctrl Pts',(19.7823810163188,-0.0507615353771658,
4.41570272077311));
#18886=CARTESIAN_POINT('Ctrl Pts',(19.8040666552467,-0.23976299482565,4.3837755623668));
#18887=CARTESIAN_POINT('Ctrl Pts',(19.8416575728622,-0.481212499922896,
4.10168523844358));
#18888=CARTESIAN_POINT('Ctrl Pts',(19.8893734089251,-0.345789702982467,
3.65023692191923));
#18889=CARTESIAN_POINT('Ctrl Pts',(19.9370892449879,0.107175910646637,3.51998011832295));
#18890=CARTESIAN_POINT('Ctrl Pts',(19.9848050810508,0.461722480014006,3.83053541934297));
#18891=CARTESIAN_POINT('Ctrl Pts',(20.0313088847476,0.394022427012164,4.28486673161383));
#18892=CARTESIAN_POINT('Ctrl Pts',(20.0619074097569,0.127288937001902,4.4157433330307));
#18893=CARTESIAN_POINT('Ctrl Pts',(20.0766006560786,-0.000186622634748109,
4.41645953600834));
#18894=CARTESIAN_POINT('Ctrl Pts',(19.8733993439214,-0.000322938566065196,
4.41548189938477));
#18895=CARTESIAN_POINT('Ctrl Pts',(19.8787108960032,-0.0466836533228258,
4.41581668875846));
#18896=CARTESIAN_POINT('Ctrl Pts',(19.8999277267727,-0.231469429366377,
4.38724295332581));
#18897=CARTESIAN_POINT('Ctrl Pts',(19.9370498362297,-0.47800980043334,4.11581244897344));
#18898=CARTESIAN_POINT('Ctrl Pts',(19.9847656722926,-0.355939225796451,
3.66057517601247));
#18899=CARTESIAN_POINT('Ctrl Pts',(20.0324815083554,0.0929888682922082,
3.51702731322357));
#18900=CARTESIAN_POINT('Ctrl Pts',(20.0801973444182,0.456536973876988,3.81701888067549));
#18901=CARTESIAN_POINT('Ctrl Pts',(20.1271699562736,0.401683300383188,4.27772103607547));
#18902=CARTESIAN_POINT('Ctrl Pts',(20.1582372894413,0.131382308576697,4.41603903277767));
#18903=CARTESIAN_POINT('Ctrl Pts',(20.1733993439214,-0.000111611226006447,
4.41653056081536));
#18904=CARTESIAN_POINT('Origin',(3.42660065607856,0.,4.));
#18905=CARTESIAN_POINT('',(19.4766006560786,0.000302289446139524,4.41543216566181));
#18906=CARTESIAN_POINT('',(19.5733993439214,0.000255464646300079,4.41534829948978));
#18907=CARTESIAN_POINT('',(3.42660065607856,4.87367679877478E-13,4.415875));
#18908=CARTESIAN_POINT('Ctrl Pts',(19.4766006560786,0.000302289446139546,
4.41543216566181));
#18909=CARTESIAN_POINT('Ctrl Pts',(19.4869493441932,-0.0900510892866153,
4.41482666801407));
#18910=CARTESIAN_POINT('Ctrl Pts',(19.5132033109954,-0.320168095705801,
4.3413809155508));
#18911=CARTESIAN_POINT('Ctrl Pts',(19.5553625564852,-0.490312813065352,
3.96128857502183));
#18912=CARTESIAN_POINT('Ctrl Pts',(19.603078392548,-0.232620797759261,3.56664935826393));
#18913=CARTESIAN_POINT('Ctrl Pts',(19.6507942286109,0.238690449241969,3.56996267500769));
#18914=CARTESIAN_POINT('Ctrl Pts',(19.6985100646737,0.490808633485035,3.96818593857384));
#18915=CARTESIAN_POINT('Ctrl Pts',(19.7404455404963,0.316268156276861,4.34384396940031));
#18916=CARTESIAN_POINT('Ctrl Pts',(19.7664757376312,0.0881410531427697,
4.41484304213512));
#18917=CARTESIAN_POINT('Ctrl Pts',(19.7766006560786,-0.000280998963924181,
4.41539029291088));
#18918=CARTESIAN_POINT('Ctrl Pts',(19.5733993439214,0.000255464646300094,
4.41534829948978));
#18919=CARTESIAN_POINT('Ctrl Pts',(19.5832792238775,-0.0860485087386658,
4.41486588036018));
#18920=CARTESIAN_POINT('Ctrl Pts',(19.6090643825213,-0.311990568344336,
4.34649332259355));
#18921=CARTESIAN_POINT('Ctrl Pts',(19.6507548198527,-0.491240257057309,
3.97574594767572));
#18922=CARTESIAN_POINT('Ctrl Pts',(19.6984706559155,-0.245282818621706,
3.57368850533185));
#18923=CARTESIAN_POINT('Ctrl Pts',(19.7461864919783,0.225921452997342,3.56311925573479));
#18924=CARTESIAN_POINT('Ctrl Pts',(19.7939023280412,0.489658867576397,3.95374471702426));
#18925=CARTESIAN_POINT('Ctrl Pts',(19.8363066120222,0.324430886710512,4.33863507066385));
#18926=CARTESIAN_POINT('Ctrl Pts',(19.8628056173156,0.0921420753912029,
4.4148141723173));
#18927=CARTESIAN_POINT('Ctrl Pts',(19.8733993439214,-0.000322938566065196,
4.41548189938477));
#18928=CARTESIAN_POINT('Origin',(3.42660065607856,0.,4.));
#18929=CARTESIAN_POINT('',(19.1766006560786,0.000155842099650094,4.41649089206047));
#18930=CARTESIAN_POINT('',(19.2733993439214,0.000220989830587742,4.4164164649367));
#18931=CARTESIAN_POINT('',(3.42660065607856,4.87367679877478E-13,4.415875));
#18932=CARTESIAN_POINT('Ctrl Pts',(19.1766006560786,0.000155842099650088,
4.41649089206047));
#18933=CARTESIAN_POINT('Ctrl Pts',(19.1915176720675,-0.129233580897558,
4.41587069825202));
#18934=CARTESIAN_POINT('Ctrl Pts',(19.2223399667441,-0.397695790553126,
4.28149179527637));
#18935=CARTESIAN_POINT('Ctrl Pts',(19.2690675401082,-0.459293044881286,
3.82405931712685));
#18936=CARTESIAN_POINT('Ctrl Pts',(19.316783376171,-0.100417177000157,3.51852142809106));
#18937=CARTESIAN_POINT('Ctrl Pts',(19.3644992122339,0.350673329058588,3.65513271950473));
#18938=CARTESIAN_POINT('Ctrl Pts',(19.4122150482967,0.479735122332443,4.10844094226069));
#18939=CARTESIAN_POINT('Ctrl Pts',(19.4495821962449,0.235804435834584,4.38544967282755));
#18940=CARTESIAN_POINT('Ctrl Pts',(19.4710440655056,0.0488163355692654,
4.4157572795781));
#18941=CARTESIAN_POINT('Ctrl Pts',(19.4766006560786,0.000302289446139546,
4.41543216566181));
#18942=CARTESIAN_POINT('Ctrl Pts',(19.2733993439214,0.000220989830587761,
4.4164164649367));
#18943=CARTESIAN_POINT('Ctrl Pts',(19.2878475517519,-0.125161313229646,
4.41561068768233));
#18944=CARTESIAN_POINT('Ctrl Pts',(19.31820103827,-0.389985711500173,4.28851341748863));
#18945=CARTESIAN_POINT('Ctrl Pts',(19.3644598034757,-0.464275578741542,
3.8376626582024));
#18946=CARTESIAN_POINT('Ctrl Pts',(19.4121756395385,-0.114554038379521,
3.52168776344319));
#18947=CARTESIAN_POINT('Ctrl Pts',(19.4598914756013,0.340364234683876,3.64495435060606));
#18948=CARTESIAN_POINT('Ctrl Pts',(19.5076073116642,0.482720800247919,4.09426482953845));
#18949=CARTESIAN_POINT('Ctrl Pts',(19.5454432677708,0.244097666198316,4.38190156491584));
#18950=CARTESIAN_POINT('Ctrl Pts',(19.5673739451899,0.0528892875329133,
4.41564251031262));
#18951=CARTESIAN_POINT('Ctrl Pts',(19.5733993439214,0.000255464646300094,
4.41534829948978));
#18952=CARTESIAN_POINT('Origin',(3.42660065607856,0.,4.));
#18953=CARTESIAN_POINT('',(18.8766006560785,-0.00038196507782994,4.41590683121974));
#18954=CARTESIAN_POINT('',(18.9733993439214,-0.000368287616214491,4.41603142687637));
#18955=CARTESIAN_POINT('',(3.42660065607856,4.87367679877478E-13,4.415875));
#18956=CARTESIAN_POINT('Ctrl Pts',(18.8766006560785,-0.000381965077829925,
4.41590683121974));
#18957=CARTESIAN_POINT('Ctrl Pts',(18.8801807212542,-0.0315488007868432,
4.41619587167324));
#18958=CARTESIAN_POINT('Ctrl Pts',(18.8996660651174,-0.200861076696893,
4.39874895857547));
#18959=CARTESIAN_POINT('Ctrl Pts',(18.9350566876684,-0.462607878309702,
4.16703046362027));
#18960=CARTESIAN_POINT('Ctrl Pts',(18.9827725237311,-0.39069124519864,3.70122654773242));
#18961=CARTESIAN_POINT('Ctrl Pts',(19.030488359794,0.0400031699426168,3.50979089028978));
#18962=CARTESIAN_POINT('Ctrl Pts',(19.0782041958568,0.433962058584907,3.76852180111673));
#18963=CARTESIAN_POINT('Ctrl Pts',(19.1259200319197,0.429406911488226,4.23982270375453));
#18964=CARTESIAN_POINT('Ctrl Pts',(19.1587188519936,0.155221332864305,4.41240136130926));
#18965=CARTESIAN_POINT('Ctrl Pts',(19.1756123933799,0.00872798149047904,
4.41653198033223));
#18966=CARTESIAN_POINT('Ctrl Pts',(19.1766006560786,0.000155842099650088,
4.41649089206047));
#18967=CARTESIAN_POINT('Ctrl Pts',(18.9733993439214,-0.000368287616214533,
4.41603142687637));
#18968=CARTESIAN_POINT('Ctrl Pts',(18.9765106009386,-0.0274330213022572,
4.4162811262788));
#18969=CARTESIAN_POINT('Ctrl Pts',(18.9955271366434,-0.192586232161443,
4.40152565608163));
#18970=CARTESIAN_POINT('Ctrl Pts',(19.0304489510358,-0.457487847288108,
4.18058265263639));
#18971=CARTESIAN_POINT('Ctrl Pts',(19.0781647870987,-0.399321187381313,
3.71286272589862));
#18972=CARTESIAN_POINT('Ctrl Pts',(19.1258806231614,0.0255482632835279,
3.50882537619781));
#18973=CARTESIAN_POINT('Ctrl Pts',(19.1735964592243,0.426956350589889,3.75584124112414));
#18974=CARTESIAN_POINT('Ctrl Pts',(19.2213122952871,0.436283851722622,4.22707185138688));
#18975=CARTESIAN_POINT('Ctrl Pts',(19.2545799235195,0.163455264474221,4.41023200720537));
#18976=CARTESIAN_POINT('Ctrl Pts',(19.2719422730642,0.0128655269200745,
4.41649772584937));
#18977=CARTESIAN_POINT('Ctrl Pts',(19.2733993439214,0.000220989830587761,
4.4164164649367));
#18978=CARTESIAN_POINT('Origin',(3.42660065607856,0.,4.));
#18979=CARTESIAN_POINT('',(18.5766006560786,2.82854505807383E-5,4.41518799822097));
#18980=CARTESIAN_POINT('',(18.6733993439214,-3.94222854199766E-5,4.41518963037823));
#18981=CARTESIAN_POINT('',(3.42660065607856,4.87367679877478E-13,4.415875));
#18982=CARTESIAN_POINT('Ctrl Pts',(18.5766006560786,2.82854505807215E-5,
4.41518799822097));
#18983=CARTESIAN_POINT('Ctrl Pts',(18.5847490491285,-0.0712192880865648,
4.41514491699706));
#18984=CARTESIAN_POINT('Ctrl Pts',(18.6088027208661,-0.281596950705947,
4.36382162423513));
#18985=CARTESIAN_POINT('Ctrl Pts',(18.6487616712913,-0.49096944006335,4.0292272779409));
#18986=CARTESIAN_POINT('Ctrl Pts',(18.6964775073541,-0.290120809601049,
3.60284116440841));
#18987=CARTESIAN_POINT('Ctrl Pts',(18.744193343417,0.177150224400508,3.54117212067402));
#18988=CARTESIAN_POINT('Ctrl Pts',(18.7919091794797,0.481741481528227,3.90085177849878));
#18989=CARTESIAN_POINT('Ctrl Pts',(18.836044950367,0.354281053487698,4.31776308733785));
#18990=CARTESIAN_POINT('Ctrl Pts',(18.8642754425666,0.106917172161326,4.4149117417093));
#18991=CARTESIAN_POINT('Ctrl Pts',(18.8766006560785,-0.000381965077829925,
4.41590683121974));
#18992=CARTESIAN_POINT('Ctrl Pts',(18.6733993439214,-3.94222854199489E-5,
4.41518963037823));
#18993=CARTESIAN_POINT('Ctrl Pts',(18.6810789288129,-0.0671871929144198,
4.41524623173262));
#18994=CARTESIAN_POINT('Ctrl Pts',(18.704663792392,-0.273330541024821,4.36810584919535));
#18995=CARTESIAN_POINT('Ctrl Pts',(18.7441539346588,-0.489895661254576,
4.0436745456279));
#18996=CARTESIAN_POINT('Ctrl Pts',(18.7918697707216,-0.301692008317894,
3.6115580391236));
#18997=CARTESIAN_POINT('Ctrl Pts',(18.8395856067845,0.163560057986223,3.53615376224111));
#18998=CARTESIAN_POINT('Ctrl Pts',(18.8873014428472,0.478612406344963,3.88670662268212));
#18999=CARTESIAN_POINT('Ctrl Pts',(18.9319060218929,0.362263203066427,4.31165738429376));
#19000=CARTESIAN_POINT('Ctrl Pts',(18.960605322251,0.110926532249199,4.41500462017153));
#19001=CARTESIAN_POINT('Ctrl Pts',(18.9733993439214,-0.000368287616214533,
4.41603142687637));
#19002=CARTESIAN_POINT('Origin',(3.42660065607856,0.,4.));
#19003=CARTESIAN_POINT('',(18.2766006560786,0.000371443240938316,4.41601098728712));
#19004=CARTESIAN_POINT('',(18.3733993439214,0.000382963303967143,4.41588626824893));
#19005=CARTESIAN_POINT('',(3.42660065607856,4.87367679877478E-13,4.415875));
#19006=CARTESIAN_POINT('Ctrl Pts',(18.2766006560785,0.000371443240938293,
4.41601098728712));
#19007=CARTESIAN_POINT('Ctrl Pts',(18.2893173770028,-0.110264925490287,
4.41498710445335));
#19008=CARTESIAN_POINT('Ctrl Pts',(18.3179393766147,-0.360950442388199,
4.31267773405576));
#19009=CARTESIAN_POINT('Ctrl Pts',(18.3624666549143,-0.479157019140895,
3.88903254594255));
#19010=CARTESIAN_POINT('Ctrl Pts',(18.4101824909771,-0.165810997523729,
3.5369536330429));
#19011=CARTESIAN_POINT('Ctrl Pts',(18.4578983270399,0.299801814449608,3.61009732380414));
#19012=CARTESIAN_POINT('Ctrl Pts',(18.5056141631028,0.49010200717001,4.04129464153984));
#19013=CARTESIAN_POINT('Ctrl Pts',(18.5451816061157,0.274694351318236,4.36741107590602));
#19014=CARTESIAN_POINT('Ctrl Pts',(18.5688437704409,0.0678526130816757,
4.41522900951301));
#19015=CARTESIAN_POINT('Ctrl Pts',(18.5766006560786,2.82854505807215E-5,
4.41518799822097));
#19016=CARTESIAN_POINT('Ctrl Pts',(18.3733993439214,0.000382963303967157,
4.41588626824893));
#19017=CARTESIAN_POINT('Ctrl Pts',(18.3856472566872,-0.106256708375174,
4.41489942083623));
#19018=CARTESIAN_POINT('Ctrl Pts',(18.4138004481407,-0.352960303644862,
4.31875095920395));
#19019=CARTESIAN_POINT('Ctrl Pts',(18.4578589182817,-0.482217355384067,
3.90319273261591));
#19020=CARTESIAN_POINT('Ctrl Pts',(18.5055747543446,-0.179376629827252,
3.54203793877243));
#19021=CARTESIAN_POINT('Ctrl Pts',(18.5532905904074,0.288188414964166,3.60143675240633));
#19022=CARTESIAN_POINT('Ctrl Pts',(18.6010064264702,0.491105603945206,4.02684232898929));
#19023=CARTESIAN_POINT('Ctrl Pts',(18.6410426776416,0.282958802096416,4.36309886994028));
#19024=CARTESIAN_POINT('Ctrl Pts',(18.6651736501253,0.0718833454275778,
4.41512900400112));
#19025=CARTESIAN_POINT('Ctrl Pts',(18.6733993439214,-3.94222854199489E-5,
4.41518963037823));
#19026=CARTESIAN_POINT('Origin',(3.42660065607856,0.,4.));
#19027=CARTESIAN_POINT('',(17.9766006560786,-0.000210814279110197,4.41643020456723));
#19028=CARTESIAN_POINT('',(18.0733993439214,-0.000144384975211464,4.41650095473263));
#19029=CARTESIAN_POINT('',(3.42660065607856,4.87367679877478E-13,4.415875));
#19030=CARTESIAN_POINT('Ctrl Pts',(17.9766006560786,-0.000210814279110157,
4.41643020456723));
#19031=CARTESIAN_POINT('Ctrl Pts',(17.9779804261896,-0.0121834889824064,
4.41650424974197));
#19032=CARTESIAN_POINT('Ctrl Pts',(17.9952654749882,-0.162096873242269,
4.41059855206721));
#19033=CARTESIAN_POINT('Ctrl Pts',(18.0284558024744,-0.435175833605105,
4.22918817311999));
#19034=CARTESIAN_POINT('Ctrl Pts',(18.0761716385373,-0.428137176707308,
3.75791781814212));
#19035=CARTESIAN_POINT('Ctrl Pts',(18.1238874746,-0.0279335627019553,3.5089552556775));
#19036=CARTESIAN_POINT('Ctrl Pts',(18.1716033106629,0.397921871745719,3.71092663761881));
#19037=CARTESIAN_POINT('Ctrl Pts',(18.2193191467257,0.458359528554279,4.17835853620019));
#19038=CARTESIAN_POINT('Ctrl Pts',(18.2543182618643,0.193950155243433,4.40107745006558));
#19039=CARTESIAN_POINT('Ctrl Pts',(18.2734120983152,0.0281121206155762,
4.41626771302466));
#19040=CARTESIAN_POINT('Ctrl Pts',(18.2766006560785,0.000371443240938293,
4.41601098728712));
#19041=CARTESIAN_POINT('Ctrl Pts',(18.0733993439214,-0.000144384975211439,
4.41650095473263));
#19042=CARTESIAN_POINT('Ctrl Pts',(18.0743103058739,-0.00804551399413891,
4.41653639380418));
#19043=CARTESIAN_POINT('Ctrl Pts',(18.0911265465141,-0.153864670001157,
4.41274680364665));
#19044=CARTESIAN_POINT('Ctrl Pts',(18.1238480658419,-0.428237044548737,
4.24190547436581));
#19045=CARTESIAN_POINT('Ctrl Pts',(18.1715639019047,-0.435081213444543,
3.7706322547532));
#19046=CARTESIAN_POINT('Ctrl Pts',(18.2192797379675,-0.0423836094492617,
3.50999096487715));
#19047=CARTESIAN_POINT('Ctrl Pts',(18.2669955740304,0.389235515258945,3.69933251171255));
#19048=CARTESIAN_POINT('Ctrl Pts',(18.3147114100932,0.463413677146622,4.16478163940629));
#19049=CARTESIAN_POINT('Ctrl Pts',(18.3501793333902,0.202226156869028,4.39827758107438));
#19050=CARTESIAN_POINT('Ctrl Pts',(18.3697419779996,0.0322267809866215,
4.41618095209965));
#19051=CARTESIAN_POINT('Ctrl Pts',(18.3733993439214,0.000382963303967157,
4.41588626824893));
#19052=CARTESIAN_POINT('Origin',(3.42660065607856,0.,4.));
#19053=CARTESIAN_POINT('',(17.6766006560786,-0.000263771022561219,4.41536107794487));
#19054=CARTESIAN_POINT('',(17.7733993439214,-0.000309142357869163,4.41544738986064));
#19055=CARTESIAN_POINT('',(3.42660065607856,4.87367679877478E-13,4.415875));
#19056=CARTESIAN_POINT('Ctrl Pts',(17.6766006560786,-0.000263771022561289,
4.41536107794487));
#19057=CARTESIAN_POINT('Ctrl Pts',(17.6825487540639,-0.0522183410383149,
4.41566152300153));
#19058=CARTESIAN_POINT('Ctrl Pts',(17.7044021307368,-0.24273028972288,4.38249735042552));
#19059=CARTESIAN_POINT('Ctrl Pts',(17.7421607860973,-0.48225726547346,4.09660825404716));
#19060=CARTESIAN_POINT('Ctrl Pts',(17.7898766221602,-0.342084653792828,
3.64661166616396));
#19061=CARTESIAN_POINT('Ctrl Pts',(17.837592458223,0.112229559114723,3.52113702282083));
#19062=CARTESIAN_POINT('Ctrl Pts',(17.8853082942859,0.463481641013499,3.83540961967535));
#19063=CARTESIAN_POINT('Ctrl Pts',(17.9316443602377,0.391261919872151,4.28736986940801));
#19064=CARTESIAN_POINT('Ctrl Pts',(17.962075147502,0.125831334120538,4.41565069513148));
#19065=CARTESIAN_POINT('Ctrl Pts',(17.9766006560786,-0.000210814279110157,
4.41643020456723));
#19066=CARTESIAN_POINT('Ctrl Pts',(17.7733993439214,-0.000309142357869142,
4.41544738986064));
#19067=CARTESIAN_POINT('Ctrl Pts',(17.7788786337482,-0.0481438769258273,
4.41577602216682));
#19068=CARTESIAN_POINT('Ctrl Pts',(17.8002632022627,-0.23443694547481,4.38601982759396));
#19069=CARTESIAN_POINT('Ctrl Pts',(17.8375530494648,-0.479202773223469,
4.11076970247734));
#19070=CARTESIAN_POINT('Ctrl Pts',(17.8852688855277,-0.352344189444135,
3.65683998336499));
#19071=CARTESIAN_POINT('Ctrl Pts',(17.9329847215905,0.0980774850139738,
3.51803938772416));
#19072=CARTESIAN_POINT('Ctrl Pts',(17.9807005576534,0.458433095867658,3.82183063825345));
#19073=CARTESIAN_POINT('Ctrl Pts',(18.0275054317636,0.3989600628602,4.28031410431705));
#19074=CARTESIAN_POINT('Ctrl Pts',(18.0584050271863,0.129907183855675,4.41591763216682));
#19075=CARTESIAN_POINT('Ctrl Pts',(18.0733993439214,-0.000144384975211439,
4.41650095473263));
#19076=CARTESIAN_POINT('Origin',(3.42660065607856,0.,4.));
#19077=CARTESIAN_POINT('',(17.3766006560786,0.000316824918469052,4.41546566829253));
#19078=CARTESIAN_POINT('',(17.4733993439214,0.000273208168652644,4.41537657040552));
#19079=CARTESIAN_POINT('',(3.42660065607856,4.87367679877478E-13,4.415875));
#19080=CARTESIAN_POINT('Ctrl Pts',(17.3766006560786,0.000316824918469058,
4.41546566829253));
#19081=CARTESIAN_POINT('Ctrl Pts',(17.3871170819382,-0.0914824399419538,
4.4148173972429));
#19082=CARTESIAN_POINT('Ctrl Pts',(17.4135387864855,-0.323087181591141,
4.33950699049548));
#19083=CARTESIAN_POINT('Ctrl Pts',(17.4558657697204,-0.489877595596684,
3.956123284257));
#19084=CARTESIAN_POINT('Ctrl Pts',(17.5035816057832,-0.228040769637767,
3.56422180844494));
#19085=CARTESIAN_POINT('Ctrl Pts',(17.551297441846,0.243209403937772,3.57250215124727));
#19086=CARTESIAN_POINT('Ctrl Pts',(17.5990132779089,0.491116639619549,3.97336034645914));
#19087=CARTESIAN_POINT('Ctrl Pts',(17.6407810159864,0.313340775136121,4.34566293955037));
#19088=CARTESIAN_POINT('Ctrl Pts',(17.6666434753763,0.0867087440962768,
4.41485812965324));
#19089=CARTESIAN_POINT('Ctrl Pts',(17.6766006560786,-0.000263771022561289,
4.41536107794487));
#19090=CARTESIAN_POINT('Ctrl Pts',(17.4733993439214,0.000273208168652693,
4.41537657040552));
#19091=CARTESIAN_POINT('Ctrl Pts',(17.4834469616226,-0.0874810350323011,
4.41484969107387));
#19092=CARTESIAN_POINT('Ctrl Pts',(17.5093998580114,-0.314919534962053,
4.34468516187688));
#19093=CARTESIAN_POINT('Ctrl Pts',(17.5512580330878,-0.490957336521241,
3.97057010757845));
#19094=CARTESIAN_POINT('Ctrl Pts',(17.5989738691507,-0.240776309167652,
3.57112706567612));
#19095=CARTESIAN_POINT('Ctrl Pts',(17.6466897052135,0.230513307714322,3.56552463842171));
#19096=CARTESIAN_POINT('Ctrl Pts',(17.6944055412763,0.490119007219086,3.95890762096741));
#19097=CARTESIAN_POINT('Ctrl Pts',(17.7366420875123,0.321513805022658,4.34052027563639));
#19098=CARTESIAN_POINT('Ctrl Pts',(17.7629733550606,0.090710757213051,4.41482206853766));
#19099=CARTESIAN_POINT('Ctrl Pts',(17.7733993439214,-0.000309142357869142,
4.41544738986064));
#19100=CARTESIAN_POINT('Origin',(3.42660065607856,0.,4.));
#19101=CARTESIAN_POINT('',(17.0766006560786,0.000130763213737631,4.41651185352269));
#19102=CARTESIAN_POINT('',(17.1733993439214,0.000198609043858391,4.41644558073401));
#19103=CARTESIAN_POINT('',(3.42660065607856,4.87367679877478E-13,4.415875));
#19104=CARTESIAN_POINT('Ctrl Pts',(17.0766006560786,0.000130763213737628,
4.41651185352269));
#19105=CARTESIAN_POINT('Ctrl Pts',(17.0916854098125,-0.130696083011285,
4.41597403242798));
#19106=CARTESIAN_POINT('Ctrl Pts',(17.1226754422341,-0.400436570105288,
4.2789290971087));
#19107=CARTESIAN_POINT('Ctrl Pts',(17.1695707533433,-0.457413284126125,
3.81922856321607));
#19108=CARTESIAN_POINT('Ctrl Pts',(17.2172865894061,-0.0953372598908034,
3.51748986360026));
#19109=CARTESIAN_POINT('Ctrl Pts',(17.265002425469,0.354288437054553,3.6588476466131));
#19110=CARTESIAN_POINT('Ctrl Pts',(17.3127182615318,0.478565610824392,4.11349088504481));
#19111=CARTESIAN_POINT('Ctrl Pts',(17.349917671735,0.232837083242772,4.38668157013213));
#19112=CARTESIAN_POINT('Ctrl Pts',(17.3712118032506,0.0473568302064652,
4.41579785693967));
#19113=CARTESIAN_POINT('Ctrl Pts',(17.3766006560786,0.000316824918469058,
4.41546566829253));
#19114=CARTESIAN_POINT('Ctrl Pts',(17.1733993439214,0.000198609043858397,
4.41644558073401));
#19115=CARTESIAN_POINT('Ctrl Pts',(17.1880152894969,-0.126615914365149,
4.41569892234974));
#19116=CARTESIAN_POINT('Ctrl Pts',(17.2185365137601,-0.392752582168809,
4.28602487069057));
#19117=CARTESIAN_POINT('Ctrl Pts',(17.2649630167107,-0.462538907526291,
3.83277863809798));
#19118=CARTESIAN_POINT('Ctrl Pts',(17.3126788527736,-0.109506707187599,
3.52050703244687));
#19119=CARTESIAN_POINT('Ctrl Pts',(17.3603946888365,0.344087187338735,3.64856119684745));
#19120=CARTESIAN_POINT('Ctrl Pts',(17.4081105248993,0.481700523269991,4.09934702176407));
#19121=CARTESIAN_POINT('Ctrl Pts',(17.4457787432609,0.241130489326423,4.3831889686244));
#19122=CARTESIAN_POINT('Ctrl Pts',(17.467541682935,0.0514330574063097,4.41568373580506));
#19123=CARTESIAN_POINT('Ctrl Pts',(17.4733993439214,0.000273208168652693,
4.41537657040552));
#19124=CARTESIAN_POINT('Origin',(3.42660065607856,0.,4.));
#19125=CARTESIAN_POINT('',(16.7766006560786,-0.000383680820852129,4.41586226484778));
#19126=CARTESIAN_POINT('',(16.8733993439214,-0.000374684679869397,4.41598699190495));
#19127=CARTESIAN_POINT('',(3.42660065607856,4.87367679877478E-13,4.415875));
#19128=CARTESIAN_POINT('Ctrl Pts',(16.7766006560786,-0.000383680820852189,
4.41586226484779));
#19129=CARTESIAN_POINT('Ctrl Pts',(16.7803484589992,-0.0330197262611539,
4.41616320579436));
#19130=CARTESIAN_POINT('Ctrl Pts',(16.8000015406075,-0.203823433586872,
4.39772119122577));
#19131=CARTESIAN_POINT('Ctrl Pts',(16.8355599009034,-0.464342533291602,
4.16214572651883));
#19132=CARTESIAN_POINT('Ctrl Pts',(16.8832757369663,-0.387520750342007,
3.69712561530174));
#19133=CARTESIAN_POINT('Ctrl Pts',(16.9309915730291,0.0451673004198413,
3.51023971187451));
#19134=CARTESIAN_POINT('Ctrl Pts',(16.978707409092,0.436377524217892,3.7731082169636));
#19135=CARTESIAN_POINT('Ctrl Pts',(17.0264232451548,0.426855552995382,4.24433493759383));
#19136=CARTESIAN_POINT('Ctrl Pts',(17.0590543274837,0.152277829190936,4.41314658311127));
#19137=CARTESIAN_POINT('Ctrl Pts',(17.0757801311249,0.00724700082869906,
4.41654110793655));
#19138=CARTESIAN_POINT('Ctrl Pts',(17.0766006560786,0.000130763213737628,
4.41651185352269));
#19139=CARTESIAN_POINT('Ctrl Pts',(16.8733993439214,-0.000374684679869387,
4.41598699190495));
#19140=CARTESIAN_POINT('Ctrl Pts',(16.8766783386836,-0.0289064002234668,
4.4162516892709));
#19141=CARTESIAN_POINT('Ctrl Pts',(16.8958626121335,-0.195546116663039,
4.40054826733105));
#19142=CARTESIAN_POINT('Ctrl Pts',(16.9309521642709,-0.459365614209645,
4.17575112327883));
#19143=CARTESIAN_POINT('Ctrl Pts',(16.9786680003337,-0.396272847821079,
3.70867019559999));
#19144=CARTESIAN_POINT('Ctrl Pts',(17.0263838363966,0.0307233721630972,
3.5091219099869));
#19145=CARTESIAN_POINT('Ctrl Pts',(17.0740996724594,0.429505846750062,3.76035452756312));
#19146=CARTESIAN_POINT('Ctrl Pts',(17.1218155085223,0.433866493469502,4.23165726989771));
#19147=CARTESIAN_POINT('Ctrl Pts',(17.1549153990096,0.160507997039396,4.41102293437065));
#19148=CARTESIAN_POINT('Ctrl Pts',(17.1721100108093,0.0113854435377776,
4.41651144656345));
#19149=CARTESIAN_POINT('Ctrl Pts',(17.1733993439214,0.000198609043858397,
4.41644558073401));
#19150=CARTESIAN_POINT('Origin',(3.42660065607856,0.,4.));
#19151=CARTESIAN_POINT('',(16.4766006560786,5.2409936866527E-5,4.41519222098806));
#19152=CARTESIAN_POINT('',(16.5733993439214,-1.52272386678698E-5,4.41518677123726));
#19153=CARTESIAN_POINT('',(3.42660065607856,4.87367679877478E-13,4.415875));
#19154=CARTESIAN_POINT('Ctrl Pts',(16.4766006560786,5.2409936866539E-5,
4.41519222098806));
#19155=CARTESIAN_POINT('Ctrl Pts',(16.4849167868736,-0.0726599781719204,
4.41511070701236));
#19156=CARTESIAN_POINT('Ctrl Pts',(16.5091381963562,-0.284551613766983,
4.36224737480062));
#19157=CARTESIAN_POINT('Ctrl Pts',(16.5492648845264,-0.4912502013546,4.02405128938415));
#19158=CARTESIAN_POINT('Ctrl Pts',(16.5969807205893,-0.285919008936969,
3.59980561575594));
#19159=CARTESIAN_POINT('Ctrl Pts',(16.6446965566521,0.181976008816936,3.54306460296116));
#19160=CARTESIAN_POINT('Ctrl Pts',(16.6924123927149,0.482759657613431,3.90593439612197));
#19161=CARTESIAN_POINT('Ctrl Pts',(16.7363804258571,0.351413532087107,4.31989995948535));
#19162=CARTESIAN_POINT('Ctrl Pts',(16.7644431803116,0.105484194296011,4.41488604428797));
#19163=CARTESIAN_POINT('Ctrl Pts',(16.7766006560786,-0.000383680820852189,
4.41586226484779));
#19164=CARTESIAN_POINT('Ctrl Pts',(16.5733993439214,-1.52272386678906E-5,
4.41518677123726));
#19165=CARTESIAN_POINT('Ctrl Pts',(16.5812466665579,-0.0686308195205231,
4.41520910309265));
#19166=CARTESIAN_POINT('Ctrl Pts',(16.6049992678821,-0.276289552895371,
4.36659242126669));
#19167=CARTESIAN_POINT('Ctrl Pts',(16.6446571478939,-0.490328743065594,
4.03850907134293));
#19168=CARTESIAN_POINT('Ctrl Pts',(16.6923729839567,-0.297581432841348,
3.60840005658827));
#19169=CARTESIAN_POINT('Ctrl Pts',(16.7400888200196,0.168439486040012,3.53790329540825));
#19170=CARTESIAN_POINT('Ctrl Pts',(16.7878046560824,0.479779833116189,3.89175704832657));
#19171=CARTESIAN_POINT('Ctrl Pts',(16.832241497383,0.359412856911567,4.31386464726761));
#19172=CARTESIAN_POINT('Ctrl Pts',(16.860773059996,0.109491163683573,4.41496773315674));
#19173=CARTESIAN_POINT('Ctrl Pts',(16.8733993439214,-0.000374684679869387,
4.41598699190495));
#19174=CARTESIAN_POINT('Origin',(3.42660065607856,0.,4.));
#19175=CARTESIAN_POINT('',(16.1766006560786,0.000364146841390381,4.41605523138122));
#19176=CARTESIAN_POINT('',(16.2733993439214,0.000380345806842055,4.41593091837313));
#19177=CARTESIAN_POINT('',(3.42660065607856,4.87367679877478E-13,4.415875));
#19178=CARTESIAN_POINT('Ctrl Pts',(16.1766006560786,0.000364146841390366,
4.41605523138122));
#19179=CARTESIAN_POINT('Ctrl Pts',(16.1894851147479,-0.111700864104492,
4.41502624848758));
#19180=CARTESIAN_POINT('Ctrl Pts',(16.2182748521048,-0.363797281821349,
4.31045679267864));
#19181=CARTESIAN_POINT('Ctrl Pts',(16.2629698681494,-0.477960913216358,
3.88398883549692));
#19182=CARTESIAN_POINT('Ctrl Pts',(16.3106857042122,-0.160921706883503,
3.53523185446324));
#19183=CARTESIAN_POINT('Ctrl Pts',(16.358401540275,0.303894378979202,3.6132786128531));
#19184=CARTESIAN_POINT('Ctrl Pts',(16.4061173763379,0.489639580609251,4.04645757153336));
#19185=CARTESIAN_POINT('Ctrl Pts',(16.4455170816057,0.271734615807756,4.36891289568356));
#19186=CARTESIAN_POINT('Ctrl Pts',(16.4690115081859,0.0664083969439258,
4.41526660914191));
#19187=CARTESIAN_POINT('Ctrl Pts',(16.4766006560786,5.2409936866539E-5,
4.41519222098806));
#19188=CARTESIAN_POINT('Ctrl Pts',(16.2733993439214,0.000380345806842052,
4.41593091837313));
#19189=CARTESIAN_POINT('Ctrl Pts',(16.2858149944323,-0.107690075887363,
4.41492720978183));
#19190=CARTESIAN_POINT('Ctrl Pts',(16.3141359236307,-0.35582464097624,4.31660057631701));
#19191=CARTESIAN_POINT('Ctrl Pts',(16.3583621315169,-0.481170314810987,
3.89811598262401));
#19192=CARTESIAN_POINT('Ctrl Pts',(16.4060779675797,-0.174540169679895,
3.54017290856226));
#19193=CARTESIAN_POINT('Ctrl Pts',(16.4537938036425,0.292372898913969,3.60449612791703));
#19194=CARTESIAN_POINT('Ctrl Pts',(16.5015096397054,0.490795435699827,4.0320166386149));
#19195=CARTESIAN_POINT('Ctrl Pts',(16.5413781531317,0.280003220364278,4.36466130212541));
#19196=CARTESIAN_POINT('Ctrl Pts',(16.5653413878703,0.0704421061260754,
4.4151638399628));
#19197=CARTESIAN_POINT('Ctrl Pts',(16.5733993439214,-1.52272386678906E-5,
4.41518677123726));
#19198=CARTESIAN_POINT('Origin',(3.42660065607856,0.,4.));
#19199=CARTESIAN_POINT('',(15.8766006560786,-0.00023258108979477,4.41639972388928));
#19200=CARTESIAN_POINT('',(15.9733993439214,-0.000169011902647176,4.4164782780785));
#19201=CARTESIAN_POINT('',(3.42660065607856,4.87367679877478E-13,4.415875));
#19202=CARTESIAN_POINT('Ctrl Pts',(15.8766006560786,-0.000232581089794846,
4.41639972388928));
#19203=CARTESIAN_POINT('Ctrl Pts',(15.8781481639346,-0.0136633580705269,
4.41648966084242));
#19204=CARTESIAN_POINT('Ctrl Pts',(15.8956009504782,-0.165044849757219,
4.40979870506104));
#19205=CARTESIAN_POINT('Ctrl Pts',(15.9289590157095,-0.437567097060412,
4.22458909239344));
#19206=CARTESIAN_POINT('Ctrl Pts',(15.9766748517724,-0.425562075928853,
3.75341909160864));
#19207=CARTESIAN_POINT('Ctrl Pts',(16.0243906878352,-0.0227568523576073,
3.50868813313462));
#19208=CARTESIAN_POINT('Ctrl Pts',(16.072106523898,0.400946338892803,3.71513642180785));
#19209=CARTESIAN_POINT('Ctrl Pts',(16.1198223599609,0.456454337785543,4.1831793175245));
#19210=CARTESIAN_POINT('Ctrl Pts',(16.1546537373544,0.190990792023167,4.40204523666471));
#19211=CARTESIAN_POINT('Ctrl Pts',(16.1735798360603,0.0266382990664043,
4.41629648110721));
#19212=CARTESIAN_POINT('Ctrl Pts',(16.1766006560786,0.000364146841390366,
4.41605523138122));
#19213=CARTESIAN_POINT('Ctrl Pts',(15.9733993439214,-0.000169011902647174,
4.4164782780785));
#19214=CARTESIAN_POINT('Ctrl Pts',(15.974478043619,-0.00952634975615679,
4.4165263696097));
#19215=CARTESIAN_POINT('Ctrl Pts',(15.9914620220042,-0.156808910032117,
4.4119928338179));
#19216=CARTESIAN_POINT('Ctrl Pts',(16.024351279077,-0.430762722000766,4.23737881579128));
#19217=CARTESIAN_POINT('Ctrl Pts',(16.0720671151398,-0.432639725453012,
3.76605963834362));
#19218=CARTESIAN_POINT('Ctrl Pts',(16.1197829512026,-0.0372170120039125,
3.50957149464017));
#19219=CARTESIAN_POINT('Ctrl Pts',(16.1674987872655,0.392382656225717,3.70345139362117));
#19220=CARTESIAN_POINT('Ctrl Pts',(16.2152146233283,0.461651293660056,4.16965644082667));
#19221=CARTESIAN_POINT('Ctrl Pts',(16.2505148088803,0.199264245432362,4.39929555075695));
#19222=CARTESIAN_POINT('Ctrl Pts',(16.2699097157447,0.0307553622657438,
4.41621302761729));
#19223=CARTESIAN_POINT('Ctrl Pts',(16.2733993439214,0.000380345806842052,
4.41593091837313));
#19224=CARTESIAN_POINT('Origin',(3.42660065607856,0.,4.));
#19225=CARTESIAN_POINT('',(15.5766006560786,-0.000245472137683418,4.41533389801214));
#19226=CARTESIAN_POINT('',(15.6733993439214,-0.00029394562308721,4.41541483535501));
#19227=CARTESIAN_POINT('',(3.42660065607856,4.87367679877478E-13,4.415875));
#19228=CARTESIAN_POINT('Ctrl Pts',(15.5766006560786,-0.000245472137683396,
4.41533389801214));
#19229=CARTESIAN_POINT('Ctrl Pts',(15.5827164918089,-0.0536739331835165,
4.41562024719655));
#19230=CARTESIAN_POINT('Ctrl Pts',(15.6047376062269,-0.245697356182912,
4.38119912149661));
#19231=CARTESIAN_POINT('Ctrl Pts',(15.6426639993325,-0.483248643997369,
4.09152034160055));
#19232=CARTESIAN_POINT('Ctrl Pts',(15.6903798353953,-0.338341267922855,
3.64302603558196));
#19233=CARTESIAN_POINT('Ctrl Pts',(15.7380956714582,0.117270100534806,3.52234641383892));
#19234=CARTESIAN_POINT('Ctrl Pts',(15.785811507521,0.465190531238913,3.84030342991275));
#19235=CARTESIAN_POINT('Ctrl Pts',(15.8319798357278,0.388490242362186,4.28984418805176));
#19236=CARTESIAN_POINT('Ctrl Pts',(15.862242885247,0.124378106492246,4.41556528924811));
#19237=CARTESIAN_POINT('Ctrl Pts',(15.8766006560786,-0.000232581089794846,
4.41639972388928));
#19238=CARTESIAN_POINT('Ctrl Pts',(15.6733993439214,-0.000293945623087231,
4.41541483535501));
#19239=CARTESIAN_POINT('Ctrl Pts',(15.6790463714933,-0.0496027558454661,
4.41573527017753));
#19240=CARTESIAN_POINT('Ctrl Pts',(15.7005986777528,-0.23740431922453,4.38477730872224));
#19241=CARTESIAN_POINT('Ctrl Pts',(15.7380562626999,-0.480343569999647,
4.1057131950703));
#19242=CARTESIAN_POINT('Ctrl Pts',(15.7857720987628,-0.348708030819167,
3.6531456586776));
#19243=CARTESIAN_POINT('Ctrl Pts',(15.8334879348256,0.103151458625294,3.5190998009613));
#19244=CARTESIAN_POINT('Ctrl Pts',(15.8812037708885,0.460285376424935,3.82667199562295));
#19245=CARTESIAN_POINT('Ctrl Pts',(15.9278409072537,0.396214095655672,4.28286244744368));
#19246=CARTESIAN_POINT('Ctrl Pts',(15.9585727649314,0.128446309981357,4.41581726659612));
#19247=CARTESIAN_POINT('Ctrl Pts',(15.9733993439214,-0.000169011902647174,
4.4164782780785));
#19248=CARTESIAN_POINT('Origin',(3.42660065607856,0.,4.));
#19249=CARTESIAN_POINT('',(15.2766006560786,0.000330084823988869,4.41550084660604));
#19250=CARTESIAN_POINT('',(15.3733993439214,0.000289868078815952,4.41540680128743));
#19251=CARTESIAN_POINT('',(3.42660065607856,4.87367679877478E-13,4.415875));
#19252=CARTESIAN_POINT('Ctrl Pts',(15.2766006560786,0.000330084823988861,
4.41550084660604));
#19253=CARTESIAN_POINT('Ctrl Pts',(15.2872848196833,-0.0929135079625664,
4.41481081573461));
#19254=CARTESIAN_POINT('Ctrl Pts',(15.3138742619755,-0.32600240339937,4.33760928826424));
#19255=CARTESIAN_POINT('Ctrl Pts',(15.3563689829555,-0.489387968817152,
3.95096286275689));
#19256=CARTESIAN_POINT('Ctrl Pts',(15.4040848190183,-0.223435404337718,
3.56184267101825));
#19257=CARTESIAN_POINT('Ctrl Pts',(15.4518006550811,0.24770132994065,3.57508909640066));
#19258=CARTESIAN_POINT('Ctrl Pts',(15.499516491144,0.491370121559653,3.97853774265298));
#19259=CARTESIAN_POINT('Ctrl Pts',(15.5411164914764,0.310410063586636,4.3474585185963));
#19260=CARTESIAN_POINT('Ctrl Pts',(15.5668112131213,0.0852759340546689,
4.41487554708019));
#19261=CARTESIAN_POINT('Ctrl Pts',(15.5766006560786,-0.000245472137683396,
4.41533389801214));
#19262=CARTESIAN_POINT('Ctrl Pts',(15.3733993439214,0.000289868078815973,
4.41540680128743));
#19263=CARTESIAN_POINT('Ctrl Pts',(15.3836146993676,-0.0889130762729256,
4.41483587894927));
#19264=CARTESIAN_POINT('Ctrl Pts',(15.4097353335015,-0.317845114095608,
4.34285359523591));
#19265=CARTESIAN_POINT('Ctrl Pts',(15.4517612463229,-0.490619905976795,
3.96539750426199));
#19266=CARTESIAN_POINT('Ctrl Pts',(15.4994770823858,-0.236243011612202,
3.56861332390027));
#19267=CARTESIAN_POINT('Ctrl Pts',(15.5471929184486,0.235079475381852,3.56797816593814));
#19268=CARTESIAN_POINT('Ctrl Pts',(15.5949087545115,0.490524862970081,3.9640753057054));
#19269=CARTESIAN_POINT('Ctrl Pts',(15.6369775630024,0.318592711010818,4.34238143198936));
#19270=CARTESIAN_POINT('Ctrl Pts',(15.6631410928057,0.0892792238074376,
4.41483274135358));
#19271=CARTESIAN_POINT('Ctrl Pts',(15.6733993439214,-0.000293945623087231,
4.41541483535501));
#19272=CARTESIAN_POINT('Origin',(3.42660065607856,0.,4.));
#19273=CARTESIAN_POINT('',(14.9766006560786,0.000104941934236194,4.41652945172571));
#19274=CARTESIAN_POINT('',(15.0733993439214,0.000175165248676303,4.41647198785975));
#19275=CARTESIAN_POINT('',(3.42660065607856,4.87367679877478E-13,4.415875));
#19276=CARTESIAN_POINT('Ctrl Pts',(14.9766006560786,0.000104941934236227,
4.41652945172572));
#19277=CARTESIAN_POINT('Ctrl Pts',(14.9918531475576,-0.132161740438444,
4.41608294134065));
#19278=CARTESIAN_POINT('Ctrl Pts',(15.0230109177242,-0.40316752945992,4.27633971254324));
#19279=CARTESIAN_POINT('Ctrl Pts',(15.0700739665785,-0.455482716161518,
3.8144178884426));
#19280=CARTESIAN_POINT('Ctrl Pts',(15.1177898026413,-0.0902467530057116,
3.51651189422706));
#19281=CARTESIAN_POINT('Ctrl Pts',(15.1655056387041,0.357864192060027,3.66260046696357));
#19282=CARTESIAN_POINT('Ctrl Pts',(15.2132214747669,0.47734294310866,4.11852822244656));
#19283=CARTESIAN_POINT('Ctrl Pts',(15.2502531472251,0.229869832763757,4.3878938710325));
#19284=CARTESIAN_POINT('Ctrl Pts',(15.2713795409956,0.0458961718568525,
4.41583804947224));
#19285=CARTESIAN_POINT('Ctrl Pts',(15.2766006560786,0.000330084823988861,
4.41550084660604));
#19286=CARTESIAN_POINT('Ctrl Pts',(15.0733993439214,0.000175165248676341,
4.41647198785975));
#19287=CARTESIAN_POINT('Ctrl Pts',(15.0881830272419,-0.128073190246274,
4.41579247653651));
#19288=CARTESIAN_POINT('Ctrl Pts',(15.1188719892501,-0.395510344386944,
4.28350986851547));
#19289=CARTESIAN_POINT('Ctrl Pts',(15.1654662299459,-0.46075086019608,3.82791319143947));
#19290=CARTESIAN_POINT('Ctrl Pts',(15.2131820660087,-0.104447211543591,
3.51937956259357));
#19291=CARTESIAN_POINT('Ctrl Pts',(15.2608979020716,0.347771918596306,3.652207076714));
#19292=CARTESIAN_POINT('Ctrl Pts',(15.3086137381344,0.480626744730421,4.10441818376995));
#19293=CARTESIAN_POINT('Ctrl Pts',(15.346114218751,0.238163166260598,4.38445638366753));
#19294=CARTESIAN_POINT('Ctrl Pts',(15.36770942068,0.0499756483669043,4.41572480336754));
#19295=CARTESIAN_POINT('Ctrl Pts',(15.3733993439214,0.000289868078815973,
4.41540680128743));
#19296=CARTESIAN_POINT('Origin',(3.42660065607856,0.,4.));
#19297=CARTESIAN_POINT('',(14.6766006560786,-0.000383732061438463,4.41581798673635));
#19298=CARTESIAN_POINT('',(14.7733993439214,-0.000379407362125217,4.41594234696178));
#19299=CARTESIAN_POINT('',(3.42660065607856,4.87367679877478E-13,4.415875));
#19300=CARTESIAN_POINT('Ctrl Pts',(14.6766006560786,-0.000383732061438387,
4.41581798673635));
#19301=CARTESIAN_POINT('Ctrl Pts',(14.6805161967443,-0.0344897130604965,
4.41612948839573));
#19302=CARTESIAN_POINT('Ctrl Pts',(14.7003370160976,-0.206786574235377,
4.39667515056147));
#19303=CARTESIAN_POINT('Ctrl Pts',(14.7360631141386,-0.466025611307368,
4.15724297904063));
#19304=CARTESIAN_POINT('Ctrl Pts',(14.7837789502014,-0.38430721152129,3.69305832471834));
#19305=CARTESIAN_POINT('Ctrl Pts',(14.8314947862642,0.0503264139313189,
3.51074293371195));
#19306=CARTESIAN_POINT('Ctrl Pts',(14.8792106223271,0.438744519099385,3.77771983486548));
#19307=CARTESIAN_POINT('Ctrl Pts',(14.9269264583899,0.42425678142631,4.24882003188202));
#19308=CARTESIAN_POINT('Ctrl Pts',(14.9593898029737,0.149335702075518,4.41387566524124));
#19309=CARTESIAN_POINT('Ctrl Pts',(14.97594786887,0.00576578747519492,4.41654856180149));
#19310=CARTESIAN_POINT('Ctrl Pts',(14.9766006560786,0.000104941934236227,
4.41652945172572));
#19311=CARTESIAN_POINT('Ctrl Pts',(14.7733993439214,-0.000379407362125234,
4.41594234696178));
#19312=CARTESIAN_POINT('Ctrl Pts',(14.7768460764287,-0.0303789312965351,
4.41622104989506));
#19313=CARTESIAN_POINT('Ctrl Pts',(14.7961980876235,-0.198506931257387,
4.39955296987463));
#19314=CARTESIAN_POINT('Ctrl Pts',(14.831455377506,-0.461192356972643,4.17090007232882));
#19315=CARTESIAN_POINT('Ctrl Pts',(14.8791712135689,-0.393180492164677,
3.7045100248179));
#19316=CARTESIAN_POINT('Ctrl Pts',(14.9268870496317,0.0358950684576197,
3.50947296821438));
#19317=CARTESIAN_POINT('Ctrl Pts',(14.9746028856945,0.432007635398663,3.76489443262817));
#19318=CARTESIAN_POINT('Ctrl Pts',(15.0223187217574,0.431400943461215,4.23621695712364));
#19319=CARTESIAN_POINT('Ctrl Pts',(15.0552508744997,0.157562060208247,4.41179740605063));
#19320=CARTESIAN_POINT('Ctrl Pts',(15.0722777485543,0.00990499767517082,
4.41652354042182));
#19321=CARTESIAN_POINT('Ctrl Pts',(15.0733993439214,0.000175165248676341,
4.41647198785975));
#19322=CARTESIAN_POINT('Origin',(3.42660065607856,0.,4.));
#19323=CARTESIAN_POINT('',(14.3766006560786,7.63317591858645E-5,4.41519896243726));
#19324=CARTESIAN_POINT('',(14.4733993439214,9.02664646690309E-6,4.41518644689786));
#19325=CARTESIAN_POINT('',(3.42660065607856,4.87367679877478E-13,4.415875));
#19326=CARTESIAN_POINT('Ctrl Pts',(14.3766006560786,7.63317591858798E-5,
4.41519896243726));
#19327=CARTESIAN_POINT('Ctrl Pts',(14.3850845246186,-0.0740996743586071,
4.41507773880187));
#19328=CARTESIAN_POINT('Ctrl Pts',(14.4094736718463,-0.287504468978829,
4.360651101065));
#19329=CARTESIAN_POINT('Ctrl Pts',(14.4497680977616,-0.491476396904638,
4.01887262932433));
#19330=CARTESIAN_POINT('Ctrl Pts',(14.4974839338244,-0.281685449746218,
3.59681451879656));
#19331=CARTESIAN_POINT('Ctrl Pts',(14.5451997698872,0.186781580201919,3.54500783946397));
#19332=CARTESIAN_POINT('Ctrl Pts',(14.59291560595,0.483724211046603,3.91102746210588));
#19333=CARTESIAN_POINT('Ctrl Pts',(14.6367159013472,0.348540265561382,4.32201186060262));
#19334=CARTESIAN_POINT('Ctrl Pts',(14.6646109180567,0.104051852208848,4.41486414061182));
#19335=CARTESIAN_POINT('Ctrl Pts',(14.6766006560786,-0.000383732061438387,
4.41581798673635));
#19336=CARTESIAN_POINT('Ctrl Pts',(14.4733993439214,9.0266464668684E-6,
4.41518644689786));
#19337=CARTESIAN_POINT('Ctrl Pts',(14.481414404303,-0.0700733710850898,
4.41517292627706));
#19338=CARTESIAN_POINT('Ctrl Pts',(14.5053347433722,-0.279247125311621,
4.3650573561381));
#19339=CARTESIAN_POINT('Ctrl Pts',(14.545160361129,-0.490707361486496,4.03333931965322));
#19340=CARTESIAN_POINT('Ctrl Pts',(14.5928761971918,-0.293437803431633,
3.60528557111603));
#19341=CARTESIAN_POINT('Ctrl Pts',(14.6405920332547,0.173300204635467,3.53970415608515));
#19342=CARTESIAN_POINT('Ctrl Pts',(14.6883078693175,0.480893968219416,3.89681949708321));
#19343=CARTESIAN_POINT('Ctrl Pts',(14.7325769728731,0.356556173733762,4.31604662460621));
#19344=CARTESIAN_POINT('Ctrl Pts',(14.760940797741,0.10805675748006,4.41493494840171));
#19345=CARTESIAN_POINT('Ctrl Pts',(14.7733993439214,-0.000379407362125234,
4.41594234696178));
#19346=CARTESIAN_POINT('Origin',(3.42660065607856,0.,4.));
#19347=CARTESIAN_POINT('',(14.0766006560786,0.000355193352615291,4.41609897421413));
#19348=CARTESIAN_POINT('',(14.1733993439214,0.000376051973931104,4.41597558743442));
#19349=CARTESIAN_POINT('',(3.42660065607856,4.87367679877478E-13,4.415875));
#19350=CARTESIAN_POINT('Ctrl Pts',(14.0766006560786,0.000355193352615277,
4.41609897421413));
#19351=CARTESIAN_POINT('Ctrl Pts',(14.0896528524929,-0.113137957382804,
4.41506966208575));
#19352=CARTESIAN_POINT('Ctrl Pts',(14.1186103275949,-0.366637448157006,
4.30821039815648));
#19353=CARTESIAN_POINT('Ctrl Pts',(14.1634730813845,-0.476711717661702,
3.87895801102093));
#19354=CARTESIAN_POINT('Ctrl Pts',(14.2111889174473,-0.156014541823709,
3.53356170012368));
#19355=CARTESIAN_POINT('Ctrl Pts',(14.2589047535102,0.307953188363286,3.61650285707861));
#19356=CARTESIAN_POINT('Ctrl Pts',(14.306620589573,0.4891227672074,4.05161534124029));
#19357=CARTESIAN_POINT('Ctrl Pts',(14.3458525570958,0.268773633406098,4.37039329245586));
#19358=CARTESIAN_POINT('Ctrl Pts',(14.369179245931,0.0649630708582953,4.4153050049005));
#19359=CARTESIAN_POINT('Ctrl Pts',(14.3766006560786,7.63317591858798E-5,
4.41519896243726));
#19360=CARTESIAN_POINT('Ctrl Pts',(14.1733993439214,0.000376051973931098,
4.41597558743442));
#19361=CARTESIAN_POINT('Ctrl Pts',(14.1859827321773,-0.109124255432428,
4.41495896305428));
#19362=CARTESIAN_POINT('Ctrl Pts',(14.2144713991208,-0.358682910161539,
4.31442504752535));
#19363=CARTESIAN_POINT('Ctrl Pts',(14.258865344752,-0.480069828122688,3.8930505494253));
#19364=CARTESIAN_POINT('Ctrl Pts',(14.3065811808148,-0.169684322438749,
3.53835895376334));
#19365=CARTESIAN_POINT('Ctrl Pts',(14.3542970168777,0.296524907469595,3.60759943412104));
#19366=CARTESIAN_POINT('Ctrl Pts',(14.4020128529405,0.49043075222644,4.0371873919842));
#19367=CARTESIAN_POINT('Ctrl Pts',(14.4417136286217,0.277046036654804,4.36620192284859));
#19368=CARTESIAN_POINT('Ctrl Pts',(14.4655091256154,0.0689998253659925,
4.41519975692232));
#19369=CARTESIAN_POINT('Ctrl Pts',(14.4733993439214,9.0266464668684E-6,
4.41518644689786));
#19370=CARTESIAN_POINT('Origin',(3.42660065607856,0.,4.));
#19371=CARTESIAN_POINT('',(13.7766006560786,-0.000253139125078747,4.41636688691614));
#19372=CARTESIAN_POINT('',(13.8733993439214,-0.000192710833643805,4.4164526008213));
#19373=CARTESIAN_POINT('',(3.42660065607856,4.87367679877478E-13,4.415875));
#19374=CARTESIAN_POINT('Ctrl Pts',(13.7766006560786,-0.000253139125078718,
4.41636688691614));
#19375=CARTESIAN_POINT('Ctrl Pts',(13.7783159016796,-0.0151427949580853,
4.41647347977994));
#19376=CARTESIAN_POINT('Ctrl Pts',(13.7959364259683,-0.167994124135391,
4.40898222403799));
#19377=CARTESIAN_POINT('Ctrl Pts',(13.8294622289446,-0.439909757638992,
4.21996506537626));
#19378=CARTESIAN_POINT('Ctrl Pts',(13.8771780650075,-0.422939705734467,
3.74894775411238));
#19379=CARTESIAN_POINT('Ctrl Pts',(13.9248939010703,-0.0175776142901187,
3.50847558318244));
#19380=CARTESIAN_POINT('Ctrl Pts',(13.9726097371332,0.403926270823208,3.71937784729135));
#19381=CARTESIAN_POINT('Ctrl Pts',(14.020325573196,0.454498446235019,4.18797975215946));
#19382=CARTESIAN_POINT('Ctrl Pts',(14.0549892128445,0.188032430710383,4.40299531219535));
#19383=CARTESIAN_POINT('Ctrl Pts',(14.0737475738053,0.0251636842930195,
4.41632397176197));
#19384=CARTESIAN_POINT('Ctrl Pts',(14.0766006560786,0.000355193352615277,
4.41609897421413));
#19385=CARTESIAN_POINT('Ctrl Pts',(13.8733993439214,-0.000192710833643682,
4.4164526008213));
#19386=CARTESIAN_POINT('Ctrl Pts',(13.874645781364,-0.0110068809386406,
4.41651469495978));
#19387=CARTESIAN_POINT('Ctrl Pts',(13.8917974974943,-0.15975450351916,4.41122255187585));
#19388=CARTESIAN_POINT('Ctrl Pts',(13.9248544923121,-0.433240552373761,
4.23282579030437));
#19389=CARTESIAN_POINT('Ctrl Pts',(13.9725703283749,-0.430150181893835,
3.76151300691929));
#19390=CARTESIAN_POINT('Ctrl Pts',(14.0202861644378,-0.032046280669499,
3.50920649887429));
#19391=CARTESIAN_POINT('Ctrl Pts',(14.0680020005006,0.39548621318905,3.70760321474174));
#19392=CARTESIAN_POINT('Ctrl Pts',(14.1157178365634,0.459837632138507,4.1745123976147));
#19393=CARTESIAN_POINT('Ctrl Pts',(14.1508502843704,0.196303200904851,4.40029544879449));
#19394=CARTESIAN_POINT('Ctrl Pts',(14.1700774534897,0.0292830534939708,
4.41624396624722));
#19395=CARTESIAN_POINT('Ctrl Pts',(14.1733993439214,0.000376051973931098,
4.41597558743442));
#19396=CARTESIAN_POINT('Origin',(3.42660065607856,0.,4.));
#19397=CARTESIAN_POINT('',(13.4766006560786,-0.000226204729293368,4.4153088088013));
#19398=CARTESIAN_POINT('',(13.5733993439214,-0.000277574767750837,4.41538411867388));
#19399=CARTESIAN_POINT('',(3.42660065607856,4.87367679877478E-13,4.415875));
#19400=CARTESIAN_POINT('Ctrl Pts',(13.4766006560786,-0.000226204729293314,
4.4153088088013));
#19401=CARTESIAN_POINT('Ctrl Pts',(13.482884229554,-0.0551283395969922,
4.41557894444213));
#19402=CARTESIAN_POINT('Ctrl Pts',(13.505073081717,-0.248664136397309,4.37988069596112));
#19403=CARTESIAN_POINT('Ctrl Pts',(13.5431672125676,-0.484186345555107,
4.08642226350871));
#19404=CARTESIAN_POINT('Ctrl Pts',(13.5908830486304,-0.334560300710407,
3.63948005597396));
#19405=CARTESIAN_POINT('Ctrl Pts',(13.6385988846933,0.122297616148583,3.52360886035071));
#19406=CARTESIAN_POINT('Ctrl Pts',(13.6863147207561,0.466847750307624,3.8452149784873));
#19407=CARTESIAN_POINT('Ctrl Pts',(13.7323153112179,0.38570983934117,4.29229218593957));
#19408=CARTESIAN_POINT('Ctrl Pts',(13.762410622992,0.122927301498021,4.41548505619568));
#19409=CARTESIAN_POINT('Ctrl Pts',(13.7766006560786,-0.000253139125078718,
4.41636688691614));
#19410=CARTESIAN_POINT('Ctrl Pts',(13.5733993439214,-0.000277574767750817,
4.41538411867388));
#19411=CARTESIAN_POINT('Ctrl Pts',(13.5792141092383,-0.0510604653080308,
4.41569425641003));
#19412=CARTESIAN_POINT('Ctrl Pts',(13.6009341532429,-0.240371663949131,
4.38351498152559));
#19413=CARTESIAN_POINT('Ctrl Pts',(13.6385594759351,-0.481431012491488,
4.10064494554323));
#19414=CARTESIAN_POINT('Ctrl Pts',(13.6862753119979,-0.345033139360895,
3.64948986092447));
#19415=CARTESIAN_POINT('Ctrl Pts',(13.7339911480608,0.108213974662067,3.52021363031051));
#19416=CARTESIAN_POINT('Ctrl Pts',(13.7817069841236,0.462086530666827,3.83153260544464));
#19417=CARTESIAN_POINT('Ctrl Pts',(13.8281763827438,0.393458703070077,4.28538422885222));
#19418=CARTESIAN_POINT('Ctrl Pts',(13.8587405026764,0.126988323162951,4.4157223370415));
#19419=CARTESIAN_POINT('Ctrl Pts',(13.8733993439214,-0.000192710833643682,
4.4164526008213));
#19420=CARTESIAN_POINT('Origin',(3.42660065607856,0.,4.));
#19421=CARTESIAN_POINT('',(13.1766006560786,0.000342007958933446,4.41553758638116));
#19422=CARTESIAN_POINT('',(13.2733993439214,0.000305371599794934,4.41543889539504));
#19423=CARTESIAN_POINT('',(3.42660065607856,4.87367679877478E-13,4.415875));
#19424=CARTESIAN_POINT('Ctrl Pts',(13.1766006560786,0.000342007958933428,
4.41553758638117));
#19425=CARTESIAN_POINT('Ctrl Pts',(13.1874525574283,-0.0943443719380771,
4.41480703635833));
#19426=CARTESIAN_POINT('Ctrl Pts',(13.2142097374657,-0.328913583769224,
4.33568767983454));
#19427=CARTESIAN_POINT('Ctrl Pts',(13.2568721961906,-0.488843983144383,
3.94580788806928));
#19428=CARTESIAN_POINT('Ctrl Pts',(13.3045880322534,-0.218805220893238,
3.55951220202843));
#19429=CARTESIAN_POINT('Ctrl Pts',(13.3523038683163,0.252165742455243,3.57772323864086));
#19430=CARTESIAN_POINT('Ctrl Pts',(13.4000197043791,0.491569024438394,3.98371752277252));
#19431=CARTESIAN_POINT('Ctrl Pts',(13.4414519669665,0.307476227900318,4.34923088347422));
#19432=CARTESIAN_POINT('Ctrl Pts',(13.4669789508664,0.0838425436168888,
4.41489516431802));
#19433=CARTESIAN_POINT('Ctrl Pts',(13.4766006560786,-0.000226204729293314,
4.4153088088013));
#19434=CARTESIAN_POINT('Ctrl Pts',(13.2733993439214,0.000305371599794949,
4.41543889539504));
#19435=CARTESIAN_POINT('Ctrl Pts',(13.2837824371127,-0.0903447040275099,
4.41482455235666));
#19436=CARTESIAN_POINT('Ctrl Pts',(13.3100708089916,-0.320767143545349,
4.3409984814332));
#19437=CARTESIAN_POINT('Ctrl Pts',(13.352264459558,-0.490227979701372,3.96022874442655));
#19438=CARTESIAN_POINT('Ctrl Pts',(13.3999802956209,-0.23168347330409,3.56614749850931));
#19439=CARTESIAN_POINT('Ctrl Pts',(13.4476961316837,0.239619531536799,3.57047968038978));
#19440=CARTESIAN_POINT('Ctrl Pts',(13.4954119677466,0.490876233547033,3.96924698078795));
#19441=CARTESIAN_POINT('Ctrl Pts',(13.5373130384925,0.315668023336251,4.34421900798688));
#19442=CARTESIAN_POINT('Ctrl Pts',(13.5633088305507,0.0878472949503496,
4.41484592860038));
#19443=CARTESIAN_POINT('Ctrl Pts',(13.5733993439214,-0.000277574767750817,
4.41538411867388));
#19444=CARTESIAN_POINT('Origin',(3.42660065607856,0.,4.));
#19445=CARTESIAN_POINT('',(12.8766006560786,7.85109994957766E-5,4.41654344863055));
#19446=CARTESIAN_POINT('',(12.9733993439214,0.000150764780949702,4.41649545414489));
#19447=CARTESIAN_POINT('',(3.42660065607856,4.87367679877478E-13,4.415875));
#19448=CARTESIAN_POINT('Ctrl Pts',(12.8766006560786,7.85109994958138E-5,
4.41654344863055));
#19449=CARTESIAN_POINT('Ctrl Pts',(12.8920208853026,-0.133630732206743,
4.41619751255639));
#19450=CARTESIAN_POINT('Ctrl Pts',(12.9233463932143,-0.405888408666218,
4.27372356364211));
#19451=CARTESIAN_POINT('Ctrl Pts',(12.9705771798136,-0.453501555338242,
3.80962782724943));
#19452=CARTESIAN_POINT('Ctrl Pts',(13.0182930158764,-0.0851462219395619,
3.51558762841831));
#19453=CARTESIAN_POINT('Ctrl Pts',(13.0660088519392,0.361400197209248,3.66639076405307));
#19454=CARTESIAN_POINT('Ctrl Pts',(13.1137246880021,0.476067254403989,4.1235523942958));
#19455=CARTESIAN_POINT('Ctrl Pts',(13.1505886227152,0.226902767145371,4.38908671404106));
#19456=CARTESIAN_POINT('Ctrl Pts',(13.1715472787407,0.0444343739838573,
4.41587777975472));
#19457=CARTESIAN_POINT('Ctrl Pts',(13.1766006560786,0.000342007958933428,
4.41553758638117));
#19458=CARTESIAN_POINT('Ctrl Pts',(12.9733993439214,0.000150764780949724,
4.4164954541449));
#19459=CARTESIAN_POINT('Ctrl Pts',(12.988350764987,-0.12953330947047,4.41589144324702));
#19460=CARTESIAN_POINT('Ctrl Pts',(13.0192074647402,-0.39825874617628,4.28096832590395));
#19461=CARTESIAN_POINT('Ctrl Pts',(13.065969443181,-0.458911634846768,3.82306685936703));
#19462=CARTESIAN_POINT('Ctrl Pts',(13.1136852792439,-0.0993761143989603,
3.51830547777773));
#19463=CARTESIAN_POINT('Ctrl Pts',(13.1614011153067,0.351418020999476,3.65589158776806));
#19464=CARTESIAN_POINT('Ctrl Pts',(13.2091169513695,0.479499580452807,4.10947774749948));
#19465=CARTESIAN_POINT('Ctrl Pts',(13.2464496942411,0.235195791588524,4.38570395495548));
#19466=CARTESIAN_POINT('Ctrl Pts',(13.2678771584251,0.0485170676377186,
4.41576563003508));
#19467=CARTESIAN_POINT('Ctrl Pts',(13.2733993439214,0.000305371599794949,
4.41543889539504));
#19468=CARTESIAN_POINT('Origin',(3.42660065607856,0.,4.));
#19469=CARTESIAN_POINT('',(12.5766006560786,-0.000382134531266273,4.41577416496379));
#19470=CARTESIAN_POINT('',(12.6733993439214,-0.000382453243898073,4.41589767499446));
#19471=CARTESIAN_POINT('',(3.42660065607856,4.87367679877478E-13,4.415875));
#19472=CARTESIAN_POINT('Ctrl Pts',(12.5766006560786,-0.000382134531266193,
4.41577416496379));
#19473=CARTESIAN_POINT('Ctrl Pts',(12.5806839344893,-0.0359587315295452,
4.41609477791077));
#19474=CARTESIAN_POINT('Ctrl Pts',(12.6006724915877,-0.209750441210566,
4.39561070447123));
#19475=CARTESIAN_POINT('Ctrl Pts',(12.6365663273737,-0.4676569254097,4.15232276575852));
#19476=CARTESIAN_POINT('Ctrl Pts',(12.6842821634365,-0.381050985679211,
3.68902512775968));
#19477=CARTESIAN_POINT('Ctrl Pts',(12.7319979994994,0.0554799374235607,
3.5113004999026));
#19478=CARTESIAN_POINT('Ctrl Pts',(12.7797138355622,0.441062780321708,3.78235614259331));
#19479=CARTESIAN_POINT('Ctrl Pts',(12.8274296716251,0.421610885427219,4.2532774884218));
#19480=CARTESIAN_POINT('Ctrl Pts',(12.8597252784638,0.146394963767536,4.4145887178469));
#19481=CARTESIAN_POINT('Ctrl Pts',(12.876115606615,0.00428438860018927,
4.4165543301878));
#19482=CARTESIAN_POINT('Ctrl Pts',(12.8766006560786,7.85109994958138E-5,
4.41654344863055));
#19483=CARTESIAN_POINT('Ctrl Pts',(12.6733993439214,-0.000382453243898042,
4.41589767499447));
#19484=CARTESIAN_POINT('Ctrl Pts',(12.6770138141737,-0.0318505807336982,
4.4161892599907));
#19485=CARTESIAN_POINT('Ctrl Pts',(12.6965335631136,-0.201468625965512,
4.39853963407534));
#19486=CARTESIAN_POINT('Ctrl Pts',(12.7319585907412,-0.462967872677167,
4.16603003860975));
#19487=CARTESIAN_POINT('Ctrl Pts',(12.779674426804,-0.390044463885,3.70038267566003));
#19488=CARTESIAN_POINT('Ctrl Pts',(12.8273902628668,0.0410627776982723,
3.50987851185683));
#19489=CARTESIAN_POINT('Ctrl Pts',(12.8751060989297,0.434461438689172,3.76946045210395));
#19490=CARTESIAN_POINT('Ctrl Pts',(12.9228219349925,0.42888747548329,4.24075040649094));
#19491=CARTESIAN_POINT('Ctrl Pts',(12.9555863499897,0.154617472482897,4.41255553662561));
#19492=CARTESIAN_POINT('Ctrl Pts',(12.9724454862994,0.00842423538524961,
4.41653398830136));
#19493=CARTESIAN_POINT('Ctrl Pts',(12.9733993439214,0.000150764780949724,
4.4164954541449));
#19494=CARTESIAN_POINT('Origin',(3.42660065607856,0.,4.));
#19495=CARTESIAN_POINT('',(12.2766006560786,9.99581421417901E-5,4.41520820259509));
#19496=CARTESIAN_POINT('',(12.3733993439214,3.32456539758885E-5,4.41518865831861));
#19497=CARTESIAN_POINT('',(3.42660065607856,4.87367679877478E-13,4.415875));
#19498=CARTESIAN_POINT('Ctrl Pts',(12.2766006560786,9.99581421418094E-5,
4.41520820259509));
#19499=CARTESIAN_POINT('Ctrl Pts',(12.2852522623637,-0.0755384113923865,
4.41504611816934));
#19500=CARTESIAN_POINT('Ctrl Pts',(12.3098091473364,-0.290455378639464,
4.35903266527152));
#19501=CARTESIAN_POINT('Ctrl Pts',(12.3502713109967,-0.49164800158875,4.0136918729824));
#19502=CARTESIAN_POINT('Ctrl Pts',(12.3979871470595,-0.277420602272412,
3.59386820576715));
#19503=CARTESIAN_POINT('Ctrl Pts',(12.4457029831224,0.191566404775332,3.54700161433684));
#19504=CARTESIAN_POINT('Ctrl Pts',(12.4934188191852,0.484635034689867,3.91613041073711));
#19505=CARTESIAN_POINT('Ctrl Pts',(12.5370513768373,0.345661459897227,4.32409890635003));
#19506=CARTESIAN_POINT('Ctrl Pts',(12.5647786558017,0.102620036091023,4.41484591908716));
#19507=CARTESIAN_POINT('Ctrl Pts',(12.5766006560786,-0.000382134531266193,
4.41577416496379));
#19508=CARTESIAN_POINT('Ctrl Pts',(12.3733993439214,3.32456539758746E-5,
4.41518865831861));
#19509=CARTESIAN_POINT('Ctrl Pts',(12.381582142048,-0.071514873974996,4.41513780400291));
#19510=CARTESIAN_POINT('Ctrl Pts',(12.4056702188623,-0.282203129244181,
4.36350051499509));
#19511=CARTESIAN_POINT('Ctrl Pts',(12.4456635743641,-0.491031474462283,
4.0281658647901));
#19512=CARTESIAN_POINT('Ctrl Pts',(12.493379410427,-0.289261580343189,3.60221492864948));
#19513=CARTESIAN_POINT('Ctrl Pts',(12.5410952464898,0.178141673866572,3.54155614424011));
#19514=CARTESIAN_POINT('Ctrl Pts',(12.5888110825527,0.481954687902679,3.90189340664049));
#19515=CARTESIAN_POINT('Ctrl Pts',(12.6329124483632,0.353693368040787,4.31820342736526));
#19516=CARTESIAN_POINT('Ctrl Pts',(12.6611085354861,0.106623193447456,4.41490615616012));
#19517=CARTESIAN_POINT('Ctrl Pts',(12.6733993439214,-0.000382453243898042,
4.41589767499447));
#19518=CARTESIAN_POINT('Origin',(3.42660065607856,0.,4.));
#19519=CARTESIAN_POINT('',(11.9766006560786,0.000344603143201134,4.41614202049347));
#19520=CARTESIAN_POINT('',(12.0733993439214,0.00037008249145147,4.41602009379307));
#19521=CARTESIAN_POINT('',(3.42660065607856,4.87367679877478E-13,4.415875));
#19522=CARTESIAN_POINT('Ctrl Pts',(11.9766006560786,0.000344603143201134,
4.41614202049347));
#19523=CARTESIAN_POINT('Ctrl Pts',(11.989820590238,-0.114576335025177,4.41511745277426));
#19524=CARTESIAN_POINT('Ctrl Pts',(12.018945803085,-0.369470719226983,4.30593844396252));
#19525=CARTESIAN_POINT('Ctrl Pts',(12.0639762946196,-0.475409571231627,
3.87394063131468));
#19526=CARTESIAN_POINT('Ctrl Pts',(12.1116921306825,-0.151090047408964,
3.53194335553704));
#19527=CARTESIAN_POINT('Ctrl Pts',(12.1594079667453,0.311977791768556,3.61976969834691));
#19528=CARTESIAN_POINT('Ctrl Pts',(12.2071238028081,0.488551624369653,4.05676737776005));
#19529=CARTESIAN_POINT('Ctrl Pts',(12.2461880325859,0.265811525316043,4.37185240566124));
#19530=CARTESIAN_POINT('Ctrl Pts',(12.269346983676,0.0635166157645696,4.41534409728183));
#19531=CARTESIAN_POINT('Ctrl Pts',(12.2766006560786,9.99581421418094E-5,
4.41520820259509));
#19532=CARTESIAN_POINT('Ctrl Pts',(12.0733993439214,0.000370082491451453,
4.41602009379308));
#19533=CARTESIAN_POINT('Ctrl Pts',(12.0861504699224,-0.110559366248508,
4.41499479059613));
#19534=CARTESIAN_POINT('Ctrl Pts',(12.1148068746109,-0.361534897467509,
4.3122242613332));
#19535=CARTESIAN_POINT('Ctrl Pts',(12.1593685579871,-0.478916017555994,
3.88799699566402));
#19536=CARTESIAN_POINT('Ctrl Pts',(12.2070843940499,-0.164809627468288,
3.53659627586117));
#19537=CARTESIAN_POINT('Ctrl Pts',(12.2548002301128,0.300643979445627,3.61074632631782));
#19538=CARTESIAN_POINT('Ctrl Pts',(12.3025160661756,0.490011594032383,4.04235401475446));
#19539=CARTESIAN_POINT('Ctrl Pts',(12.3420491041118,0.274087380788525,4.36772087084377));
#19540=CARTESIAN_POINT('Ctrl Pts',(12.3656768633604,0.0675564760281007,
4.41523665186048));
#19541=CARTESIAN_POINT('Ctrl Pts',(12.3733993439214,3.32456539758746E-5,
4.41518865831861));
#19542=CARTESIAN_POINT('Origin',(3.42660065607856,0.,4.));
#19543=CARTESIAN_POINT('',(11.6766006560786,-0.000272404999166542,4.41633191892761));
#19544=CARTESIAN_POINT('',(11.7733993439214,-0.000215373091504267,4.41642415578018));
#19545=CARTESIAN_POINT('',(3.42660065607856,4.87367679877478E-13,4.415875));
#19546=CARTESIAN_POINT('Ctrl Pts',(11.6766006560786,-0.000272404999166455,
4.41633191892761));
#19547=CARTESIAN_POINT('Ctrl Pts',(11.6784836394247,-0.0166217551361539,
4.41645573239506));
#19548=CARTESIAN_POINT('Ctrl Pts',(11.6962719014584,-0.170944672110958,
4.40814899119985));
#19549=CARTESIAN_POINT('Ctrl Pts',(11.7299654421798,-0.44220355512924,4.21531660568344));
#19550=CARTESIAN_POINT('Ctrl Pts',(11.7776812782426,-0.420270357404582,
3.74450430230823));
#19551=CARTESIAN_POINT('Ctrl Pts',(11.8253971143054,-0.0123964237846327,
3.50831762943));
#19552=CARTESIAN_POINT('Ctrl Pts',(11.8731129503683,0.406861336540243,3.72365044295193));
#19553=CARTESIAN_POINT('Ctrl Pts',(11.9208287864311,0.452492071153857,4.1927593068956));
#19554=CARTESIAN_POINT('Ctrl Pts',(11.9553246883346,0.185075114683736,4.40392780377));
#19555=CARTESIAN_POINT('Ctrl Pts',(11.9739153115504,0.0236883133891,4.41635013933017));
#19556=CARTESIAN_POINT('Ctrl Pts',(11.9766006560786,0.000344603143201134,
4.41614202049347));
#19557=CARTESIAN_POINT('Ctrl Pts',(11.7733993439214,-0.000215373091504231,
4.41642415578018));
#19558=CARTESIAN_POINT('Ctrl Pts',(11.7748135191091,-0.0124870613922979,
4.41650138834433));
#19559=CARTESIAN_POINT('Ctrl Pts',(11.7921329729843,-0.162701432614141,
4.41043584391465));
#19560=CARTESIAN_POINT('Ctrl Pts',(11.8253577055472,-0.435670260442099,
4.22824690363353));
#19561=CARTESIAN_POINT('Ctrl Pts',(11.8730735416101,-0.427612859293677,
3.75699286549843));
#19562=CARTESIAN_POINT('Ctrl Pts',(11.9207893776729,-0.0268719897862959,
3.50889601812151));
#19563=CARTESIAN_POINT('Ctrl Pts',(11.9685052137357,0.398545841420554,3.71178751390968));
#19564=CARTESIAN_POINT('Ctrl Pts',(12.0162210497986,0.457972894034889,4.17934897039372));
#19565=CARTESIAN_POINT('Ctrl Pts',(12.0511857598605,0.193343073938706,4.40127740506484));
#19566=CARTESIAN_POINT('Ctrl Pts',(12.0702451912347,0.0278098881012828,
4.41627371553856));
#19567=CARTESIAN_POINT('Ctrl Pts',(12.0733993439214,0.000370082491451453,
4.41602009379308));
#19568=CARTESIAN_POINT('Origin',(3.42660065607856,0.,4.));
#19569=CARTESIAN_POINT('',(11.3766006560786,-0.000206048103233091,4.41528588740701));
#19570=CARTESIAN_POINT('',(11.4733993439214,-0.000260100423148973,4.41535533657191));
#19571=CARTESIAN_POINT('',(3.42660065607856,4.87367679877478E-13,4.415875));
#19572=CARTESIAN_POINT('Ctrl Pts',(11.3766006560786,-0.000206048103232999,
4.41528588740701));
#19573=CARTESIAN_POINT('Ctrl Pts',(11.383051967299,-0.0565815589273492,
4.41553770218085));
#19574=CARTESIAN_POINT('Ctrl Pts',(11.4054085572071,-0.251630532720247,
4.37854193442951));
#19575=CARTESIAN_POINT('Ctrl Pts',(11.4436704258028,-0.485070265991237,
4.08131458604192));
#19576=CARTESIAN_POINT('Ctrl Pts',(11.4913862618656,-0.330742172127369,
3.63597412121053));
#19577=CARTESIAN_POINT('Ctrl Pts',(11.5391020979284,0.127311547523522,3.52492422212962));
#19578=CARTESIAN_POINT('Ctrl Pts',(11.5868179339912,0.468453114143607,3.85014371984754));
#19579=CARTESIAN_POINT('Ctrl Pts',(11.632650786708,0.382920955827079,4.29471395365306));
#19580=CARTESIAN_POINT('Ctrl Pts',(11.6625783607371,0.121478760105588,4.41540989855421));
#19581=CARTESIAN_POINT('Ctrl Pts',(11.6766006560786,-0.000272404999166455,
4.41633191892761));
#19582=CARTESIAN_POINT('Ctrl Pts',(11.4733993439214,-0.000260100423148869,
4.41535533657191));
#19583=CARTESIAN_POINT('Ctrl Pts',(11.4793818469834,-0.0525169974224216,
4.41565306322741));
#19584=CARTESIAN_POINT('Ctrl Pts',(11.501269628733,-0.243338890257842,4.3822327073369));
#19585=CARTESIAN_POINT('Ctrl Pts',(11.5390626891702,-0.482464979911041,
4.09556551685319));
#19586=CARTESIAN_POINT('Ctrl Pts',(11.586778525233,-0.341319923258817,3.64587299617429));
#19587=CARTESIAN_POINT('Ctrl Pts',(11.6344943612959,0.113264470804062,3.5213807520529));
#19588=CARTESIAN_POINT('Ctrl Pts',(11.6822101973587,0.463836358529674,3.83641192782507));
#19589=CARTESIAN_POINT('Ctrl Pts',(11.7285118582339,0.390694138047139,4.28787953265104));
#19590=CARTESIAN_POINT('Ctrl Pts',(11.7589082404215,0.125533053862222,4.41563275094549));
#19591=CARTESIAN_POINT('Ctrl Pts',(11.7733993439214,-0.000215373091504231,
4.41642415578018));
#19592=CARTESIAN_POINT('Origin',(3.42660065607856,0.,4.));
#19593=CARTESIAN_POINT('',(11.0766006560786,0.000352537510456688,4.41557576695298));
#19594=CARTESIAN_POINT('',(11.1733993439214,0.000319650745578964,4.41547275084625));
#19595=CARTESIAN_POINT('',(3.42660065607856,4.87367679877478E-13,4.415875));
#19596=CARTESIAN_POINT('Ctrl Pts',(11.0766006560786,0.000352537510456667,
4.41557576695298));
#19597=CARTESIAN_POINT('Ctrl Pts',(11.0876202951733,-0.0957751134661499,
4.41480617263661));
#19598=CARTESIAN_POINT('Ctrl Pts',(11.1145452129557,-0.331820540820521,
4.33374203885914));
#19599=CARTESIAN_POINT('Ctrl Pts',(11.1573754094257,-0.488245699001722,
3.94065893278431));
#19600=CARTESIAN_POINT('Ctrl Pts',(11.2050912454886,-0.214150733603143,
3.55723066033293));
#19601=CARTESIAN_POINT('Ctrl Pts',(11.2528070815514,0.256602145595791,3.58040428537983));
#19602=CARTESIAN_POINT('Ctrl Pts',(11.3005229176142,0.491713326162588,3.98889911147238));
#19603=CARTESIAN_POINT('Ctrl Pts',(11.3417874424566,0.304539430122629,4.35098016691413));
#19604=CARTESIAN_POINT('Ctrl Pts',(11.3671466886114,0.0824085130402235,
4.41491686960609));
#19605=CARTESIAN_POINT('Ctrl Pts',(11.3766006560786,-0.000206048103232999,
4.41528588740701));
#19606=CARTESIAN_POINT('Ctrl Pts',(11.1733993439214,0.000319650745578978,
4.41547275084625));
#19607=CARTESIAN_POINT('Ctrl Pts',(11.1839501748577,-0.0917759901056567,
4.4148158243975));
#19608=CARTESIAN_POINT('Ctrl Pts',(11.2104062844816,-0.32368545017211,4.33911969104981));
#19609=CARTESIAN_POINT('Ctrl Pts',(11.2527676727932,-0.489781601228288,
3.95506440219344));
#19610=CARTESIAN_POINT('Ctrl Pts',(11.300483508856,-0.227098200695192,3.56372986339542));
#19611=CARTESIAN_POINT('Ctrl Pts',(11.3481993449188,0.244132971891272,3.57302890392028));
#19612=CARTESIAN_POINT('Ctrl Pts',(11.3959151809817,0.491173079921361,3.97442207176994));
#19613=CARTESIAN_POINT('Ctrl Pts',(11.4376485139825,0.312739912806573,4.34603313379779));
#19614=CARTESIAN_POINT('Ctrl Pts',(11.4634765682958,0.0864149014017155,
4.41486151738456));
#19615=CARTESIAN_POINT('Ctrl Pts',(11.4733993439214,-0.000260100423148869,
4.41535533657191));
#19616=CARTESIAN_POINT('Origin',(3.42660065607856,0.,4.));
#19617=CARTESIAN_POINT('',(10.7766006560786,5.16128798610187E-5,4.41655360457584));
#19618=CARTESIAN_POINT('',(10.8733993439214,0.000125523266313186,4.41651574507477));
#19619=CARTESIAN_POINT('',(3.42660065607856,4.87367679877478E-13,4.415875));
#19620=CARTESIAN_POINT('Ctrl Pts',(10.7766006560786,5.16128798610299E-5,
4.41655360457584));
#19621=CARTESIAN_POINT('Ctrl Pts',(10.7921886230477,-0.135103241057852,
4.41631783152902));
#19622=CARTESIAN_POINT('Ctrl Pts',(10.8236818687044,-0.408598944994929,
4.27108057505162));
#19623=CARTESIAN_POINT('Ctrl Pts',(10.8710803930487,-0.451470021714238,
3.80485891169382));
#19624=CARTESIAN_POINT('Ctrl Pts',(10.9187962291115,-0.080036233235122,
3.51471716883706));
#19625=CARTESIAN_POINT('Ctrl Pts',(10.9665120651743,0.364896059739551,3.6702181168734));
#19626=CARTESIAN_POINT('Ctrl Pts',(11.0142279012372,0.47473868640782,4.1285628425314));
#19627=CARTESIAN_POINT('Ctrl Pts',(11.0509240982053,0.223935965514619,4.3902602363912));
#19628=CARTESIAN_POINT('Ctrl Pts',(11.0717150164857,0.0429714521173939,
4.4159169723618));
#19629=CARTESIAN_POINT('Ctrl Pts',(11.0766006560786,0.000352537510456667,
4.41557576695298));
#19630=CARTESIAN_POINT('Ctrl Pts',(10.8733993439214,0.000125523266313226,
4.41651574507477));
#19631=CARTESIAN_POINT('Ctrl Pts',(10.888518502732,-0.130996444363694,4.41599591363288));
#19632=CARTESIAN_POINT('Ctrl Pts',(10.9195429402303,-0.400997532511054,
4.27840016053723));
#19633=CARTESIAN_POINT('Ctrl Pts',(10.9664726564161,-0.45702143577077,3.81824018018824));
#19634=CARTESIAN_POINT('Ctrl Pts',(11.014188492479,-0.0942939790271268,
3.51728489730359));
#19635=CARTESIAN_POINT('Ctrl Pts',(11.0619043285418,0.355025089556487,3.65961432075161));
#19636=CARTESIAN_POINT('Ctrl Pts',(11.1096201646047,0.478319155637209,4.11452515096033));
#19637=CARTESIAN_POINT('Ctrl Pts',(11.1467851697312,0.23222845252417,4.38693182090163));
#19638=CARTESIAN_POINT('Ctrl Pts',(11.1680448961701,0.0470573247768451,
4.41580613485813));
#19639=CARTESIAN_POINT('Ctrl Pts',(11.1733993439214,0.000319650745578978,
4.41547275084625));
#19640=CARTESIAN_POINT('Origin',(3.42660065607856,0.,4.));
#19641=CARTESIAN_POINT('',(10.4766006560786,-0.000378910032885682,4.4157309619862));
#19642=CARTESIAN_POINT('',(10.5733993439214,-0.000383826598418624,4.41585315377736));
#19643=CARTESIAN_POINT('',(3.42660065607856,4.87367679877478E-13,4.415875));
#19644=CARTESIAN_POINT('Ctrl Pts',(10.4766006560786,-0.000378910032885704,
4.4157309619862));
#19645=CARTESIAN_POINT('Ctrl Pts',(10.4808516722344,-0.0374267536145521,
4.41605913507464));
#19646=CARTESIAN_POINT('Ctrl Pts',(10.5010079670778,-0.212714974368116,
4.3945277200383));
#19647=CARTESIAN_POINT('Ctrl Pts',(10.5370695406088,-0.469236294399976,
4.14738563318641));
#19648=CARTESIAN_POINT('Ctrl Pts',(10.5847853766716,-0.377752434501872,
3.68502647241413));
#19649=CARTESIAN_POINT('Ctrl Pts',(10.6325012127345,0.0606272984676223,
3.51191234851464));
#19650=CARTESIAN_POINT('Ctrl Pts',(10.6802170487973,0.443332050383407,3.78701662516801));
#19651=CARTESIAN_POINT('Ctrl Pts',(10.7279328848602,0.418918158891686,4.25770681210006));
#19652=CARTESIAN_POINT('Ctrl Pts',(10.7600607539539,0.143455624352724,4.41528584951654));
#19653=CARTESIAN_POINT('Ctrl Pts',(10.7762833443601,0.00280285164340033,
4.41655840401831));
#19654=CARTESIAN_POINT('Ctrl Pts',(10.7766006560786,5.16128798610299E-5,
4.41655360457584));
#19655=CARTESIAN_POINT('Ctrl Pts',(10.5733993439214,-0.000383826598418617,
4.41585315377736));
#19656=CARTESIAN_POINT('Ctrl Pts',(10.5771815519187,-0.0333213161677604,
4.41615637378185));
#19657=CARTESIAN_POINT('Ctrl Pts',(10.5968690386037,-0.20443114816448,4.39750812937281));
#19658=CARTESIAN_POINT('Ctrl Pts',(10.6324618039763,-0.464691964107356,
4.16114156306187));
#19659=CARTESIAN_POINT('Ctrl Pts',(10.6801776400391,-0.386865111317189,
3.69628860657276));
#19660=CARTESIAN_POINT('Ctrl Pts',(10.7278934761019,0.0462259258804368,
3.51033849586834));
#19661=CARTESIAN_POINT('Ctrl Pts',(10.7756093121648,0.436866984064762,3.77405207881873));
#19662=CARTESIAN_POINT('Ctrl Pts',(10.8233251482276,0.426326368719826,4.24525711444552));
#19663=CARTESIAN_POINT('Ctrl Pts',(10.8559218254798,0.151674250044741,4.4132974389186));
#19664=CARTESIAN_POINT('Ctrl Pts',(10.8726132240444,0.00694320316194716,
4.41654277368359));
#19665=CARTESIAN_POINT('Ctrl Pts',(10.8733993439214,0.000125523266313226,
4.41651574507477));
#19666=CARTESIAN_POINT('Origin',(3.42660065607856,0.,4.));
#19667=CARTESIAN_POINT('',(10.1766006560786,0.000123197149224082,4.41521991402453));
#19668=CARTESIAN_POINT('',(10.2733993439214,5.7336166378985E-5,4.41519339896199));
#19669=CARTESIAN_POINT('',(3.42660065607856,4.87367679877478E-13,4.415875));
#19670=CARTESIAN_POINT('Ctrl Pts',(10.1766006560786,0.000123197149224097,
4.41521991402453));
#19671=CARTESIAN_POINT('Ctrl Pts',(10.1854200001087,-0.0769762270984491,
4.41501595190525));
#19672=CARTESIAN_POINT('Ctrl Pts',(10.2101446228264,-0.293404201931947,
4.35739193013711));
#19673=CARTESIAN_POINT('Ctrl Pts',(10.2507745242318,-0.491764996345908,
4.00850959581219));
#19674=CARTESIAN_POINT('Ctrl Pts',(10.2984903602946,-0.273124940234581,
3.59096700393021));
#19675=CARTESIAN_POINT('Ctrl Pts',(10.3462061963575,0.196329951061554,3.54904570612073));
#19676=CARTESIAN_POINT('Ctrl Pts',(10.3939220324203,0.485492027373267,3.92124267520431));
#19677=CARTESIAN_POINT('Ctrl Pts',(10.4373868523273,0.34277731801193,4.32616121393696));
#19678=CARTESIAN_POINT('Ctrl Pts',(10.4649463935468,0.101188639822117,4.41483126760997));
#19679=CARTESIAN_POINT('Ctrl Pts',(10.4766006560786,-0.000378910032885704,
4.4157309619862));
#19680=CARTESIAN_POINT('Ctrl Pts',(10.2733993439214,5.73361663789851E-5,
4.41519339896199));
#19681=CARTESIAN_POINT('Ctrl Pts',(10.2817498797931,-0.0729553575157724,
4.41510384014646));
#19682=CARTESIAN_POINT('Ctrl Pts',(10.3060056943524,-0.285157432566911,
4.36192175935665));
#19683=CARTESIAN_POINT('Ctrl Pts',(10.3461667875993,-0.491301045992024,
4.02298928139638));
#19684=CARTESIAN_POINT('Ctrl Pts',(10.3938826236621,-0.285053227451061,
3.599188470261));
#19685=CARTESIAN_POINT('Ctrl Pts',(10.4415984597249,0.182963355965895,3.54345905416307));
#19686=CARTESIAN_POINT('Ctrl Pts',(10.4893142957878,0.482961874346273,3.9069782134126));
#19687=CARTESIAN_POINT('Ctrl Pts',(10.5332479238533,0.35082465130295,4.32033516829581));
#19688=CARTESIAN_POINT('Ctrl Pts',(10.5612762732311,0.105190355120073,4.41488124595214));
#19689=CARTESIAN_POINT('Ctrl Pts',(10.5733993439214,-0.000383826598418617,
4.41585315377736));
#19690=CARTESIAN_POINT('Origin',(3.42660065607856,0.,4.));
#19691=CARTESIAN_POINT('',(9.87660065607859,0.000332404019580576,4.41618417038907));
#19692=CARTESIAN_POINT('',(9.9733993439214,0.000362444897862246,4.41606425076498));
#19693=CARTESIAN_POINT('',(3.42660065607856,4.87367679877478E-13,4.415875));
#19694=CARTESIAN_POINT('Ctrl Pts',(9.87660065607859,0.000332404019580564,
4.41618417038907));
#19695=CARTESIAN_POINT('Ctrl Pts',(9.88998832798303,-0.116016130490024,
4.41516972706101));
#19696=CARTESIAN_POINT('Ctrl Pts',(9.91928127857509,-0.372296869871387,
4.30364082544554));
#19697=CARTESIAN_POINT('Ctrl Pts',(9.96447950785476,-0.474054618562381,
3.8689372536849));
#19698=CARTESIAN_POINT('Ctrl Pts',(10.0121953439176,-0.146148770628728,
3.53037700046135));
#19699=CARTESIAN_POINT('Ctrl Pts',(10.0599111799804,0.315967742161179,3.62307877379278));
#19700=CARTESIAN_POINT('Ctrl Pts',(10.1076270160433,0.487926215535836,4.06191310882887));
#19701=CARTESIAN_POINT('Ctrl Pts',(10.146523508076,0.262848409674369,4.37329037489646));
#19702=CARTESIAN_POINT('Ctrl Pts',(10.1695147214211,0.062069015396409,4.41538378814543));
#19703=CARTESIAN_POINT('Ctrl Pts',(10.1766006560786,0.000123197149224097,
4.41521991402453));
#19704=CARTESIAN_POINT('Ctrl Pts',(9.9733993439214,0.000362444897862267,
4.41606425076498));
#19705=CARTESIAN_POINT('Ctrl Pts',(9.9863182076674,-0.111995531308361,4.41503480155798));
#19706=CARTESIAN_POINT('Ctrl Pts',(10.015142350101,-0.364380386131072,4.30999810797653));
#19707=CARTESIAN_POINT('Ctrl Pts',(10.0598717712222,-0.477709011270712,
3.88295588266498));
#19708=CARTESIAN_POINT('Ctrl Pts',(10.1075876072851,-0.159916626226494,
3.53488507064564));
#19709=CARTESIAN_POINT('Ctrl Pts',(10.1553034433479,0.304729657315094,3.61393645496551));
#19710=CARTESIAN_POINT('Ctrl Pts',(10.2030192794107,0.489538007675758,4.04751593304174));
#19711=CARTESIAN_POINT('Ctrl Pts',(10.2423845796019,0.271127379494919,4.3692182851415));
#19712=CARTESIAN_POINT('Ctrl Pts',(10.2658446011055,0.0661120339180705,
4.41527442296197));
#19713=CARTESIAN_POINT('Ctrl Pts',(10.2733993439214,5.73361663789851E-5,
4.41519339896199));
#19714=CARTESIAN_POINT('Origin',(3.42660065607856,0.,4.));
#19715=CARTESIAN_POINT('',(9.57660065607859,-0.000290304052950346,4.41629504206998));
#19716=CARTESIAN_POINT('',(9.6733993439214,-0.000236899196693507,4.41639317328699));
#19717=CARTESIAN_POINT('',(3.42660065607856,4.87367679877478E-13,4.415875));
#19718=CARTESIAN_POINT('Ctrl Pts',(9.57660065607859,-0.000290304052950335,
4.41629504206998));
#19719=CARTESIAN_POINT('Ctrl Pts',(9.57865137716975,-0.0181001948149981,
4.41643644713422));
#19720=CARTESIAN_POINT('Ctrl Pts',(9.59660737694851,-0.173896467062472,
4.40729888742394));
#19721=CARTESIAN_POINT('Ctrl Pts',(9.63046865541489,-0.444448234747017,
4.21064422964382));
#19722=CARTESIAN_POINT('Ctrl Pts',(9.67818449147773,-0.41755432743774,3.74008922975375));
#19723=CARTESIAN_POINT('Ctrl Pts',(9.72590032754057,-0.00721385634321597,
3.50821428942208));
#19724=CARTESIAN_POINT('Ctrl Pts',(9.77361616360341,0.40975121003073,3.72795373420991));
#19725=CARTESIAN_POINT('Ctrl Pts',(9.82133199966624,0.450435435400681,4.19751745084266));
#19726=CARTESIAN_POINT('Ctrl Pts',(9.85566016382464,0.182118884769847,4.40484283743537));
#19727=CARTESIAN_POINT('Ctrl Pts',(9.87408304929542,0.0222122246324328,
4.41637494063069));
#19728=CARTESIAN_POINT('Ctrl Pts',(9.87660065607859,0.000332404019580564,
4.41618417038907));
#19729=CARTESIAN_POINT('Ctrl Pts',(9.6733993439214,-0.00023689919669354,
4.41639317328699));
#19730=CARTESIAN_POINT('Ctrl Pts',(9.67498125685411,-0.0139668454918635,
4.4164864708936));
#19731=CARTESIAN_POINT('Ctrl Pts',(9.69246844847443,-0.165649677201134,
4.40963259460397));
#19732=CARTESIAN_POINT('Ctrl Pts',(9.72586091878235,-0.438051576325333,
4.22364266437974));
#19733=CARTESIAN_POINT('Ctrl Pts',(9.77357675484519,-0.425028039486299,
3.75249971615691));
#19734=CARTESIAN_POINT('Ctrl Pts',(9.82129259090803,-0.0216947140899849,
3.50864008686857));
#19735=CARTESIAN_POINT('Ctrl Pts',(9.86900842697087,0.401561201071248,3.7160038263529));
#19736=CARTESIAN_POINT('Ctrl Pts',(9.91672426303371,0.456057286475463,4.18416562194019));
#19737=CARTESIAN_POINT('Ctrl Pts',(9.95152123535055,0.190383912560376,4.40224154849284));
#19738=CARTESIAN_POINT('Ctrl Pts',(9.97041292897978,0.0263359008882403,
4.4163022254471));
#19739=CARTESIAN_POINT('Ctrl Pts',(9.9733993439214,0.000362444897862267,
4.41606425076498));
#19740=CARTESIAN_POINT('Origin',(3.42660065607856,0.,4.));
#19741=CARTESIAN_POINT('',(9.27660065607858,-0.000185084181660103,4.41526520375254));
#19742=CARTESIAN_POINT('',(9.37339934392141,-0.000241596553487405,4.41532857883968));
#19743=CARTESIAN_POINT('',(3.42660065607856,4.87367679877478E-13,4.415875));
#19744=CARTESIAN_POINT('Ctrl Pts',(9.27660065607858,-0.000185084181660189,
4.41526520375254));
#19745=CARTESIAN_POINT('Ctrl Pts',(9.28321970504406,-0.0580335922681754,
4.4154966095816));
#19746=CARTESIAN_POINT('Ctrl Pts',(9.30574403269715,-0.254596444523232,
4.37718269734299));
#19747=CARTESIAN_POINT('Ctrl Pts',(9.34417363903789,-0.485900307124067,
4.07619787653679));
#19748=CARTESIAN_POINT('Ctrl Pts',(9.39188947510068,-0.326887306273347,
3.63250862071426));
#19749=CARTESIAN_POINT('Ctrl Pts',(9.43960531116356,0.13231133773591,3.52629235307153));
#19750=CARTESIAN_POINT('Ctrl Pts',(9.48732114722637,0.470006444430667,3.85508910653225));
#19751=CARTESIAN_POINT('Ctrl Pts',(9.53298626219807,0.380123833963086,4.29710958399465));
#19752=CARTESIAN_POINT('Ctrl Pts',(9.56274609848214,0.120032327051623,4.41533971732329));
#19753=CARTESIAN_POINT('Ctrl Pts',(9.57660065607859,-0.000290304052950335,
4.41629504206998));
#19754=CARTESIAN_POINT('Ctrl Pts',(9.3733993439214,-0.000241596553487357,
4.41532857883968));
#19755=CARTESIAN_POINT('Ctrl Pts',(9.37954958472843,-0.0539723465869793,
4.41561177485228));
#19756=CARTESIAN_POINT('Ctrl Pts',(9.40160510422307,-0.246305905820531,
4.3809303471886));
#19757=CARTESIAN_POINT('Ctrl Pts',(9.43956590240532,-0.483445357410111,
4.09047547319903));
#19758=CARTESIAN_POINT('Ctrl Pts',(9.48728173846818,-0.337568794959357,
3.64229546617122));
#19759=CARTESIAN_POINT('Ctrl Pts',(9.53499757453099,0.118302386066128,3.5226010365501));
#19760=CARTESIAN_POINT('Ctrl Pts',(9.58271341059386,0.465534665650901,3.84130942079228));
#19761=CARTESIAN_POINT('Ctrl Pts',(9.62884733372396,0.387920650713885,4.29034844530944));
#19762=CARTESIAN_POINT('Ctrl Pts',(9.65907597816649,0.124080336294106,4.41554841393524));
#19763=CARTESIAN_POINT('Ctrl Pts',(9.6733993439214,-0.00023689919669354,
4.41639317328699));
#19764=CARTESIAN_POINT('Origin',(3.42660065607856,0.,4.));
#19765=CARTESIAN_POINT('',(8.97660065607858,0.000361621133123973,4.41561526113518));
#19766=CARTESIAN_POINT('',(9.0733993439214,0.00033264130393823,4.41550825894961));
#19767=CARTESIAN_POINT('',(3.42660065607856,4.87367679877478E-13,4.415875));
#19768=CARTESIAN_POINT('Ctrl Pts',(8.97660065607858,0.000361621133123963,
4.41561526113518));
#19769=CARTESIAN_POINT('Ctrl Pts',(8.98778803291839,-0.097205817696177,
4.41480833810253));
#19770=CARTESIAN_POINT('Ctrl Pts',(9.01488068844582,-0.334723089553266,
4.33177224018802));
#19771=CARTESIAN_POINT('Ctrl Pts',(9.05787862266083,-0.487593182843731,
3.93551656882348));
#19772=CARTESIAN_POINT('Ctrl Pts',(9.10559445872368,-0.209472459465777,
3.55499829935456));
#19773=CARTESIAN_POINT('Ctrl Pts',(9.15331029478651,0.261010046587687,3.58313193881964));
#19774=CARTESIAN_POINT('Ctrl Pts',(9.20102613084934,0.491803010703882,3.99408193320625));
#19775=CARTESIAN_POINT('Ctrl Pts',(9.24212291794672,0.301599829163518,4.35270650246492));
#19776=CARTESIAN_POINT('Ctrl Pts',(9.26731442635645,0.0809737859182142,
4.41494055172187));
#19777=CARTESIAN_POINT('Ctrl Pts',(9.27660065607858,-0.000185084181660189,
4.41526520375254));
#19778=CARTESIAN_POINT('Ctrl Pts',(9.0733993439214,0.000332641303938268,
4.41550825894961));
#19779=CARTESIAN_POINT('Ctrl Pts',(9.08411791260276,-0.093207009794584,
4.4148098083896));
#19780=CARTESIAN_POINT('Ctrl Pts',(9.11074175997173,-0.326599857706223,
4.33721709571948));
#19781=CARTESIAN_POINT('Ctrl Pts',(9.1532708860283,-0.489280820139143,3.94990505119329));
#19782=CARTESIAN_POINT('Ctrl Pts',(9.20098672209113,-0.222487703095825,
3.56136068709803));
#19783=CARTESIAN_POINT('Ctrl Pts',(9.24870255815399,0.248619295113741,3.57562555337399));
#19784=CARTESIAN_POINT('Ctrl Pts',(9.29641839421681,0.49141536912078,3.97960000382683));
#19785=CARTESIAN_POINT('Ctrl Pts',(9.33798398947263,0.309808547095179,4.34782394055348));
#19786=CARTESIAN_POINT('Ctrl Pts',(9.36364430604082,0.0849819773478622,
4.41487939515448));
#19787=CARTESIAN_POINT('Ctrl Pts',(9.3733993439214,-0.000241596553487357,
4.41532857883968));
#19788=CARTESIAN_POINT('Origin',(3.42660065607856,0.,4.));
#19789=CARTESIAN_POINT('',(8.67660065607859,2.43999233753954E-5,4.41655967853978));
#19790=CARTESIAN_POINT('',(8.77339934392141,9.9565801791445E-5,4.41653262406943));
#19791=CARTESIAN_POINT('',(3.42660065607856,4.87367679877478E-13,4.415875));
#19792=CARTESIAN_POINT('Ctrl Pts',(8.67660065607859,2.43999233753836E-5,
4.41655967853978));
#19793=CARTESIAN_POINT('Ctrl Pts',(8.69235636079272,-0.136579453435425,
4.41644398151286));
#19794=CARTESIAN_POINT('Ctrl Pts',(8.72401734419445,-0.411298873006737,
4.26841067400337));
#19795=CARTESIAN_POINT('Ctrl Pts',(8.7715836062838,-0.449388340942622,3.80011167148426));
#19796=CARTESIAN_POINT('Ctrl Pts',(8.81929944234665,-0.0749173544856965,
3.51390061216986));
#19797=CARTESIAN_POINT('Ctrl Pts',(8.86701527840948,0.368351391347115,3.67408210030036));
#19798=CARTESIAN_POINT('Ctrl Pts',(8.91473111447233,0.473357386691186,4.13355901061654));
#19799=CARTESIAN_POINT('Ctrl Pts',(8.95125957369535,0.220969504140389,4.39141457480799));
#19800=CARTESIAN_POINT('Ctrl Pts',(8.97188275423077,0.0415074238114615,
4.41595555392421));
#19801=CARTESIAN_POINT('Ctrl Pts',(8.97660065607858,0.000361621133123963,
4.41561526113518));
#19802=CARTESIAN_POINT('Ctrl Pts',(8.77339934392141,9.95658017914599E-5,
4.41653262406943));
#19803=CARTESIAN_POINT('Ctrl Pts',(8.78868624047708,-0.132462770989084,
4.416105976883));
#19804=CARTESIAN_POINT('Ctrl Pts',(8.81987841572037,-0.403726445587972,
4.27580529254432));
#19805=CARTESIAN_POINT('Ctrl Pts',(8.86697586965126,-0.455080472922433,
3.81343369002772));
#19806=CARTESIAN_POINT('Ctrl Pts',(8.91469170571412,-0.0892013699275644,
3.51631793453238));
#19807=CARTESIAN_POINT('Ctrl Pts',(8.96240754177693,0.358592723611288,3.66337486216116));
#19808=CARTESIAN_POINT('Ctrl Pts',(9.0101233778398,0.477085601399612,4.11955983351088));
#19809=CARTESIAN_POINT('Ctrl Pts',(9.04712064522126,0.229261233371815,4.38814011953822));
#19810=CARTESIAN_POINT('Ctrl Pts',(9.06821263391514,0.0455964315317218,
4.41584623882512));
#19811=CARTESIAN_POINT('Ctrl Pts',(9.0733993439214,0.000332641303938268,
4.41550825894961));
#19812=CARTESIAN_POINT('Origin',(3.42660065607856,0.,4.));
#19813=CARTESIAN_POINT('',(8.37660065607859,-0.000374086211409503,4.41568853448753));
#19814=CARTESIAN_POINT('',(8.47339934392141,-0.000383538171196851,4.41580895574666));
#19815=CARTESIAN_POINT('',(3.42660065607856,4.87367679877478E-13,4.415875));
#19816=CARTESIAN_POINT('Ctrl Pts',(8.37660065607859,-0.000374086211409545,
4.41568853448753));
#19817=CARTESIAN_POINT('Ctrl Pts',(8.38101940997943,-0.0388937529272332,
4.41602262289185));
#19818=CARTESIAN_POINT('Ctrl Pts',(8.40134344256788,-0.215680110827853,
4.3934260635833));
#19819=CARTESIAN_POINT('Ctrl Pts',(8.43757275384394,-0.470763542849379,
4.14243212971755));
#19820=CARTESIAN_POINT('Ctrl Pts',(8.48528858990678,-0.37441192437669,3.68106280283335));
#19821=CARTESIAN_POINT('Ctrl Pts',(8.53300442596962,0.0657679253190804,
3.51257841158684));
#19822=CARTESIAN_POINT('Ctrl Pts',(8.58072026203246,0.445552077224736,3.79170076492532));
#19823=CARTESIAN_POINT('Ctrl Pts',(8.62843609809529,0.41617890091499,4.26210751092856));
#19824=CARTESIAN_POINT('Ctrl Pts',(8.66039622944401,0.140517691799823,4.41596716726027));
#19825=CARTESIAN_POINT('Ctrl Pts',(8.6764510821051,0.00132122424898086,
4.41656077688887));
#19826=CARTESIAN_POINT('Ctrl Pts',(8.67660065607859,2.43999233753836E-5,
4.41655967853978));
#19827=CARTESIAN_POINT('Ctrl Pts',(8.47339934392141,-0.000383538171196768,
4.41580895574666));
#19828=CARTESIAN_POINT('Ctrl Pts',(8.47734928966379,-0.0347911067166248,
4.41612244784963));
#19829=CARTESIAN_POINT('Ctrl Pts',(8.4972045140938,-0.207394442561863,4.39645832432586));
#19830=CARTESIAN_POINT('Ctrl Pts',(8.5329650172114,-0.466364439759318,4.15623518867385));
#19831=CARTESIAN_POINT('Ctrl Pts',(8.58068085327425,-0.383642787608637,
3.69222827230584));
#19832=CARTESIAN_POINT('Ctrl Pts',(8.62839668933707,0.0513839395061145,
3.51085286915611));
#19833=CARTESIAN_POINT('Ctrl Pts',(8.67611252539993,0.439224004328866,3.77866880275638));
#19834=CARTESIAN_POINT('Ctrl Pts',(8.72382836146275,0.42371790764641,4.24973658040369));
#19835=CARTESIAN_POINT('Ctrl Pts',(8.75625730096992,0.148732406864234,4.41402322426773));
#19836=CARTESIAN_POINT('Ctrl Pts',(8.77278096178947,0.00546194790078228,
4.41654988270631));
#19837=CARTESIAN_POINT('Ctrl Pts',(8.77339934392141,9.95658017914599E-5,
4.41653262406943));
#19838=CARTESIAN_POINT('Origin',(3.42660065607856,0.,4.));
#19839=CARTESIAN_POINT('',(8.07660065607859,0.000145957947245773,4.41523406184916));
#19840=CARTESIAN_POINT('',(8.1733993439214,8.12049300508987E-5,4.41520065480005));
#19841=CARTESIAN_POINT('',(3.42660065607856,4.87367679877478E-13,4.415875));
#19842=CARTESIAN_POINT('Ctrl Pts',(8.07660065607858,0.00014595794724577,
4.41523406184916));
#19843=CARTESIAN_POINT('Ctrl Pts',(8.08558773785375,-0.0784131624224431,
4.41498734772332));
#19844=CARTESIAN_POINT('Ctrl Pts',(8.11048009831652,-0.296350794919178,
4.35572875890285));
#19845=CARTESIAN_POINT('Ctrl Pts',(8.15127773746691,-0.491827368180951,
4.00332637343646));
#19846=CARTESIAN_POINT('Ctrl Pts',(8.19899357352975,-0.268798940774433,
3.58811123553743));
#19847=CARTESIAN_POINT('Ctrl Pts',(8.24670940959259,0.201071689948468,3.55113988776764));
#19848=CARTESIAN_POINT('Ctrl Pts',(8.29442524565542,0.486295093906121,3.92636368766143));
#19849=CARTESIAN_POINT('Ctrl Pts',(8.33772232781743,0.339888039743562,4.32819890206972));
#19850=CARTESIAN_POINT('Ctrl Pts',(8.36511413129181,0.0997575609540166,
4.41482007364463));
#19851=CARTESIAN_POINT('Ctrl Pts',(8.37660065607859,-0.000374086211409545,
4.41568853448753));
#19852=CARTESIAN_POINT('Ctrl Pts',(8.1733993439214,8.12049300509751E-5,
4.41520065480005));
#19853=CARTESIAN_POINT('Ctrl Pts',(8.18191761753811,-0.0743948540356096,
4.41507113968239));
#19854=CARTESIAN_POINT('Ctrl Pts',(8.20634116984244,-0.288109900049694,
4.36032095112539));
#19855=CARTESIAN_POINT('Ctrl Pts',(8.24667000083438,-0.491516046133,4.01781014446235));
#19856=CARTESIAN_POINT('Ctrl Pts',(8.29438583689722,-0.280813212199106,
3.59620653211525));
#19857=CARTESIAN_POINT('Ctrl Pts',(8.34210167296004,0.187764715363875,3.54541267448783));
#19858=CARTESIAN_POINT('Ctrl Pts',(8.38981750902289,0.483915415676709,3.91207335260334));
#19859=CARTESIAN_POINT('Ctrl Pts',(8.43358339934334,0.347950231939931,4.32244196179047));
#19860=CARTESIAN_POINT('Ctrl Pts',(8.46144401097618,0.1037581297464,4.41486010664565));
#19861=CARTESIAN_POINT('Ctrl Pts',(8.47339934392141,-0.000383538171196768,
4.41580895574666));
#19862=CARTESIAN_POINT('Origin',(3.42660065607856,0.,4.));
#19863=CARTESIAN_POINT('',(7.77660065607858,0.000318631424802313,4.41622521972442));
#19864=CARTESIAN_POINT('',(7.8733993439214,0.000353153796088606,4.4161078667978));
#19865=CARTESIAN_POINT('',(3.42660065607856,4.87367679877478E-13,4.415875));
#19866=CARTESIAN_POINT('Ctrl Pts',(7.77660065607859,0.000318631424802297,
4.41622521972442));
#19867=CARTESIAN_POINT('Ctrl Pts',(7.79015606572807,-0.117457481003694,
4.41522659035305));
#19868=CARTESIAN_POINT('Ctrl Pts',(7.81961675406517,-0.375115671948731,
4.30131743988157));
#19869=CARTESIAN_POINT('Ctrl Pts',(7.86498272108989,-0.472647010158531,
3.86394843388276));
#19870=CARTESIAN_POINT('Ctrl Pts',(7.91269855715272,-0.141191260335066,
3.52886280888004));
#19871=CARTESIAN_POINT('Ctrl Pts',(7.96041439321556,0.31992259635559,3.62642971585976));
#19872=CARTESIAN_POINT('Ctrl Pts',(8.0081302292784,0.48724661017382,4.0670519628834));
#19873=CARTESIAN_POINT('Ctrl Pts',(8.04685898356608,0.259884401562094,4.37470733986759));
#19874=CARTESIAN_POINT('Ctrl Pts',(8.06968245916614,0.0606202562326388,
4.41542398077349));
#19875=CARTESIAN_POINT('Ctrl Pts',(8.07660065607858,0.00014595794724577,
4.41523406184916));
#19876=CARTESIAN_POINT('Ctrl Pts',(7.8733993439214,0.000353153796088627,
4.4161078667978));
#19877=CARTESIAN_POINT('Ctrl Pts',(7.88648594541244,-0.113432877329791,
4.41507910421771));
#19878=CARTESIAN_POINT('Ctrl Pts',(7.9154778255911,-0.367219156371593,4.30774647947464));
#19879=CARTESIAN_POINT('Ctrl Pts',(7.96037498445733,-0.476448943335793,
3.87792777037096));
#19880=CARTESIAN_POINT('Ctrl Pts',(8.0080908205202,-0.1550058622045,3.53322552818936));
#19881=CARTESIAN_POINT('Ctrl Pts',(8.05580665658301,0.308781487260178,3.61716946571973));
#19882=CARTESIAN_POINT('Ctrl Pts',(8.10352249264587,0.489010045760349,4.0526725734847));
#19883=CARTESIAN_POINT('Ctrl Pts',(8.14272005509199,0.26816615642074,4.37069430501912));
#19884=CARTESIAN_POINT('Ctrl Pts',(8.1660123388505,0.064666477720629,4.4153129696744));
#19885=CARTESIAN_POINT('Ctrl Pts',(8.1733993439214,8.12049300509751E-5,
4.41520065480005));
#19886=CARTESIAN_POINT('Origin',(3.42660065607856,0.,4.));
#19887=CARTESIAN_POINT('',(7.47660065607859,-0.000306770237538029,4.41625647512786));
#19888=CARTESIAN_POINT('',(7.5733993439214,-0.000257198714157858,4.41635988094829));
#19889=CARTESIAN_POINT('',(3.42660065607856,4.87367679877478E-13,4.415875));
#19890=CARTESIAN_POINT('Ctrl Pts',(7.47660065607859,-0.00030677023753798,
4.41625647512786));
#19891=CARTESIAN_POINT('Ctrl Pts',(7.47881911491479,-0.0195780710793754,
4.41641565502598));
#19892=CARTESIAN_POINT('Ctrl Pts',(7.4969428524386,-0.176849480241104,4.4064317922735));
#19893=CARTESIAN_POINT('Ctrl Pts',(7.53097186865002,-0.44664354691983,4.20594845626764));
#19894=CARTESIAN_POINT('Ctrl Pts',(7.57868770471286,-0.414791917646955,
3.73570302684109));
#19895=CARTESIAN_POINT('Ctrl Pts',(7.62640354077569,-0.00203048755240202,
3.50816557464413));
#19896=CARTESIAN_POINT('Ctrl Pts',(7.67411937683853,0.412595570264971,3.73228724307244));
#19897=CARTESIAN_POINT('Ctrl Pts',(7.72183521290137,0.448328767436039,4.20225365549051));
#19898=CARTESIAN_POINT('Ctrl Pts',(7.75599563931472,0.179163779268806,4.40574053813273));
#19899=CARTESIAN_POINT('Ctrl Pts',(7.77425078704046,0.0207354574140521,
4.41639833498254));
#19900=CARTESIAN_POINT('Ctrl Pts',(7.77660065607859,0.000318631424802297,
4.41622521972442));
#19901=CARTESIAN_POINT('Ctrl Pts',(7.5733993439214,-0.000257198714157839,
4.41635988094829));
#19902=CARTESIAN_POINT('Ctrl Pts',(7.57514899459915,-0.0154461882200338,
4.41646996636401));
#19903=CARTESIAN_POINT('Ctrl Pts',(7.59280392396451,-0.168599214901356,
4.40881268721627));
#19904=CARTESIAN_POINT('Ctrl Pts',(7.62636413201748,-0.440384235482588,
4.21901358396786));
#19905=CARTESIAN_POINT('Ctrl Pts',(7.67407996808031,-0.422396009600076,
3.7480340579683));
#19906=CARTESIAN_POINT('Ctrl Pts',(7.72179580414317,-0.0165150286377962,
3.50843873354525));
#19907=CARTESIAN_POINT('Ctrl Pts',(7.76951164020598,0.404531957204003,3.72025168374225));
#19908=CARTESIAN_POINT('Ctrl Pts',(7.81722747626884,0.454091022239626,4.18896181724392));
#19909=CARTESIAN_POINT('Ctrl Pts',(7.85185671084063,0.187425762196077,4.40318800700955));
#19910=CARTESIAN_POINT('Ctrl Pts',(7.87058066672482,0.02486112795907,4.41632944836175));
#19911=CARTESIAN_POINT('Ctrl Pts',(7.8733993439214,0.000353153796088627,
4.4161078667978));
#19912=CARTESIAN_POINT('Origin',(3.42660065607856,0.,4.));
#19913=CARTESIAN_POINT('',(7.17660065607858,-0.000163391746992416,4.4152468210878));
#19914=CARTESIAN_POINT('',(7.2733993439214,-0.000222139526412562,4.4153039283715));
#19915=CARTESIAN_POINT('',(3.42660065607856,4.87367679877478E-13,4.415875));
#19916=CARTESIAN_POINT('Ctrl Pts',(7.17660065607859,-0.000163391746992363,
4.4152468210878));
#19917=CARTESIAN_POINT('Ctrl Pts',(7.18338744278911,-0.0594844418834033,
4.41545575762517));
#19918=CARTESIAN_POINT('Ctrl Pts',(7.20607950818724,-0.257561782965025,
4.37580284351512));
#19919=CARTESIAN_POINT('Ctrl Pts',(7.24467685227299,-0.486676365692783,
4.07107270446015));
#19920=CARTESIAN_POINT('Ctrl Pts',(7.29239268833582,-0.322996137187983,
3.62908393881966));
#19921=CARTESIAN_POINT('Ctrl Pts',(7.34010852439867,0.137296434535941,3.52771310152703));
#19922=CARTESIAN_POINT('Ctrl Pts',(7.3878243604615,0.471507566988788,3.86005058906394));
#19923=CARTESIAN_POINT('Ctrl Pts',(7.43332173768814,0.377318713751663,4.29947917201381));
#19924=CARTESIAN_POINT('Ctrl Pts',(7.46291383622717,0.118587850938607,4.41527441201542));
#19925=CARTESIAN_POINT('Ctrl Pts',(7.47660065607859,-0.00030677023753798,
4.41625647512786));
#19926=CARTESIAN_POINT('Ctrl Pts',(7.2733993439214,-0.000222139526412493,
4.4153039283715));
#19927=CARTESIAN_POINT('Ctrl Pts',(7.27971732247348,-0.0554265094472961,
4.41557047734173));
#19928=CARTESIAN_POINT('Ctrl Pts',(7.30194057971316,-0.249272617462211,
4.37960776139715));
#19929=CARTESIAN_POINT('Ctrl Pts',(7.34006911564044,-0.484372034479295,
4.08537538031203));
#19930=CARTESIAN_POINT('Ctrl Pts',(7.3877849517033,-0.333780171974684,3.63875766810317));
#19931=CARTESIAN_POINT('Ctrl Pts',(7.43550078776612,0.123327161313159,3.52387434835784));
#19932=CARTESIAN_POINT('Ctrl Pts',(7.48321662382897,0.467181263150904,3.84622454030349));
#19933=CARTESIAN_POINT('Ctrl Pts',(7.52918280921405,0.385138488472668,4.29279105563264));
#19934=CARTESIAN_POINT('Ctrl Pts',(7.55924371591154,0.122630008444172,4.41546922990911));
#19935=CARTESIAN_POINT('Ctrl Pts',(7.5733993439214,-0.000257198714157839,
4.41635988094829));
#19936=CARTESIAN_POINT('Origin',(3.42660065607856,0.,4.));
#19937=CARTESIAN_POINT('',(6.87660065607859,0.000369753976522709,4.4156559906262));
#19938=CARTESIAN_POINT('',(6.9733993439214,0.000344359613660638,4.41554532105972));
#19939=CARTESIAN_POINT('',(3.42660065607856,4.87367679877478E-13,4.415875));
#19940=CARTESIAN_POINT('Ctrl Pts',(6.87660065607859,0.000369753976522759,
4.4156559906262));
#19941=CARTESIAN_POINT('Ctrl Pts',(6.88795577066343,-0.0986361616094132,
4.41481368816743));
#19942=CARTESIAN_POINT('Ctrl Pts',(6.91521616393589,-0.337621850525623,
4.32977807754403));
#19943=CARTESIAN_POINT('Ctrl Pts',(6.95838183589596,-0.486886005735063,
3.93038141845316));
#19944=CARTESIAN_POINT('Ctrl Pts',(7.0060976719588,-0.204771183672361,3.55281534000283));
#19945=CARTESIAN_POINT('Ctrl Pts',(7.05381350802163,0.265389096458903,3.58590591031157));
#19946=CARTESIAN_POINT('Ctrl Pts',(7.10152934408448,0.491837993618785,3.99926540470374));
#19947=CARTESIAN_POINT('Ctrl Pts',(7.14245839343679,0.298657604039877,4.35441002681052));
#19948=CARTESIAN_POINT('Ctrl Pts',(7.16748216410149,0.0795383202432945,
4.41496610118));
#19949=CARTESIAN_POINT('Ctrl Pts',(7.17660065607859,-0.000163391746992363,
4.4152468210878));
#19950=CARTESIAN_POINT('Ctrl Pts',(6.9733993439214,0.00034435961366068,
4.41554532105972));
#19951=CARTESIAN_POINT('Ctrl Pts',(6.9842856503478,-0.0946377878655052,
4.41480662962373));
#19952=CARTESIAN_POINT('Ctrl Pts',(7.0110772354618,-0.329510302625179,4.33529054280597));
#19953=CARTESIAN_POINT('Ctrl Pts',(7.05377409926342,-0.488725618924084,
3.94475128051735));
#19954=CARTESIAN_POINT('Ctrl Pts',(7.10148993532626,-0.21785253135038,3.55904022429238));
#19955=CARTESIAN_POINT('Ctrl Pts',(7.14920577138909,0.253078023397415,3.57826934481931));
#19956=CARTESIAN_POINT('Ctrl Pts',(7.19692160745195,0.491603063369337,3.98478019943955));
#19957=CARTESIAN_POINT('Ctrl Pts',(7.2383194649627,0.306874094293292,4.34959156107453));
#19958=CARTESIAN_POINT('Ctrl Pts',(7.26381204378586,0.0835484619188193,
4.41489945011039));
#19959=CARTESIAN_POINT('Ctrl Pts',(7.2733993439214,-0.000222139526412493,
4.4153039283715));
#19960=CARTESIAN_POINT('Origin',(3.42660065607856,0.,4.));
#19961=CARTESIAN_POINT('',(6.57660065607858,1.8302248101926E-5,4.41656360501758));
#19962=CARTESIAN_POINT('',(6.6733993439214,7.63499956435865E-5,4.4165465803965));
#19963=CARTESIAN_POINT('',(3.42660065607856,4.87367679877478E-13,4.415875));
#19964=CARTESIAN_POINT('Ctrl Pts',(6.57660065607858,1.83022481018748E-5,
4.41656360501758));
#19965=CARTESIAN_POINT('Ctrl Pts',(6.57661881985014,-0.000139156870309867,
4.41656362372179));
#19966=CARTESIAN_POINT('Ctrl Pts',(6.59254226230931,-0.138177237712184,
4.41649399470799));
#19967=CARTESIAN_POINT('Ctrl Pts',(6.62437098345609,-0.41404349770976,4.26553045144514));
#19968=CARTESIAN_POINT('Ctrl Pts',(6.67208681951894,-0.447234019333667,
3.79538894860702));
#19969=CARTESIAN_POINT('Ctrl Pts',(6.71980265558177,-0.0698021891909718,
3.51313682319347));
#19970=CARTESIAN_POINT('Ctrl Pts',(6.76751849164461,0.371772181936036,3.67798293440124));
#19971=CARTESIAN_POINT('Ctrl Pts',(6.81523432770745,0.471920133146607,4.13853999974893));
#19972=CARTESIAN_POINT('Ctrl Pts',(6.85159504918544,0.21800401543618,4.39254992240466));
#19973=CARTESIAN_POINT('Ctrl Pts',(6.87205049197582,0.0400429038769189,
4.41599351380864));
#19974=CARTESIAN_POINT('Ctrl Pts',(6.87660065607859,0.000369753976522759,
4.4156559906262));
#19975=CARTESIAN_POINT('Ctrl Pts',(6.6733993439214,7.63499956435956E-5,
4.4165465803965));
#19976=CARTESIAN_POINT('Ctrl Pts',(6.68885397822212,-0.133927014866661,
4.41622291450327));
#19977=CARTESIAN_POINT('Ctrl Pts',(6.72021389121046,-0.406451392834186,
4.27318229388465));
#19978=CARTESIAN_POINT('Ctrl Pts',(6.76747908288639,-0.453085647428837,
3.80864864857145));
#19979=CARTESIAN_POINT('Ctrl Pts',(6.81519491894923,-0.0841006081168706,
3.51540431248109));
#19980=CARTESIAN_POINT('Ctrl Pts',(6.86291075501207,0.362121456530253,3.66717299786736));
#19981=CARTESIAN_POINT('Ctrl Pts',(6.91062659107491,0.475798562415156,4.124581128109));
#19982=CARTESIAN_POINT('Ctrl Pts',(6.94745612071136,0.226294304474162,4.38932900794447));
#19983=CARTESIAN_POINT('Ctrl Pts',(6.96838037166019,0.0441344886838037,
4.41588588393584));
#19984=CARTESIAN_POINT('Ctrl Pts',(6.9733993439214,0.00034435961366068,
4.41554532105972));
#19985=CARTESIAN_POINT('Origin',(3.42660065607856,0.,4.));
#19986=CARTESIAN_POINT('',(6.27660065607859,-8.94903747701068E-6,4.41582842213685));
#19987=CARTESIAN_POINT('',(6.3733993439214,-0.000441664590319634,4.4157663968931));
#19988=CARTESIAN_POINT('',(3.42660065607856,4.87367679877478E-13,4.415875));
#19989=CARTESIAN_POINT('Ctrl Pts',(6.27660065607859,-8.94903747701223E-6,
4.41582842213685));
#19990=CARTESIAN_POINT('Ctrl Pts',(6.28118714772447,-0.0399801639742102,
4.41579747358059));
#19991=CARTESIAN_POINT('Ctrl Pts',(6.29372627871415,-0.149263049162913,
4.40013952362907));
#19992=CARTESIAN_POINT('Ctrl Pts',(6.31421804904765,-0.307151379675736,
4.3060270879454));
#19993=CARTESIAN_POINT('Ctrl Pts',(6.33807596707907,-0.416657206472865,
4.12081787696614));
#19994=CARTESIAN_POINT('Ctrl Pts',(6.36193388511048,-0.422829889105799,
3.9075587958503));
#19995=CARTESIAN_POINT('Ctrl Pts',(6.39374444248571,-0.296437506874183,
3.64987069373525));
#19996=CARTESIAN_POINT('Ctrl Pts',(6.43350763920474,0.0703302468340302,
3.51324810367198));
#19997=CARTESIAN_POINT('Ctrl Pts',(6.48122347526758,0.448014600657906,3.7964368525222));
#19998=CARTESIAN_POINT('Ctrl Pts',(6.52892114755886,0.413253290380966,4.26628466471864));
#19999=CARTESIAN_POINT('Ctrl Pts',(6.56071354116253,0.137741412285014,4.41654724519979));
#20000=CARTESIAN_POINT('Ctrl Pts',(6.57660065607858,1.83022481018748E-5,
4.41656360501758));
#20001=CARTESIAN_POINT('Ctrl Pts',(6.3733993439214,-0.000441664590319611,
4.4157663968931));
#20002=CARTESIAN_POINT('Ctrl Pts',(6.37751702740883,-0.0362476131304844,
4.41610293027605));
#20003=CARTESIAN_POINT('Ctrl Pts',(6.39753998958387,-0.210006484715375,
4.39546152579387));
#20004=CARTESIAN_POINT('Ctrl Pts',(6.43346823044653,-0.468271923807345,
4.15124960425567));
#20005=CARTESIAN_POINT('Ctrl Pts',(6.48118406650937,-0.380227249479543,
3.6882349865083));
#20006=CARTESIAN_POINT('Ctrl Pts',(6.52889990257221,0.0564566449812287,
3.51140415777354));
#20007=CARTESIAN_POINT('Ctrl Pts',(6.57661573863504,0.441574375138847,3.78331933667001));
#20008=CARTESIAN_POINT('Ctrl Pts',(6.62433157469789,0.421040068198854,4.25418342072721));
#20009=CARTESIAN_POINT('Ctrl Pts',(6.65659277646,0.145792717270209,4.41473316952435));
#20010=CARTESIAN_POINT('Ctrl Pts',(6.6729486995345,0.00398377756883227,
4.41655601822694));
#20011=CARTESIAN_POINT('Ctrl Pts',(6.6733993439214,7.63499956435956E-5,
4.4165465803965));
#20012=CARTESIAN_POINT('Origin',(3.42660065607856,0.,4.));
#20013=CARTESIAN_POINT('',(5.97660065607859,-9.19412645702589E-6,4.41589218083175));
#20014=CARTESIAN_POINT('',(6.0733993439214,-6.65563173402051E-6,4.41590255337155));
#20015=CARTESIAN_POINT('',(3.42660065607856,4.87367679877478E-13,4.415875));
#20016=CARTESIAN_POINT('Ctrl Pts',(5.97660065607858,-9.19412645705893E-6,
4.41589218083175));
#20017=CARTESIAN_POINT('Ctrl Pts',(5.97780283625498,-0.0104787976275591,
4.4159022685469));
#20018=CARTESIAN_POINT('Ctrl Pts',(5.98695765577519,-0.0902010538040918,
4.41295272969856));
#20019=CARTESIAN_POINT('Ctrl Pts',(6.0040651146392,-0.23587461323539,4.36380751861078));
#20020=CARTESIAN_POINT('Ctrl Pts',(6.02792303267061,-0.381351759249696,
4.20630938167977));
#20021=CARTESIAN_POINT('Ctrl Pts',(6.05178095070204,-0.433578399193506,
3.9983625870902));
#20022=CARTESIAN_POINT('Ctrl Pts',(6.07563886873346,-0.379782579589031,
3.79081692866841));
#20023=CARTESIAN_POINT('Ctrl Pts',(6.09949678676487,-0.233120953551068,
3.63442082419035));
#20024=CARTESIAN_POINT('Ctrl Pts',(6.12335470479629,-0.0294522997972467,
3.5674214393556));
#20025=CARTESIAN_POINT('Ctrl Pts',(6.14721262282771,0.181413325723775,3.60619428643423));
#20026=CARTESIAN_POINT('Ctrl Pts',(6.17107054085913,0.347927737305898,3.74127281623538));
#20027=CARTESIAN_POINT('Ctrl Pts',(6.19492845889055,0.429346806292137,3.93959933010928));
#20028=CARTESIAN_POINT('Ctrl Pts',(6.21878637692197,0.405811992579865,4.15272917617017));
#20029=CARTESIAN_POINT('Ctrl Pts',(6.24264429495339,0.282982581651336,4.32844890303245));
#20030=CARTESIAN_POINT('Ctrl Pts',(6.26191572133893,0.127967070080381,4.40561019629887));
#20031=CARTESIAN_POINT('Ctrl Pts',(6.27323450838066,0.029326984292613,4.415851136102));
#20032=CARTESIAN_POINT('Ctrl Pts',(6.27660065607859,-8.94903747701223E-6,
4.41582842213685));
#20033=CARTESIAN_POINT('Ctrl Pts',(6.0733993439214,-6.65563173397714E-6,
4.41590255337156));
#20034=CARTESIAN_POINT('Ctrl Pts',(6.07413271593935,-0.00639299139291402,
4.41590724351385));
#20035=CARTESIAN_POINT('Ctrl Pts',(6.0828187273011,-0.0820297780542147,
4.41420140028919));
#20036=CARTESIAN_POINT('Ctrl Pts',(6.09945737800665,-0.2250554921608,4.3705991908187));
#20037=CARTESIAN_POINT('Ctrl Pts',(6.12331529603809,-0.375113923638194,
4.21744656883549));
#20038=CARTESIAN_POINT('Ctrl Pts',(6.1471732140695,-0.433431396087355,4.01114207710762));
#20039=CARTESIAN_POINT('Ctrl Pts',(6.17103113210093,-0.385792139046387,
3.80207577201042));
#20040=CARTESIAN_POINT('Ctrl Pts',(6.19488905013233,-0.243761337718234,
3.64147770828707));
#20041=CARTESIAN_POINT('Ctrl Pts',(6.21874696816376,-0.042227823444436,
3.56841523311022));
#20042=CARTESIAN_POINT('Ctrl Pts',(6.24260488619517,0.16982704650124,3.60113783246665));
#20043=CARTESIAN_POINT('Ctrl Pts',(6.2664628042266,0.339985970990829,3.73091992247201));
#20044=CARTESIAN_POINT('Ctrl Pts',(6.29032072225801,0.427700638223926,3.92738904240251));
#20045=CARTESIAN_POINT('Ctrl Pts',(6.31417864028943,0.409561128158778,4.13996490148311));
#20046=CARTESIAN_POINT('Ctrl Pts',(6.34187151417723,0.27471212230801,4.35031587281991));
#20047=CARTESIAN_POINT('Ctrl Pts',(6.36161174872122,0.102059178040878,4.41480301073152));
#20048=CARTESIAN_POINT('Ctrl Pts',(6.3733993439214,-0.000441664590319611,
4.4157663968931));
#20049=CARTESIAN_POINT('Origin',(3.42660065607856,0.,4.));
#20050=CARTESIAN_POINT('',(5.67660065607858,1.06631253201556E-5,4.41586554077139));
#20051=CARTESIAN_POINT('',(5.7733993439214,9.17748676071416E-6,4.4158542849441));
#20052=CARTESIAN_POINT('',(3.42660065607856,4.87367679877478E-13,4.415875));
#20053=CARTESIAN_POINT('Ctrl Pts',(5.67660065607858,1.06631253201268E-5,
4.41586554077139));
#20054=CARTESIAN_POINT('Ctrl Pts',(5.68237116412931,-0.050253077703417,
4.41581669384736));
#20055=CARTESIAN_POINT('Ctrl Pts',(5.69609431152383,-0.169828933264711,
4.3941204493343));
#20056=CARTESIAN_POINT('Ctrl Pts',(5.71777009826218,-0.329222253834466,
4.28214440376531));
#20057=CARTESIAN_POINT('Ctrl Pts',(5.74162801629359,-0.424158110434281,
4.08990358344764));
#20058=CARTESIAN_POINT('Ctrl Pts',(5.76548593432501,-0.415375755386326,
3.8756788878607));
#20059=CARTESIAN_POINT('Ctrl Pts',(5.78934385235642,-0.305022713182347,
3.69185409099321));
#20060=CARTESIAN_POINT('Ctrl Pts',(5.81320177038785,-0.120083309624962,
3.58337936191985));
#20061=CARTESIAN_POINT('Ctrl Pts',(5.83705968841926,0.0942197354074567,
3.57677972866706));
#20062=CARTESIAN_POINT('Ctrl Pts',(5.86091760645069,0.285483486244351,3.673668977605));
#20063=CARTESIAN_POINT('Ctrl Pts',(5.8847755244821,0.406938752801468,3.85035505520226));
#20064=CARTESIAN_POINT('Ctrl Pts',(5.90863344251353,0.428886400972996,4.06363338935351));
#20065=CARTESIAN_POINT('Ctrl Pts',(5.93249136054494,0.345959657594393,4.261351642888));
#20066=CARTESIAN_POINT('Ctrl Pts',(5.95514709839996,0.186877681905787,4.38841966610496));
#20067=CARTESIAN_POINT('Ctrl Pts',(5.96985019691118,0.0587795235055939,
4.41583553648629));
#20068=CARTESIAN_POINT('Ctrl Pts',(5.97660065607858,-9.19412645705893E-6,
4.41589218083175));
#20069=CARTESIAN_POINT('Ctrl Pts',(5.7733993439214,9.17748676073846E-6,
4.4158542849441));
#20070=CARTESIAN_POINT('Ctrl Pts',(5.77870104381367,-0.0461746181927863,
4.41581721944429));
#20071=CARTESIAN_POINT('Ctrl Pts',(5.79195538304975,-0.161664917198308,
4.3966319946429));
#20072=CARTESIAN_POINT('Ctrl Pts',(5.81316236162963,-0.320769768688322,
4.29171820750724));
#20073=CARTESIAN_POINT('Ctrl Pts',(5.83702027966105,-0.421326288178809,
4.10235681181338));
#20074=CARTESIAN_POINT('Ctrl Pts',(5.86087819769247,-0.418857046020503,
3.88796639709818));
#20075=CARTESIAN_POINT('Ctrl Pts',(5.88473611572389,-0.313965860818636,
3.70097123187977));
#20076=CARTESIAN_POINT('Ctrl Pts',(5.90859403375531,-0.132301443679057,
3.58709678011166));
#20077=CARTESIAN_POINT('Ctrl Pts',(5.93245195178673,0.0817142298265842,
3.57418834816524));
#20078=CARTESIAN_POINT('Ctrl Pts',(5.95630986981814,0.275748643515392,3.66540258613358));
#20079=CARTESIAN_POINT('Ctrl Pts',(5.98016778784957,0.402354822815078,3.83843477537114));
#20080=CARTESIAN_POINT('Ctrl Pts',(6.00402570588098,0.430574627524036,4.05097449853386));
#20081=CARTESIAN_POINT('Ctrl Pts',(6.02788362391241,0.353506566116634,4.25104874587108));
#20082=CARTESIAN_POINT('Ctrl Pts',(6.05100816992587,0.195023852357142,4.38547315270063));
#20083=CARTESIAN_POINT('Ctrl Pts',(6.06618007659554,0.06286002589468,4.4158563839102));
#20084=CARTESIAN_POINT('Ctrl Pts',(6.0733993439214,-6.65563173397714E-6,
4.41590255337156));
#20085=CARTESIAN_POINT('Origin',(3.42660065607856,0.,4.));
#20086=CARTESIAN_POINT('',(5.37660065607858,-1.01751121954902E-5,4.41586038335289));
#20087=CARTESIAN_POINT('',(5.4733993439214,-1.09014992595302E-5,4.41587264340464));
#20088=CARTESIAN_POINT('',(3.42660065607856,4.87367679877478E-13,4.415875));
#20089=CARTESIAN_POINT('Ctrl Pts',(5.37660065607859,-1.01751121954468E-5,
4.41586038335289));
#20090=CARTESIAN_POINT('Ctrl Pts',(5.37898685265982,-0.0207957689391596,
4.41587928195339));
#20091=CARTESIAN_POINT('Ctrl Pts',(5.38932568858487,-0.110842971866809,
4.40924760552439));
#20092=CARTESIAN_POINT('Ctrl Pts',(5.40761716385372,-0.26226226804932,4.34526983614494));
#20093=CARTESIAN_POINT('Ctrl Pts',(5.43147508188515,-0.395631058815178,
4.17739453851434));
#20094=CARTESIAN_POINT('Ctrl Pts',(5.45533299991656,-0.432257278927009,
3.96614144408682));
#20095=CARTESIAN_POINT('Ctrl Pts',(5.47919091794798,-0.363184819889405,
3.76316768886851));
#20096=CARTESIAN_POINT('Ctrl Pts',(5.5030488359794,-0.205303779432806,3.61810588490468));
#20097=CARTESIAN_POINT('Ctrl Pts',(5.52690675401082,0.00277962745745752,
3.56642759466814));
#20098=CARTESIAN_POINT('Ctrl Pts',(5.55076467204224,0.210183339719457,3.62076956781107));
#20099=CARTESIAN_POINT('Ctrl Pts',(5.57462259007365,0.36619150013966,3.76784371165257));
#20100=CARTESIAN_POINT('Ctrl Pts',(5.59848050810508,0.432655863921731,3.97168639180759));
#20101=CARTESIAN_POINT('Ctrl Pts',(5.62233842613649,0.393324083661671,4.18245252040861));
#20102=CARTESIAN_POINT('Ctrl Pts',(5.64619634416792,0.257813851021257,4.34860403787086));
#20103=CARTESIAN_POINT('Ctrl Pts',(5.66428375414861,0.107285005985459,4.40994309575933));
#20104=CARTESIAN_POINT('Ctrl Pts',(5.6744185247855,0.0190180158238588,4.41588401235146));
#20105=CARTESIAN_POINT('Ctrl Pts',(5.67660065607858,1.06631253201268E-5,
4.41586554077139));
#20106=CARTESIAN_POINT('Ctrl Pts',(5.4733993439214,-1.0901499259525E-5,
4.41587264340464));
#20107=CARTESIAN_POINT('Ctrl Pts',(5.47531673234419,-0.0167114040746605,
4.41588973972128));
#20108=CARTESIAN_POINT('Ctrl Pts',(5.48518676011079,-0.102669266038577,
4.41080986982701));
#20109=CARTESIAN_POINT('Ctrl Pts',(5.50300942722118,-0.251979671819092,
4.35284416104532));
#20110=CARTESIAN_POINT('Ctrl Pts',(5.52686734525261,-0.390234841353927,
4.18896964197264));
#20111=CARTESIAN_POINT('Ctrl Pts',(5.55072526328402,-0.433066962396004,
3.97888689800548));
#20112=CARTESIAN_POINT('Ctrl Pts',(5.57458318131544,-0.370002414621403,
3.77396688259));
#20113=CARTESIAN_POINT('Ctrl Pts',(5.59844109934686,-0.21646219781534,3.62431812139094));
#20114=CARTESIAN_POINT('Ctrl Pts',(5.62229901737828,-0.00999107731853999,
3.56653381289738));
#20115=CARTESIAN_POINT('Ctrl Pts',(5.64615693540971,0.198923133709572,3.61474379450078));
#20116=CARTESIAN_POINT('Ctrl Pts',(5.67001485344111,0.359195220034686,3.75715941257656));
#20117=CARTESIAN_POINT('Ctrl Pts',(5.69387277147254,0.431634290692432,3.95895616900985));
#20118=CARTESIAN_POINT('Ctrl Pts',(5.71773068950395,0.398527019959163,4.1707892603438));
#20119=CARTESIAN_POINT('Ctrl Pts',(5.74158860753538,0.267969036875697,4.34085972491723));
#20120=CARTESIAN_POINT('Ctrl Pts',(5.76014482567452,0.115458993192439,4.40830959117706));
#20121=CARTESIAN_POINT('Ctrl Pts',(5.77074840446986,0.0231018550196917,
4.41587281831976));
#20122=CARTESIAN_POINT('Ctrl Pts',(5.7733993439214,9.17748676073846E-6,
4.4158542849441));
#20123=CARTESIAN_POINT('Origin',(3.42660065607856,0.,4.));
#20124=CARTESIAN_POINT('',(5.07660065607859,8.10857529294212E-6,4.41589722116852));
#20125=CARTESIAN_POINT('',(5.1733993439214,1.02299162792543E-5,4.4158851107878));
#20126=CARTESIAN_POINT('',(3.42660065607856,4.87367679877478E-13,4.415875));
#20127=CARTESIAN_POINT('Ctrl Pts',(5.07660065607858,8.10857529294148E-6,
4.41589722116852));
#20128=CARTESIAN_POINT('Ctrl Pts',(5.08355518053415,-0.060555656273516,
4.41584370653314));
#20129=CARTESIAN_POINT('Ctrl Pts',(5.09846234433351,-0.190424342306974,
4.38715451669839));
#20130=CARTESIAN_POINT('Ctrl Pts',(5.1213221474767,-0.349282119693095,4.256894448863));
#20131=CARTESIAN_POINT('Ctrl Pts',(5.1451800655081,-0.4296670234643,4.05812921762123));
#20132=CARTESIAN_POINT('Ctrl Pts',(5.16903798353954,-0.404986636103755,
3.84514980926298));
#20133=CARTESIAN_POINT('Ctrl Pts',(5.19289590157095,-0.281275984601366,
3.67003549057442));
#20134=CARTESIAN_POINT('Ctrl Pts',(5.21675381960238,-0.0887856930599551,
3.5756064824932));
#20135=CARTESIAN_POINT('Ctrl Pts',(5.24061173763379,0.125415118908336,3.58495324968971));
#20136=CARTESIAN_POINT('Ctrl Pts',(5.26446965566521,0.308948518064291,3.69579025298356));
#20137=CARTESIAN_POINT('Ctrl Pts',(5.28832757369662,0.416935588964862,3.88101482593007));
#20138=CARTESIAN_POINT('Ctrl Pts',(5.31218549172805,0.422970551266107,4.09533451502773));
#20139=CARTESIAN_POINT('Ctrl Pts',(5.33604340975946,0.325577692296299,4.28634231834109));
#20140=CARTESIAN_POINT('Ctrl Pts',(5.35751513120965,0.166275769440666,4.39523064161658));
#20141=CARTESIAN_POINT('Ctrl Pts',(5.37103421331602,0.0484777907299229,
4.41581629730449));
#20142=CARTESIAN_POINT('Ctrl Pts',(5.37660065607859,-1.01751121954468E-5,
4.41586038335289));
#20143=CARTESIAN_POINT('Ctrl Pts',(5.1733993439214,1.02299162792474E-5,
4.4158851107878));
#20144=CARTESIAN_POINT('Ctrl Pts',(5.17988506021851,-0.0564756498766958,
4.41582730150705));
#20145=CARTESIAN_POINT('Ctrl Pts',(5.19432341585943,-0.182274442988225,
4.39002065289559));
#20146=CARTESIAN_POINT('Ctrl Pts',(5.21671441084416,-0.341564590845109,
4.26707000444592));
#20147=CARTESIAN_POINT('Ctrl Pts',(5.24057232887557,-0.427768622694993,
4.07075847957352));
#20148=CARTESIAN_POINT('Ctrl Pts',(5.264430246907,-0.409371574112622,3.85714457902312));
#20149=CARTESIAN_POINT('Ctrl Pts',(5.2882881649384,-0.290872024601924,3.6784627202051));
#20150=CARTESIAN_POINT('Ctrl Pts',(5.31214608296984,-0.101246341881189,
3.57840548479658));
#20151=CARTESIAN_POINT('Ctrl Pts',(5.33600400100125,0.113136829324483,3.58143959235932));
#20152=CARTESIAN_POINT('Ctrl Pts',(5.35986191903268,0.299854963974951,3.68682312094679));
#20153=CARTESIAN_POINT('Ctrl Pts',(5.38371983706408,0.413250392048343,3.8687869272297));
#20154=CARTESIAN_POINT('Ctrl Pts',(5.40757775509551,0.425594842551202,4.08283590397723));
#20155=CARTESIAN_POINT('Ctrl Pts',(5.43143567312693,0.333869761079625,4.27662924579771));
#20156=CARTESIAN_POINT('Ctrl Pts',(5.45337620273556,0.174437273907163,4.39264091290779));
#20157=CARTESIAN_POINT('Ctrl Pts',(5.46736409300038,0.0525562895569378,
4.41581883033293));
#20158=CARTESIAN_POINT('Ctrl Pts',(5.4733993439214,-1.0901499259525E-5,
4.41587264340464));
#20159=CARTESIAN_POINT('Origin',(3.42660065607856,0.,4.));
#20160=CARTESIAN_POINT('',(4.77660065607858,-3.27394476109793E-6,4.41584059078716));
#20161=CARTESIAN_POINT('',(4.8733993439214,-6.67049670156904E-6,4.4158459349409));
#20162=CARTESIAN_POINT('',(3.42660065607856,4.87367679877478E-13,4.415875));
#20163=CARTESIAN_POINT('Ctrl Pts',(4.77660065607858,-3.27394476113199E-6,
4.41584059078717));
#20164=CARTESIAN_POINT('Ctrl Pts',(4.78017086906467,-0.0311067951354469,
4.4158491206715));
#20165=CARTESIAN_POINT('Ctrl Pts',(4.79169372139456,-0.131487321212171,
4.40473555835468));
#20166=CARTESIAN_POINT('Ctrl Pts',(4.81116921306824,-0.287199161490599,
4.32482210305491));
#20167=CARTESIAN_POINT('Ctrl Pts',(4.83502713109967,-0.407721671464292,
4.14749845969467));
#20168=CARTESIAN_POINT('Ctrl Pts',(4.85888504913109,-0.42854512664958,3.93410742516172));
#20169=CARTESIAN_POINT('Ctrl Pts',(4.8827429671625,-0.344577625034195,3.73682892005441));
#20170=CARTESIAN_POINT('Ctrl Pts',(4.90660088519393,-0.176351507991885,
3.60390291263011));
#20171=CARTESIAN_POINT('Ctrl Pts',(4.93045880322534,0.0349973564730633,
3.56783343253575));
#20172=CARTESIAN_POINT('Ctrl Pts',(4.95431672125677,0.237788413971502,3.63744045016736));
#20173=CARTESIAN_POINT('Ctrl Pts',(4.97817463928818,0.382433727027559,3.79570315365689));
#20174=CARTESIAN_POINT('Ctrl Pts',(5.0020325573196,0.433563576539811,4.00392200101168));
#20175=CARTESIAN_POINT('Ctrl Pts',(5.02589047535102,0.378675321553375,4.21118181228595));
#20176=CARTESIAN_POINT('Ctrl Pts',(5.04974839338244,0.231190635538481,4.36680191797922));
#20177=CARTESIAN_POINT('Ctrl Pts',(5.0666517869583,0.086644022961884,4.4135113916189));
#20178=CARTESIAN_POINT('Ctrl Pts',(5.07560254119034,0.00870023350343714,
4.41590490160082));
#20179=CARTESIAN_POINT('Ctrl Pts',(5.07660065607858,8.10857529294148E-6,
4.41589722116852));
#20180=CARTESIAN_POINT('Ctrl Pts',(4.8733993439214,-6.67049670157252E-6,
4.41584593494091));
#20181=CARTESIAN_POINT('Ctrl Pts',(4.87650074874903,-0.0270249643080214,
4.41586127519519));
#20182=CARTESIAN_POINT('Ctrl Pts',(4.88755479292047,-0.123313358466266,
4.40662010077424));
#20183=CARTESIAN_POINT('Ctrl Pts',(4.90656147643571,-0.277507970732168,
4.33313973520738));
#20184=CARTESIAN_POINT('Ctrl Pts',(4.93041939446713,-0.403200703213916,
4.15944262266324));
#20185=CARTESIAN_POINT('Ctrl Pts',(4.95427731249855,-0.430299880793222,
3.94675744574809));
#20186=CARTESIAN_POINT('Ctrl Pts',(4.97813523052996,-0.352179016385168,
3.7470915236456));
#20187=CARTESIAN_POINT('Ctrl Pts',(5.00199314856139,-0.187940789307144,
3.60926861310034));
#20188=CARTESIAN_POINT('Ctrl Pts',(5.0258510665928,0.0222540801607904,3.56699016996131));
#20189=CARTESIAN_POINT('Ctrl Pts',(5.04970898462423,0.227007220840439,3.63059442521772));
#20190=CARTESIAN_POINT('Ctrl Pts',(5.07356690265564,0.376250912472057,3.7845284059142));
#20191=CARTESIAN_POINT('Ctrl Pts',(5.09742482068706,0.433491007135177,3.99115106069306));
#20192=CARTESIAN_POINT('Ctrl Pts',(5.12128273871848,0.384730742495793,4.19993752217271));
#20193=CARTESIAN_POINT('Ctrl Pts',(5.1451406567499,0.241893331461176,4.35983381329239));
#20194=CARTESIAN_POINT('Ctrl Pts',(5.16251285848421,0.0948160588051851,
4.41219316122439));
#20195=CARTESIAN_POINT('Ctrl Pts',(5.17193242087471,0.0127860645481494,
4.41589818594594));
#20196=CARTESIAN_POINT('Ctrl Pts',(5.1733993439214,1.02299162792474E-5,
4.4158851107878));
#20197=CARTESIAN_POINT('Origin',(3.42660065607856,0.,4.));
#20198=CARTESIAN_POINT('',(4.47660065607858,-1.72413508574122E-6,4.41591032029986));
#20199=CARTESIAN_POINT('',(4.5733993439214,2.6062779713001E-6,4.4159095790646));
#20200=CARTESIAN_POINT('',(3.42660065607856,4.87367679877478E-13,4.415875));
#20201=CARTESIAN_POINT('Ctrl Pts',(4.47660065607858,-1.72413508575881E-6,
4.41591032029986));
#20202=CARTESIAN_POINT('Ctrl Pts',(4.47678655759518,-0.00162050728124812,
4.41591069657345));
#20203=CARTESIAN_POINT('Ctrl Pts',(4.48492509845559,-0.0724886630755744,
4.4155056303295));
#20204=CARTESIAN_POINT('Ctrl Pts',(4.5010162786598,-0.212178818846594,4.37811758201071));
#20205=CARTESIAN_POINT('Ctrl Pts',(4.52487419669122,-0.367409789343613,
4.23022337776645));
#20206=CARTESIAN_POINT('Ctrl Pts',(4.54873211472264,-0.432799058467291,
4.02603328640456));
#20207=CARTESIAN_POINT('Ctrl Pts',(4.57259003275406,-0.392357168499796,
3.8154773474345));
#20208=CARTESIAN_POINT('Ctrl Pts',(4.59644795078547,-0.255973263285106,
3.65004222328625));
#20209=CARTESIAN_POINT('Ctrl Pts',(4.6203058688169,-0.0569969226013119,
3.57018130821703));
#20210=CARTESIAN_POINT('Ctrl Pts',(4.64416378684831,0.155916718210686,3.59542277130738));
#20211=CARTESIAN_POINT('Ctrl Pts',(4.66802170487973,0.330704474340828,3.71959438727947));
#20212=CARTESIAN_POINT('Ctrl Pts',(4.69187962291115,0.424625978282027,3.91233281365517));
#20213=CARTESIAN_POINT('Ctrl Pts',(4.71573754094257,0.41471486395576,4.1265082550995));
#20214=CARTESIAN_POINT('Ctrl Pts',(4.73959545897399,0.303394668785218,4.30974898215573));
#20215=CARTESIAN_POINT('Ctrl Pts',(4.75988316401932,0.145646585585232,4.40116103141851));
#20216=CARTESIAN_POINT('Ctrl Pts',(4.77221822972086,0.0381762104768988,
4.41583012037823));
#20217=CARTESIAN_POINT('Ctrl Pts',(4.77660065607858,-3.27394476113199E-6,
4.41584059078717));
#20218=CARTESIAN_POINT('Ctrl Pts',(4.5733993439214,2.60627797130011E-6,
4.4159095790646));
#20219=CARTESIAN_POINT('Ctrl Pts',(4.58106907662335,-0.0667838229435618,
4.4158868274511));
#20220=CARTESIAN_POINT('Ctrl Pts',(4.59669144866912,-0.202842099803805,
4.38250385602613));
#20221=CARTESIAN_POINT('Ctrl Pts',(4.62026646005868,-0.360469908510665,
4.24094439618412));
#20222=CARTESIAN_POINT('Ctrl Pts',(4.6441243780901,-0.431844582779732,4.03876871570463));
#20223=CARTESIAN_POINT('Ctrl Pts',(4.66798229612152,-0.397621493350665,
3.82711302819544));
#20224=CARTESIAN_POINT('Ctrl Pts',(4.69184021415294,-0.266169117804412,
3.65773291463971));
#20225=CARTESIAN_POINT('Ctrl Pts',(4.71569813218436,-0.0696311426542753,
3.57204642662242));
#20226=CARTESIAN_POINT('Ctrl Pts',(4.73955605021577,0.143933543589337,3.59100624451743));
#20227=CARTESIAN_POINT('Ctrl Pts',(4.76341396824719,0.322302557754209,3.70997617639404));
#20228=CARTESIAN_POINT('Ctrl Pts',(4.78727188627862,0.421859817202848,3.8998648332327));
#20229=CARTESIAN_POINT('Ctrl Pts',(4.81112980431003,0.41826086011465,4.11423926597311));
#20230=CARTESIAN_POINT('Ctrl Pts',(4.83498772234146,0.312385729531365,4.30067908636799));
#20231=CARTESIAN_POINT('Ctrl Pts',(4.85574423554524,0.15381688120809,4.39891624198015));
#20232=CARTESIAN_POINT('Ctrl Pts',(4.86854810940522,0.04225549351942,4.41582193963064));
#20233=CARTESIAN_POINT('Ctrl Pts',(4.8733993439214,-6.67049670157252E-6,
4.41584593494091));
#20234=CARTESIAN_POINT('Origin',(3.42660065607856,0.,4.));
#20235=CARTESIAN_POINT('',(4.17660065607858,5.88453344125852E-6,4.41584444980552));
#20236=CARTESIAN_POINT('',(4.2733993439214,2.51014653358805E-6,4.41583996132385));
#20237=CARTESIAN_POINT('',(3.42660065607856,4.87367679877478E-13,4.415875));
#20238=CARTESIAN_POINT('Ctrl Pts',(4.17660065607858,5.88453344126799E-6,
4.41584444980552));
#20239=CARTESIAN_POINT('Ctrl Pts',(4.18135488546951,-0.0414115481342504,
4.41582334930757));
#20240=CARTESIAN_POINT('Ctrl Pts',(4.19406175420423,-0.152126265423154,
4.3993918905015));
#20241=CARTESIAN_POINT('Ctrl Pts',(4.21472126228278,-0.310547447266788,
4.30257739619942));
#20242=CARTESIAN_POINT('Ctrl Pts',(4.23857918031418,-0.417556725585918,
4.11678647978038));
#20243=CARTESIAN_POINT('Ctrl Pts',(4.26243709834561,-0.422462345057068,
3.90243789311793));
#20244=CARTESIAN_POINT('Ctrl Pts',(4.28629501637703,-0.324064236326554,
3.71194600226016));
#20245=CARTESIAN_POINT('Ctrl Pts',(4.31015293440845,-0.146423688323203,
3.59189110566319));
#20246=CARTESIAN_POINT('Ctrl Pts',(4.33401085243986,0.0670214896752265,
3.5716299793216));
#20247=CARTESIAN_POINT('Ctrl Pts',(4.35786877047129,0.264078061498623,3.65611697628114));
#20248=CARTESIAN_POINT('Ctrl Pts',(4.38172668850271,0.396560367883193,3.82469274783887));
#20249=CARTESIAN_POINT('Ctrl Pts',(4.40558460653412,0.432072854850341,4.03613591352675));
#20250=CARTESIAN_POINT('Ctrl Pts',(4.42944252456555,0.361931763288092,4.23874286631049));
#20251=CARTESIAN_POINT('Ctrl Pts',(4.45311454108036,0.204524647174786,4.38184685695289));
#20252=CARTESIAN_POINT('Ctrl Pts',(4.46883391825138,0.0676290543833733,
4.4158946000499));
#20253=CARTESIAN_POINT('Ctrl Pts',(4.47660065607858,-1.72413508575881E-6,
4.41591032029986));
#20254=CARTESIAN_POINT('Ctrl Pts',(4.2733993439214,2.51014653359152E-6,
4.41583996132385));
#20255=CARTESIAN_POINT('Ctrl Pts',(4.27768476515387,-0.0373320337329404,
4.41583213221101));
#20256=CARTESIAN_POINT('Ctrl Pts',(4.28992282573015,-0.143955736965383,
4.40160880992953));
#20257=CARTESIAN_POINT('Ctrl Pts',(4.31011352565024,-0.301501118270308,
4.3115924136571));
#20258=CARTESIAN_POINT('Ctrl Pts',(4.33397144368164,-0.413936097932681,
4.12903358037428));
#20259=CARTESIAN_POINT('Ctrl Pts',(4.35782936171308,-0.425152419412173,
3.91492252699502));
#20260=CARTESIAN_POINT('Ctrl Pts',(4.38168727974448,-0.332407397051365,
3.72161523052345));
#20261=CARTESIAN_POINT('Ctrl Pts',(4.40554519777592,-0.158379709595794,
3.5963805946708));
#20262=CARTESIAN_POINT('Ctrl Pts',(4.42940311580732,0.0543761300157755,
3.56984189703405));
#20263=CARTESIAN_POINT('Ctrl Pts',(4.45326103383876,0.25383552520097,3.64848857324589));
#20264=CARTESIAN_POINT('Ctrl Pts',(4.47711895187016,0.39122521984844,3.81308936806525));
#20265=CARTESIAN_POINT('Ctrl Pts',(4.50097686990159,0.432949691632991,4.02339490384879));
#20266=CARTESIAN_POINT('Ctrl Pts',(4.524834787933,0.368806170420464,4.22797974831721));
#20267=CARTESIAN_POINT('Ctrl Pts',(4.54869270596443,0.214479494504121,4.37681733431002));
#20268=CARTESIAN_POINT('Ctrl Pts',(4.56488089129389,0.0741790848482271,
4.4152866170047));
#20269=CARTESIAN_POINT('Ctrl Pts',(4.57311643727954,0.0024660981813593,
4.41591041828323));
#20270=CARTESIAN_POINT('Ctrl Pts',(4.5733993439214,2.60627797130011E-6,
4.4159095790646));
#20271=CARTESIAN_POINT('Ctrl Pts',(3.95224475517895,0.178288362465424,4.37571967666652));
#20272=CARTESIAN_POINT('Ctrl Pts',(3.96019739452275,0.115708609995841,4.40541533085819));
#20273=CARTESIAN_POINT('Ctrl Pts',(3.97610267321037,-0.0245105356436035,
4.43290545314371));
#20274=CARTESIAN_POINT('Ctrl Pts',(3.99996059124178,-0.228962993402626,
4.36819499612132));
#20275=CARTESIAN_POINT('Ctrl Pts',(4.0238185092732,-0.377374743411151,4.21349068386271));
#20276=CARTESIAN_POINT('Ctrl Pts',(4.04767642730463,-0.433534992178268,
4.00656196868444));
#20277=CARTESIAN_POINT('Ctrl Pts',(4.07153434533603,-0.383670022685343,
3.79803920418254));
#20278=CARTESIAN_POINT('Ctrl Pts',(4.09539226336747,-0.239994733226421,
3.63889579340969));
#20279=CARTESIAN_POINT('Ctrl Pts',(4.11925018139887,-0.0376302499649443,
3.56805514133307));
#20280=CARTESIAN_POINT('Ctrl Pts',(4.1431080994303,0.173933765839147,3.60283521426327));
#20281=CARTESIAN_POINT('Ctrl Pts',(4.16696601746172,0.342967344134064,3.73473372141871));
#20282=CARTESIAN_POINT('Ctrl Pts',(4.19082393549313,0.428135478754777,3.93149662217858));
#20283=CARTESIAN_POINT('Ctrl Pts',(4.21468185352456,0.40861313688017,4.1450106963618));
#20284=CARTESIAN_POINT('Ctrl Pts',(4.23853977155597,0.289173588337559,4.32306558264197));
#20285=CARTESIAN_POINT('Ctrl Pts',(4.2623976895874,0.0990233075312312,4.42212219878201));
#20286=CARTESIAN_POINT('Ctrl Pts',(4.28625560761881,-0.115340915390822,
4.41795840454656));
#20287=CARTESIAN_POINT('Ctrl Pts',(4.31011352565024,-0.301501118270308,
4.3115924136571));
#20288=CARTESIAN_POINT('Ctrl Pts',(4.33397144368164,-0.413936097932681,
4.12903358037428));
#20289=CARTESIAN_POINT('Ctrl Pts',(4.35782936171308,-0.425152419412173,
3.91492252699502));
#20290=CARTESIAN_POINT('Ctrl Pts',(4.38168727974448,-0.332407397051365,
3.72161523052345));
#20291=CARTESIAN_POINT('Ctrl Pts',(4.40554519777592,-0.158379709595794,
3.5963805946708));
#20292=CARTESIAN_POINT('Ctrl Pts',(4.42940311580732,0.0543761300157755,
3.56984189703405));
#20293=CARTESIAN_POINT('Ctrl Pts',(4.45326103383876,0.25383552520097,3.64848857324589));
#20294=CARTESIAN_POINT('Ctrl Pts',(4.47711895187016,0.39122521984844,3.81308936806525));
#20295=CARTESIAN_POINT('Ctrl Pts',(4.50097686990159,0.432949691632991,4.02339490384879));
#20296=CARTESIAN_POINT('Ctrl Pts',(4.524834787933,0.368806170420464,4.22797974831721));
#20297=CARTESIAN_POINT('Ctrl Pts',(4.54869270596443,0.214479494504121,4.37681733431002));
#20298=CARTESIAN_POINT('Ctrl Pts',(4.57255062399584,0.00770673985495463,
4.4335128177492));
#20299=CARTESIAN_POINT('Ctrl Pts',(4.59640854202726,-0.200950522604244,
4.38420260860549));
#20300=CARTESIAN_POINT('Ctrl Pts',(4.62026646005868,-0.360469908510665,
4.24094439618412));
#20301=CARTESIAN_POINT('Ctrl Pts',(4.6441243780901,-0.431844582779732,4.03876871570463));
#20302=CARTESIAN_POINT('Ctrl Pts',(4.66798229612152,-0.397621493350665,
3.82711302819544));
#20303=CARTESIAN_POINT('Ctrl Pts',(4.69184021415294,-0.266169117804412,
3.65773291463971));
#20304=CARTESIAN_POINT('Ctrl Pts',(4.71569813218436,-0.0696311426542753,
3.57204642662242));
#20305=CARTESIAN_POINT('Ctrl Pts',(4.73955605021577,0.143933543589337,3.59100624451743));
#20306=CARTESIAN_POINT('Ctrl Pts',(4.76341396824719,0.322302557754209,3.70997617639404));
#20307=CARTESIAN_POINT('Ctrl Pts',(4.78727188627862,0.421859817202848,3.8998648332327));
#20308=CARTESIAN_POINT('Ctrl Pts',(4.81112980431003,0.41826086011465,4.11423926597311));
#20309=CARTESIAN_POINT('Ctrl Pts',(4.83498772234146,0.312385729531365,4.30067908636799));
#20310=CARTESIAN_POINT('Ctrl Pts',(4.85884564037287,0.130123778861223,4.41359467981201));
#20311=CARTESIAN_POINT('Ctrl Pts',(4.88270355840429,-0.0839569802410516,
4.42537510794913));
#20312=CARTESIAN_POINT('Ctrl Pts',(4.90656147643571,-0.277507970732168,
4.33313973520738));
#20313=CARTESIAN_POINT('Ctrl Pts',(4.93041939446713,-0.403200703213916,
4.15944262266324));
#20314=CARTESIAN_POINT('Ctrl Pts',(4.95427731249855,-0.430299880793222,
3.94675744574809));
#20315=CARTESIAN_POINT('Ctrl Pts',(4.97813523052996,-0.352179016385168,
3.7470915236456));
#20316=CARTESIAN_POINT('Ctrl Pts',(5.00199314856139,-0.187940789307144,
3.60926861310034));
#20317=CARTESIAN_POINT('Ctrl Pts',(5.0258510665928,0.0222540801607904,3.56699016996131));
#20318=CARTESIAN_POINT('Ctrl Pts',(5.04970898462423,0.227007220840439,3.63059442521772));
#20319=CARTESIAN_POINT('Ctrl Pts',(5.07356690265564,0.376250912472057,3.7845284059142));
#20320=CARTESIAN_POINT('Ctrl Pts',(5.09742482068706,0.433491007135177,3.99115106069306));
#20321=CARTESIAN_POINT('Ctrl Pts',(5.12128273871848,0.384730742495793,4.19993752217271));
#20322=CARTESIAN_POINT('Ctrl Pts',(5.1451406567499,0.241893331461176,4.35983381329239));
#20323=CARTESIAN_POINT('Ctrl Pts',(5.16899857478132,0.0399064118422473,
4.43174093538579));
#20324=CARTESIAN_POINT('Ctrl Pts',(5.19285649281273,-0.171838712500945,
4.39807563839043));
#20325=CARTESIAN_POINT('Ctrl Pts',(5.21671441084416,-0.341564590845109,
4.26707000444592));
#20326=CARTESIAN_POINT('Ctrl Pts',(5.24057232887557,-0.427768622694993,
4.07075847957352));
#20327=CARTESIAN_POINT('Ctrl Pts',(5.264430246907,-0.409371574112622,3.85714457902312));
#20328=CARTESIAN_POINT('Ctrl Pts',(5.2882881649384,-0.290872024601924,3.6784627202051));
#20329=CARTESIAN_POINT('Ctrl Pts',(5.31214608296984,-0.101246341881189,
3.57840548479658));
#20330=CARTESIAN_POINT('Ctrl Pts',(5.33600400100125,0.113136829324483,3.58143959235932));
#20331=CARTESIAN_POINT('Ctrl Pts',(5.35986191903268,0.299854963974951,3.68682312094679));
#20332=CARTESIAN_POINT('Ctrl Pts',(5.38371983706408,0.413250392048343,3.8687869272297));
#20333=CARTESIAN_POINT('Ctrl Pts',(5.40757775509551,0.425594842551202,4.08283590397723));
#20334=CARTESIAN_POINT('Ctrl Pts',(5.43143567312693,0.333869761079625,4.27662924579771));
#20335=CARTESIAN_POINT('Ctrl Pts',(5.45529359115834,0.160504428594232,4.4027792017911));
#20336=CARTESIAN_POINT('Ctrl Pts',(5.47915150918977,-0.0521086087350157,
4.43043867146175));
#20337=CARTESIAN_POINT('Ctrl Pts',(5.50300942722118,-0.251979671819092,
4.35284416104532));
#20338=CARTESIAN_POINT('Ctrl Pts',(5.52686734525261,-0.390234841353927,
4.18896964197264));
#20339=CARTESIAN_POINT('Ctrl Pts',(5.55072526328402,-0.433066962396004,
3.97888689800548));
#20340=CARTESIAN_POINT('Ctrl Pts',(5.57458318131544,-0.370002414621403,
3.77396688259));
#20341=CARTESIAN_POINT('Ctrl Pts',(5.59844109934686,-0.21646219781534,3.62431812139094));
#20342=CARTESIAN_POINT('Ctrl Pts',(5.62229901737828,-0.00999107731853999,
3.56653381289738));
#20343=CARTESIAN_POINT('Ctrl Pts',(5.64615693540971,0.198923133709572,3.61474379450078));
#20344=CARTESIAN_POINT('Ctrl Pts',(5.67001485344111,0.359195220034686,3.75715941257656));
#20345=CARTESIAN_POINT('Ctrl Pts',(5.69387277147254,0.431634290692432,3.95895616900985));
#20346=CARTESIAN_POINT('Ctrl Pts',(5.71773068950395,0.398527019959163,4.1707892603438));
#20347=CARTESIAN_POINT('Ctrl Pts',(5.74158860753538,0.267969036875697,4.34085972491723));
#20348=CARTESIAN_POINT('Ctrl Pts',(5.76544652556679,0.0718853255354575,
4.42758070267197));
#20349=CARTESIAN_POINT('Ctrl Pts',(5.78930444359821,-0.141776307127955,
4.40974655013133));
#20350=CARTESIAN_POINT('Ctrl Pts',(5.81316236162963,-0.320769768688322,
4.29171820750724));
#20351=CARTESIAN_POINT('Ctrl Pts',(5.83702027966105,-0.421326288178809,
4.10235681181338));
#20352=CARTESIAN_POINT('Ctrl Pts',(5.86087819769247,-0.418857046020503,
3.88796639709818));
#20353=CARTESIAN_POINT('Ctrl Pts',(5.88473611572389,-0.313965860818636,
3.70097123187977));
#20354=CARTESIAN_POINT('Ctrl Pts',(5.90859403375531,-0.132301443679057,
3.58709678011166));
#20355=CARTESIAN_POINT('Ctrl Pts',(5.93245195178673,0.0817142298265842,
3.57418834816524));
#20356=CARTESIAN_POINT('Ctrl Pts',(5.95630986981814,0.275748643515392,3.66540258613358));
#20357=CARTESIAN_POINT('Ctrl Pts',(5.98016778784957,0.402354822815078,3.83843477537114));
#20358=CARTESIAN_POINT('Ctrl Pts',(6.00402570588098,0.430574627524036,4.05097449853386));
#20359=CARTESIAN_POINT('Ctrl Pts',(6.02788362391241,0.353506566116634,4.25104874587108));
#20360=CARTESIAN_POINT('Ctrl Pts',(6.05174154194382,0.189997730437525,4.38973628930191));
#20361=CARTESIAN_POINT('Ctrl Pts',(6.07559945997525,-0.0199730113800777,
4.43311976162365));
#20362=CARTESIAN_POINT('Ctrl Pts',(6.09945737800665,-0.2250554921608,4.3705991908187));
#20363=CARTESIAN_POINT('Ctrl Pts',(6.12331529603809,-0.375113923638194,
4.21744656883549));
#20364=CARTESIAN_POINT('Ctrl Pts',(6.1471732140695,-0.433431396087355,4.01114207710762));
#20365=CARTESIAN_POINT('Ctrl Pts',(6.17103113210093,-0.385792139046387,
3.80207577201042));
#20366=CARTESIAN_POINT('Ctrl Pts',(6.19488905013233,-0.243761337718234,
3.64147770828707));
#20367=CARTESIAN_POINT('Ctrl Pts',(6.21874696816376,-0.042227823444436,
3.56841523311022));
#20368=CARTESIAN_POINT('Ctrl Pts',(6.24260488619517,0.16982704650124,3.60113783246665));
#20369=CARTESIAN_POINT('Ctrl Pts',(6.2664628042266,0.339985970990829,3.73091992247201));
#20370=CARTESIAN_POINT('Ctrl Pts',(6.29032072225801,0.427700638223926,3.92738904240251));
#20371=CARTESIAN_POINT('Ctrl Pts',(6.31417864028943,0.409561128158778,4.13996490148311));
#20372=CARTESIAN_POINT('Ctrl Pts',(6.34598919766466,0.254661277208374,4.38159318714805));
#20373=CARTESIAN_POINT('Ctrl Pts',(6.38575239438369,-0.125272905304917,
4.47558432627151));
#20374=CARTESIAN_POINT('Ctrl Pts',(6.43346823044653,-0.468271923807345,
4.15124960425567));
#20375=CARTESIAN_POINT('Ctrl Pts',(6.48118406650937,-0.380227249479543,
3.6882349865083));
#20376=CARTESIAN_POINT('Ctrl Pts',(6.52889990257221,0.0564566449812287,
3.51140415777354));
#20377=CARTESIAN_POINT('Ctrl Pts',(6.57661573863504,0.441574375138847,3.78331933667001));
#20378=CARTESIAN_POINT('Ctrl Pts',(6.62433157469789,0.421040068198854,4.25418342072721));
#20379=CARTESIAN_POINT('Ctrl Pts',(6.67204741076071,0.0139362792425842,
4.49164405688148));
#20380=CARTESIAN_POINT('Ctrl Pts',(6.71976324682356,-0.406006764042365,
4.27761133505345));
#20381=CARTESIAN_POINT('Ctrl Pts',(6.76747908288639,-0.453085647428837,
3.80864864857145));
#20382=CARTESIAN_POINT('Ctrl Pts',(6.81519491894923,-0.0841006081168706,
3.51540431248109));
#20383=CARTESIAN_POINT('Ctrl Pts',(6.86291075501207,0.362121456530253,3.66717299786736));
#20384=CARTESIAN_POINT('Ctrl Pts',(6.91062659107491,0.475798562415156,4.124581128109));
#20385=CARTESIAN_POINT('Ctrl Pts',(6.95834242713775,0.152544250279933,4.46758486877347));
#20386=CARTESIAN_POINT('Ctrl Pts',(7.00605826320058,-0.310794706562241,
4.38119802990972));
#20387=CARTESIAN_POINT('Ctrl Pts',(7.05377409926342,-0.488725618924084,
3.94475128051735));
#20388=CARTESIAN_POINT('Ctrl Pts',(7.10148993532626,-0.21785253135038,3.55904022429238));
#20389=CARTESIAN_POINT('Ctrl Pts',(7.14920577138909,0.253078023397415,3.57826934481931));
#20390=CARTESIAN_POINT('Ctrl Pts',(7.19692160745195,0.491603063369337,3.98478019943955));
#20391=CARTESIAN_POINT('Ctrl Pts',(7.24463744351477,0.278681483980911,4.40526763942622));
#20392=CARTESIAN_POINT('Ctrl Pts',(7.29235327957762,-0.190157610347023,
4.45359156587464));
#20393=CARTESIAN_POINT('Ctrl Pts',(7.34006911564044,-0.484372034479295,
4.08537538031203));
#20394=CARTESIAN_POINT('Ctrl Pts',(7.3877849517033,-0.333780171974684,3.63875766810317));
#20395=CARTESIAN_POINT('Ctrl Pts',(7.43550078776612,0.123327161313159,3.52387434835784));
#20396=CARTESIAN_POINT('Ctrl Pts',(7.48321662382897,0.467181263150904,3.84622454030349));
#20397=CARTESIAN_POINT('Ctrl Pts',(7.5309324598918,0.382015623368301,4.30978910321172));
#20398=CARTESIAN_POINT('Ctrl Pts',(7.57864829595465,-0.0539608418635878,
4.4888695658253));
#20399=CARTESIAN_POINT('Ctrl Pts',(7.62636413201748,-0.440384235482588,
4.21901358396786));
#20400=CARTESIAN_POINT('Ctrl Pts',(7.67407996808031,-0.422396009600076,
3.7480340579683));
#20401=CARTESIAN_POINT('Ctrl Pts',(7.72179580414317,-0.0165150286377962,
3.50843873354525));
#20402=CARTESIAN_POINT('Ctrl Pts',(7.76951164020598,0.404531957204003,3.72025168374225));
#20403=CARTESIAN_POINT('Ctrl Pts',(7.81722747626884,0.454091022239626,4.18896181724392));
#20404=CARTESIAN_POINT('Ctrl Pts',(7.86494331233166,0.0866513144543145,
4.48414540641706));
#20405=CARTESIAN_POINT('Ctrl Pts',(7.91265914839452,-0.360361628691054,
4.33473081934393));
#20406=CARTESIAN_POINT('Ctrl Pts',(7.96037498445733,-0.476448943335793,
3.87792777037096));
#20407=CARTESIAN_POINT('Ctrl Pts',(8.0080908205202,-0.1550058622045,3.53322552818936));
#20408=CARTESIAN_POINT('Ctrl Pts',(8.05580665658301,0.308781487260178,3.61716946571973));
#20409=CARTESIAN_POINT('Ctrl Pts',(8.10352249264587,0.489010045760349,4.0526725734847));
#20410=CARTESIAN_POINT('Ctrl Pts',(8.1512383287087,0.220173154851853,4.43980564654689));
#20411=CARTESIAN_POINT('Ctrl Pts',(8.19895416477154,-0.250852131956433,
4.4230584271054));
#20412=CARTESIAN_POINT('Ctrl Pts',(8.24667000083438,-0.491516046133,4.01781014446235));
#20413=CARTESIAN_POINT('Ctrl Pts',(8.29438583689722,-0.280813212199106,
3.59620653211525));
#20414=CARTESIAN_POINT('Ctrl Pts',(8.34210167296004,0.187764715363875,3.54541267448783));
#20415=CARTESIAN_POINT('Ctrl Pts',(8.38981750902289,0.483915415676709,3.91207335260334));
#20416=CARTESIAN_POINT('Ctrl Pts',(8.43753334508573,0.335679143777854,4.35947842394856));
#20417=CARTESIAN_POINT('Ctrl Pts',(8.48524918114857,-0.120816450939738,
4.4767689272953));
#20418=CARTESIAN_POINT('Ctrl Pts',(8.5329650172114,-0.466364439759318,4.15623518867385));
#20419=CARTESIAN_POINT('Ctrl Pts',(8.58068085327425,-0.383642787608637,
3.69222827230584));
#20420=CARTESIAN_POINT('Ctrl Pts',(8.62839668933707,0.0513839395061145,
3.51085286915611));
#20421=CARTESIAN_POINT('Ctrl Pts',(8.67611252539993,0.439224004328866,3.77866880275638));
#20422=CARTESIAN_POINT('Ctrl Pts',(8.72382836146275,0.42371790764641,4.24973658040369));
#20423=CARTESIAN_POINT('Ctrl Pts',(8.7715441975256,0.0191051366342138,4.49146741357506));
#20424=CARTESIAN_POINT('Ctrl Pts',(8.81926003358843,-0.403052175319494,
4.28187615866228));
#20425=CARTESIAN_POINT('Ctrl Pts',(8.86697586965126,-0.455080472922433,
3.81343369002772));
#20426=CARTESIAN_POINT('Ctrl Pts',(8.91469170571412,-0.0892013699275644,
3.51631793453238));
#20427=CARTESIAN_POINT('Ctrl Pts',(8.96240754177693,0.358592723611288,3.66337486216116));
#20428=CARTESIAN_POINT('Ctrl Pts',(9.0101233778398,0.477085601399612,4.11955983351088));
#20429=CARTESIAN_POINT('Ctrl Pts',(9.05783921390261,0.157463430517111,4.46595117008304));
#20430=CARTESIAN_POINT('Ctrl Pts',(9.10555504996547,-0.306759831495564,
4.38445237758765));
#20431=CARTESIAN_POINT('Ctrl Pts',(9.1532708860283,-0.489280820139143,3.94990505119329));
#20432=CARTESIAN_POINT('Ctrl Pts',(9.20098672209113,-0.222487703095825,
3.56136068709803));
#20433=CARTESIAN_POINT('Ctrl Pts',(9.24870255815399,0.248619295113741,3.57562555337399));
#20434=CARTESIAN_POINT('Ctrl Pts',(9.29641839421681,0.49141536912078,3.97960000382683));
#20435=CARTESIAN_POINT('Ctrl Pts',(9.34413423027966,0.282937148266828,4.40230808465976));
#20436=CARTESIAN_POINT('Ctrl Pts',(9.39185006634249,-0.185366609388173,
4.45557046104408));
#20437=CARTESIAN_POINT('Ctrl Pts',(9.43956590240532,-0.483445357410111,
4.09047547319903));
#20438=CARTESIAN_POINT('Ctrl Pts',(9.48728173846818,-0.337568794959357,
3.64229546617122));
#20439=CARTESIAN_POINT('Ctrl Pts',(9.53499757453099,0.118302386066128,3.5226010365501));
#20440=CARTESIAN_POINT('Ctrl Pts',(9.58271341059386,0.465534665650901,3.84130942079228));
#20441=CARTESIAN_POINT('Ctrl Pts',(9.63042924665667,0.385259298596883,4.30574580568933));
#20442=CARTESIAN_POINT('Ctrl Pts',(9.67814508271952,-0.0488056103349303,
4.48941111271794));
#20443=CARTESIAN_POINT('Ctrl Pts',(9.72586091878235,-0.438051576325333,
4.22364266437974));
#20444=CARTESIAN_POINT('Ctrl Pts',(9.77357675484519,-0.425028039486299,
3.75249971615691));
#20445=CARTESIAN_POINT('Ctrl Pts',(9.82129259090803,-0.0216947140899849,
3.50864008686857));
#20446=CARTESIAN_POINT('Ctrl Pts',(9.86900842697087,0.401561201071248,3.7160038263529));
#20447=CARTESIAN_POINT('Ctrl Pts',(9.91672426303371,0.456057286475463,4.18416562194019));
#20448=CARTESIAN_POINT('Ctrl Pts',(9.96444009909655,0.0917489483659128,
4.48320529314746));
#20449=CARTESIAN_POINT('Ctrl Pts',(10.0121559351594,-0.356813860767086,
4.3385101085883));
#20450=CARTESIAN_POINT('Ctrl Pts',(10.0598717712222,-0.477709011270712,
3.88295588266498));
#20451=CARTESIAN_POINT('Ctrl Pts',(10.1075876072851,-0.159916626226494,
3.53488507064564));
#20452=CARTESIAN_POINT('Ctrl Pts',(10.1553034433479,0.304729657315094,3.61393645496551));
#20453=CARTESIAN_POINT('Ctrl Pts',(10.2030192794107,0.489538007675758,4.04751593304174));
#20454=CARTESIAN_POINT('Ctrl Pts',(10.2507351154736,0.224796073077312,4.43746079867915));
#20455=CARTESIAN_POINT('Ctrl Pts',(10.2984509515364,-0.246379554360218,
4.42567868168988));
#20456=CARTESIAN_POINT('Ctrl Pts',(10.3461667875993,-0.491301045992024,
4.02298928139638));
#20457=CARTESIAN_POINT('Ctrl Pts',(10.3938826236621,-0.285053227451061,
3.599188470261));
#20458=CARTESIAN_POINT('Ctrl Pts',(10.4415984597249,0.182963355965895,3.54345905416307));
#20459=CARTESIAN_POINT('Ctrl Pts',(10.4893142957878,0.482961874346273,3.9069782134126));
#20460=CARTESIAN_POINT('Ctrl Pts',(10.5370301318506,0.339449072190825,4.35592071060949));
#20461=CARTESIAN_POINT('Ctrl Pts',(10.5847459679134,-0.115785036052801,
4.47801574270962));
#20462=CARTESIAN_POINT('Ctrl Pts',(10.6324618039763,-0.464691964107356,
4.16114156306187));
#20463=CARTESIAN_POINT('Ctrl Pts',(10.6801776400391,-0.386865111317189,
3.69628860657276));
#20464=CARTESIAN_POINT('Ctrl Pts',(10.7278934761019,0.0462259258804368,
3.51033849586834));
#20465=CARTESIAN_POINT('Ctrl Pts',(10.7756093121648,0.436866984064762,3.77405207881873));
#20466=CARTESIAN_POINT('Ctrl Pts',(10.8233251482276,0.426326368719826,4.24525711444552));
#20467=CARTESIAN_POINT('Ctrl Pts',(10.8710409842905,0.0242836891050981,
4.49123876811122));
#20468=CARTESIAN_POINT('Ctrl Pts',(10.9187568203533,-0.400059075867425,
4.28610830234036));
#20469=CARTESIAN_POINT('Ctrl Pts',(10.9664726564161,-0.45702143577077,3.81824018018824));
#20470=CARTESIAN_POINT('Ctrl Pts',(11.014188492479,-0.0942939790271268,
3.51728489730359));
#20471=CARTESIAN_POINT('Ctrl Pts',(11.0619043285418,0.355025089556487,3.65961432075161));
#20472=CARTESIAN_POINT('Ctrl Pts',(11.1096201646047,0.478319155637209,4.11452515096033));
#20473=CARTESIAN_POINT('Ctrl Pts',(11.1573360006675,0.16236538121005,4.46426577284621));
#20474=CARTESIAN_POINT('Ctrl Pts',(11.2050518367304,-0.302691021094817,
4.38766399188028));
#20475=CARTESIAN_POINT('Ctrl Pts',(11.2527676727932,-0.489781601228288,
3.95506440219344));
#20476=CARTESIAN_POINT('Ctrl Pts',(11.300483508856,-0.227098200695192,3.56372986339542));
#20477=CARTESIAN_POINT('Ctrl Pts',(11.3481993449188,0.244132971891272,3.57302890392028));
#20478=CARTESIAN_POINT('Ctrl Pts',(11.3959151809817,0.491173079921361,3.97442207176994));
#20479=CARTESIAN_POINT('Ctrl Pts',(11.4436310170445,0.287161390990383,4.39930384468027));
#20480=CARTESIAN_POINT('Ctrl Pts',(11.4913468531074,-0.180555021833016,
4.45749875294131));
#20481=CARTESIAN_POINT('Ctrl Pts',(11.5390626891702,-0.482464979911041,
4.09556551685319));
#20482=CARTESIAN_POINT('Ctrl Pts',(11.586778525233,-0.341319923258817,3.64587299617429));
#20483=CARTESIAN_POINT('Ctrl Pts',(11.6344943612959,0.113264470804062,3.5213807520529));
#20484=CARTESIAN_POINT('Ctrl Pts',(11.6822101973587,0.463836358529674,3.83641192782507));
#20485=CARTESIAN_POINT('Ctrl Pts',(11.7299260334216,0.38846018117773,4.30166854740152));
#20486=CARTESIAN_POINT('Ctrl Pts',(11.7776418694844,-0.0436449577779122,
4.48989829813191));
#20487=CARTESIAN_POINT('Ctrl Pts',(11.8253577055472,-0.435670260442099,
4.22824690363353));
#20488=CARTESIAN_POINT('Ctrl Pts',(11.8730735416101,-0.427612859293677,
3.75699286549843));
#20489=CARTESIAN_POINT('Ctrl Pts',(11.9207893776729,-0.0268719897862959,
3.50889601812151));
#20490=CARTESIAN_POINT('Ctrl Pts',(11.9685052137357,0.398545841420554,3.71178751390968));
#20491=CARTESIAN_POINT('Ctrl Pts',(12.0162210497986,0.457972894034889,4.17934897039372));
#20492=CARTESIAN_POINT('Ctrl Pts',(12.0639368858614,0.0968363912382316,
4.48221150772657));
#20493=CARTESIAN_POINT('Ctrl Pts',(12.1116527219243,-0.353226459651896,
4.34225179773635));
#20494=CARTESIAN_POINT('Ctrl Pts',(12.1593685579871,-0.478916017555994,
3.88799699566402));
#20495=CARTESIAN_POINT('Ctrl Pts',(12.2070843940499,-0.164809627468288,
3.53659627586117));
#20496=CARTESIAN_POINT('Ctrl Pts',(12.2548002301128,0.300643979445627,3.61074632631782));
#20497=CARTESIAN_POINT('Ctrl Pts',(12.3025160661756,0.490011594032383,4.04235401475446));
#20498=CARTESIAN_POINT('Ctrl Pts',(12.3502319022385,0.229394022021679,4.43506735974179));
#20499=CARTESIAN_POINT('Ctrl Pts',(12.3979477383013,-0.241879610092261,
4.42825165390643));
#20500=CARTESIAN_POINT('Ctrl Pts',(12.4456635743641,-0.491031474462283,
4.0281658647901));
#20501=CARTESIAN_POINT('Ctrl Pts',(12.493379410427,-0.289261580343189,3.60221492864948));
#20502=CARTESIAN_POINT('Ctrl Pts',(12.5410952464898,0.178141673866572,3.54155614424011));
#20503=CARTESIAN_POINT('Ctrl Pts',(12.5888110825527,0.481954687902679,3.90189340664049));
#20504=CARTESIAN_POINT('Ctrl Pts',(12.6365269186155,0.343181296211668,4.35232346328687));
#20505=CARTESIAN_POINT('Ctrl Pts',(12.6842427546783,-0.110740760313508,
4.47920946240362));
#20506=CARTESIAN_POINT('Ctrl Pts',(12.7319585907412,-0.462967872677167,
4.16603003860975));
#20507=CARTESIAN_POINT('Ctrl Pts',(12.779674426804,-0.390044463885,3.70038267566003));
#20508=CARTESIAN_POINT('Ctrl Pts',(12.8273902628668,0.0410627776982723,
3.50987851185683));
#20509=CARTESIAN_POINT('Ctrl Pts',(12.8751060989297,0.434461438689172,3.76946045210395));
#20510=CARTESIAN_POINT('Ctrl Pts',(12.9228219349925,0.42888747548329,4.24075040649094));
#20511=CARTESIAN_POINT('Ctrl Pts',(12.9705377710553,0.0294595442590321,
4.49095555817611));
#20512=CARTESIAN_POINT('Ctrl Pts',(13.0182536071182,-0.397021539751646,
4.29030866646591));
#20513=CARTESIAN_POINT('Ctrl Pts',(13.065969443181,-0.458911634846768,3.82306685936703));
#20514=CARTESIAN_POINT('Ctrl Pts',(13.1136852792439,-0.0993761143989603,
3.51830547777773));
#20515=CARTESIAN_POINT('Ctrl Pts',(13.1614011153067,0.351418020999476,3.65589158776806));
#20516=CARTESIAN_POINT('Ctrl Pts',(13.2091169513695,0.479499580452807,4.10947774749948));
#20517=CARTESIAN_POINT('Ctrl Pts',(13.2568327874324,0.167249297126924,4.46252880717046));
#20518=CARTESIAN_POINT('Ctrl Pts',(13.3045486234952,-0.298588589211839,
4.39083254629632));
#20519=CARTESIAN_POINT('Ctrl Pts',(13.352264459558,-0.490227979701372,3.96022874442655));
#20520=CARTESIAN_POINT('Ctrl Pts',(13.3999802956209,-0.23168347330409,3.56614749850931));
#20521=CARTESIAN_POINT('Ctrl Pts',(13.4476961316837,0.239619531536799,3.57047968038978));
#20522=CARTESIAN_POINT('Ctrl Pts',(13.4954119677466,0.490876233547033,3.96924698078795));
#20523=CARTESIAN_POINT('Ctrl Pts',(13.5431278038094,0.291353737189313,4.39625525192456));
#20524=CARTESIAN_POINT('Ctrl Pts',(13.5908436398722,-0.175723379082843,
4.45937622804808));
#20525=CARTESIAN_POINT('Ctrl Pts',(13.6385594759351,-0.481431012491488,
4.10064494554323));
#20526=CARTESIAN_POINT('Ctrl Pts',(13.6862753119979,-0.345033139360895,
3.64948986092447));
#20527=CARTESIAN_POINT('Ctrl Pts',(13.7339911480608,0.108213974662067,3.52021363031051));
#20528=CARTESIAN_POINT('Ctrl Pts',(13.7817069841236,0.462086530666827,3.83153260544464));
#20529=CARTESIAN_POINT('Ctrl Pts',(13.8294228201864,0.391617915445045,4.297557781203));
#20530=CARTESIAN_POINT('Ctrl Pts',(13.8771386562493,-0.0384794573460961,
4.49033106796769));
#20531=CARTESIAN_POINT('Ctrl Pts',(13.9248544923121,-0.433240552373761,
4.23282579030437));
#20532=CARTESIAN_POINT('Ctrl Pts',(13.9725703283749,-0.430150181893835,
3.76151300691929));
#20533=CARTESIAN_POINT('Ctrl Pts',(14.0202861644378,-0.032046280669499,
3.50920649887429));
#20534=CARTESIAN_POINT('Ctrl Pts',(14.0680020005006,0.39548621318905,3.70760321474174));
#20535=CARTESIAN_POINT('Ctrl Pts',(14.1157178365634,0.459837632138507,4.1745123976147));
#20536=CARTESIAN_POINT('Ctrl Pts',(14.1634336726263,0.101913077983734,4.48116416053968));
#20537=CARTESIAN_POINT('Ctrl Pts',(14.2111495086891,-0.349599823817769,
4.34595547117883));
#20538=CARTESIAN_POINT('Ctrl Pts',(14.258865344752,-0.480069828122688,3.8930505494253));
#20539=CARTESIAN_POINT('Ctrl Pts',(14.3065811808148,-0.169684322438749,
3.53835895376334));
#20540=CARTESIAN_POINT('Ctrl Pts',(14.3542970168777,0.296524907469595,3.60759943412104));
#20541=CARTESIAN_POINT('Ctrl Pts',(14.4020128529405,0.49043075222644,4.0371873919842));
#20542=CARTESIAN_POINT('Ctrl Pts',(14.4497286890033,0.233966490966644,4.43262559558668));
#20543=CARTESIAN_POINT('Ctrl Pts',(14.4974445250662,-0.237352798985028,
4.43077705796148));
#20544=CARTESIAN_POINT('Ctrl Pts',(14.545160361129,-0.490707361486496,4.03333931965322));
#20545=CARTESIAN_POINT('Ctrl Pts',(14.5928761971918,-0.293437803431633,
3.60528557111603));
#20546=CARTESIAN_POINT('Ctrl Pts',(14.6405920332547,0.173300204635467,3.53970415608515));
#20547=CARTESIAN_POINT('Ctrl Pts',(14.6883078693175,0.480893968219416,3.89681949708321));
#20548=CARTESIAN_POINT('Ctrl Pts',(14.7360237053804,0.346875401282657,4.34868708154587));
#20549=CARTESIAN_POINT('Ctrl Pts',(14.7837395414432,-0.10568418401607,4.48034995378457));
#20550=CARTESIAN_POINT('Ctrl Pts',(14.831455377506,-0.461192356972643,4.17090007232882));
#20551=CARTESIAN_POINT('Ctrl Pts',(14.8791712135689,-0.393180492164677,
3.7045100248179));
#20552=CARTESIAN_POINT('Ctrl Pts',(14.9268870496317,0.0358950684576197,
3.50947296821438));
#20553=CARTESIAN_POINT('Ctrl Pts',(14.9746028856945,0.432007635398663,3.76489443262817));
#20554=CARTESIAN_POINT('Ctrl Pts',(15.0223187217574,0.431400943461215,4.23621695712364));
#20555=CARTESIAN_POINT('Ctrl Pts',(15.0700345578202,0.0346321271865876,
4.4906178152274));
#20556=CARTESIAN_POINT('Ctrl Pts',(15.1177503938831,-0.393939904367254,
4.2944767844824));
#20557=CARTESIAN_POINT('Ctrl Pts',(15.1654662299459,-0.46075086019608,3.82791319143947));
#20558=CARTESIAN_POINT('Ctrl Pts',(15.2131820660087,-0.104447211543591,
3.51937956259357));
#20559=CARTESIAN_POINT('Ctrl Pts',(15.2608979020716,0.347771918596306,3.652207076714));
#20560=CARTESIAN_POINT('Ctrl Pts',(15.3086137381344,0.480626744730421,4.10441818376995));
#20561=CARTESIAN_POINT('Ctrl Pts',(15.3563295741973,0.172114635785536,4.46074046598969));
#20562=CARTESIAN_POINT('Ctrl Pts',(15.4040454102601,-0.294452991525291,
4.39395768888776));
#20563=CARTESIAN_POINT('Ctrl Pts',(15.4517612463229,-0.490619905976795,
3.96539750426199));
#20564=CARTESIAN_POINT('Ctrl Pts',(15.4994770823858,-0.236243011612202,
3.56861332390027));
#20565=CARTESIAN_POINT('Ctrl Pts',(15.5471929184486,0.235079475381852,3.56797816593814));
#20566=CARTESIAN_POINT('Ctrl Pts',(15.5949087545115,0.490524862970081,3.9640753057054));
#20567=CARTESIAN_POINT('Ctrl Pts',(15.6426245905743,0.295513721197704,4.39316264501585));
#20568=CARTESIAN_POINT('Ctrl Pts',(15.6903404266371,-0.170872217813597,
4.46120267782338));
#20569=CARTESIAN_POINT('Ctrl Pts',(15.7380562626999,-0.480343569999647,
4.1057131950703));
#20570=CARTESIAN_POINT('Ctrl Pts',(15.7857720987628,-0.348708030819167,
3.6531456586776));
#20571=CARTESIAN_POINT('Ctrl Pts',(15.8334879348256,0.103151458625294,3.5190998009613));
#20572=CARTESIAN_POINT('Ctrl Pts',(15.8812037708885,0.460285376424935,3.82667199562295));
#20573=CARTESIAN_POINT('Ctrl Pts',(15.9289196069513,0.39473215065269,4.29341396369818));
#20574=CARTESIAN_POINT('Ctrl Pts',(15.9766354430142,-0.033309682798763,
4.49070937415524));
#20575=CARTESIAN_POINT('Ctrl Pts',(16.024351279077,-0.430762722000766,4.23737881579128));
#20576=CARTESIAN_POINT('Ctrl Pts',(16.0720671151398,-0.432639725453012,
3.76605963834362));
#20577=CARTESIAN_POINT('Ctrl Pts',(16.1197829512026,-0.0372170120039125,
3.50957149464017));
#20578=CARTESIAN_POINT('Ctrl Pts',(16.1674987872655,0.392382656225717,3.70345139362117));
#20579=CARTESIAN_POINT('Ctrl Pts',(16.2152146233283,0.461651293660056,4.16965644082667));
#20580=CARTESIAN_POINT('Ctrl Pts',(16.2629304593912,0.106978444708158,4.48006336792116));
#20581=CARTESIAN_POINT('Ctrl Pts',(16.310646295454,-0.345934356094203,4.34962071752925));
#20582=CARTESIAN_POINT('Ctrl Pts',(16.3583621315169,-0.481170314810987,
3.89811598262401));
#20583=CARTESIAN_POINT('Ctrl Pts',(16.4060779675797,-0.174540169679895,
3.54017290856226));
#20584=CARTESIAN_POINT('Ctrl Pts',(16.4537938036425,0.292372898913969,3.60449612791703));
#20585=CARTESIAN_POINT('Ctrl Pts',(16.5015096397054,0.490795435699827,4.0320166386149));
#20586=CARTESIAN_POINT('Ctrl Pts',(16.5492254757682,0.238512972024049,4.4301357774334));
#20587=CARTESIAN_POINT('Ctrl Pts',(16.596941311831,-0.23279962385521,4.43325461334514));
#20588=CARTESIAN_POINT('Ctrl Pts',(16.6446571478939,-0.490328743065594,
4.03850907134293));
#20589=CARTESIAN_POINT('Ctrl Pts',(16.6923729839567,-0.297581432841348,
3.60840005658827));
#20590=CARTESIAN_POINT('Ctrl Pts',(16.7400888200196,0.168439486040012,3.53790329540825));
#20591=CARTESIAN_POINT('Ctrl Pts',(16.7878046560824,0.479779833116189,3.89175704832657));
#20592=CARTESIAN_POINT('Ctrl Pts',(16.8355204921452,0.350530977080134,4.3450119692985));
#20593=CARTESIAN_POINT('Ctrl Pts',(16.8832363282081,-0.100615868820984,
4.4814370901721));
#20594=CARTESIAN_POINT('Ctrl Pts',(16.9309521642709,-0.459365614209645,
4.17575112327883));
#20595=CARTESIAN_POINT('Ctrl Pts',(16.9786680003337,-0.396272847821079,
3.70867019559999));
#20596=CARTESIAN_POINT('Ctrl Pts',(17.0263838363966,0.0307233721630972,
3.5091219099869));
#20597=CARTESIAN_POINT('Ctrl Pts',(17.0740996724594,0.429505846750062,3.76035452756312));
#20598=CARTESIAN_POINT('Ctrl Pts',(17.1218155085223,0.433866493469502,4.23165726989771));
#20599=CARTESIAN_POINT('Ctrl Pts',(17.1695313445851,0.039800863341802,4.49022557677993));
#20600=CARTESIAN_POINT('Ctrl Pts',(17.217247180648,-0.390814512007675,4.29861219341511));
#20601=CARTESIAN_POINT('Ctrl Pts',(17.2649630167107,-0.462538907526291,
3.83277863809798));
#20602=CARTESIAN_POINT('Ctrl Pts',(17.3126788527736,-0.109506707187599,
3.52050703244687));
#20603=CARTESIAN_POINT('Ctrl Pts',(17.3603946888365,0.344087187338735,3.64856119684745));
#20604=CARTESIAN_POINT('Ctrl Pts',(17.4081105248993,0.481700523269991,4.09934702176407));
#20605=CARTESIAN_POINT('Ctrl Pts',(17.4558263609621,0.176960856767158,4.45890094794434));
#20606=CARTESIAN_POINT('Ctrl Pts',(17.503542197025,-0.290284687397741,4.39703907252861));
#20607=CARTESIAN_POINT('Ctrl Pts',(17.5512580330878,-0.490957336521241,
3.97057010757845));
#20608=CARTESIAN_POINT('Ctrl Pts',(17.5989738691507,-0.240776309167652,
3.57112706567612));
#20609=CARTESIAN_POINT('Ctrl Pts',(17.6466897052135,0.230513307714322,3.56552463842171));
#20610=CARTESIAN_POINT('Ctrl Pts',(17.6944055412763,0.490119007219086,3.95890762096741));
#20611=CARTESIAN_POINT('Ctrl Pts',(17.7421213773392,0.299640880944266,4.39002636746625));
#20612=CARTESIAN_POINT('Ctrl Pts',(17.789837213402,-0.166002076869247,4.46297789939377));
#20613=CARTESIAN_POINT('Ctrl Pts',(17.8375530494648,-0.479202773223469,
4.11076970247734));
#20614=CARTESIAN_POINT('Ctrl Pts',(17.8852688855277,-0.352344189444135,
3.65683998336499));
#20615=CARTESIAN_POINT('Ctrl Pts',(17.9329847215905,0.0980774850139738,
3.51803938772416));
#20616=CARTESIAN_POINT('Ctrl Pts',(17.9807005576534,0.458433095867658,3.82183063825345));
#20617=CARTESIAN_POINT('Ctrl Pts',(18.0284163937162,0.397802540886209,4.28923755516265));
#20618=CARTESIAN_POINT('Ctrl Pts',(18.076132229779,-0.0281362083699241,
4.49103317467411));
#20619=CARTESIAN_POINT('Ctrl Pts',(18.1238480658419,-0.428237044548737,
4.24190547436581));
#20620=CARTESIAN_POINT('Ctrl Pts',(18.1715639019047,-0.435081213444543,
3.7706322547532));
#20621=CARTESIAN_POINT('Ctrl Pts',(18.2192797379675,-0.0423836094492617,
3.50999096487715));
#20622=CARTESIAN_POINT('Ctrl Pts',(18.2669955740304,0.389235515258945,3.69933251171255));
#20623=CARTESIAN_POINT('Ctrl Pts',(18.3147114100932,0.463413677146622,4.16478163940629));
#20624=CARTESIAN_POINT('Ctrl Pts',(18.3624272461561,0.112031928774586,4.4789092521418));
#20625=CARTESIAN_POINT('Ctrl Pts',(18.4101430822189,-0.342230463623947,
4.35324712966946));
#20626=CARTESIAN_POINT('Ctrl Pts',(18.4578589182817,-0.482217355384067,
3.90319273261591));
#20627=CARTESIAN_POINT('Ctrl Pts',(18.5055747543446,-0.179376629827252,
3.54203793877243));
#20628=CARTESIAN_POINT('Ctrl Pts',(18.5532905904074,0.288188414964166,3.60143675240633));
#20629=CARTESIAN_POINT('Ctrl Pts',(18.6010064264702,0.491105603945206,4.02684232898929));
#20630=CARTESIAN_POINT('Ctrl Pts',(18.6487222625331,0.243032960192409,4.42759818183915));
#20631=CARTESIAN_POINT('Ctrl Pts',(18.6964380985959,-0.228220590447982,
4.43568404486223));
#20632=CARTESIAN_POINT('Ctrl Pts',(18.7441539346588,-0.489895661254576,
4.0436745456279));
#20633=CARTESIAN_POINT('Ctrl Pts',(18.7918697707216,-0.301692008317894,
3.6115580391236));
#20634=CARTESIAN_POINT('Ctrl Pts',(18.8395856067845,0.163560057986223,3.53615376224111));
#20635=CARTESIAN_POINT('Ctrl Pts',(18.8873014428472,0.478612406344963,3.88670662268212));
#20636=CARTESIAN_POINT('Ctrl Pts',(18.9350172789101,0.35414761756175,4.34129853476112));
#20637=CARTESIAN_POINT('Ctrl Pts',(18.982733114973,-0.0955363776958117,
4.48247075080787));
#20638=CARTESIAN_POINT('Ctrl Pts',(19.0304489510358,-0.457487847288108,
4.18058265263639));
#20639=CARTESIAN_POINT('Ctrl Pts',(19.0781647870987,-0.399321187381313,
3.71286272589862));
#20640=CARTESIAN_POINT('Ctrl Pts',(19.1258806231614,0.0255482632835279,
3.50882537619781));
#20641=CARTESIAN_POINT('Ctrl Pts',(19.1735964592243,0.426956350589889,3.75584124112414));
#20642=CARTESIAN_POINT('Ctrl Pts',(19.2213122952871,0.436283851722622,4.22707185138688));
#20643=CARTESIAN_POINT('Ctrl Pts',(19.26902813135,0.0449651784623906,4.48977888620274));
#20644=CARTESIAN_POINT('Ctrl Pts',(19.3167439674128,-0.387645709555542,
4.3027144342981));
#20645=CARTESIAN_POINT('Ctrl Pts',(19.3644598034757,-0.464275578741542,
3.8376626582024));
#20646=CARTESIAN_POINT('Ctrl Pts',(19.4121756395385,-0.114554038379521,
3.52168776344319));
#20647=CARTESIAN_POINT('Ctrl Pts',(19.4598914756013,0.340364234683876,3.64495435060606));
#20648=CARTESIAN_POINT('Ctrl Pts',(19.5076073116642,0.482720800247919,4.09426482953845));
#20649=CARTESIAN_POINT('Ctrl Pts',(19.555323147727,0.181787415268628,4.45701044834135));
#20650=CARTESIAN_POINT('Ctrl Pts',(19.6030389837899,-0.28608412753634,4.40007637198121));
#20651=CARTESIAN_POINT('Ctrl Pts',(19.6507548198527,-0.491240257057309,
3.97574594767572));
#20652=CARTESIAN_POINT('Ctrl Pts',(19.6984706559155,-0.245282818621706,
3.57368850533185));
#20653=CARTESIAN_POINT('Ctrl Pts',(19.7461864919783,0.225921452997342,3.56311925573479));
#20654=CARTESIAN_POINT('Ctrl Pts',(19.7939023280412,0.489658867576397,3.95374471702426));
#20655=CARTESIAN_POINT('Ctrl Pts',(19.841618164104,0.303734463062876,4.38684635894002));
#20656=CARTESIAN_POINT('Ctrl Pts',(19.8893340001669,-0.161112940293692,
4.46470246728215));
#20657=CARTESIAN_POINT('Ctrl Pts',(19.9370498362297,-0.47800980043334,4.11581244897344));
#20658=CARTESIAN_POINT('Ctrl Pts',(19.9847656722926,-0.355939225796451,
3.66057517601247));
#20659=CARTESIAN_POINT('Ctrl Pts',(20.0324815083554,0.0929888682922082,
3.51702731322357));
#20660=CARTESIAN_POINT('Ctrl Pts',(20.0801973444182,0.456536973876988,3.81701888067549));
#20661=CARTESIAN_POINT('Ctrl Pts',(20.1279131804811,0.400815378068436,4.28501049648274));
#20662=CARTESIAN_POINT('Ctrl Pts',(20.1756290165439,-0.022934367574535,
4.49133741301101));
#20663=CARTESIAN_POINT('Ctrl Pts',(20.2233448526067,-0.425711472830213,
4.24633918020534));
#20664=CARTESIAN_POINT('Ctrl Pts',(20.2710606886696,-0.437384262562023,
3.77535541015343));
#20665=CARTESIAN_POINT('Ctrl Pts',(20.3187765247324,-0.0477164433392854,
3.51022640082505));
#20666=CARTESIAN_POINT('Ctrl Pts',(20.3664923607953,0.386374384143037,3.69571627142296));
#20667=CARTESIAN_POINT('Ctrl Pts',(20.4062555575143,0.45143962727185,4.08165775845481));
#20668=CARTESIAN_POINT('Ctrl Pts',(20.4380661148895,0.291471375703242,4.31996082336987));
#20669=CARTESIAN_POINT('Ctrl Pts',(20.461924032921,0.103697252552815,4.42124466395835));
#20670=CARTESIAN_POINT('Ctrl Pts',(20.4857819509523,-0.111451542568667,
4.41901444157942));
#20671=CARTESIAN_POINT('Ctrl Pts',(20.5096398689838,-0.298255971346869,
4.31460392554555));
#20672=CARTESIAN_POINT('Ctrl Pts',(20.5334977870152,-0.412709509332759,
4.13311446574462));
#20673=CARTESIAN_POINT('Ctrl Pts',(20.5573557050466,-0.425936384696969,
3.91915434697803));
#20674=CARTESIAN_POINT('Ctrl Pts',(20.581213623078,-0.335173342752607,3.72492109335083));
#20675=CARTESIAN_POINT('Ctrl Pts',(20.6050715411095,-0.162364888615448,
3.59797442377207));
#20676=CARTESIAN_POINT('Ctrl Pts',(20.6289294591408,0.0501004451364318,
3.56932214892951));
#20677=CARTESIAN_POINT('Ctrl Pts',(20.6527873771723,0.250339089241223,3.64598859455508));
#20678=CARTESIAN_POINT('Ctrl Pts',(20.6766452952037,0.389350172549011,3.80921715950176));
#20679=CARTESIAN_POINT('Ctrl Pts',(20.7005032132352,0.433161330121289,4.01909908002448));
#20680=CARTESIAN_POINT('Ctrl Pts',(20.7243611312665,0.371049143609512,4.22430982617278));
#20681=CARTESIAN_POINT('Ctrl Pts',(20.748219049298,0.218207240773441,4.37467120177868));
#20682=CARTESIAN_POINT('Ctrl Pts',(20.7720769673293,0.01200671405148,4.43341500212799));
#20683=CARTESIAN_POINT('Ctrl Pts',(20.7959348853608,-0.197129246586683,
4.38617716647524));
#20684=CARTESIAN_POINT('Ctrl Pts',(20.8197928033922,-0.358062019934396,
4.24450842127602));
#20685=CARTESIAN_POINT('Ctrl Pts',(20.8436507214237,-0.431438726014498,
4.04305074550709));
#20686=CARTESIAN_POINT('Ctrl Pts',(20.867508639455,-0.399316990859146,3.83106596928302));
#20687=CARTESIAN_POINT('Ctrl Pts',(20.8913665574865,-0.269551332195825,
3.66039017609669));
#20688=CARTESIAN_POINT('Ctrl Pts',(20.9152244755179,-0.0738730526583281,
3.57275822989076));
#20689=CARTESIAN_POINT('Ctrl Pts',(20.9390823935493,0.139869212314499,3.58959853735383));
#20690=CARTESIAN_POINT('Ctrl Pts',(20.9629403115807,0.319409638666883,3.70679317993256));
#20691=CARTESIAN_POINT('Ctrl Pts',(20.9867982296122,0.420845711130686,3.8956848776653));
#20692=CARTESIAN_POINT('Ctrl Pts',(21.0106561476436,0.419373541863394,4.11008446384341));
#20693=CARTESIAN_POINT('Ctrl Pts',(21.034514065675,0.315353119032788,4.29756540021079));
#20694=CARTESIAN_POINT('Ctrl Pts',(21.0583719837064,0.134220268060588,4.41228349058099));
#20695=CARTESIAN_POINT('Ctrl Pts',(21.0822299017379,-0.079733094278782,
4.42618703719455));
#20696=CARTESIAN_POINT('Ctrl Pts',(21.1060878197692,-0.274189543318984,
4.33587624407661));
#20697=CARTESIAN_POINT('Ctrl Pts',(21.1299457378007,-0.401599180171465,
4.16343456021562));
#20698=CARTESIAN_POINT('Ctrl Pts',(21.1538036558321,-0.430806878168669,
3.95102867450389));
#20699=CARTESIAN_POINT('Ctrl Pts',(21.1776615738635,-0.354670559489406,
3.75059761183336));
#20700=CARTESIAN_POINT('Ctrl Pts',(21.2015194918949,-0.191807627993766,
3.61115222665144));
#20701=CARTESIAN_POINT('Ctrl Pts',(21.2253774099264,0.0179574932869785,
3.56679071405539));
#20702=CARTESIAN_POINT('Ctrl Pts',(21.2492353279577,0.223331518303719,3.62836067225603));
#20703=CARTESIAN_POINT('Ctrl Pts',(21.2730932459892,0.374094903668402,3.78080656934254));
#20704=CARTESIAN_POINT('Ctrl Pts',(21.2969511640206,0.433381894944723,3.98685123093373));
#20705=CARTESIAN_POINT('Ctrl Pts',(21.320809082052,0.386695207821707,4.19611112472705));
#20706=CARTESIAN_POINT('Ctrl Pts',(21.3446670000834,0.245451009020076,4.35741650656472));
#20707=CARTESIAN_POINT('Ctrl Pts',(21.3685249181149,0.0441873525619181,
4.43132381671722));
#20708=CARTESIAN_POINT('Ctrl Pts',(21.3923828361462,-0.167881315237013,
4.39976070465745));
#20709=CARTESIAN_POINT('Ctrl Pts',(21.4162407541777,-0.338898428465248,
4.27044521104599));
#20710=CARTESIAN_POINT('Ctrl Pts',(21.4400986722091,-0.427045644525908,
4.07499849655415));
#20711=CARTESIAN_POINT('Ctrl Pts',(21.4639565902406,-0.410768568010174,
3.86121260673678));
#20712=CARTESIAN_POINT('Ctrl Pts',(21.4878145082719,-0.294047387504818,
3.68136401506497));
#20713=CARTESIAN_POINT('Ctrl Pts',(21.5116724263034,-0.105423611064507,
3.57943060117972));
#20714=CARTESIAN_POINT('Ctrl Pts',(21.5355303443348,0.108979109962582,3.58033786138646));
#20715=CARTESIAN_POINT('Ctrl Pts',(21.5593882623662,0.296733470072461,3.68386394585134));
#20716=CARTESIAN_POINT('Ctrl Pts',(21.5832461803976,0.411928413892185,3.86469390692879));
#20717=CARTESIAN_POINT('Ctrl Pts',(21.6071040984291,0.426395639810567,4.07860989342611));
#20718=CARTESIAN_POINT('Ctrl Pts',(21.6309620164605,0.33659751701124,4.27330361969026));
#20719=CARTESIAN_POINT('Ctrl Pts',(21.6548199344919,0.164492132570386,4.401167166299));
#20720=CARTESIAN_POINT('Ctrl Pts',(21.6786778525233,-0.0478360589596606,
4.43093441317345));
#20721=CARTESIAN_POINT('Ctrl Pts',(21.7025357705547,-0.248467031045983,
4.35532645760922));
#20722=CARTESIAN_POINT('Ctrl Pts',(21.7263936885861,-0.388341045935521,
4.1928315042612));
#20723=CARTESIAN_POINT('Ctrl Pts',(21.7502516066176,-0.433255096896122,
3.98318399549658));
#20724=CARTESIAN_POINT('Ctrl Pts',(21.774109524649,-0.372226475033738,3.77764845789182));
#20725=CARTESIAN_POINT('Ctrl Pts',(21.7979674426804,-0.220178340780001,
3.62648392906691));
#20726=CARTESIAN_POINT('Ctrl Pts',(21.8218253607118,-0.0142906046679706,
3.56665425395863));
#20727=CARTESIAN_POINT('Ctrl Pts',(21.8456832787432,0.195091573553633,3.61278941785858));
#20728=CARTESIAN_POINT('Ctrl Pts',(21.8695411967747,0.356768547853618,3.75360811649661));
#20729=CARTESIAN_POINT('Ctrl Pts',(21.8933991148061,0.431205894023261,3.95467634223136));
#20730=CARTESIAN_POINT('Ctrl Pts',(21.9172570328375,0.400201653291494,4.16682743688221));
#20731=CARTESIAN_POINT('Ctrl Pts',(21.941114950869,0.271337207055788,4.33818467892719));
#20732=CARTESIAN_POINT('Ctrl Pts',(21.9649728689003,0.0761234226178432,
4.4268465550088));
#20733=CARTESIAN_POINT('Ctrl Pts',(21.9888307869318,-0.137704612210607,
4.41113282132402));
#20734=CARTESIAN_POINT('Ctrl Pts',(22.0126887049632,-0.317860118355158,
4.29488591379237));
#20735=CARTESIAN_POINT('Ctrl Pts',(22.0365466229946,-0.420290167226249,
4.10653136780738));
#20736=CARTESIAN_POINT('Ctrl Pts',(22.060404541026,-0.419947821735935,3.89212700053744));
#20737=CARTESIAN_POINT('Ctrl Pts',(22.0842624590574,-0.316916794682727,
3.70410052003731));
#20738=CARTESIAN_POINT('Ctrl Pts',(22.1081203770888,-0.136390978688423,
3.58842952252864));
#20739=CARTESIAN_POINT('Ctrl Pts',(22.1319782951203,0.0774861468089536,
3.57339871771534));
#20740=CARTESIAN_POINT('Ctrl Pts',(22.1558362131517,0.27241579873489,3.66268354680831));
#20741=CARTESIAN_POINT('Ctrl Pts',(22.1796941311831,0.400732367405962,3.83445143701846));
#20742=CARTESIAN_POINT('Ctrl Pts',(22.2035520492145,0.431058956528623,4.04670046033727));
#20743=CARTESIAN_POINT('Ctrl Pts',(22.227409967246,0.355979888945518,4.24752994899471));
#20744=CARTESIAN_POINT('Ctrl Pts',(22.2512678852773,0.193854041863619,4.38783162256878));
#20745=CARTESIAN_POINT('Ctrl Pts',(22.2751258033088,-0.0156743990186396,
4.43329790005389));
#20746=CARTESIAN_POINT('Ctrl Pts',(22.2989837213402,-0.221370022215225,
4.37281103827166));
#20747=CARTESIAN_POINT('Ctrl Pts',(22.3228416393716,-0.372934645290675,
4.22116172228637));
#20748=CARTESIAN_POINT('Ctrl Pts',(22.346699557403,-0.43330658847365,4.01543234121164));
#20749=CARTESIAN_POINT('Ctrl Pts',(22.3705574754345,-0.387723268841402,
3.80592933171158));
#20750=CARTESIAN_POINT('Ctrl Pts',(22.3944153934659,-0.247331046528593,
3.64388188817752));
#20751=CARTESIAN_POINT('Ctrl Pts',(22.4182733114973,-0.0464596501027702,
3.56891502119853));
#20752=CARTESIAN_POINT('Ctrl Pts',(22.4421312295287,0.165772403721094,3.59936017830047));
#20753=CARTESIAN_POINT('Ctrl Pts',(22.4659891475602,0.337468575289321,3.7277726770023));
#20754=CARTESIAN_POINT('Ctrl Pts',(22.4898470655915,0.426644514167594,3.92275218663495));
#20755=CARTESIAN_POINT('Ctrl Pts',(22.513704983623,0.411494197867752,4.13662086224655));
#20756=CARTESIAN_POINT('Ctrl Pts',(22.5375629016544,0.295722435535401,4.31708206952049));
#20757=CARTESIAN_POINT('Ctrl Pts',(22.5614208196858,0.107638304484935,4.42000797176855));
#20758=CARTESIAN_POINT('Ctrl Pts',(22.5852787377172,-0.106765988085903,
4.42023067651324));
#20759=CARTESIAN_POINT('Ctrl Pts',(22.6091366557487,-0.295063722636797,
4.31769517074077));
#20760=CARTESIAN_POINT('Ctrl Pts',(22.6329945737801,-0.411209141905604,
4.13747522778479));
#20761=CARTESIAN_POINT('Ctrl Pts',(22.6568524918115,-0.426804986482714,
3.92363755172126));
#20762=CARTESIAN_POINT('Ctrl Pts',(22.6807104098429,-0.33803111495158,3.72847502015617));
#20763=CARTESIAN_POINT('Ctrl Pts',(22.7045683278743,-0.16660749730952,3.59970312177549));
#20764=CARTESIAN_POINT('Ctrl Pts',(22.7284262459057,0.0455714674079685,
3.56882345794434));
#20765=CARTESIAN_POINT('Ctrl Pts',(22.7522841639372,0.246577802732478,3.64336153500176));
#20766=CARTESIAN_POINT('Ctrl Pts',(22.7761420819686,0.387346815298129,3.80514019809748));
#20767=CARTESIAN_POINT('Ctrl Pts',(22.7920473606562,0.417963038852713,3.94471011778788));
#20768=CARTESIAN_POINT('Ctrl Pts',(22.8,0.415641328671541,4.01393920819689));
#20769=CARTESIAN_POINT('Ctrl Pts',(3.96816317011929,0.203757107801821,4.42939176513376));
#20770=CARTESIAN_POINT('Ctrl Pts',(3.9761158094631,0.132237748973037,4.46332948562603));
#20771=CARTESIAN_POINT('Ctrl Pts',(3.99202108815071,-0.0280119004087947,
4.49474661085258));
#20772=CARTESIAN_POINT('Ctrl Pts',(4.01587900618213,-0.261670681609628,
4.42079217330492));
#20773=CARTESIAN_POINT('Ctrl Pts',(4.03973692421355,-0.431283260509235,
4.24398813071681));
#20774=CARTESIAN_POINT('Ctrl Pts',(4.06359484224497,-0.495466080430727,
4.00749935521381));
#20775=CARTESIAN_POINT('Ctrl Pts',(4.08745276027639,-0.438477829352452,
3.76918881818141));
#20776=CARTESIAN_POINT('Ctrl Pts',(4.11131067830781,-0.274278321106756,
3.5873115455631));
#20777=CARTESIAN_POINT('Ctrl Pts',(4.13516859633923,-0.0430057845205295,
3.50635120590702));
#20778=CARTESIAN_POINT('Ctrl Pts',(4.15902651437064,0.198780450874126,3.54609966156282));
#20779=CARTESIAN_POINT('Ctrl Pts',(4.18288443240206,0.391960715466274,3.69684005745713));
#20780=CARTESIAN_POINT('Ctrl Pts',(4.20674235043348,0.489295238859844,3.92171081754005));
#20781=CARTESIAN_POINT('Ctrl Pts',(4.2306002684649,0.466984102771714,4.16572567991789));
#20782=CARTESIAN_POINT('Ctrl Pts',(4.25445818649632,0.330482445391075,4.36921595913043));
#20783=CARTESIAN_POINT('Ctrl Pts',(4.27831610452774,0.113168927396708,4.48242295331799));
#20784=CARTESIAN_POINT('Ctrl Pts',(4.30217402255916,-0.131817528672551,
4.47766435517297));
#20785=CARTESIAN_POINT('Ctrl Pts',(4.32603194059057,-0.344570980451485,
4.35610383169054));
#20786=CARTESIAN_POINT('Ctrl Pts',(4.349889858622,-0.473067456356951,4.14746621026076));
#20787=CARTESIAN_POINT('Ctrl Pts',(4.37374777665341,-0.485886045261059,
3.9027690893624));
#20788=CARTESIAN_POINT('Ctrl Pts',(4.39760569468484,-0.379892264971952,
3.68184757153936));
#20789=CARTESIAN_POINT('Ctrl Pts',(4.42146361271625,-0.181004475645389,
3.53872299041084));
#20790=CARTESIAN_POINT('Ctrl Pts',(4.44532153074767,0.0621438372772935,
3.50839320219298));
#20791=CARTESIAN_POINT('Ctrl Pts',(4.46917944877909,0.290096289836991,3.5982746675986));
#20792=CARTESIAN_POINT('Ctrl Pts',(4.49303736681051,0.447112297141319,3.78638891931142));
#20793=CARTESIAN_POINT('Ctrl Pts',(4.51689528484194,0.494797168872773,4.02673689903048));
#20794=CARTESIAN_POINT('Ctrl Pts',(4.54075320287334,0.421490654719143,4.26054697856981));
#20795=CARTESIAN_POINT('Ctrl Pts',(4.56461112090478,0.245118194360182,4.43064622472778));
#20796=CARTESIAN_POINT('Ctrl Pts',(4.58846903893618,0.00880765856895839,
4.49544073835303));
#20797=CARTESIAN_POINT('Ctrl Pts',(4.61232695696761,-0.229656589644598,
4.43908649592634));
#20798=CARTESIAN_POINT('Ctrl Pts',(4.63618487499902,-0.411963545977342,
4.2753636447643));
#20799=CARTESIAN_POINT('Ctrl Pts',(4.66004279303045,-0.493534193653132,
4.04430688170513));
#20800=CARTESIAN_POINT('Ctrl Pts',(4.68390071106186,-0.454422287381232,
3.80241587917234));
#20801=CARTESIAN_POINT('Ctrl Pts',(4.70775862909328,-0.304191753628974,
3.60883957626609));
#20802=CARTESIAN_POINT('Ctrl Pts',(4.7316165471247,-0.0795780500979935,
3.51091265195837));
#20803=CARTESIAN_POINT('Ctrl Pts',(4.75547446515612,0.164494654344808,3.53258090671894));
#20804=CARTESIAN_POINT('Ctrl Pts',(4.77933238318754,0.368343935055725,3.66854586202706));
#20805=CARTESIAN_POINT('Ctrl Pts',(4.80319030121895,0.482123090158262,3.88556038269908));
#20806=CARTESIAN_POINT('Ctrl Pts',(4.82704821925038,0.478010016947761,4.13055850707372));
#20807=CARTESIAN_POINT('Ctrl Pts',(4.85090613728179,0.357010473862124,4.34363152012653));
#20808=CARTESIAN_POINT('Ctrl Pts',(4.87476405531322,0.14871214514713,4.47267726617372));
#20809=CARTESIAN_POINT('Ctrl Pts',(4.89862197334463,-0.0959503538938319,
4.48614054517122));
#20810=CARTESIAN_POINT('Ctrl Pts',(4.92247989137606,-0.317150377772593,
4.38072921867179));
#20811=CARTESIAN_POINT('Ctrl Pts',(4.94633780940747,-0.460798495283114,
4.1822192273514));
#20812=CARTESIAN_POINT('Ctrl Pts',(4.97019572743889,-0.49176882879792,3.93915167139151));
#20813=CARTESIAN_POINT('Ctrl Pts',(4.99405364547031,-0.40248828815769,3.71096318925158));
#20814=CARTESIAN_POINT('Ctrl Pts',(5.01791156350173,-0.214788397502062,
3.55345208054429));
#20815=CARTESIAN_POINT('Ctrl Pts',(5.04176948153314,0.0254331070612992,
3.50513410186502));
#20816=CARTESIAN_POINT('Ctrl Pts',(5.06562739956457,0.259435524164246,3.57782431515618));
#20817=CARTESIAN_POINT('Ctrl Pts',(5.08948531759598,0.429998888727244,3.75374798322641));
#20818=CARTESIAN_POINT('Ctrl Pts',(5.11334323562741,0.495415812061873,3.98988697716804));
#20819=CARTESIAN_POINT('Ctrl Pts',(5.13720115365882,0.439690074491602,4.2284988806653));
#20820=CARTESIAN_POINT('Ctrl Pts',(5.16105907169025,0.276448136790977,4.41123658365534));
#20821=CARTESIAN_POINT('Ctrl Pts',(5.18491698972166,0.0456070993489057,
4.49341574008204));
#20822=CARTESIAN_POINT('Ctrl Pts',(5.20877490775308,-0.196386116196418,
4.45494130768376));
#20823=CARTESIAN_POINT('Ctrl Pts',(5.2326328257845,-0.390357576881318,4.3052213332044));
#20824=CARTESIAN_POINT('Ctrl Pts',(5.25649074381592,-0.488875976891831,
4.08086642869437));
#20825=CARTESIAN_POINT('Ctrl Pts',(5.28034866184734,-0.467850883838054,
3.83673747961128));
#20826=CARTESIAN_POINT('Ctrl Pts',(5.30420657987876,-0.332423505683668,
3.632530663945));
#20827=CARTESIAN_POINT('Ctrl Pts',(5.32806449791017,-0.115709525355139,
3.5181801106079));
#20828=CARTESIAN_POINT('Ctrl Pts',(5.3519224159416,0.129298585786916,3.52164764473745));
#20829=CARTESIAN_POINT('Ctrl Pts',(5.37578033397301,0.342689670681295,3.64208535978523));
#20830=CARTESIAN_POINT('Ctrl Pts',(5.39963825200445,0.472283796414913,3.85004295376459));
#20831=CARTESIAN_POINT('Ctrl Pts',(5.42349617003584,0.48639166917272,4.09466913029638));
#20832=CARTESIAN_POINT('Ctrl Pts',(5.44735408806728,0.381563529774833,4.31614612573549));
#20833=CARTESIAN_POINT('Ctrl Pts',(5.47121200609869,0.183432713764955,4.46031678178449));
#20834=CARTESIAN_POINT('Ctrl Pts',(5.49506992413012,-0.059552397366927,
4.49192744591021));
#20835=CARTESIAN_POINT('Ctrl Pts',(5.51892784216153,-0.287975325168481,
4.40324844967551));
#20836=CARTESIAN_POINT('Ctrl Pts',(5.54278576019295,-0.445980441674811,
4.21596422322942));
#20837=CARTESIAN_POINT('Ctrl Pts',(5.56664367822437,-0.494931191930538,
3.97587086145358));
#20838=CARTESIAN_POINT('Ctrl Pts',(5.59050159625579,-0.422857784100094,
3.74167773132221));
#20839=CARTESIAN_POINT('Ctrl Pts',(5.61435951428721,-0.247384129650275,
3.57065143242979));
#20840=CARTESIAN_POINT('Ctrl Pts',(5.63821743231862,-0.0114183168777074,
3.50461255354752));
#20841=CARTESIAN_POINT('Ctrl Pts',(5.66207535035005,0.227339585372105,3.55970939936999));
#20842=CARTESIAN_POINT('Ctrl Pts',(5.68593326838146,0.410506766445453,3.72246929038963));
#20843=CARTESIAN_POINT('Ctrl Pts',(5.70979118641288,0.493293861043031,3.9530929995654));
#20844=CARTESIAN_POINT('Ctrl Pts',(5.73364910444431,0.455457169749513,4.19518674831082));
#20845=CARTESIAN_POINT('Ctrl Pts',(5.75750702247572,0.306248793691327,4.38955201985635));
#20846=CARTESIAN_POINT('Ctrl Pts',(5.78136494050715,0.0821542461994931,
4.48866121222712));
#20847=CARTESIAN_POINT('Ctrl Pts',(5.80522285853855,-0.162029253596618,
4.46827942571263));
#20848=CARTESIAN_POINT('Ctrl Pts',(5.82908077656998,-0.366592184898752,
4.33339056701663));
#20849=CARTESIAN_POINT('Ctrl Pts',(5.85293869460139,-0.481513345756758,
4.11697862749145));
#20850=CARTESIAN_POINT('Ctrl Pts',(5.87679661263282,-0.478691368855474,
3.87196223809426));
#20851=CARTESIAN_POINT('Ctrl Pts',(5.90065453066423,-0.358816329143926,
3.65825454842257));
#20852=CARTESIAN_POINT('Ctrl Pts',(5.92451244869565,-0.151200892471453,
3.52811296978032));
#20853=CARTESIAN_POINT('Ctrl Pts',(5.94837036672708,0.093387223403125,3.5133605500302));
#20854=CARTESIAN_POINT('Ctrl Pts',(5.97222828475848,0.315139728168714,3.61760487120619));
#20855=CARTESIAN_POINT('Ctrl Pts',(5.99608620278992,0.459831779670103,3.81535495398299));
#20856=CARTESIAN_POINT('Ctrl Pts',(6.01994412082132,0.492082823488737,4.05825627791571));
#20857=CARTESIAN_POINT('Ctrl Pts',(6.04380203885276,0.404005480250355,4.28691141512903));
#20858=CARTESIAN_POINT('Ctrl Pts',(6.06765995688416,0.21713917558903,4.44541067075535));
#20859=CARTESIAN_POINT('Ctrl Pts',(6.09151787491559,-0.0228261843714051,
4.49499153360272));
#20860=CARTESIAN_POINT('Ctrl Pts',(6.11537579294701,-0.257204988275768,
4.42353981062321));
#20861=CARTESIAN_POINT('Ctrl Pts',(6.13923371097843,-0.428699479426561,
4.24850911946619));
#20862=CARTESIAN_POINT('Ctrl Pts',(6.16309162900984,-0.49534768549136,4.01273373861842));
#20863=CARTESIAN_POINT('Ctrl Pts',(6.18694954704127,-0.440903093044182,
3.77380201544612));
#20864=CARTESIAN_POINT('Ctrl Pts',(6.21080746507268,-0.278582990390117,
3.59026229064107));
#20865=CARTESIAN_POINT('Ctrl Pts',(6.23466538310411,-0.048260127889517,
3.50676273730504));
#20866=CARTESIAN_POINT('Ctrl Pts',(6.25852330113552,0.194087080856728,3.5441598063702));
#20867=CARTESIAN_POINT('Ctrl Pts',(6.28238121916694,0.388553448942855,3.69248145192407));
#20868=CARTESIAN_POINT('Ctrl Pts',(6.30623913719837,0.488798280742691,3.9170164641697));
#20869=CARTESIAN_POINT('Ctrl Pts',(6.33009705522977,0.468067515948433,4.15995908608738));
#20870=CARTESIAN_POINT('Ctrl Pts',(6.36190761260502,0.291040001689194,4.43610431491443));
#20871=CARTESIAN_POINT('Ctrl Pts',(6.40167080932402,-0.143168317426403,
4.54352222151223));
#20872=CARTESIAN_POINT('Ctrl Pts',(6.44938664538688,-0.535165231989368,
4.17285582464912));
#20873=CARTESIAN_POINT('Ctrl Pts',(6.49710248144971,-0.434543251113388,
3.64369891234367));
#20874=CARTESIAN_POINT('Ctrl Pts',(6.54481831751255,0.0645215567551043,
3.4416075490323));
#20875=CARTESIAN_POINT('Ctrl Pts',(6.59253415357539,0.504653900644641,3.75236619672659));
#20876=CARTESIAN_POINT('Ctrl Pts',(6.64024998963822,0.481186238846835,4.29049388273239));
#20877=CARTESIAN_POINT('Ctrl Pts',(6.68796582570107,0.01592709648968,4.56187610740764));
#20878=CARTESIAN_POINT('Ctrl Pts',(6.7356816617639,-0.464005405879062,4.31726850783359));
#20879=CARTESIAN_POINT('Ctrl Pts',(6.78339749782674,-0.517809574500644,
3.78131383674221));
#20880=CARTESIAN_POINT('Ctrl Pts',(6.83111333388957,-0.0961144992151805,
3.44617913151078));
#20881=CARTESIAN_POINT('Ctrl Pts',(6.87882916995242,0.413851019972934,3.61962818876606));
#20882=CARTESIAN_POINT('Ctrl Pts',(6.92654500601525,0.543767061592725,4.14237771887731));
#20883=CARTESIAN_POINT('Ctrl Pts',(6.97426084207809,0.174335412693353,4.53438003016987));
#20884=CARTESIAN_POINT('Ctrl Pts',(7.02197667814094,-0.355192171006393,
4.43565270890428));
#20885=CARTESIAN_POINT('Ctrl Pts',(7.06969251420376,-0.558540766450571,
3.93685892261342));
#20886=CARTESIAN_POINT('Ctrl Pts',(7.11740835026661,-0.248973074301851,
3.49604849518665));
#20887=CARTESIAN_POINT('Ctrl Pts',(7.16512418632944,0.289230577826905,3.51802452284194));
#20888=CARTESIAN_POINT('Ctrl Pts',(7.21284002239229,0.561829257914175,3.98260602935256));
#20889=CARTESIAN_POINT('Ctrl Pts',(7.26055585845511,0.318491529052478,4.46316069626365));
#20890=CARTESIAN_POINT('Ctrl Pts',(7.30827169451797,-0.217321894570402,
4.51838776411367));
#20891=CARTESIAN_POINT('Ctrl Pts',(7.35598753058078,-0.553565266295818,
4.09757137442565));
#20892=CARTESIAN_POINT('Ctrl Pts',(7.40370336664365,-0.381461142739227,
3.58715368886071));
#20893=CARTESIAN_POINT('Ctrl Pts',(7.45141920270646,0.140944621146953,3.45585912402047));
#20894=CARTESIAN_POINT('Ctrl Pts',(7.49913503876933,0.533918768911932,3.82425749787944));
#20895=CARTESIAN_POINT('Ctrl Pts',(7.54685087483214,0.436587096747522,4.3540429157916));
#20896=CARTESIAN_POINT('Ctrl Pts',(7.594566710895,-0.0616692246238245,4.5587052763707));
#20897=CARTESIAN_POINT('Ctrl Pts',(7.64228254695782,-0.503293747851232,
4.25029998493175));
#20898=CARTESIAN_POINT('Ctrl Pts',(7.68999838302067,-0.482735878399531,
3.7120403659385));
#20899=CARTESIAN_POINT('Ctrl Pts',(7.7377142190835,-0.0188742238918736,
3.43821850974892));
#20900=CARTESIAN_POINT('Ctrl Pts',(7.78543005514633,0.462319920793015,3.6802892401675));
#20901=CARTESIAN_POINT('Ctrl Pts',(7.83314589120918,0.518958568528469,4.21595528072725));
#20902=CARTESIAN_POINT('Ctrl Pts',(7.88086172727202,0.099029577569048,4.55330626409362));
#20903=CARTESIAN_POINT('Ctrl Pts',(7.92857756333485,-0.411839798232008,
4.38254759143289));
#20904=CARTESIAN_POINT('Ctrl Pts',(7.9762933993977,-0.544510350349916,3.86048957930736));
#20905=CARTESIAN_POINT('Ctrl Pts',(8.02400923546053,-0.177148669371157,
3.466546133148));
#20906=CARTESIAN_POINT('Ctrl Pts',(8.07172507152338,0.352891360472903,3.56248158116143));
#20907=CARTESIAN_POINT('Ctrl Pts',(8.1194409075862,0.558865824063627,4.06019692528064));
#20908=CARTESIAN_POINT('Ctrl Pts',(8.16715674364906,0.251625202160443,4.50263250666582));
#20909=CARTESIAN_POINT('Ctrl Pts',(8.21487257971187,-0.286686714637947,
4.48349292318459));
#20910=CARTESIAN_POINT('Ctrl Pts',(8.26258841577472,-0.561729810142263,
4.02035434884804));
#20911=CARTESIAN_POINT('Ctrl Pts',(8.31030425183756,-0.32092777766878,3.53852406277244));
#20912=CARTESIAN_POINT('Ctrl Pts',(8.3580200879004,0.21458717114652,3.4804742305729));
#20913=CARTESIAN_POINT('Ctrl Pts',(8.40573592396324,0.553043418849938,3.89951290636976));
#20914=CARTESIAN_POINT('Ctrl Pts',(8.45345176002607,0.383631385356639,4.41083042643994));
#20915=CARTESIAN_POINT('Ctrl Pts',(8.50116759608892,-0.13807525223727,4.54487604447167));
#20916=CARTESIAN_POINT('Ctrl Pts',(8.54888343215175,-0.532985261140852,
4.17855360686946));
#20917=CARTESIAN_POINT('Ctrl Pts',(8.59659926821459,-0.43844670370641,3.64826264467864));
#20918=CARTESIAN_POINT('Ctrl Pts',(8.64431510427743,0.0587242081113278,
3.4409775080543));
#20919=CARTESIAN_POINT('Ctrl Pts',(8.69203094034026,0.501967776032349,3.74705132745037));
#20920=CARTESIAN_POINT('Ctrl Pts',(8.73974677640311,0.484246611455832,4.28541180496438));
#20921=CARTESIAN_POINT('Ctrl Pts',(8.78746261246592,0.021834332487559,4.56167423035448));
#20922=CARTESIAN_POINT('Ctrl Pts',(8.83517844852879,-0.460628749968427,
4.32214256754115));
#20923=CARTESIAN_POINT('Ctrl Pts',(8.88289428459161,-0.520089363644054,
3.78678242815423));
#20924=CARTESIAN_POINT('Ctrl Pts',(8.93061012065447,-0.101943912081849,
3.44722326576734));
#20925=CARTESIAN_POINT('Ctrl Pts',(8.97832595671729,0.409818202553832,3.61528748398963));
#20926=CARTESIAN_POINT('Ctrl Pts',(9.02604179278014,0.545237955920739,4.1366391252272));
#20927=CARTESIAN_POINT('Ctrl Pts',(9.07375762884296,0.179957304801303,4.53251295530543));
#20928=CARTESIAN_POINT('Ctrl Pts',(9.12147346490582,-0.350580908316224,
4.43937194476168));
#20929=CARTESIAN_POINT('Ctrl Pts',(9.16918930096864,-0.559175278946307,
3.94274891673689));
#20930=CARTESIAN_POINT('Ctrl Pts',(9.21690513703149,-0.254270386902387,
3.49870043939378));
#20931=CARTESIAN_POINT('Ctrl Pts',(9.26462097309432,0.284134913886797,3.51500306204057));
#20932=CARTESIAN_POINT('Ctrl Pts',(9.31233680915716,0.56161475127612,3.97668583545263));
#20933=CARTESIAN_POINT('Ctrl Pts',(9.36005264522,0.323355121014866,4.45977836490307));
#20934=CARTESIAN_POINT('Ctrl Pts',(9.40776848128284,-0.211846492332409,
4.52064934726353));
#20935=CARTESIAN_POINT('Ctrl Pts',(9.45548431734568,-0.552506212093558,
4.10340002281193));
#20936=CARTESIAN_POINT('Ctrl Pts',(9.50320015340851,-0.385790975888367,
3.59119686639829));
#20937=CARTESIAN_POINT('Ctrl Pts',(9.55091598947136,0.135202049632292,3.45440391781584));
#20938=CARTESIAN_POINT('Ctrl Pts',(9.59863182553417,0.532036952624682,3.81864024657791));
#20939=CARTESIAN_POINT('Ctrl Pts',(9.64634766159704,0.440294135581046,4.34942202748599));
#20940=CARTESIAN_POINT('Ctrl Pts',(9.69406349765985,-0.0557775609627595,
4.55932418400469));
#20941=CARTESIAN_POINT('Ctrl Pts',(9.74177933372271,-0.500627865026369,
4.25559033604309));
#20942=CARTESIAN_POINT('Ctrl Pts',(9.78949516978553,-0.485743897486414,
3.71714394973028));
#20943=CARTESIAN_POINT('Ctrl Pts',(9.83721100584839,-0.0247938347541151,
3.43844862667992));
#20944=CARTESIAN_POINT('Ctrl Pts',(9.88492684191122,0.458924787935076,3.67543457032792));
#20945=CARTESIAN_POINT('Ctrl Pts',(9.93264267797406,0.521205716397956,4.21047394212484));
#20946=CARTESIAN_POINT('Ctrl Pts',(9.98035851403688,0.104855415711801,4.55223185431066));
#20947=CARTESIAN_POINT('Ctrl Pts',(10.0280743500997,-0.407785226630454,
4.3868667575037));
#20948=CARTESIAN_POINT('Ctrl Pts',(10.0757901861625,-0.54595042077573,3.86623596457089));
#20949=CARTESIAN_POINT('Ctrl Pts',(10.1235060222254,-0.182760942995651,
3.46844274359687));
#20950=CARTESIAN_POINT('Ctrl Pts',(10.1712218582882,0.34826072087591,3.55878673023755));
#20951=CARTESIAN_POINT('Ctrl Pts',(10.2189376943511,0.559469206087141,4.05430365143988));
#20952=CARTESIAN_POINT('Ctrl Pts',(10.2666535304139,0.256908510808291,4.49995269395588));
#20953=CARTESIAN_POINT('Ctrl Pts',(10.3143693664768,-0.281575222991369,
4.4864874848512));
#20954=CARTESIAN_POINT('Ctrl Pts',(10.3620852025396,-0.561484096926345,
4.02627333283551));
#20955=CARTESIAN_POINT('Ctrl Pts',(10.4098010386024,-0.325773485110519,
3.5419319750098));
#20956=CARTESIAN_POINT('Ctrl Pts',(10.4575168746653,0.209099930751681,3.47824153281512));
#20957=CARTESIAN_POINT('Ctrl Pts',(10.5052327107281,0.55195366278862,3.89368991932227));
#20958=CARTESIAN_POINT('Ctrl Pts',(10.552948546791,0.387939853388008,4.40676448870664));
#20959=CARTESIAN_POINT('Ctrl Pts',(10.6006643828538,-0.13232509260073,4.54630096923553));
#20960=CARTESIAN_POINT('Ctrl Pts',(10.6483802189166,-0.531073869970951,
4.18416086379456));
#20961=CARTESIAN_POINT('Ctrl Pts',(10.6960960549795,-0.442129340924997,
3.6529030034519));
#20962=CARTESIAN_POINT('Ctrl Pts',(10.7438118910423,0.0528293649267388,
3.44038965581316));
#20963=CARTESIAN_POINT('Ctrl Pts',(10.7915277271051,0.499274052081986,3.74177509795313));
#20964=CARTESIAN_POINT('Ctrl Pts',(10.839243563168,0.487227694891584,4.28029244094358));
#20965=CARTESIAN_POINT('Ctrl Pts',(10.8869593992308,0.0277526485205102,
4.56141292256198));
#20966=CARTESIAN_POINT('Ctrl Pts',(10.9346752352937,-0.457208082016334,
4.32697927894352));
#20967=CARTESIAN_POINT('Ctrl Pts',(10.9823910713565,-0.522307595786967,
3.79227553224832));
#20968=CARTESIAN_POINT('Ctrl Pts',(11.0301069074193,-0.107764007611043,
3.44832836054127));
#20969=CARTESIAN_POINT('Ctrl Pts',(11.0778227434822,0.405740926916492,3.61098974390844));
#20970=CARTESIAN_POINT('Ctrl Pts',(11.125538579545,0.54664772512998,4.13088523113667));
#20971=CARTESIAN_POINT('Ctrl Pts',(11.1732544156078,0.185559506100192,4.53058679668394));
#20972=CARTESIAN_POINT('Ctrl Pts',(11.2209702516707,-0.345930862581405,
4.4430423427091));
#20973=CARTESIAN_POINT('Ctrl Pts',(11.2686860877335,-0.559747597323992,
3.94864528834179));
#20974=CARTESIAN_POINT('Ctrl Pts',(11.3164019237964,-0.259539500620097,
3.50140805588402));
#20975=CARTESIAN_POINT('Ctrl Pts',(11.3641177598592,0.279007713031768,3.51203547753114));
#20976=CARTESIAN_POINT('Ctrl Pts',(11.411833595922,0.561337850721073,3.97076822846069));
#20977=CARTESIAN_POINT('Ctrl Pts',(11.4595494319849,0.328182802800164,4.45634496498341));
#20978=CARTESIAN_POINT('Ctrl Pts',(11.5072652680477,-0.206347562673641,
4.52285309839201));
#20979=CARTESIAN_POINT('Ctrl Pts',(11.5549811041106,-0.551385786278872,
4.10921718641821));
#20980=CARTESIAN_POINT('Ctrl Pts',(11.6026969401734,-0.390077958183356,
3.59528545163414));
#20981=CARTESIAN_POINT('Ctrl Pts',(11.6504127762362,0.129444461032819,3.45300931394821));
#20982=CARTESIAN_POINT('Ctrl Pts',(11.6981286122991,0.530096039923511,3.8130431397972));
#20983=CARTESIAN_POINT('Ctrl Pts',(11.7458444483619,0.443952268776438,4.34476232707146));
#20984=CARTESIAN_POINT('Ctrl Pts',(11.7935602844247,-0.0498797018717475,
4.55988096454574));
#20985=CARTESIAN_POINT('Ctrl Pts',(11.8412761204876,-0.497906374793238,
4.26085229740167));
#20986=CARTESIAN_POINT('Ctrl Pts',(11.8889919565504,-0.48869796246776,3.72227895182515));
#20987=CARTESIAN_POINT('Ctrl Pts',(11.9367077926133,-0.0307106916234339,
3.43874111807518));
#20988=CARTESIAN_POINT('Ctrl Pts',(11.9844236286761,0.455478679883424,3.67061595167475));
#20989=CARTESIAN_POINT('Ctrl Pts',(12.0321394647389,0.523394971212992,4.20496922507643));
#20990=CARTESIAN_POINT('Ctrl Pts',(12.0798553008018,0.110669607010866,4.5510961052335));
#20991=CARTESIAN_POINT('Ctrl Pts',(12.1275711368646,-0.403685360180124,
4.39114295225112));
#20992=CARTESIAN_POINT('Ctrl Pts',(12.1752869729274,-0.547329849620031,
3.8719972077086));
#20993=CARTESIAN_POINT('Ctrl Pts',(12.2230028089903,-0.188352916401613,
3.4703983969034));
#20994=CARTESIAN_POINT('Ctrl Pts',(12.2707186450531,0.34359139813055,3.55514088718992));
#20995=CARTESIAN_POINT('Ctrl Pts',(12.318434481116,0.560010444926212,4.04840434580723));
#20996=CARTESIAN_POINT('Ctrl Pts',(12.3661503171788,0.262163283277844,4.49721734887317));
#20997=CARTESIAN_POINT('Ctrl Pts',(12.4138661532417,-0.276432455305192,
4.48942800979656));
#20998=CARTESIAN_POINT('Ctrl Pts',(12.4615819893045,-0.561176016721412,
4.03218939850585));
#20999=CARTESIAN_POINT('Ctrl Pts',(12.5092978253673,-0.330583007179444,
3.54539076726965));
#21000=CARTESIAN_POINT('Ctrl Pts',(12.5570136614301,0.203589464528802,3.47606678951191));
#21001=CARTESIAN_POINT('Ctrl Pts',(12.604729497493,0.550802598333678,3.88787874069406));
#21002=CARTESIAN_POINT('Ctrl Pts',(12.6524453335558,0.392205230901379,4.40265336950419));
#21003=CARTESIAN_POINT('Ctrl Pts',(12.7001611696187,-0.126560234920843,
4.54766521348015));
#21004=CARTESIAN_POINT('Ctrl Pts',(12.7478770056815,-0.529103489635726,
4.18974766500481));
#21005=CARTESIAN_POINT('Ctrl Pts',(12.7955928417443,-0.44576286851447,3.65758191611243));
#21006=CARTESIAN_POINT('Ctrl Pts',(12.8433086778072,0.0469286537069902,
3.43986396243348));
#21007=CARTESIAN_POINT('Ctrl Pts',(12.89102451387,0.496524871139168,3.73652755085263));
#21008=CARTESIAN_POINT('Ctrl Pts',(12.9387403499328,0.490154659387074,4.27514194336855));
#21009=CARTESIAN_POINT('Ctrl Pts',(12.9864561859957,0.0336678819209607,
4.56108925568614));
#21010=CARTESIAN_POINT('Ctrl Pts',(13.0341720220585,-0.45373662956012,4.33177967103923));
#21011=CARTESIAN_POINT('Ctrl Pts',(13.0818878581214,-0.524467812480695,
3.79779170939055));
#21012=CARTESIAN_POINT('Ctrl Pts',(13.1296036941842,-0.113572133225654,
3.44949473238301));
#21013=CARTESIAN_POINT('Ctrl Pts',(13.177319530247,0.401618583502394,3.60673521324049));
#21014=CARTESIAN_POINT('Ctrl Pts',(13.2250353663099,0.547996775303968,4.12511679893576));
#21015=CARTESIAN_POINT('Ctrl Pts',(13.2727512023727,0.191141096329688,4.52860170299893));
#21016=CARTESIAN_POINT('Ctrl Pts',(13.3204670384356,-0.341242392487953,
4.4466635296155));
#21017=CARTESIAN_POINT('Ctrl Pts',(13.3681828744984,-0.560257741594785,
3.95454736418435));
#21018=CARTESIAN_POINT('Ctrl Pts',(13.4158987105612,-0.264779785921688,
3.5041710536014));
#21019=CARTESIAN_POINT('Ctrl Pts',(13.4636145466241,0.273849521323983,3.50912209380529));
#21020=CARTESIAN_POINT('Ctrl Pts',(13.5113303826869,0.560998599421335,3.96485386839523));
#21021=CARTESIAN_POINT('Ctrl Pts',(13.5590462187498,0.332974031597074,4.45286087643057));
#21022=CARTESIAN_POINT('Ctrl Pts',(13.6067620548126,-0.200825712906817,
4.52499877347948));
#21023=CARTESIAN_POINT('Ctrl Pts',(13.6544778908754,-0.550204115147588,
4.11502221869768));
#21024=CARTESIAN_POINT('Ctrl Pts',(13.7021937269383,-0.394321612469819,
3.5994189906415));
#21025=CARTESIAN_POINT('Ctrl Pts',(13.7499095630011,0.123672494356884,3.45167546721031));
#21026=CARTESIAN_POINT('Ctrl Pts',(13.7976253990639,0.528096246669736,3.80746679929733));
#21027=CARTESIAN_POINT('Ctrl Pts',(13.8453412351268,0.44756108986054,4.34006433209368));
#21028=CARTESIAN_POINT('Ctrl Pts',(13.8930570711896,-0.0439763023801491,
4.56037555616609));
#21029=CARTESIAN_POINT('Ctrl Pts',(13.9407729072525,-0.495129579482757,
4.26608528452492));
#21030=CARTESIAN_POINT('Ctrl Pts',(13.9884887433153,-0.491597745198497,
3.72744480185615));
#21031=CARTESIAN_POINT('Ctrl Pts',(14.0362045793781,-0.0366241372948624,
3.43909595144367));
#21032=CARTESIAN_POINT('Ctrl Pts',(14.083920415441,0.451981979421435,3.66583391943861));
#21033=CARTESIAN_POINT('Ctrl Pts',(14.1316362515038,0.525526089798339,4.19944174101915));
#21034=CARTESIAN_POINT('Ctrl Pts',(14.1793520875667,0.11647150565515,4.54989914301615));
#21035=CARTESIAN_POINT('Ctrl Pts',(14.2270679236295,-0.399540654275635,
4.39537570069553));
#21036=CARTESIAN_POINT('Ctrl Pts',(14.2747837596924,-0.548648483661927,
3.87777266878906));
#21037=CARTESIAN_POINT('Ctrl Pts',(14.3224995957551,-0.193923968459428,
3.47241287584284));
#21038=CARTESIAN_POINT('Ctrl Pts',(14.370215431818,0.338883910883161,3.5515444569815));
#21039=CARTESIAN_POINT('Ctrl Pts',(14.4179312678808,0.560489480462528,4.04249966364955));
#21040=CARTESIAN_POINT('Ctrl Pts',(14.4656471039437,0.267388935893957,4.49442677524682));
#21041=CARTESIAN_POINT('Ctrl Pts',(14.5133629400065,-0.271258982813659,
4.49231417140114));
#21042=CARTESIAN_POINT('Ctrl Pts',(14.5610787760694,-0.560805603747543,
4.03810188873054));
#21043=CARTESIAN_POINT('Ctrl Pts',(14.6087946121322,-0.335355809656676,
3.54890005536578));
#21044=CARTESIAN_POINT('Ctrl Pts',(14.656510448195,0.198056384554314,3.47395024222346));
#21045=CARTESIAN_POINT('Ctrl Pts',(14.7042262842579,0.549590353339887,3.88208001596329));
#21046=CARTESIAN_POINT('Ctrl Pts',(14.7519421203207,0.396427044118869,4.3984975254762));
#21047=CARTESIAN_POINT('Ctrl Pts',(14.7996579563836,-0.120781319530639,
4.54896862567174));
#21048=CARTESIAN_POINT('Ctrl Pts',(14.8473737924464,-0.527074338995675,
4.19531338994486));
#21049=CARTESIAN_POINT('Ctrl Pts',(14.8950896285092,-0.449346882879826,
3.66229886294881));
#21050=CARTESIAN_POINT('Ctrl Pts',(14.9428054645721,0.041022729875082,3.43940048630678));
#21051=CARTESIAN_POINT('Ctrl Pts',(14.9905213006349,0.493720538569869,3.73130926902151));
#21052=CARTESIAN_POINT('Ctrl Pts',(15.0382371366977,0.493027179828974,4.2699608843321));
#21053=CARTESIAN_POINT('Ctrl Pts',(15.0859529727606,0.0395793756528551,
4.56070326567839));
#21054=CARTESIAN_POINT('Ctrl Pts',(15.1336688088234,-0.450214778192253,
4.33654321062351));
#21055=CARTESIAN_POINT('Ctrl Pts',(15.1813846448863,-0.526569773778615,
3.80333034687015));
#21056=CARTESIAN_POINT('Ctrl Pts',(15.2291004809491,-0.119367643786657,
3.45072225173751));
#21057=CARTESIAN_POINT('Ctrl Pts',(15.2768163170119,0.397451630201876,3.60252436455885));
#21058=CARTESIAN_POINT('Ctrl Pts',(15.3245321530748,0.549284956596614,4.11933446935456));
#21059=CARTESIAN_POINT('Ctrl Pts',(15.3722479891376,0.196701455513243,4.52655789474516));
#21060=CARTESIAN_POINT('Ctrl Pts',(15.4199638252005,-0.336516018808871,
4.45023510325662));
#21061=CARTESIAN_POINT('Ctrl Pts',(15.4676796612633,-0.560705655094284,
3.96045448869));
#21062=CARTESIAN_POINT('Ctrl Pts',(15.5153954973261,-0.269990660741143,
3.50698912564524));
#21063=CARTESIAN_POINT('Ctrl Pts',(15.5631113333889,0.268660911710894,3.50626323446785));
#21064=CARTESIAN_POINT('Ctrl Pts',(15.6108271694518,0.560597035059331,3.95894341219528));
#21065=CARTESIAN_POINT('Ctrl Pts',(15.6585430055146,0.337728275218647,4.44932648624059));
#21066=CARTESIAN_POINT('Ctrl Pts',(15.7062588415775,-0.1952815563728,4.52708613419449));
#21067=CARTESIAN_POINT('Ctrl Pts',(15.7539746776403,-0.548961329954127,
4.12081447485494));
#21068=CARTESIAN_POINT('Ctrl Pts',(15.8016905137031,-0.398521467382777,
3.60359702428645));
#21069=CARTESIAN_POINT('Ctrl Pts',(15.849406349766,0.117886790727162,3.4504025257595));
#21070=CARTESIAN_POINT('Ctrl Pts',(15.8971221858288,0.526037794990907,3.80191184447176));
#21071=CARTESIAN_POINT('Ctrl Pts',(15.9448380218916,0.451120197982628,4.33532856438364));
#21072=CARTESIAN_POINT('Ctrl Pts',(15.9925538579545,-0.0380680182095728,
4.56080790392885));
#21073=CARTESIAN_POINT('Ctrl Pts',(16.0402696940173,-0.492297787528177,
4.27128871615743));
#21074=CARTESIAN_POINT('Ctrl Pts',(16.0879855300802,-0.494442923584513,
3.73264092602517));
#21075=CARTESIAN_POINT('Ctrl Pts',(16.135701366143,-0.0425335149309099,
3.43951308737216));
#21076=CARTESIAN_POINT('Ctrl Pts',(16.1834172022058,0.448435074945997,3.66108900478495));
#21077=CARTESIAN_POINT('Ctrl Pts',(16.2311330382687,0.52759883543946,4.19389210391969));
#21078=CARTESIAN_POINT('Ctrl Pts',(16.2788488743315,0.122260467197297,4.54864110061148));
#21079=CARTESIAN_POINT('Ctrl Pts',(16.3265647103944,-0.395351569291248,
4.39956453268331));
#21080=CARTESIAN_POINT('Ctrl Pts',(16.3742805464572,-0.549906176433804,
3.88356170630145));
#21081=CARTESIAN_POINT('Ctrl Pts',(16.42199638252,-0.199473480363076,3.47448595665642));
#21082=CARTESIAN_POINT('Ctrl Pts',(16.4697122185829,0.334138782019088,3.54799783908671));
#21083=CARTESIAN_POINT('Ctrl Pts',(16.5174280546457,0.560906259487099,4.0365902608309));
#21084=CARTESIAN_POINT('Ctrl Pts',(16.5651438907085,0.272584888215931,4.49158128304055));
#21085=CARTESIAN_POINT('Ctrl Pts',(16.6128597267714,-0.26605538016154,4.49514564908375));
#21086=CARTESIAN_POINT('Ctrl Pts',(16.6605755628342,-0.560372899148451,
4.04401014677825));
#21087=CARTESIAN_POINT('Ctrl Pts',(16.7082913988971,-0.340091362401967,
3.55245944950311));
#21088=CARTESIAN_POINT('Ctrl Pts',(16.7560072349599,0.19250130541649,3.4718921260458));
#21089=CARTESIAN_POINT('Ctrl Pts',(16.8037230710227,0.548317062457662,3.87629438922476));
#21090=CARTESIAN_POINT('Ctrl Pts',(16.8514389070856,0.400604824101502,4.39429741823411));
#21091=CARTESIAN_POINT('Ctrl Pts',(16.8991547431484,-0.114988988324618,
4.55021106103346));
#21092=CARTESIAN_POINT('Ctrl Pts',(16.9468705792113,-0.524986643439221,
4.20085742040038));
#21093=CARTESIAN_POINT('Ctrl Pts',(16.9945864152741,-0.45288098592576,3.66705332002498));
#21094=CARTESIAN_POINT('Ctrl Pts',(17.0423022513369,0.0351122494330066,
3.4389992789138));
#21095=CARTESIAN_POINT('Ctrl Pts',(17.0900180873998,0.490861365866046,3.72612083208173));
#21096=CARTESIAN_POINT('Ctrl Pts',(17.1377339234626,0.49584493715134,4.26474983932169));
#21097=CARTESIAN_POINT('Ctrl Pts',(17.1854497595254,0.0454864730955262,
4.56025499541263));
#21098=CARTESIAN_POINT('Ctrl Pts',(17.2331655955883,-0.446642919103261,
4.34126936858499));
#21099=CARTESIAN_POINT('Ctrl Pts',(17.2808814316511,-0.528613246204851,
3.80889082948154));
#21100=CARTESIAN_POINT('Ctrl Pts',(17.328597267714,-0.125149895556227,3.45201078225777));
#21101=CARTESIAN_POINT('Ctrl Pts',(17.3763131037768,0.393240529860342,3.59835766558462));
#21102=CARTESIAN_POINT('Ctrl Pts',(17.4240289398397,0.55051212592285,4.1135388846668));
#21103=CARTESIAN_POINT('Ctrl Pts',(17.4717447759024,0.202239966032548,4.52445559893916));
#21104=CARTESIAN_POINT('Ctrl Pts',(17.5194606119653,-0.331752266527324,
4.45375666691904));
#21105=CARTESIAN_POINT('Ctrl Pts',(17.5671764480281,-0.561091288070378,
3.96636600572338));
#21106=CARTESIAN_POINT('Ctrl Pts',(17.614892284091,-0.275171546279217,3.50986195899749));
#21107=CARTESIAN_POINT('Ctrl Pts',(17.6626081201538,0.263442460518632,3.50345921706735));
#21108=CARTESIAN_POINT('Ctrl Pts',(17.7103239562167,0.560133202238927,3.95303751636628));
#21109=CARTESIAN_POINT('Ctrl Pts',(17.7580397922795,0.342445005586054,4.44574218699675));
#21110=CARTESIAN_POINT('Ctrl Pts',(17.8057556283423,-0.189715708890181,
4.52911494868296));
#21111=CARTESIAN_POINT('Ctrl Pts',(17.8534714644052,-0.547657568741173,
4.12659331151364));
#21112=CARTESIAN_POINT('Ctrl Pts',(17.901187300468,-0.402677056422281,3.60781908849286));
#21113=CARTESIAN_POINT('Ctrl Pts',(17.9489031365308,0.112087992792125,3.44919063098808));
#21114=CARTESIAN_POINT('Ctrl Pts',(17.9966189725937,0.523920913530056,3.79637889233847));
#21115=CARTESIAN_POINT('Ctrl Pts',(18.0443348086565,0.454629197813879,4.33055554996792));
#21116=CARTESIAN_POINT('Ctrl Pts',(18.0920506447194,-0.0321555056241734,
4.56117795981091));
#21117=CARTESIAN_POINT('Ctrl Pts',(18.1397664807822,-0.489411313471489,
4.27646201432672));
#21118=CARTESIAN_POINT('Ctrl Pts',(18.1874823168451,-0.497233181596917,
3.73786674717144));
#21119=CARTESIAN_POINT('Ctrl Pts',(18.2351981529079,-0.0484381681459794,
3.43999247952716));
#21120=CARTESIAN_POINT('Ctrl Pts',(18.2829139889707,0.444838360430441,3.65638173475637));
#21121=CARTESIAN_POINT('Ctrl Pts',(18.3306298250336,0.529612977905601,4.18832093020544));
#21122=CARTESIAN_POINT('Ctrl Pts',(18.3783456610964,0.128035848626906,4.54732211775687));
#21123=CARTESIAN_POINT('Ctrl Pts',(18.4260614971592,-0.391118570530631,
4.40370898293889));
#21124=CARTESIAN_POINT('Ctrl Pts',(18.4737773332221,-0.551102788237131,
3.88936367722697));
#21125=CARTESIAN_POINT('Ctrl Pts',(18.5214931692849,-0.205000835699102,
3.47661740907615));
#21126=CARTESIAN_POINT('Ctrl Pts',(18.5692090053478,0.329356538604741,3.54450142744705));
#21127=CARTESIAN_POINT('Ctrl Pts',(18.6169248414106,0.561260735706054,4.03067679373969));
#21128=CARTESIAN_POINT('Ctrl Pts',(18.6646406774734,0.2777505631021,4.48868118831814));
#21129=CARTESIAN_POINT('Ctrl Pts',(18.7123565135363,-0.260822225340423,
4.49792212833724));
#21130=CARTESIAN_POINT('Ctrl Pts',(18.7600723495991,-0.559877950986752,
4.04991351638789));
#21131=CARTESIAN_POINT('Ctrl Pts',(18.8077881856619,-0.344789139412875,
3.55606855432066));
#21132=CARTESIAN_POINT('Ctrl Pts',(18.8555040217248,0.186924844147682,3.46989266958543));
#21133=CARTESIAN_POINT('Ctrl Pts',(18.9032198577876,0.546982867117114,3.87052250311704));
#21134=CARTESIAN_POINT('Ctrl Pts',(18.9509356938504,0.404738106803207,4.39005351430856));
#21135=CARTESIAN_POINT('Ctrl Pts',(18.9986515299133,-0.109183884691052,
4.55139238155646));
#21136=CARTESIAN_POINT('Ctrl Pts',(19.0463673659761,-0.522840634850846,
4.20637914057629));
#21137=CARTESIAN_POINT('Ctrl Pts',(19.094083202039,-0.456364785113784,3.67184475922049));
#21138=CARTESIAN_POINT('Ctrl Pts',(19.1417990381018,0.029197868913272,3.43866038485254));
#21139=CARTESIAN_POINT('Ctrl Pts',(19.1895148741647,0.487947670564988,3.72096281627648));
#21140=CARTESIAN_POINT('Ctrl Pts',(19.2372307102275,0.498607618457993,4.25950938727589));
#21141=CARTESIAN_POINT('Ctrl Pts',(19.2849465462903,0.0513885179525073,
4.55974449445321));
#21142=CARTESIAN_POINT('Ctrl Pts',(19.3326623823531,-0.44302144872845,4.34595762039384));
#21143=CARTESIAN_POINT('Ctrl Pts',(19.380378218416,-0.530598003365269,3.81447253878192));
#21144=CARTESIAN_POINT('Ctrl Pts',(19.4280940544788,-0.130918245164485,
3.45336018235082));
#21145=CARTESIAN_POINT('Ctrl Pts',(19.4758098905417,0.38898574814073,3.59423557624425));
#21146=CARTESIAN_POINT('Ctrl Pts',(19.5235257266045,0.551678150913516,4.10773069407674));
#21147=CARTESIAN_POINT('Ctrl Pts',(19.5712415626673,0.207756005258534,4.52229503878775));
#21148=CARTESIAN_POINT('Ctrl Pts',(19.6189573987302,-0.326951650734615,
4.4572278489044));
#21149=CARTESIAN_POINT('Ctrl Pts',(19.666673234793,-0.561414624206118,3.9722812219163));
#21150=CARTESIAN_POINT('Ctrl Pts',(19.7143890708559,-0.280321816997631,
3.51278930393937));
#21151=CARTESIAN_POINT('Ctrl Pts',(19.7621049069187,0.258194652845487,3.5007102220535));
#21152=CARTESIAN_POINT('Ctrl Pts',(19.8098207429815,0.559607330995945,3.94713708427543));
#21153=CARTESIAN_POINT('Ctrl Pts',(19.8575365790444,0.347123361713752,4.44210790974427));
#21154=CARTESIAN_POINT('Ctrl Pts',(19.9052524151072,-0.184128152223511,
4.53108587353909));
#21155=CARTESIAN_POINT('Ctrl Pts',(19.9529682511701,-0.546294178096705,
4.13235642149579));
#21156=CARTESIAN_POINT('Ctrl Pts',(20.0006840872329,-0.406785648814185,
3.61208785870539));
#21157=CARTESIAN_POINT('Ctrl Pts',(20.0483999232957,0.106272459957556,3.44803398021027));
#21158=CARTESIAN_POINT('Ctrl Pts',(20.0961157593586,0.5217539278249,3.7908797683689));
#21159=CARTESIAN_POINT('Ctrl Pts',(20.1438315954214,0.458072423058868,4.32572464996293));
#21160=CARTESIAN_POINT('Ctrl Pts',(20.1915474314842,-0.0262105744965466,
4.56152565902554));
#21161=CARTESIAN_POINT('Ctrl Pts',(20.2392632675471,-0.486524960252488,
4.28152908133109));
#21162=CARTESIAN_POINT('Ctrl Pts',(20.2869791036099,-0.499865224545849,
3.74326461201656));
#21163=CARTESIAN_POINT('Ctrl Pts',(20.3346949396728,-0.0545328049175168,
3.440261547834));
#21164=CARTESIAN_POINT('Ctrl Pts',(20.3824107757356,0.441568512678419,3.6522489094147));
#21165=CARTESIAN_POINT('Ctrl Pts',(20.4221739724547,0.515928418030698,4.09332268501583));
#21166=CARTESIAN_POINT('Ctrl Pts',(20.4539845298298,0.333108474939506,4.36566768059473));
#21167=CARTESIAN_POINT('Ctrl Pts',(20.4778424478613,0.118510552090848,4.48142006140068));
#21168=CARTESIAN_POINT('Ctrl Pts',(20.5017003658927,-0.127372553428812,
4.47887124859312));
#21169=CARTESIAN_POINT('Ctrl Pts',(20.5255582839241,-0.340862259689409,
4.35954554232165));
#21170=CARTESIAN_POINT('Ctrl Pts',(20.5494162019555,-0.471665647836603,
4.15213005589169));
#21171=CARTESIAN_POINT('Ctrl Pts',(20.5732741199869,-0.486782001098211,
3.90760543082941));
#21172=CARTESIAN_POINT('Ctrl Pts',(20.5971320380184,-0.38305332993788,3.68562568155832));
#21173=CARTESIAN_POINT('Ctrl Pts',(20.6209899560498,-0.185558943137764,
3.54054450025879));
#21174=CARTESIAN_POINT('Ctrl Pts',(20.6448478740812,0.0572573647513246,
3.50779920733485));
#21175=CARTESIAN_POINT('Ctrl Pts',(20.6687057921126,0.28610038304352,3.59541756340761));
#21176=CARTESIAN_POINT('Ctrl Pts',(20.6925637101441,0.444969396676924,3.78196356026503));
#21177=CARTESIAN_POINT('Ctrl Pts',(20.7164216281754,0.495039040219165,4.02182741068269));
#21178=CARTESIAN_POINT('Ctrl Pts',(20.7402795462069,0.424054039808096,4.25635280284423));
#21179=CARTESIAN_POINT('Ctrl Pts',(20.7641374642383,0.249378454468877,4.42819351412177));
#21180=CARTESIAN_POINT('Ctrl Pts',(20.7879953822697,0.0137218901755031,
4.49532894963167));
#21181=CARTESIAN_POINT('Ctrl Pts',(20.8118533003011,-0.22528943893053,4.44134312218709));
#21182=CARTESIAN_POINT('Ctrl Pts',(20.8357112183326,-0.409211687104306,
4.27943679589328));
#21183=CARTESIAN_POINT('Ctrl Pts',(20.859569136364,-0.493070359673604,4.04920060553547));
#21184=CARTESIAN_POINT('Ctrl Pts',(20.8834270543954,-0.456359989112496,
3.80693350349834));
#21185=CARTESIAN_POINT('Ctrl Pts',(20.9072849724268,-0.308057122141145,
3.61187643128937));
#21186=CARTESIAN_POINT('Ctrl Pts',(20.9311428904583,-0.0844259229598539,
3.51172613733272));
#21187=CARTESIAN_POINT('Ctrl Pts',(20.9550008084896,0.159849727585384,3.53097210659131));
#21188=CARTESIAN_POINT('Ctrl Pts',(20.9788587265211,0.365037758375503,3.66490817000854));
#21189=CARTESIAN_POINT('Ctrl Pts',(21.0027166445525,0.480964117596,3.88078331455297));
#21190=CARTESIAN_POINT('Ctrl Pts',(21.026574562584,0.479281646861755,4.12581018556955));
#21191=CARTESIAN_POINT('Ctrl Pts',(21.0504324806153,0.360401759160676,4.34007303948752));
#21192=CARTESIAN_POINT('Ctrl Pts',(21.0742903986468,0.153393823636192,4.47117877170218));
#21193=CARTESIAN_POINT('Ctrl Pts',(21.0981483166782,-0.0911230798336762,
4.48706845966041));
#21194=CARTESIAN_POINT('Ctrl Pts',(21.1220062347096,-0.313357908298923,
4.38385664171252));
#21195=CARTESIAN_POINT('Ctrl Pts',(21.145864152741,-0.458968192403581,4.18678141884249));
#21196=CARTESIAN_POINT('Ctrl Pts',(21.1697220707724,-0.492348251467217,
3.94403305123036));
#21197=CARTESIAN_POINT('Ctrl Pts',(21.1935799888039,-0.405335751726616,
3.71497012710753));
#21198=CARTESIAN_POINT('Ctrl Pts',(21.2174379068353,-0.21920761957706,3.55560477096155));
#21199=CARTESIAN_POINT('Ctrl Pts',(21.2412958248667,0.0205227466613194,
3.50490615340017));
#21200=CARTESIAN_POINT('Ctrl Pts',(21.2651537428981,0.255234742309135,3.57527146741714));
#21201=CARTESIAN_POINT('Ctrl Pts',(21.2890116609295,0.427534891009427,3.74949447702405));
#21202=CARTESIAN_POINT('Ctrl Pts',(21.312869578961,0.495291113040325,3.98497291063177));
#21203=CARTESIAN_POINT('Ctrl Pts',(21.3367274969923,0.441935166474334,4.22412587691986));
#21204=CARTESIAN_POINT('Ctrl Pts',(21.3605854150238,0.280514033632862,4.40847396123464));
#21205=CARTESIAN_POINT('Ctrl Pts',(21.3844433330552,0.0504995785194436,
4.49293903542029));
#21206=CARTESIAN_POINT('Ctrl Pts',(21.4083012510867,-0.191863399122956,
4.45686708805594));
#21207=CARTESIAN_POINT('Ctrl Pts',(21.432159169118,-0.387310549425693,4.3090786928523));
#21208=CARTESIAN_POINT('Ctrl Pts',(21.4560170871495,-0.488049720266331,
4.08571213811173));
#21209=CARTESIAN_POINT('Ctrl Pts',(21.4798750051809,-0.469447440294381,
3.84138663085107));
#21210=CARTESIAN_POINT('Ctrl Pts',(21.5037329232123,-0.336052473678932,
3.63584641288874));
#21211=CARTESIAN_POINT('Ctrl Pts',(21.5275908412437,-0.120483523363382,
3.51935166631968));
#21212=CARTESIAN_POINT('Ctrl Pts',(21.5514487592752,0.124546930319796,3.5203885299332));
#21213=CARTESIAN_POINT('Ctrl Pts',(21.5753066773065,0.339122266949511,3.63870346233219));
#21214=CARTESIAN_POINT('Ctrl Pts',(21.599164595338,0.470772971804989,3.84536523971104));
#21215=CARTESIAN_POINT('Ctrl Pts',(21.6230225133694,0.487306861455871,4.08983942814686));
#21216=CARTESIAN_POINT('Ctrl Pts',(21.6468804314008,0.384680949508402,4.31234542922385));
#21217=CARTESIAN_POINT('Ctrl Pts',(21.6707383494323,0.187990066907445,4.45847446473699));
#21218=CARTESIAN_POINT('Ctrl Pts',(21.6945962674636,-0.0546695077989956,
4.49249400502822));
#21219=CARTESIAN_POINT('Ctrl Pts',(21.7184541854951,-0.283960898681086,
4.40608534582272));
#21220=CARTESIAN_POINT('Ctrl Pts',(21.7423121035264,-0.443816114896065,
4.22037775802082));
#21221=CARTESIAN_POINT('Ctrl Pts',(21.766170021558,-0.495146201710716,3.98078180541326));
#21222=CARTESIAN_POINT('Ctrl Pts',(21.7900279395893,-0.425399554695369,
3.74588522487523));
#21223=CARTESIAN_POINT('Ctrl Pts',(21.8138858576208,-0.25163112890579,3.57312662880273));
#21224=CARTESIAN_POINT('Ctrl Pts',(21.8377437756521,-0.0163320378044167,
3.50475019978512));
#21225=CARTESIAN_POINT('Ctrl Pts',(21.8616016936836,0.222960681415914,3.55747583725374));
#21226=CARTESIAN_POINT('Ctrl Pts',(21.885459611715,0.407733440703041,3.71841068663001));
#21227=CARTESIAN_POINT('Ctrl Pts',(21.9093175297464,0.492804267302335,3.94820179346412));
#21228=CARTESIAN_POINT('Ctrl Pts',(21.9331754477779,0.457371026827486,4.19065897275109));
#21229=CARTESIAN_POINT('Ctrl Pts',(21.9570333658092,0.310098111756678,4.38649483975425));
#21230=CARTESIAN_POINT('Ctrl Pts',(21.9808912838407,0.0869977614584207,
4.48782219052945));
#21231=CARTESIAN_POINT('Ctrl Pts',(22.0047492018721,-0.15737591128791,4.46986372771052));
#21232=CARTESIAN_POINT('Ctrl Pts',(22.0286071199035,-0.363266886890503,
4.33701078463543));
#21233=CARTESIAN_POINT('Ctrl Pts',(22.0524650379349,-0.480329213457224,
4.12174952472744));
#21234=CARTESIAN_POINT('Ctrl Pts',(22.0763229559664,-0.479937963428243,
3.87671718963328));
#21235=CARTESIAN_POINT('Ctrl Pts',(22.1001808739978,-0.362188808094022,
3.66183085982978));
#21236=CARTESIAN_POINT('Ctrl Pts',(22.1240387920292,-0.155874623354616,
3.529636096341));
#21237=CARTESIAN_POINT('Ctrl Pts',(22.1478967100606,0.0885551527323001,
3.51245811975107));
#21238=CARTESIAN_POINT('Ctrl Pts',(22.1717546280921,0.311330781786364,3.61449741325855));
#21239=CARTESIAN_POINT('Ctrl Pts',(22.1956125461234,0.457977554205651,3.81080259009947));
#21240=CARTESIAN_POINT('Ctrl Pts',(22.2194704641549,0.492636339578261,4.05337168730347));
#21241=CARTESIAN_POINT('Ctrl Pts',(22.2433283821863,0.406832120751761,4.28288995313029));
#21242=CARTESIAN_POINT('Ctrl Pts',(22.2671863002177,0.22154636656941,4.44323391967918));
#21243=CARTESIAN_POINT('Ctrl Pts',(22.2910442182491,-0.0179135091400202,
4.49519511936025));
#21244=CARTESIAN_POINT('Ctrl Pts',(22.3149021362805,-0.2529930437236,4.42606762362056));
#21245=CARTESIAN_POINT('Ctrl Pts',(22.338760054312,-0.426208888077552,4.25275498785448));
#21246=CARTESIAN_POINT('Ctrl Pts',(22.3626179723434,-0.495205048933098,
4.01763687303198));
#21247=CARTESIAN_POINT('Ctrl Pts',(22.3864758903748,-0.443110087468167,
3.77820606161377));
#21248=CARTESIAN_POINT('Ctrl Pts',(22.4103338084062,-0.282662637164788,
3.59300991103726));
#21249=CARTESIAN_POINT('Ctrl Pts',(22.4341917264377,-0.0530964769854286,
3.50733392083031));
#21250=CARTESIAN_POINT('Ctrl Pts',(22.458049644469,0.189453226607198,3.5421282117862));
#21251=CARTESIAN_POINT('Ctrl Pts',(22.4819075625005,0.385676439696491,3.6888846179772));
#21252=CARTESIAN_POINT('Ctrl Pts',(22.5057654805319,0.487591287867653,3.9117172269821));
#21253=CARTESIAN_POINT('Ctrl Pts',(22.5296233985634,0.470276727405835,4.15613734610506));
#21254=CARTESIAN_POINT('Ctrl Pts',(22.5534813165947,0.337966804695391,4.36237769267677));
#21255=CARTESIAN_POINT('Ctrl Pts',(22.5773392346262,0.123014588878675,4.48000670597833));
#21256=CARTESIAN_POINT('Ctrl Pts',(22.6011971526576,-0.122017660845505,
4.48026122441149));
#21257=CARTESIAN_POINT('Ctrl Pts',(22.625055070689,-0.337213993725473,4.36307837627545));
#21258=CARTESIAN_POINT('Ctrl Pts',(22.6489129887204,-0.469950950795418,
4.15711375897153));
#21259=CARTESIAN_POINT('Ctrl Pts',(22.6727709067518,-0.487774683880463,
3.912729067726));
#21260=CARTESIAN_POINT('Ctrl Pts',(22.6966288247832,-0.386319338946922,
3.6896872918462));
#21261=CARTESIAN_POINT('Ctrl Pts',(22.7204867428147,-0.190407614498503,
3.54252014522276));
#21262=CARTESIAN_POINT('Ctrl Pts',(22.7443446608461,0.0520814161336476,
3.50722927763546));
#21263=CARTESIAN_POINT('Ctrl Pts',(22.7682025788775,0.281801791424649,3.59241522467272));
#21264=CARTESIAN_POINT('Ctrl Pts',(22.7920604969089,0.442679857002608,3.77730419914427));
#21265=CARTESIAN_POINT('Ctrl Pts',(22.8079657755965,0.477669651496365,3.93681187972983));
#21266=CARTESIAN_POINT('Ctrl Pts',(22.8159184149403,0.475016281724327,4.01593044384941));
#21267=CARTESIAN_POINT('Ctrl Pts',(3.98408158505964,0.229225853138217,4.48306385360099));
#21268=CARTESIAN_POINT('Ctrl Pts',(3.99203422440344,0.148766887950233,4.52124364039387));
#21269=CARTESIAN_POINT('Ctrl Pts',(4.00793950309106,-0.0315132651739855,
4.55658776856145));
#21270=CARTESIAN_POINT('Ctrl Pts',(4.03179742112247,-0.29437836981663,4.47338935048851));
#21271=CARTESIAN_POINT('Ctrl Pts',(4.0556553391539,-0.485191777607318,4.27448557757091));
#21272=CARTESIAN_POINT('Ctrl Pts',(4.07951325718531,-0.557397168683185,
4.00843674174317));
#21273=CARTESIAN_POINT('Ctrl Pts',(4.10337117521674,-0.493285636019562,
3.74033843218029));
#21274=CARTESIAN_POINT('Ctrl Pts',(4.12722909324815,-0.308561908987092,
3.53572729771651));
#21275=CARTESIAN_POINT('Ctrl Pts',(4.15108701127957,-0.0483813190761145,
3.44464727048097));
#21276=CARTESIAN_POINT('Ctrl Pts',(4.17494492931099,0.223627135909104,3.48936410886239));
#21277=CARTESIAN_POINT('Ctrl Pts',(4.19880284734241,0.440954086798485,3.65894639349553));
#21278=CARTESIAN_POINT('Ctrl Pts',(4.22266076537383,0.55045499896491,3.91192501290154));
#21279=CARTESIAN_POINT('Ctrl Pts',(4.24651868340524,0.525355068663259,4.18644066347397));
#21280=CARTESIAN_POINT('Ctrl Pts',(4.27037660143667,0.371791302444591,4.41536633561891));
#21281=CARTESIAN_POINT('Ctrl Pts',(4.29423451946808,0.127314547262185,4.54272370785395));
#21282=CARTESIAN_POINT('Ctrl Pts',(4.31809243749951,-0.14829414195428,4.5373703057994));
#21283=CARTESIAN_POINT('Ctrl Pts',(4.34195035553092,-0.387640842632661,
4.40061524972397));
#21284=CARTESIAN_POINT('Ctrl Pts',(4.36580827356235,-0.53219881478122,4.16589884014724));
#21285=CARTESIAN_POINT('Ctrl Pts',(4.38966619159376,-0.546619671109945,
3.89061565172978));
#21286=CARTESIAN_POINT('Ctrl Pts',(4.41352410962518,-0.427377132892538,
3.64207991255526));
#21287=CARTESIAN_POINT('Ctrl Pts',(4.4373820276566,-0.203629241694984,3.48106538615089));
#21288=CARTESIAN_POINT('Ctrl Pts',(4.46123994568802,0.0699115445388116,
3.44694450735191));
#21289=CARTESIAN_POINT('Ctrl Pts',(4.48509786371944,0.326357054473012,3.54806076195131));
#21290=CARTESIAN_POINT('Ctrl Pts',(4.50895578175085,0.502999374434197,3.7596884705576));
#21291=CARTESIAN_POINT('Ctrl Pts',(4.53281369978229,0.556644646112557,4.03007889421215));
#21292=CARTESIAN_POINT('Ctrl Pts',(4.55667161781369,0.474175139017821,4.29311420882242));
#21293=CARTESIAN_POINT('Ctrl Pts',(4.58052953584512,0.275756894216243,4.48447511514554));
#21294=CARTESIAN_POINT('Ctrl Pts',(4.60438745387653,0.00990857728296194,
4.55736865895685));
#21295=CARTESIAN_POINT('Ctrl Pts',(4.62824537190795,-0.258362656684952,
4.49397038324719));
#21296=CARTESIAN_POINT('Ctrl Pts',(4.65210328993938,-0.463457183444019,
4.30978289334447));
#21297=CARTESIAN_POINT('Ctrl Pts',(4.67596120797079,-0.555223804526532,
4.04984504770563));
#21298=CARTESIAN_POINT('Ctrl Pts',(4.69981912600221,-0.511223081411799,
3.77771873014923));
#21299=CARTESIAN_POINT('Ctrl Pts',(4.72367704403363,-0.342214389453536,
3.55994623789246));
#21300=CARTESIAN_POINT('Ctrl Pts',(4.74753496206505,-0.0895249575417115,
3.44977887729433));
#21301=CARTESIAN_POINT('Ctrl Pts',(4.77139288009647,0.185055765100279,3.47415556892044));
#21302=CARTESIAN_POINT('Ctrl Pts',(4.79525079812788,0.414385312357242,3.62711554766008));
#21303=CARTESIAN_POINT('Ctrl Pts',(4.81910871615931,0.542386363113676,3.87125593216545));
#21304=CARTESIAN_POINT('Ctrl Pts',(4.84296663419071,0.537759173780872,4.14687774817434));
#21305=CARTESIAN_POINT('Ctrl Pts',(4.86682455222215,0.401635218192884,4.38658395388507));
#21306=CARTESIAN_POINT('Ctrl Pts',(4.89068247025356,0.167300511433038,4.53175985253543));
#21307=CARTESIAN_POINT('Ctrl Pts',(4.91454038828499,-0.107943727546613,
4.54690598239331));
#21308=CARTESIAN_POINT('Ctrl Pts',(4.9383983063164,-0.356792784813018,4.42831870213619));
#21309=CARTESIAN_POINT('Ctrl Pts',(4.96225622434782,-0.518396287352312,
4.20499583203957));
#21310=CARTESIAN_POINT('Ctrl Pts',(4.98611414237924,-0.553237776802617,
3.93154589703492));
#21311=CARTESIAN_POINT('Ctrl Pts',(5.00997206041066,-0.452797559930213,
3.67483485485756));
#21312=CARTESIAN_POINT('Ctrl Pts',(5.03382997844208,-0.241636005696979,
3.49763554798826));
#21313=CARTESIAN_POINT('Ctrl Pts',(5.05768789647349,0.0286121339618079,
3.44327803376872));
#21314=CARTESIAN_POINT('Ctrl Pts',(5.08154581450492,0.291863827488053,3.52505420509465));
#21315=CARTESIAN_POINT('Ctrl Pts',(5.10540373253633,0.48374686498243,3.72296756053861));
#21316=CARTESIAN_POINT('Ctrl Pts',(5.12926165056775,0.557340616988569,3.98862289364304));
#21317=CARTESIAN_POINT('Ctrl Pts',(5.15311956859917,0.49464940648741,4.25706023915787));
#21318=CARTESIAN_POINT('Ctrl Pts',(5.17697748663059,0.311002942120779,4.46263935401832));
#21319=CARTESIAN_POINT('Ctrl Pts',(5.20083540466201,0.0513077868555636,
4.55509054477827));
#21320=CARTESIAN_POINT('Ctrl Pts',(5.22469332269342,-0.22093351989189,4.5118069769771));
#21321=CARTESIAN_POINT('Ctrl Pts',(5.24855124072485,-0.439150562917527,
4.34337266196288));
#21322=CARTESIAN_POINT('Ctrl Pts',(5.27240915875626,-0.549983331088669,
4.09097437781523));
#21323=CARTESIAN_POINT('Ctrl Pts',(5.29626707678769,-0.526330193563486,
3.81633038019944));
#21324=CARTESIAN_POINT('Ctrl Pts',(5.32012499481911,-0.373974986765411,
3.5865986076849));
#21325=CARTESIAN_POINT('Ctrl Pts',(5.34398291285052,-0.130172708829089,
3.45795473641922));
#21326=CARTESIAN_POINT('Ctrl Pts',(5.36784083088195,0.145460342249349,3.46185569711558));
#21327=CARTESIAN_POINT('Ctrl Pts',(5.39169874891335,0.385524377387638,3.59734759862366));
#21328=CARTESIAN_POINT('Ctrl Pts',(5.41555666694479,0.531317200781484,3.83129898029949));
#21329=CARTESIAN_POINT('Ctrl Pts',(5.4394145849762,0.547188495794237,4.10650235661553));
#21330=CARTESIAN_POINT('Ctrl Pts',(5.46327250300762,0.42925729847004,4.35566300567327));
#21331=CARTESIAN_POINT('Ctrl Pts',(5.48713042103904,0.206360998935678,4.51785436177788));
#21332=CARTESIAN_POINT('Ctrl Pts',(5.51098833907045,-0.0669961859988386,
4.55341622035867));
#21333=CARTESIAN_POINT('Ctrl Pts',(5.53484625710188,-0.323970978517869,
4.45365273830571));
#21334=CARTESIAN_POINT('Ctrl Pts',(5.55870417513329,-0.501726041995696,
4.2429588044862));
#21335=CARTESIAN_POINT('Ctrl Pts',(5.58256209316472,-0.556795421465071,
3.97285482490167));
#21336=CARTESIAN_POINT('Ctrl Pts',(5.60642001119613,-0.475713153578786,
3.70938858005442));
#21337=CARTESIAN_POINT('Ctrl Pts',(5.63027792922756,-0.27830606148521,3.51698474346866));
#21338=CARTESIAN_POINT('Ctrl Pts',(5.65413584725897,-0.0128455564368745,
3.44269129419766));
#21339=CARTESIAN_POINT('Ctrl Pts',(5.67799376529039,0.255756037034639,3.5046750042392));
#21340=CARTESIAN_POINT('Ctrl Pts',(5.70185168332181,0.46181831285622,3.68777916820271));
#21341=CARTESIAN_POINT('Ctrl Pts',(5.72570960135323,0.554953431393631,3.94722983012095));
#21342=CARTESIAN_POINT('Ctrl Pts',(5.74956751938465,0.512387319539865,4.21958423627784));
#21343=CARTESIAN_POINT('Ctrl Pts',(5.77342543741606,0.344528550506956,4.43824431479549));
#21344=CARTESIAN_POINT('Ctrl Pts',(5.79728335544749,0.0924231668635294,
4.54974172178225));
#21345=CARTESIAN_POINT('Ctrl Pts',(5.82114127347891,-0.182282200065281,
4.52681230129395));
#21346=CARTESIAN_POINT('Ctrl Pts',(5.84499919151032,-0.412414601109181,
4.37506292652603));
#21347=CARTESIAN_POINT('Ctrl Pts',(5.86885710954175,-0.541700403334708,
4.13160044316952));
#21348=CARTESIAN_POINT('Ctrl Pts',(5.89271502757316,-0.538525691690445,
3.85595807909033));
#21349=CARTESIAN_POINT('Ctrl Pts',(5.91657294560459,-0.403666797469215,
3.61553786496538));
#21350=CARTESIAN_POINT('Ctrl Pts',(5.94043086363599,-0.170100341263849,
3.46912915944898));
#21351=CARTESIAN_POINT('Ctrl Pts',(5.96428878166742,0.105060216979666,3.45253275189516));
#21352=CARTESIAN_POINT('Ctrl Pts',(5.98814669969884,0.354530812822036,3.5698071562788));
#21353=CARTESIAN_POINT('Ctrl Pts',(6.01200461773026,0.517308736525128,3.79227513259484));
#21354=CARTESIAN_POINT('Ctrl Pts',(6.03586253576167,0.553591019453439,4.06553805729756));
#21355=CARTESIAN_POINT('Ctrl Pts',(6.0597204537931,0.454504394384077,4.32277408438697));
#21356=CARTESIAN_POINT('Ctrl Pts',(6.08357837182452,0.244280620740535,4.50108505220882));
#21357=CARTESIAN_POINT('Ctrl Pts',(6.10743628985593,-0.0256793573627324,
4.55686330558177));
#21358=CARTESIAN_POINT('Ctrl Pts',(6.13129420788736,-0.289354484390735,
4.47648043042773));
#21359=CARTESIAN_POINT('Ctrl Pts',(6.15515212591877,-0.482285035214929,
4.27957167009689));
#21360=CARTESIAN_POINT('Ctrl Pts',(6.17901004395019,-0.557263974895364,
4.01432540012922));
#21361=CARTESIAN_POINT('Ctrl Pts',(6.20286796198161,-0.496014047041978,
3.74552825888183));
#21362=CARTESIAN_POINT('Ctrl Pts',(6.22672588001303,-0.313404643062,3.53904687299508));
#21363=CARTESIAN_POINT('Ctrl Pts',(6.25058379804445,-0.0542924323345977,
3.44511024149985));
#21364=CARTESIAN_POINT('Ctrl Pts',(6.27444171607587,0.218347115212216,3.48718178027374));
#21365=CARTESIAN_POINT('Ctrl Pts',(6.29829963410728,0.437120926894882,3.65404298137615));
#21366=CARTESIAN_POINT('Ctrl Pts',(6.32215755213871,0.549895923261456,3.90664388593688));
#21367=CARTESIAN_POINT('Ctrl Pts',(6.34601547017011,0.526573903738089,4.17995327069166));
#21368=CARTESIAN_POINT('Ctrl Pts',(6.37782602754536,0.327418726170013,4.4906154426808));
#21369=CARTESIAN_POINT('Ctrl Pts',(6.41758922426438,-0.161063729547888,
4.61146011675295));
#21370=CARTESIAN_POINT('Ctrl Pts',(6.46530506032721,-0.60205854017139,4.19446204504257));
#21371=CARTESIAN_POINT('Ctrl Pts',(6.51302089639007,-0.488859252747234,
3.59916283817905));
#21372=CARTESIAN_POINT('Ctrl Pts',(6.56073673245289,0.0725864685289804,
3.37181094029106));
#21373=CARTESIAN_POINT('Ctrl Pts',(6.60845256851574,0.567733426150434,3.72141305678318));
#21374=CARTESIAN_POINT('Ctrl Pts',(6.65616840457857,0.541332409494817,4.32680434473755));
#21375=CARTESIAN_POINT('Ctrl Pts',(6.70388424064141,0.0179179137367747,
4.6321081579338));
#21376=CARTESIAN_POINT('Ctrl Pts',(6.75160007670425,-0.522004047715759,
4.35692568061372));
#21377=CARTESIAN_POINT('Ctrl Pts',(6.79931591276708,-0.582533501572452,
3.75397902491298));
#21378=CARTESIAN_POINT('Ctrl Pts',(6.84703174882993,-0.10812839031349,3.37695395054049));
#21379=CARTESIAN_POINT('Ctrl Pts',(6.89474758489276,0.465580583415614,3.57208337966475));
#21380=CARTESIAN_POINT('Ctrl Pts',(6.9424634209556,0.611735560770294,4.16017430964564));
#21381=CARTESIAN_POINT('Ctrl Pts',(6.99017925701844,0.196126575106773,4.60117519156627));
#21382=CARTESIAN_POINT('Ctrl Pts',(7.03789509308127,-0.399589635450545,
4.49010738789885));
#21383=CARTESIAN_POINT('Ctrl Pts',(7.08561092914412,-0.628355913977057,
3.92896656470948));
#21384=CARTESIAN_POINT('Ctrl Pts',(7.13332676520695,-0.280093617253323,
3.43305676608093));
#21385=CARTESIAN_POINT('Ctrl Pts',(7.1810426012698,0.325383132256395,3.45777970086456));
#21386=CARTESIAN_POINT('Ctrl Pts',(7.22875843733263,0.632055452459012,3.98043185926557));
#21387=CARTESIAN_POINT('Ctrl Pts',(7.27647427339546,0.358301574124045,4.52105375310108));
#21388=CARTESIAN_POINT('Ctrl Pts',(7.32419010945831,-0.244486178793781,
4.58318396235269));
#21389=CARTESIAN_POINT('Ctrl Pts',(7.37190594552114,-0.622758498112341,
4.10976736853928));
#21390=CARTESIAN_POINT('Ctrl Pts',(7.41962178158399,-0.42914211350377,3.53554970961824));
#21391=CARTESIAN_POINT('Ctrl Pts',(7.46733761764681,0.158562080980748,3.38784389968312));
#21392=CARTESIAN_POINT('Ctrl Pts',(7.51505345370967,0.600656274672958,3.80229045545538));
#21393=CARTESIAN_POINT('Ctrl Pts',(7.56276928977248,0.491158570126743,4.3982967283715));
#21394=CARTESIAN_POINT('Ctrl Pts',(7.61048512583535,-0.0693776073840611,
4.62854098691609));
#21395=CARTESIAN_POINT('Ctrl Pts',(7.65820096189817,-0.566203260219877,
4.28158638589565));
#21396=CARTESIAN_POINT('Ctrl Pts',(7.70591679796101,-0.543075747198986,
3.67604667390869));
#21397=CARTESIAN_POINT('Ctrl Pts',(7.75363263402386,-0.0212334191459514,
3.36799828595259));
#21398=CARTESIAN_POINT('Ctrl Pts',(7.80134847008666,0.520107884382028,3.64032679659274));
#21399=CARTESIAN_POINT('Ctrl Pts',(7.84906430614954,0.583826114817312,4.24294874421058));
#21400=CARTESIAN_POINT('Ctrl Pts',(7.89678014221235,0.111407840683781,4.62246712177016));
#21401=CARTESIAN_POINT('Ctrl Pts',(7.94449597827521,-0.463317967772962,
4.43036436352186));
#21402=CARTESIAN_POINT('Ctrl Pts',(7.99221181433803,-0.612571757364041,
3.84305138824375));
#21403=CARTESIAN_POINT('Ctrl Pts',(8.03992765040088,-0.199291476537812,
3.39986673810663));
#21404=CARTESIAN_POINT('Ctrl Pts',(8.08764348646372,0.397001233685627,3.50779369660314));
#21405=CARTESIAN_POINT('Ctrl Pts',(8.13535932252656,0.628721602366905,4.06772127707659));
#21406=CARTESIAN_POINT('Ctrl Pts',(8.18307515858938,0.283077249469033,4.56545936678474));
#21407=CARTESIAN_POINT('Ctrl Pts',(8.23079099465223,-0.32252129731946,4.54392741926377));
#21408=CARTESIAN_POINT('Ctrl Pts',(8.27850683071506,-0.631943574151527,
4.02289855323374));
#21409=CARTESIAN_POINT('Ctrl Pts',(8.32622266677791,-0.361042343138453,
3.48084159342964));
#21410=CARTESIAN_POINT('Ctrl Pts',(8.37393850284074,0.241409626929164,3.41553578665797));
#21411=CARTESIAN_POINT('Ctrl Pts',(8.42165433890358,0.622171422023167,3.88695246013618));
#21412=CARTESIAN_POINT('Ctrl Pts',(8.46937017496642,0.431583626935426,4.46218242893131));
#21413=CARTESIAN_POINT('Ctrl Pts',(8.51708601102927,-0.155334053534803,
4.61298316164806));
#21414=CARTESIAN_POINT('Ctrl Pts',(8.56480184709209,-0.599606082522386,
4.20087202506506));
#21415=CARTESIAN_POINT('Ctrl Pts',(8.61251768315494,-0.493250619804184,
3.60429701705146));
#21416=CARTESIAN_POINT('Ctrl Pts',(8.66023351921777,0.0660644767165412,
3.37110214695249));
#21417=CARTESIAN_POINT('Ctrl Pts',(8.70794935528061,0.564711547735832,3.71543385214437));
#21418=CARTESIAN_POINT('Ctrl Pts',(8.75566519134344,0.544775315265253,4.32108702952508));
#21419=CARTESIAN_POINT('Ctrl Pts',(8.80338102740629,0.0245635283409047,
4.6318810471339));
#21420=CARTESIAN_POINT('Ctrl Pts',(8.85109686346912,-0.518205324617361,
4.36240897642002));
#21421=CARTESIAN_POINT('Ctrl Pts',(8.89881269953197,-0.585098254365674,
3.76013116628075));
#21422=CARTESIAN_POINT('Ctrl Pts',(8.9465285355948,-0.114686454236133,3.3781285970023));
#21423=CARTESIAN_POINT('Ctrl Pts',(8.99424437165764,0.461043681496376,3.56720010581811));
#21424=CARTESIAN_POINT('Ctrl Pts',(9.04196020772047,0.613390310441866,4.15371841694351));
#21425=CARTESIAN_POINT('Ctrl Pts',(9.08967604378332,0.202451179085494,4.59907474052783));
#21426=CARTESIAN_POINT('Ctrl Pts',(9.13739187984615,-0.394401985136886,
4.49429151193569));
#21427=CARTESIAN_POINT('Ctrl Pts',(9.18510771590899,-0.629069737753471,
3.93559278228048));
#21428=CARTESIAN_POINT('Ctrl Pts',(9.23282355197184,-0.28605307070895,3.43604019168954));
#21429=CARTESIAN_POINT('Ctrl Pts',(9.28053938803466,0.319650532659854,3.45438057070715));
#21430=CARTESIAN_POINT('Ctrl Pts',(9.32825522409751,0.631814133431458,3.97377166707843));
#21431=CARTESIAN_POINT('Ctrl Pts',(9.37597106016033,0.363773093762905,4.51724864514637));
#21432=CARTESIAN_POINT('Ctrl Pts',(9.4236868962232,-0.238326375276645,4.58572823348297));
#21433=CARTESIAN_POINT('Ctrl Pts',(9.47140273228601,-0.621567066777005,
4.11632457242483));
#21434=CARTESIAN_POINT('Ctrl Pts',(9.51911856834886,-0.434013156817378,
3.54009826662536));
#21435=CARTESIAN_POINT('Ctrl Pts',(9.5668344044117,0.152101713198456,3.38620679908157));
#21436=CARTESIAN_POINT('Ctrl Pts',(9.61455024047453,0.598539239598464,3.79597107236355));
#21437=CARTESIAN_POINT('Ctrl Pts',(9.66226607653739,0.495328972565208,4.39309824928265));
#21438=CARTESIAN_POINT('Ctrl Pts',(9.7099819126002,-0.0627495115905886,
4.62923725529147));
#21439=CARTESIAN_POINT('Ctrl Pts',(9.75769774866305,-0.563204153727404,
4.28753800770644));
#21440=CARTESIAN_POINT('Ctrl Pts',(9.80541358472588,-0.54645975548653,3.68178818330365));
#21441=CARTESIAN_POINT('Ctrl Pts',(9.85312942078873,-0.027892955418244,
3.36825716649128));
#21442=CARTESIAN_POINT('Ctrl Pts',(9.90084525685157,0.516288374798902,3.63486531430293));
#21443=CARTESIAN_POINT('Ctrl Pts',(9.9485610929144,0.58635414632045,4.2367822623095));
#21444=CARTESIAN_POINT('Ctrl Pts',(9.99627692897723,0.117961883057689,4.62125841547385));
#21445=CARTESIAN_POINT('Ctrl Pts',(10.0439927650401,-0.458756592493822,
4.4352234064191));
#21446=CARTESIAN_POINT('Ctrl Pts',(10.0917086011029,-0.614191830280748,
3.8495160464768));
#21447=CARTESIAN_POINT('Ctrl Pts',(10.1394244371658,-0.205605259764808,
3.40200041654811));
#21448=CARTESIAN_POINT('Ctrl Pts',(10.1871402732286,0.391791784436726,3.5036370055096));
#21449=CARTESIAN_POINT('Ctrl Pts',(10.2348561092915,0.629400404498524,4.06109136983801));
#21450=CARTESIAN_POINT('Ctrl Pts',(10.2825719453542,0.289020948539269,4.56244458923262));
#21451=CARTESIAN_POINT('Ctrl Pts',(10.3302877814171,-0.316770891622519,
4.54729628801251));
#21452=CARTESIAN_POINT('Ctrl Pts',(10.3780036174799,-0.631667147860668,
4.02955738427466));
#21453=CARTESIAN_POINT('Ctrl Pts',(10.4257194535428,-0.366493742769977,
3.48467547975859));
#21454=CARTESIAN_POINT('Ctrl Pts',(10.4734352896056,0.235236505537468,3.41302401146715));
#21455=CARTESIAN_POINT('Ctrl Pts',(10.5211511256685,0.620945451230968,3.88040162523195));
#21456=CARTESIAN_POINT('Ctrl Pts',(10.5688669617313,0.436430634585191,4.45760826680378));
#21457=CARTESIAN_POINT('Ctrl Pts',(10.6165827977941,-0.148865149148659,
4.61458619576145));
#21458=CARTESIAN_POINT('Ctrl Pts',(10.664298633857,-0.597455775834545,4.20718016452724));
#21459=CARTESIAN_POINT('Ctrl Pts',(10.7120144699198,-0.497393570532806,
3.60951740033105));
#21460=CARTESIAN_POINT('Ctrl Pts',(10.7597303059826,0.059432803973042,3.37044081575797));
#21461=CARTESIAN_POINT('Ctrl Pts',(10.8074461420455,0.56168112009921,3.70949811708754));
#21462=CARTESIAN_POINT('Ctrl Pts',(10.8551619781083,0.548129021063343,4.31532776744164));
#21463=CARTESIAN_POINT('Ctrl Pts',(10.9028778141712,0.0312216079359222,
4.63158707701274));
#21464=CARTESIAN_POINT('Ctrl Pts',(10.950593650234,-0.514357088165242,4.36785025554668));
#21465=CARTESIAN_POINT('Ctrl Pts',(10.9983094862968,-0.587593755803164,
3.7663108843084));
#21466=CARTESIAN_POINT('Ctrl Pts',(11.0460253223597,-0.12123403619496,3.37937182377895));
#21467=CARTESIAN_POINT('Ctrl Pts',(11.0937411584225,0.456456764276497,3.56236516706526));
#21468=CARTESIAN_POINT('Ctrl Pts',(11.1414569944854,0.61497629462275,4.14724531131301));
#21469=CARTESIAN_POINT('Ctrl Pts',(11.1891728305482,0.208753630990335,4.59690782052167));
#21470=CARTESIAN_POINT('Ctrl Pts',(11.236888666611,-0.389170704067994,4.49842069353791));
#21471=CARTESIAN_POINT('Ctrl Pts',(11.2846045026739,-0.629713593419695,
3.94222617449013));
#21472=CARTESIAN_POINT('Ctrl Pts',(11.3323203387367,-0.291980800545002,
3.43908624837263));
#21473=CARTESIAN_POINT('Ctrl Pts',(11.3800361747996,0.313882454172263,3.45104205114199));
#21474=CARTESIAN_POINT('Ctrl Pts',(11.4277520108624,0.631502621520784,3.96711438515144));
#21475=CARTESIAN_POINT('Ctrl Pts',(11.4754678469252,0.369204214609944,4.51338608528654));
#21476=CARTESIAN_POINT('Ctrl Pts',(11.5231836829881,-0.232140103514266,
4.58820744384271));
#21477=CARTESIAN_POINT('Ctrl Pts',(11.5708995190509,-0.620306592646703,
4.12286885598323));
#21478=CARTESIAN_POINT('Ctrl Pts',(11.6186153551137,-0.438835993107895,
3.54469790709399));
#21479=CARTESIAN_POINT('Ctrl Pts',(11.6663311911766,0.145624451261577,3.38463787584353));
#21480=CARTESIAN_POINT('Ctrl Pts',(11.7140470272394,0.596355721317347,3.78967435176932));
#21481=CARTESIAN_POINT('Ctrl Pts',(11.7617628633022,0.499444356375145,4.38785610674141));
#21482=CARTESIAN_POINT('Ctrl Pts',(11.8094786993651,-0.0561144459655822,
4.62986363095956));
#21483=CARTESIAN_POINT('Ctrl Pts',(11.8571945354279,-0.560142489144378,
4.29345769116983));
#21484=CARTESIAN_POINT('Ctrl Pts',(11.9049103714908,-0.549783065641843,
3.68756503815187));
#21485=CARTESIAN_POINT('Ctrl Pts',(11.9526262075536,-0.0345493934605723,
3.36858621802886));
#21486=CARTESIAN_POINT('Ctrl Pts',(12.0003420436164,0.512411518346294,3.62944438943981));
#21487=CARTESIAN_POINT('Ctrl Pts',(12.0480578796793,0.588817048391095,4.23058947975914));
#21488=CARTESIAN_POINT('Ctrl Pts',(12.0957737157421,0.1245028227835,4.61998070274044));
#21489=CARTESIAN_POINT('Ctrl Pts',(12.1434895518049,-0.454144260708352,
4.44003410676589));
#21490=CARTESIAN_POINT('Ctrl Pts',(12.1912053878678,-0.615743681684068,
3.85599741975318));
#21491=CARTESIAN_POINT('Ctrl Pts',(12.2389212239306,-0.211896205334937,
3.40420051794564));
#21492=CARTESIAN_POINT('Ctrl Pts',(12.2866370599935,0.386538816815474,3.49953544806202));
#21493=CARTESIAN_POINT('Ctrl Pts',(12.3343528960563,0.63000929582004,4.05445467686));
#21494=CARTESIAN_POINT('Ctrl Pts',(12.3820687321191,0.294932544534008,4.55936733800455));
#21495=CARTESIAN_POINT('Ctrl Pts',(12.429784568182,-0.310985300518122,4.55060436568669));
#21496=CARTESIAN_POINT('Ctrl Pts',(12.4775004042448,-0.631320558980542,
4.0362129322216));
#21497=CARTESIAN_POINT('Ctrl Pts',(12.5252162403077,-0.371904434015698,
3.48856660588983));
#21498=CARTESIAN_POINT('Ctrl Pts',(12.5729320763705,0.229037255191033,3.41057743478371));
#21499=CARTESIAN_POINT('Ctrl Pts',(12.6206479124333,0.619650508764677,3.87386407474765));
#21500=CARTESIAN_POINT('Ctrl Pts',(12.6683637484962,0.44122916559109,4.4529832757215));
#21501=CARTESIAN_POINT('Ctrl Pts',(12.716079584559,-0.142379709528176,4.61612096455669));
#21502=CARTESIAN_POINT('Ctrl Pts',(12.7637954206218,-0.595239106594286,
4.21346529139986));
#21503=CARTESIAN_POINT('Ctrl Pts',(12.8115112566847,-0.501481273143938,
3.61478115656484));
#21504=CARTESIAN_POINT('Ctrl Pts',(12.8592270927475,0.0527945297157079,
3.36984941301012));
#21505=CARTESIAN_POINT('Ctrl Pts',(12.9069429288104,0.558588303589165,3.70359464960132));
#21506=CARTESIAN_POINT('Ctrl Pts',(12.9546587648732,0.551421843290858,4.30953348024615));
#21507=CARTESIAN_POINT('Ctrl Pts',(13.002374600936,0.0378762195828894,4.63122295319618));
#21508=CARTESIAN_POINT('Ctrl Pts',(13.0500904369989,-0.510451719368595,
4.37325067561256));
#21509=CARTESIAN_POINT('Ctrl Pts',(13.0978062730617,-0.590023990114621,
3.77251655941407));
#21510=CARTESIAN_POINT('Ctrl Pts',(13.1455221091246,-0.127768152052348,
3.38068398698829));
#21511=CARTESIAN_POINT('Ctrl Pts',(13.1932379451874,0.451819146005312,3.55757883871291));
#21512=CARTESIAN_POINT('Ctrl Pts',(13.2409537812502,0.616493970155128,4.14075585037205));
#21513=CARTESIAN_POINT('Ctrl Pts',(13.2886696173131,0.215032895532453,4.59467459882739));
#21514=CARTESIAN_POINT('Ctrl Pts',(13.3363854533759,-0.383896195764066,
4.50249451293469));
#21515=CARTESIAN_POINT('Ctrl Pts',(13.3841012894387,-0.630287503488198,
3.94886598394213));
#21516=CARTESIAN_POINT('Ctrl Pts',(13.4318171255016,-0.297876098539286,
3.4421946086935));
#21517=CARTESIAN_POINT('Ctrl Pts',(13.4795329615644,0.308079511111167,3.44776450722078));
#21518=CARTESIAN_POINT('Ctrl Pts',(13.5272487976272,0.631120965295637,3.96046075600252));
#21519=CARTESIAN_POINT('Ctrl Pts',(13.5749646336901,0.374594326004835,4.50946650093658));
#21520=CARTESIAN_POINT('Ctrl Pts',(13.6226804697529,-0.225928046730791,
4.59062131891086));
#21521=CARTESIAN_POINT('Ctrl Pts',(13.6703963058158,-0.618977217803688,
4.12939949185215));
#21522=CARTESIAN_POINT('Ctrl Pts',(13.7181121418786,-0.443610085578744,
3.54934812035851));
#21523=CARTESIAN_POINT('Ctrl Pts',(13.7658279779415,0.139131014051702,3.38313730411011));
#21524=CARTESIAN_POINT('Ctrl Pts',(13.8135438140043,0.594105962672646,3.78340099315002));
#21525=CARTESIAN_POINT('Ctrl Pts',(13.8612596500671,0.503504264276035,4.38257088298437));
#21526=CARTESIAN_POINT('Ctrl Pts',(13.90897548613,-0.0494731474142026,4.63042004436449));
#21527=CARTESIAN_POINT('Ctrl Pts',(13.9566913221928,-0.557018606591754,
4.29934477874546));
#21528=CARTESIAN_POINT('Ctrl Pts',(14.0044071582556,-0.553045308503159,
3.69337659679301));
#21529=CARTESIAN_POINT('Ctrl Pts',(14.0521229943185,-0.0412019939202257,
3.36898540401303));
#21530=CARTESIAN_POINT('Ctrl Pts',(14.0998388303813,0.50847774565382,3.62406462413548));
#21531=CARTESIAN_POINT('Ctrl Pts',(14.1475546664442,0.591214547458171,4.22437108442359));
#21532=CARTESIAN_POINT('Ctrl Pts',(14.195270502507,0.131029933326566,4.61863412549262));
#21533=CARTESIAN_POINT('Ctrl Pts',(14.2429863385698,-0.4494814847335,4.44479593021223));
#21534=CARTESIAN_POINT('Ctrl Pts',(14.2907021746327,-0.617227139201166,
3.86249478815283));
#21535=CARTESIAN_POINT('Ctrl Pts',(14.3384180106955,-0.218163614480107,
3.40646679792233));
#21536=CARTESIAN_POINT('Ctrl Pts',(14.3861338467583,0.381242914296727,3.49548947984197));
#21537=CARTESIAN_POINT('Ctrl Pts',(14.4338496828212,0.630548208698617,4.0478119353149));
#21538=CARTESIAN_POINT('Ctrl Pts',(14.481565518884,0.300811380821271,4.55622795490698));
#21539=CARTESIAN_POINT('Ctrl Pts',(14.5292813549469,-0.305165166642291,
4.55385128484077));
#21540=CARTESIAN_POINT('Ctrl Pts',(14.5769971910097,-0.630903846008588,
4.04286445780787));
#21541=CARTESIAN_POINT('Ctrl Pts',(14.6247130270726,-0.37727381588172,3.49251453961553));
#21542=CARTESIAN_POINT('Ctrl Pts',(14.6724288631354,0.222812564473163,3.40819632836178));
#21543=CARTESIAN_POINT('Ctrl Pts',(14.7201446991982,0.618286738460357,3.86734053484336));
#21544=CARTESIAN_POINT('Ctrl Pts',(14.7678605352611,0.44597868695508,4.44830796940654));
#21545=CARTESIAN_POINT('Ctrl Pts',(14.8155763713239,-0.135878455045208,
4.6175872975589));
#21546=CARTESIAN_POINT('Ctrl Pts',(14.8632922073867,-0.592956321018707,
4.2197267075609));
#21547=CARTESIAN_POINT('Ctrl Pts',(14.9110080434496,-0.505513273594975,
3.62008770107973));
#21548=CARTESIAN_POINT('Ctrl Pts',(14.9587238795124,0.0461503912925444,
3.36932800439917));
#21549=CARTESIAN_POINT('Ctrl Pts',(15.0064397155752,0.555433441741075,3.69772410541485));
#21550=CARTESIAN_POINT('Ctrl Pts',(15.0541555516381,0.554653416196733,4.30370481154056));
#21551=CARTESIAN_POINT('Ctrl Pts',(15.1018713877009,0.0445266241191229,
4.63078871612938));
#21552=CARTESIAN_POINT('Ctrl Pts',(15.1495872237638,-0.506489652017253,
4.37860963676461));
#21553=CARTESIAN_POINT('Ctrl Pts',(15.1973030598266,-0.592388687361149,
3.77874750230084));
#21554=CARTESIAN_POINT('Ctrl Pts',(15.2450188958894,-0.134288076029725,
3.38206494088146));
#21555=CARTESIAN_POINT('Ctrl Pts',(15.2927347319523,0.447131341807447,3.5528416524037));
#21556=CARTESIAN_POINT('Ctrl Pts',(15.3404505680151,0.617943168462805,4.13425075493917));
#21557=CARTESIAN_POINT('Ctrl Pts',(15.3881664040779,0.221288275240951,4.59237532350063));
#21558=CARTESIAN_POINT('Ctrl Pts',(15.4358822401408,-0.378579046092452,
4.50651251762549));
#21559=CARTESIAN_POINT('Ctrl Pts',(15.4835980762036,-0.630791404211772,
3.95551147311801));
#21560=CARTESIAN_POINT('Ctrl Pts',(15.5313139122665,-0.303738309870084,
3.44536492739022));
#21561=CARTESIAN_POINT('Ctrl Pts',(15.5790297483293,0.302242348039936,3.44454830299756));
#21562=CARTESIAN_POINT('Ctrl Pts',(15.6267455843921,0.630669207148581,3.95381151868517));
#21563=CARTESIAN_POINT('Ctrl Pts',(15.674461420455,0.379942829239589,4.50549032746533));
#21564=CARTESIAN_POINT('Ctrl Pts',(15.7221772565178,-0.219690894932002,
4.59296959056563));
#21565=CARTESIAN_POINT('Ctrl Pts',(15.7698930925806,-0.617579089908608,
4.13591575463957));
#21566=CARTESIAN_POINT('Ctrl Pts',(15.8176089286435,-0.448334903946386,
3.5540483898953));
#21567=CARTESIAN_POINT('Ctrl Pts',(15.8653247647063,0.13262212282903,3.3817052505577));
#21568=CARTESIAN_POINT('Ctrl Pts',(15.9130406007692,0.591790213556878,3.77715169332057));
#21569=CARTESIAN_POINT('Ctrl Pts',(15.960756436832,0.507508245312566,4.37724316506909));
#21570=CARTESIAN_POINT('Ctrl Pts',(16.0084722728949,-0.0428263536203826,
4.63090643370248));
#21571=CARTESIAN_POINT('Ctrl Pts',(16.0561881089577,-0.553832853055588,
4.30519861652357));
#21572=CARTESIAN_POINT('Ctrl Pts',(16.1039039450205,-0.556246121716014,
3.69922221370673));
#21573=CARTESIAN_POINT('Ctrl Pts',(16.1516197810833,-0.0478500178579074,
3.36945468010413));
#21574=CARTESIAN_POINT('Ctrl Pts',(16.1993356171462,0.504487493666278,3.61872661594874));
#21575=CARTESIAN_POINT('Ctrl Pts',(16.247051453209,0.593546377218863,4.21812776701271));
#21576=CARTESIAN_POINT('Ctrl Pts',(16.2947672892719,0.137542489686435,4.61721883330181));
#21577=CARTESIAN_POINT('Ctrl Pts',(16.3424831253347,-0.444768782488292,
4.44950834783736));
#21578=CARTESIAN_POINT('Ctrl Pts',(16.3901989613976,-0.618642038056621,
3.86900742997889));
#21579=CARTESIAN_POINT('Ctrl Pts',(16.4379147974604,-0.224406791046256,
3.40879900475058));
#21580=CARTESIAN_POINT('Ctrl Pts',(16.4856306335233,0.375904665124208,3.49149955025639));
#21581=CARTESIAN_POINT('Ctrl Pts',(16.533346469586,0.631017083274371,4.04116388304691));
#21582=CARTESIAN_POINT('Ctrl Pts',(16.5810623056489,0.306656804407812,4.55302678864769));
#21583=CARTESIAN_POINT('Ctrl Pts',(16.6287781417117,-0.29931113646787,4.55703668482238));
#21584=CARTESIAN_POINT('Ctrl Pts',(16.6764939777746,-0.630417055231307,
4.04951122221356));
#21585=CARTESIAN_POINT('Ctrl Pts',(16.7242098138374,-0.382601291962586,
3.49651884241796));
#21586=CARTESIAN_POINT('Ctrl Pts',(16.7719256499003,0.216563124792967,3.40588095668335));
#21587=CARTESIAN_POINT('Ctrl Pts',(16.8196414859631,0.616854291799135,3.86083173012294));
#21588=CARTESIAN_POINT('Ctrl Pts',(16.8673573220259,0.450678671122871,4.44358286716973));
#21589=CARTESIAN_POINT('Ctrl Pts',(16.9150731580887,-0.129362107828251,
4.61898503189482));
#21590=CARTESIAN_POINT('Ctrl Pts',(16.9627889941516,-0.590607672668797,
4.22596371752193));
#21591=CARTESIAN_POINT('Ctrl Pts',(17.0105048302144,-0.509489124030439,
3.62543644444997));
#21592=CARTESIAN_POINT('Ctrl Pts',(17.0582206662773,0.0395011267029154,
3.3688766478407));
#21593=CARTESIAN_POINT('Ctrl Pts',(17.1059365023401,0.552216884982031,3.69188713660034));
#21594=CARTESIAN_POINT('Ctrl Pts',(17.153652338403,0.557823380833178,4.29784240874569));
#21595=CARTESIAN_POINT('Ctrl Pts',(17.2013681744658,0.0511720828492506,
4.63028441404532));
#21596=CARTESIAN_POINT('Ctrl Pts',(17.2490840105287,-0.502471326198846,
4.38392654375487));
#21597=CARTESIAN_POINT('Ctrl Pts',(17.2967998465914,-0.594687584883411,
3.78500302086511));
#21598=CARTESIAN_POINT('Ctrl Pts',(17.3445156826543,-0.140793083924855,
3.38351453206865));
#21599=CARTESIAN_POINT('Ctrl Pts',(17.3922315187171,0.442393872381948,3.5481541343218));
#21600=CARTESIAN_POINT('Ctrl Pts',(17.43994735478,0.61932372857571,4.1277307475695));
#21601=CARTESIAN_POINT('Ctrl Pts',(17.4876631908428,0.227519075297936,4.590010249934));
#21602=CARTESIAN_POINT('Ctrl Pts',(17.5353790269057,-0.373219845656906,
4.51047426130944));
#21603=CARTESIAN_POINT('Ctrl Pts',(17.5830948629685,-0.631225239619516,
3.96216190386831));
#21604=CARTESIAN_POINT('Ctrl Pts',(17.6308106990313,-0.309566783390781,
3.44859685231885));
#21605=CARTESIAN_POINT('Ctrl Pts',(17.6785265350942,0.29637161332294,3.44139379571298));
#21606=CARTESIAN_POINT('Ctrl Pts',(17.726242371157,0.630147397258769,3.94716741176515));
#21607=CARTESIAN_POINT('Ctrl Pts',(17.7739582072198,0.385249130227842,4.50145800652724));
#21608=CARTESIAN_POINT('Ctrl Pts',(17.8216740432827,-0.213429340911116,
4.59525199797214));
#21609=CARTESIAN_POINT('Ctrl Pts',(17.8693898793456,-0.616112364258878,
4.14241692054995));
#21610=CARTESIAN_POINT('Ctrl Pts',(17.9171057154084,-0.453009923400427,
3.55879819362073));
#21611=CARTESIAN_POINT('Ctrl Pts',(17.9648215514712,0.126098500570276,3.38034187425201));
#21612=CARTESIAN_POINT('Ctrl Pts',(18.012537387534,0.589408731192455,3.77092714642348));
#21613=CARTESIAN_POINT('Ctrl Pts',(18.0602532235969,0.511455854741549,4.3718735447732));
#21614=CARTESIAN_POINT('Ctrl Pts',(18.1079690596597,-0.0361748028784226,
4.6313227449477));
#21615=CARTESIAN_POINT('Ctrl Pts',(18.1556848957226,-0.55058558239424,4.31101855428765));
#21616=CARTESIAN_POINT('Ctrl Pts',(18.2034007317854,-0.559385149749292,
3.70510123958967));
#21617=CARTESIAN_POINT('Ctrl Pts',(18.2511165678482,-0.0544927268426965,
3.36999399417717));
#21618=CARTESIAN_POINT('Ctrl Pts',(18.2988324039111,0.500441205601937,3.6134309578002));
#21619=CARTESIAN_POINT('Ctrl Pts',(18.3465482399739,0.595812278664582,4.21186022100458));
#21620=CARTESIAN_POINT('Ctrl Pts',(18.3942640760367,0.144039768479226,4.61573498337195));
#21621=CARTESIAN_POINT('Ctrl Pts',(18.4419799120996,-0.440006677437314,
4.4541708362083));
#21622=CARTESIAN_POINT('Ctrl Pts',(18.4896957481624,-0.619988221090196,
3.87553462183804));
#21623=CARTESIAN_POINT('Ctrl Pts',(18.5374115842252,-0.230625041570952,
3.41119687937986));
#21624=CARTESIAN_POINT('Ctrl Pts',(18.5851274202881,0.370524662245315,3.48756610248778));
#21625=CARTESIAN_POINT('Ctrl Pts',(18.6328432563509,0.631415867466904,4.03451125849008));
#21626=CARTESIAN_POINT('Ctrl Pts',(18.6805590924138,0.31246816601179,4.54976419479712));
#21627=CARTESIAN_POINT('Ctrl Pts',(18.7282749284766,-0.293423860232864,
4.56016021181225));
#21628=CARTESIAN_POINT('Ctrl Pts',(18.7759907645394,-0.629860240718928,
4.05615248714788));
#21629=CARTESIAN_POINT('Ctrl Pts',(18.8237066006023,-0.387886270507855,
3.50057906951772));
#21630=CARTESIAN_POINT('Ctrl Pts',(18.8714224366651,0.210289630309142,3.40363157692976));
#21631=CARTESIAN_POINT('Ctrl Pts',(18.919138272728,0.615353327889266,3.85433838355196));
#21632=CARTESIAN_POINT('Ctrl Pts',(18.9668541087908,0.455328596044662,4.43880849385601));
#21633=CARTESIAN_POINT('Ctrl Pts',(19.0145699448537,-0.122831391686292,
4.62031401230505));
#21634=CARTESIAN_POINT('Ctrl Pts',(19.0622857809165,-0.588193422413584,
4.2321756285162));
#21635=CARTESIAN_POINT('Ctrl Pts',(19.1100016169793,-0.513408382846255,
3.63082679254236));
#21636=CARTESIAN_POINT('Ctrl Pts',(19.1577174530421,0.0328474745430158,
3.36849539350727));
#21637=CARTESIAN_POINT('Ctrl Pts',(19.205433289105,0.548938990540088,3.68608439142882));
#21638=CARTESIAN_POINT('Ctrl Pts',(19.2531491251678,0.560931385193363,4.2919469231649));
#21639=CARTESIAN_POINT('Ctrl Pts',(19.3008649612307,0.0578118574426247,
4.62971010270368));
#21640=CARTESIAN_POINT('Ctrl Pts',(19.3485807972935,-0.498397187901359,
4.38920080648958));
#21641=CARTESIAN_POINT('Ctrl Pts',(19.3962966333563,-0.596920427988996,
3.79128241936144));
#21642=CARTESIAN_POINT('Ctrl Pts',(19.4440124694192,-0.147282451949449,
3.38503260125846));
#21643=CARTESIAN_POINT('Ctrl Pts',(19.491728305482,0.437607261597584,3.54351680188243));
#21644=CARTESIAN_POINT('Ctrl Pts',(19.5394441415449,0.620635501579114,4.12119655861503));
#21645=CARTESIAN_POINT('Ctrl Pts',(19.5871599776077,0.233724595248439,4.58757962923414));
#21646=CARTESIAN_POINT('Ctrl Pts',(19.6348758136705,-0.367819173932889,
4.51437932582758));
#21647=CARTESIAN_POINT('Ctrl Pts',(19.6825916497334,-0.631588991354928,
3.96881649615688));
#21648=CARTESIAN_POINT('Ctrl Pts',(19.7303074857962,-0.315360815373557,
3.4518901025469));
#21649=CARTESIAN_POINT('Ctrl Pts',(19.778023321859,0.290467852693633,3.43830118837221));
#21650=CARTESIAN_POINT('Ctrl Pts',(19.8257391579219,0.629555794415491,3.94052945152661));
#21651=CARTESIAN_POINT('Ctrl Pts',(19.8734549939847,0.390512260364629,4.49736946054851));
#21652=CARTESIAN_POINT('Ctrl Pts',(19.9211708300476,-0.207143364153331,
4.59746927979605));
#21653=CARTESIAN_POINT('Ctrl Pts',(19.9688866661104,-0.61457855576007,4.14890039401813));
#21654=CARTESIAN_POINT('Ctrl Pts',(20.0166025021732,-0.45763207183192,3.5636005413983));
#21655=CARTESIAN_POINT('Ctrl Pts',(20.0643183382361,0.119556051622903,3.37904064719698));
#21656=CARTESIAN_POINT('Ctrl Pts',(20.1120341742989,0.586970881772813,3.7647406560623));
#21657=CARTESIAN_POINT('Ctrl Pts',(20.1597500103618,0.515329468049299,4.36643880344312));
#21658=CARTESIAN_POINT('Ctrl Pts',(20.2074658464246,-0.029486781418557,
4.63171390504007));
#21659=CARTESIAN_POINT('Ctrl Pts',(20.2551816824874,-0.547338447674763,
4.31671898245684));
#21660=CARTESIAN_POINT('Ctrl Pts',(20.3028975185503,-0.562346186529673,
3.71117381387971));
#21661=CARTESIAN_POINT('Ctrl Pts',(20.3506133546131,-0.0613491664957494,
3.37029669484294));
#21662=CARTESIAN_POINT('Ctrl Pts',(20.398329190676,0.496762641213801,3.60878154740643));
#21663=CARTESIAN_POINT('Ctrl Pts',(20.4380923873949,0.580417208789547,4.10498761157686));
#21664=CARTESIAN_POINT('Ctrl Pts',(20.4699029447702,0.374745574175769,4.41137453781958));
#21665=CARTESIAN_POINT('Ctrl Pts',(20.4937608628016,0.13332385162888,4.54159545884303));
#21666=CARTESIAN_POINT('Ctrl Pts',(20.517618780833,-0.143293564288956,4.53872805560682));
#21667=CARTESIAN_POINT('Ctrl Pts',(20.5414766988645,-0.38346854803195,4.40448715909776));
#21668=CARTESIAN_POINT('Ctrl Pts',(20.5653346168959,-0.530621786340447,
4.17114564603877));
#21669=CARTESIAN_POINT('Ctrl Pts',(20.5891925349273,-0.547627617499454,
3.89605651468078));
#21670=CARTESIAN_POINT('Ctrl Pts',(20.6130504529587,-0.430933317123153,
3.64633026976583));
#21671=CARTESIAN_POINT('Ctrl Pts',(20.6369083709901,-0.208752997660079,
3.48311457674551));
#21672=CARTESIAN_POINT('Ctrl Pts',(20.6607662890215,0.0644142843662171,
3.4462762657402));
#21673=CARTESIAN_POINT('Ctrl Pts',(20.684624207053,0.321861676845817,3.54484653226013));
#21674=CARTESIAN_POINT('Ctrl Pts',(20.7084821250844,0.500588620804837,3.75470996102831));
#21675=CARTESIAN_POINT('Ctrl Pts',(20.7323400431158,0.556916750317041,4.02455574134091));
#21676=CARTESIAN_POINT('Ctrl Pts',(20.7561979611472,0.47705893600668,4.28839577951569));
#21677=CARTESIAN_POINT('Ctrl Pts',(20.7800558791787,0.280549668164313,4.48171582646486));
#21678=CARTESIAN_POINT('Ctrl Pts',(20.8039137972101,0.0154370662995263,
4.55724289713534));
#21679=CARTESIAN_POINT('Ctrl Pts',(20.8277717152415,-0.253449631274377,
4.49650907789895));
#21680=CARTESIAN_POINT('Ctrl Pts',(20.8516296332729,-0.460361354274216,
4.31436517051053));
#21681=CARTESIAN_POINT('Ctrl Pts',(20.8754875513043,-0.554701993332711,
4.05535046556385));
#21682=CARTESIAN_POINT('Ctrl Pts',(20.8993454693358,-0.513402987365846,
3.78280103771366));
#21683=CARTESIAN_POINT('Ctrl Pts',(20.9232033873672,-0.346562912086465,
3.56336268648205));
#21684=CARTESIAN_POINT('Ctrl Pts',(20.9470613053986,-0.0949787932613798,
3.45069404477467));
#21685=CARTESIAN_POINT('Ctrl Pts',(20.97091922343,0.179830242856268,3.47234567582879));
#21686=CARTESIAN_POINT('Ctrl Pts',(20.9947771414614,0.410665878084123,3.62302316008453));
#21687=CARTESIAN_POINT('Ctrl Pts',(21.0186350594928,0.541082524061315,3.86588175144064));
#21688=CARTESIAN_POINT('Ctrl Pts',(21.0424929775243,0.539189751860116,4.14153590729571));
#21689=CARTESIAN_POINT('Ctrl Pts',(21.0663508955557,0.405450399288564,4.38258067876424));
#21690=CARTESIAN_POINT('Ctrl Pts',(21.0902088135871,0.172567379211795,4.53007405282339));
#21691=CARTESIAN_POINT('Ctrl Pts',(21.1140667316185,-0.102513065388571,
4.54794988212627));
#21692=CARTESIAN_POINT('Ctrl Pts',(21.1379246496499,-0.352526273278862,
4.43183703934844));
#21693=CARTESIAN_POINT('Ctrl Pts',(21.1617825676814,-0.516337204635697,
4.21012827746935));
#21694=CARTESIAN_POINT('Ctrl Pts',(21.1856404857128,-0.553889624765765,
3.93703742795684));
#21695=CARTESIAN_POINT('Ctrl Pts',(21.2094984037442,-0.456000943963824,
3.67934264238169));
#21696=CARTESIAN_POINT('Ctrl Pts',(21.2333563217756,-0.246607611160355,
3.50005731527167));
#21697=CARTESIAN_POINT('Ctrl Pts',(21.257214239807,0.0230880000356606,3.44302159274494));
#21698=CARTESIAN_POINT('Ctrl Pts',(21.2810721578385,0.287137966314551,3.52218226257825));
#21699=CARTESIAN_POINT('Ctrl Pts',(21.3049300758698,0.480974878350452,3.71818238470557));
#21700=CARTESIAN_POINT('Ctrl Pts',(21.3287879939013,0.557200331135927,3.9830945903298));
#21701=CARTESIAN_POINT('Ctrl Pts',(21.3526459119327,0.497175125126959,4.25214062911267));
#21702=CARTESIAN_POINT('Ctrl Pts',(21.3765038299641,0.31557705824565,4.45953141590455));
#21703=CARTESIAN_POINT('Ctrl Pts',(21.4003617479955,0.0568118044769688,
4.55455425412338));
#21704=CARTESIAN_POINT('Ctrl Pts',(21.424219666027,-0.215845483008899,4.51397347145443));
#21705=CARTESIAN_POINT('Ctrl Pts',(21.4480775840584,-0.435722670386138,
4.34771217465862));
#21706=CARTESIAN_POINT('Ctrl Pts',(21.4719355020898,-0.549053796006754,
4.0964257796693));
#21707=CARTESIAN_POINT('Ctrl Pts',(21.4957934201212,-0.528126312578589,
3.82156065496534));
#21708=CARTESIAN_POINT('Ctrl Pts',(21.5196513381527,-0.378057559853047,
3.59032881071252));
#21709=CARTESIAN_POINT('Ctrl Pts',(21.543509256184,-0.135543435662257,3.45927273145963));
#21710=CARTESIAN_POINT('Ctrl Pts',(21.5673671742155,0.14011475067701,3.46043919847993));
#21711=CARTESIAN_POINT('Ctrl Pts',(21.5912250922469,0.381511063826562,3.59354297881304));
#21712=CARTESIAN_POINT('Ctrl Pts',(21.6150830102783,0.529617529717794,3.8260365724933));
#21713=CARTESIAN_POINT('Ctrl Pts',(21.6389409283097,0.548218083101175,4.10106896286759));
#21714=CARTESIAN_POINT('Ctrl Pts',(21.6627988463412,0.432764382005563,4.35138723875747));
#21715=CARTESIAN_POINT('Ctrl Pts',(21.6866567643726,0.211488001244504,4.51578176317496));
#21716=CARTESIAN_POINT('Ctrl Pts',(21.710514682404,-0.0615029566383307,
4.55405359688301));
#21717=CARTESIAN_POINT('Ctrl Pts',(21.7343726004354,-0.319454766316188,
4.4568442340362));
#21718=CARTESIAN_POINT('Ctrl Pts',(21.7582305184669,-0.499291183856609,
4.24792401178047));
#21719=CARTESIAN_POINT('Ctrl Pts',(21.7820884364982,-0.557037306525311,
3.97837961532992));
#21720=CARTESIAN_POINT('Ctrl Pts',(21.8059463545297,-0.478572634356998,
3.71412199185867));
#21721=CARTESIAN_POINT('Ctrl Pts',(21.8298042725611,-0.283083917031579,
3.51976932853855));
#21722=CARTESIAN_POINT('Ctrl Pts',(21.8536621905926,-0.018373470940863,
3.44284614561161));
#21723=CARTESIAN_POINT('Ctrl Pts',(21.8775201086239,0.250829789278194,3.5021622566489));
#21724=CARTESIAN_POINT('Ctrl Pts',(21.9013780266554,0.458698333552465,3.68321325676341));
#21725=CARTESIAN_POINT('Ctrl Pts',(21.9252359446868,0.55440264058141,3.94172724469688));
#21726=CARTESIAN_POINT('Ctrl Pts',(21.9490938627182,0.514540400363477,4.21449050861997));
#21727=CARTESIAN_POINT('Ctrl Pts',(21.9729517807496,0.348859016457567,4.4348050005813));
#21728=CARTESIAN_POINT('Ctrl Pts',(21.996809698781,0.0978721002989983,4.54879782605011));
#21729=CARTESIAN_POINT('Ctrl Pts',(22.0206676168125,-0.177047210365213,
4.52859463409701));
#21730=CARTESIAN_POINT('Ctrl Pts',(22.0445255348439,-0.408673655425848,
4.3791356554785));
#21731=CARTESIAN_POINT('Ctrl Pts',(22.0683834528753,-0.540368259688198,
4.13696768164748));
#21732=CARTESIAN_POINT('Ctrl Pts',(22.0922413709067,-0.53992810512055,3.86130737872913));
#21733=CARTESIAN_POINT('Ctrl Pts',(22.1160992889381,-0.407460821505317,
3.61956119962225));
#21734=CARTESIAN_POINT('Ctrl Pts',(22.1399572069695,-0.175358268020808,
3.47084267015335));
#21735=CARTESIAN_POINT('Ctrl Pts',(22.163815125001,0.0996241586556461,3.45151752178681));
#21736=CARTESIAN_POINT('Ctrl Pts',(22.1876730430324,0.350245764837839,3.56631127970877));
#21737=CARTESIAN_POINT('Ctrl Pts',(22.2115309610638,0.51522274100534,3.78715374318048));
#21738=CARTESIAN_POINT('Ctrl Pts',(22.2353888790952,0.554213722627899,4.06004291426965));
#21739=CARTESIAN_POINT('Ctrl Pts',(22.2592467971266,0.457684352558003,4.31824995726588));
#21740=CARTESIAN_POINT('Ctrl Pts',(22.2831047151581,0.249238691275201,4.49863621678958));
#21741=CARTESIAN_POINT('Ctrl Pts',(22.3069626331895,-0.0201526192614011,
4.55709233866662));
#21742=CARTESIAN_POINT('Ctrl Pts',(22.3308205512209,-0.284616065231974,
4.47932420896945));
#21743=CARTESIAN_POINT('Ctrl Pts',(22.3546784692523,-0.479483130864429,
4.28434825342259));
#21744=CARTESIAN_POINT('Ctrl Pts',(22.3785363872838,-0.557103509392546,
4.01984140485232));
#21745=CARTESIAN_POINT('Ctrl Pts',(22.4023943053151,-0.498496906094933,
3.75048279151596));
#21746=CARTESIAN_POINT('Ctrl Pts',(22.4262522233466,-0.317994227800984,
3.542137933897));
#21747=CARTESIAN_POINT('Ctrl Pts',(22.450110141378,-0.0597333038680864,
3.44575282046209));
#21748=CARTESIAN_POINT('Ctrl Pts',(22.4739680594094,0.213134049493302,3.48489624527193));
#21749=CARTESIAN_POINT('Ctrl Pts',(22.4978259774408,0.433884304103661,3.6499965589521));
#21750=CARTESIAN_POINT('Ctrl Pts',(22.5216838954723,0.548538061567711,3.90068226732924));
#21751=CARTESIAN_POINT('Ctrl Pts',(22.5455418135037,0.529059256943919,4.17565382996358));
#21752=CARTESIAN_POINT('Ctrl Pts',(22.5693997315351,0.380211173855379,4.40767331583304));
#21753=CARTESIAN_POINT('Ctrl Pts',(22.5932576495665,0.138390873272415,4.54000544018811));
#21754=CARTESIAN_POINT('Ctrl Pts',(22.6171155675979,-0.137269333605106,
4.54029177230974));
#21755=CARTESIAN_POINT('Ctrl Pts',(22.6409734856293,-0.379364264814148,
4.40846158181013));
#21756=CARTESIAN_POINT('Ctrl Pts',(22.6648314036608,-0.528692759685234,
4.17675229015827));
#21757=CARTESIAN_POINT('Ctrl Pts',(22.6886893216921,-0.54874438127821,3.90182058373076));
#21758=CARTESIAN_POINT('Ctrl Pts',(22.7125472397236,-0.434607562942265,
3.65089956353622));
#21759=CARTESIAN_POINT('Ctrl Pts',(22.736405157755,-0.214207731687487,3.48533716867003));
#21760=CARTESIAN_POINT('Ctrl Pts',(22.7602630757864,0.0585913648593265,
3.44563509732658));
#21761=CARTESIAN_POINT('Ctrl Pts',(22.7841209938179,0.31702578011682,3.5414689143437));
#21762=CARTESIAN_POINT('Ctrl Pts',(22.8079789118493,0.498012898707086,3.74946820019106));
#21763=CARTESIAN_POINT('Ctrl Pts',(22.8238841905369,0.537376264140017,3.92891364167179));
#21764=CARTESIAN_POINT('Ctrl Pts',(22.8318368298807,0.534391234777113,4.01792167950194));
#21765=CARTESIAN_POINT('Ctrl Pts',(3.99999999999998,0.254694598474614,4.53673594206822));
#21766=CARTESIAN_POINT('Ctrl Pts',(4.00795263934379,0.165296026927429,4.57915779516171));
#21767=CARTESIAN_POINT('Ctrl Pts',(4.0238579180314,-0.0350146299391769,
4.61842892627033));
#21768=CARTESIAN_POINT('Ctrl Pts',(4.04771583606282,-0.327086058023631,
4.5259865276721));
#21769=CARTESIAN_POINT('Ctrl Pts',(4.07157375409423,-0.539100294705402,
4.30498302442502));
#21770=CARTESIAN_POINT('Ctrl Pts',(4.09543167212566,-0.619328256935644,
4.00937412827253));
#21771=CARTESIAN_POINT('Ctrl Pts',(4.11928959015708,-0.548093442686671,
3.71148804617917));
#21772=CARTESIAN_POINT('Ctrl Pts',(4.1431475081885,-0.342845496867427,3.48414304986991));
#21773=CARTESIAN_POINT('Ctrl Pts',(4.16700542621991,-0.0537568536316998,
3.38294333505492));
#21774=CARTESIAN_POINT('Ctrl Pts',(4.19086334425134,0.248473820944083,3.43262855616194));
#21775=CARTESIAN_POINT('Ctrl Pts',(4.21472126228276,0.489947458130694,3.62105272953394));
#21776=CARTESIAN_POINT('Ctrl Pts',(4.23857918031417,0.611614759069978,3.90213920826301));
#21777=CARTESIAN_POINT('Ctrl Pts',(4.26243709834559,0.583726034554802,4.20715564703007));
#21778=CARTESIAN_POINT('Ctrl Pts',(4.28629501637702,0.413100159498109,4.46151671210738));
#21779=CARTESIAN_POINT('Ctrl Pts',(4.31015293440843,0.141460167127662,4.60302446238992));
#21780=CARTESIAN_POINT('Ctrl Pts',(4.33401085243986,-0.164770755236008,
4.59707625642582));
#21781=CARTESIAN_POINT('Ctrl Pts',(4.35786877047126,-0.430710704813839,
4.44512666775742));
#21782=CARTESIAN_POINT('Ctrl Pts',(4.38172668850269,-0.59133017320549,4.18433147003372));
#21783=CARTESIAN_POINT('Ctrl Pts',(4.40558460653411,-0.607353296958831,
3.87846221409715));
#21784=CARTESIAN_POINT('Ctrl Pts',(4.42944252456553,-0.474862000813124,
3.60231225357117));
#21785=CARTESIAN_POINT('Ctrl Pts',(4.45330044259694,-0.226254007744579,
3.42340778189093));
#21786=CARTESIAN_POINT('Ctrl Pts',(4.47715836062837,0.0776792518003291,
3.38549581251083));
#21787=CARTESIAN_POINT('Ctrl Pts',(4.50101627865978,0.362617819109035,3.49784685630402));
#21788=CARTESIAN_POINT('Ctrl Pts',(4.5248741966912,0.558886451727075,3.73298802180378));
#21789=CARTESIAN_POINT('Ctrl Pts',(4.54873211472262,0.618492123352341,4.03342088939383));
#21790=CARTESIAN_POINT('Ctrl Pts',(4.57259003275404,0.5268596233165,4.32568143907503));
#21791=CARTESIAN_POINT('Ctrl Pts',(4.59644795078546,0.306395594072305,4.5383040055633));
#21792=CARTESIAN_POINT('Ctrl Pts',(4.62030586881688,0.0110094959969652,
4.61929657956068));
#21793=CARTESIAN_POINT('Ctrl Pts',(4.6441637868483,-0.287068723725306,4.54885427056805));
#21794=CARTESIAN_POINT('Ctrl Pts',(4.66802170487971,-0.514950820910697,
4.34420214192463));
#21795=CARTESIAN_POINT('Ctrl Pts',(4.69187962291114,-0.616913415399932,
4.05538321370614));
#21796=CARTESIAN_POINT('Ctrl Pts',(4.71573754094255,-0.568023875442366,
3.75302158112612));
#21797=CARTESIAN_POINT('Ctrl Pts',(4.73959545897398,-0.380237025278099,
3.51105289951885));
#21798=CARTESIAN_POINT('Ctrl Pts',(4.76345337700539,-0.0994718649854296,
3.38864510263028));
#21799=CARTESIAN_POINT('Ctrl Pts',(4.78731129503681,0.205616875855751,3.41573023112194));
#21800=CARTESIAN_POINT('Ctrl Pts',(4.81116921306823,0.460426689658758,3.5856852332931));
#21801=CARTESIAN_POINT('Ctrl Pts',(4.83502713109965,0.60264963606909,3.85695148163183));
#21802=CARTESIAN_POINT('Ctrl Pts',(4.85888504913107,0.597508330613982,4.16319698927494));
#21803=CARTESIAN_POINT('Ctrl Pts',(4.88274296716248,0.446259962523644,4.42953638764361));
#21804=CARTESIAN_POINT('Ctrl Pts',(4.90660088519391,0.185888877718945,4.59084243889714));
#21805=CARTESIAN_POINT('Ctrl Pts',(4.93045880322533,-0.119937101199393,
4.60767141961541));
#21806=CARTESIAN_POINT('Ctrl Pts',(4.95431672125674,-0.396435191853442,
4.47590818560059));
#21807=CARTESIAN_POINT('Ctrl Pts',(4.97817463928816,-0.575994079421511,
4.22777243672773));
#21808=CARTESIAN_POINT('Ctrl Pts',(5.00203255731958,-0.614706724807315,
3.92394012267834));
#21809=CARTESIAN_POINT('Ctrl Pts',(5.025890475351,-0.503106831702736,3.63870652046354));
#21810=CARTESIAN_POINT('Ctrl Pts',(5.04974839338242,-0.268483613891896,
3.44181901543221));
#21811=CARTESIAN_POINT('Ctrl Pts',(5.07360631141384,0.0317911608623165,
3.38142196567243));
#21812=CARTESIAN_POINT('Ctrl Pts',(5.09746422944526,0.32429213081186,3.47228409503311));
#21813=CARTESIAN_POINT('Ctrl Pts',(5.12132214747667,0.537494841237617,3.69218713785082));
#21814=CARTESIAN_POINT('Ctrl Pts',(5.1451800655081,0.619265421915264,3.98735881011802));
#21815=CARTESIAN_POINT('Ctrl Pts',(5.16903798353952,0.549608738483219,4.28562159765047));
#21816=CARTESIAN_POINT('Ctrl Pts',(5.19289590157094,0.34555774745058,4.51404212438126));
#21817=CARTESIAN_POINT('Ctrl Pts',(5.21675381960235,0.0570084743622218,
4.61676534947452));
#21818=CARTESIAN_POINT('Ctrl Pts',(5.24061173763377,-0.245480923587363,
4.56867264627043));
#21819=CARTESIAN_POINT('Ctrl Pts',(5.26446965566519,-0.487943548953736,
4.38152399072137));
#21820=CARTESIAN_POINT('Ctrl Pts',(5.28832757369661,-0.611090685285508,
4.10108232693608));
#21821=CARTESIAN_POINT('Ctrl Pts',(5.31218549172803,-0.584809503288917,
3.79592328078761));
#21822=CARTESIAN_POINT('Ctrl Pts',(5.33604340975945,-0.415526467847156,
3.5406665514248));
#21823=CARTESIAN_POINT('Ctrl Pts',(5.35990132779088,-0.144635892303038,
3.39772936223054));
#21824=CARTESIAN_POINT('Ctrl Pts',(5.38375924582228,0.161622098711782,3.40206374949372));
#21825=CARTESIAN_POINT('Ctrl Pts',(5.40761716385371,0.428359084093981,3.55260983746209));
#21826=CARTESIAN_POINT('Ctrl Pts',(5.43147508188512,0.590350605148055,3.81255500683439));
#21827=CARTESIAN_POINT('Ctrl Pts',(5.45533299991655,0.607985322415754,4.11833558293467));
#21828=CARTESIAN_POINT('Ctrl Pts',(5.47919091794796,0.476951067165249,4.39517988561105));
#21829=CARTESIAN_POINT('Ctrl Pts',(5.50304883597938,0.2292892841064,4.57539194177126));
#21830=CARTESIAN_POINT('Ctrl Pts',(5.5269067540108,-0.0744399746307492,
4.61490499480714));
#21831=CARTESIAN_POINT('Ctrl Pts',(5.55076467204222,-0.359966631867259,
4.5040570269359));
#21832=CARTESIAN_POINT('Ctrl Pts',(5.57462259007364,-0.55747164231658,4.26995338574299));
#21833=CARTESIAN_POINT('Ctrl Pts',(5.59848050810506,-0.618659650999605,
3.96983878834977));
#21834=CARTESIAN_POINT('Ctrl Pts',(5.62233842613648,-0.528568523057477,
3.67709942878664));
#21835=CARTESIAN_POINT('Ctrl Pts',(5.6461963441679,-0.309227993320144,3.46331805450751));
#21836=CARTESIAN_POINT('Ctrl Pts',(5.67005426219932,-0.0142727959960426,
3.38077003484781));
#21837=CARTESIAN_POINT('Ctrl Pts',(5.69391218023074,0.284172488697173,3.4496406091084));
#21838=CARTESIAN_POINT('Ctrl Pts',(5.71777009826216,0.513129859266986,3.65308904601577));
#21839=CARTESIAN_POINT('Ctrl Pts',(5.74162801629357,0.616613001744231,3.94136666067651));
#21840=CARTESIAN_POINT('Ctrl Pts',(5.765485934325,0.569317469330215,4.24398172424487));
#21841=CARTESIAN_POINT('Ctrl Pts',(5.78934385235641,0.382808307322586,4.48693660973462));
#21842=CARTESIAN_POINT('Ctrl Pts',(5.81320177038783,0.102692087527565,4.61082223133738));
#21843=CARTESIAN_POINT('Ctrl Pts',(5.83705968841925,-0.202535146533943,
4.58534517687525));
#21844=CARTESIAN_POINT('Ctrl Pts',(5.86091760645067,-0.458237017319611,
4.41673528603543));
#21845=CARTESIAN_POINT('Ctrl Pts',(5.88477552448209,-0.601887460912657,
4.14622225884759));
#21846=CARTESIAN_POINT('Ctrl Pts',(5.9086334425135,-0.598360014525416,3.83995392008642));
#21847=CARTESIAN_POINT('Ctrl Pts',(5.93249136054493,-0.448517265794504,
3.57282118150817));
#21848=CARTESIAN_POINT('Ctrl Pts',(5.95634927857635,-0.188999790056246,
3.41014534911766));
#21849=CARTESIAN_POINT('Ctrl Pts',(5.98020719660777,0.116733210556207,3.39170495376011));
#21850=CARTESIAN_POINT('Ctrl Pts',(6.00406511463918,0.393921897475357,3.52200944135141));
#21851=CARTESIAN_POINT('Ctrl Pts',(6.02792303267061,0.574785693380153,3.76919531120668));
#21852=CARTESIAN_POINT('Ctrl Pts',(6.05178095070201,0.61509921541814,4.07281983667942));
#21853=CARTESIAN_POINT('Ctrl Pts',(6.07563886873346,0.505003308517799,4.35863675364492));
#21854=CARTESIAN_POINT('Ctrl Pts',(6.09949678676485,0.27142206589204,4.55675943366228));
#21855=CARTESIAN_POINT('Ctrl Pts',(6.12335470479629,-0.0285325303540597,
4.61873507756083));
#21856=CARTESIAN_POINT('Ctrl Pts',(6.14721262282769,-0.321503980505702,
4.52942105023226));
#21857=CARTESIAN_POINT('Ctrl Pts',(6.17107054085913,-0.535870591003297,
4.31063422072759));
#21858=CARTESIAN_POINT('Ctrl Pts',(6.19492845889052,-0.619180264299368,
4.01591706164003));
#21859=CARTESIAN_POINT('Ctrl Pts',(6.21878637692196,-0.551125001039776,
3.71725450231754));
#21860=CARTESIAN_POINT('Ctrl Pts',(6.24264429495337,-0.348226295733882,
3.48783145534908));
#21861=CARTESIAN_POINT('Ctrl Pts',(6.2665022129848,-0.0603247367796791,
3.38345774569467));
#21862=CARTESIAN_POINT('Ctrl Pts',(6.29036013101621,0.242607149567705,3.43020375417728));
#21863=CARTESIAN_POINT('Ctrl Pts',(6.31421804904763,0.485688404846908,3.61560451082823));
#21864=CARTESIAN_POINT('Ctrl Pts',(6.33807596707905,0.61099356578022,3.89627130770405));
#21865=CARTESIAN_POINT('Ctrl Pts',(6.36193388511046,0.585080291527744,4.19994745529594));
#21866=CARTESIAN_POINT('Ctrl Pts',(6.3937444424857,0.363797450650833,4.54512657044717));
#21867=CARTESIAN_POINT('Ctrl Pts',(6.43350763920472,-0.178959141669374,
4.67939801199369));
#21868=CARTESIAN_POINT('Ctrl Pts',(6.48122347526757,-0.668951848353412,
4.21606826543601));
#21869=CARTESIAN_POINT('Ctrl Pts',(6.5289393113304,-0.543175254381078,3.55462676401443));
#21870=CARTESIAN_POINT('Ctrl Pts',(6.57665514739324,0.0806513803028556,
3.30201433154981));
#21871=CARTESIAN_POINT('Ctrl Pts',(6.62437098345608,0.630812951656228,3.69045991683978));
#21872=CARTESIAN_POINT('Ctrl Pts',(6.67208681951892,0.601478580142798,4.36311480674272));
#21873=CARTESIAN_POINT('Ctrl Pts',(6.71980265558175,0.0199087309838695,
4.70234020845997));
#21874=CARTESIAN_POINT('Ctrl Pts',(6.76751849164459,-0.580002689552455,
4.39658285339385));
#21875=CARTESIAN_POINT('Ctrl Pts',(6.81523432770743,-0.64725742864426,3.72664421308375));
#21876=CARTESIAN_POINT('Ctrl Pts',(6.86295016377027,-0.120142281411799,
3.30772876957018));
#21877=CARTESIAN_POINT('Ctrl Pts',(6.91066599983311,0.517310146858294,3.52453857056345));
#21878=CARTESIAN_POINT('Ctrl Pts',(6.95838183589594,0.679704059947864,4.17797090041396));
#21879=CARTESIAN_POINT('Ctrl Pts',(7.00609767195879,0.217917737520193,4.66797035296266));
#21880=CARTESIAN_POINT('Ctrl Pts',(7.05381350802161,-0.443987099894697,
4.54456206689342));
#21881=CARTESIAN_POINT('Ctrl Pts',(7.10152934408447,-0.698171061503544,
3.92107420680554));
#21882=CARTESIAN_POINT('Ctrl Pts',(7.14924518014729,-0.311214160204793,
3.3700650369752));
#21883=CARTESIAN_POINT('Ctrl Pts',(7.19696101621015,0.361535686685884,3.39753487888718));
#21884=CARTESIAN_POINT('Ctrl Pts',(7.24467685227297,0.702281647003851,3.97825768917858));
#21885=CARTESIAN_POINT('Ctrl Pts',(7.29239268833582,0.398111619195611,4.5789468099385));
#21886=CARTESIAN_POINT('Ctrl Pts',(7.34010852439865,-0.271650463017158,
4.64798016059173));
#21887=CARTESIAN_POINT('Ctrl Pts',(7.38782436046149,-0.691951729928866,
4.1219633626529));
#21888=CARTESIAN_POINT('Ctrl Pts',(7.43554019652432,-0.476823084268312,
3.48394573037578));
#21889=CARTESIAN_POINT('Ctrl Pts',(7.48325603258717,0.17617954081454,3.31982867534575));
#21890=CARTESIAN_POINT('Ctrl Pts',(7.53097186865001,0.667393780433987,3.78032341303133));
#21891=CARTESIAN_POINT('Ctrl Pts',(7.57868770471284,0.545730043505963,4.44255054095139));
#21892=CARTESIAN_POINT('Ctrl Pts',(7.62640354077568,-0.077085990144297,
4.69837669746149));
#21893=CARTESIAN_POINT('Ctrl Pts',(7.67411937683852,-0.629112772588521,
4.31287278685955));
#21894=CARTESIAN_POINT('Ctrl Pts',(7.72183521290136,-0.603415615998442,
3.64005298187887));
#21895=CARTESIAN_POINT('Ctrl Pts',(7.76955104896419,-0.0235926144000291,
3.29777806215626));
#21896=CARTESIAN_POINT('Ctrl Pts',(7.81726688502703,0.577895847971041,3.60036435301798));
#21897=CARTESIAN_POINT('Ctrl Pts',(7.86498272108987,0.648693661106154,4.26994220769392));
#21898=CARTESIAN_POINT('Ctrl Pts',(7.9126985571527,0.123786103798515,4.6916279794467));
#21899=CARTESIAN_POINT('Ctrl Pts',(7.96041439321555,-0.514796137313916,
4.47818113561083));
#21900=CARTESIAN_POINT('Ctrl Pts',(8.00813022927838,-0.680633164378164,
3.82561319718015));
#21901=CARTESIAN_POINT('Ctrl Pts',(8.05584606534123,-0.221434283704469,
3.33318734306526));
#21902=CARTESIAN_POINT('Ctrl Pts',(8.10356190140405,0.441111106898351,3.45310581204486));
#21903=CARTESIAN_POINT('Ctrl Pts',(8.1512777374669,0.698577380670183,4.07524562887252));
#21904=CARTESIAN_POINT('Ctrl Pts',(8.19899357352974,0.314529296777622,4.62828622690367));
#21905=CARTESIAN_POINT('Ctrl Pts',(8.24670940959258,-0.358355880000973,
4.60436191534297));
#21906=CARTESIAN_POINT('Ctrl Pts',(8.29442524565541,-0.70215733816079,4.02544275761943));
#21907=CARTESIAN_POINT('Ctrl Pts',(8.34214108171825,-0.401156908608127,
3.42315912408683));
#21908=CARTESIAN_POINT('Ctrl Pts',(8.3898569177811,0.268232082711808,3.35059734274305));
#21909=CARTESIAN_POINT('Ctrl Pts',(8.43757275384392,0.691299425196396,3.8743920139026));
#21910=CARTESIAN_POINT('Ctrl Pts',(8.48528858990677,0.479535868514212,4.51353443142269));
#21911=CARTESIAN_POINT('Ctrl Pts',(8.53300442596961,-0.172592854832336,
4.68109027882443));
#21912=CARTESIAN_POINT('Ctrl Pts',(8.58072026203244,-0.66622690390392,4.22319044326068));
#21913=CARTESIAN_POINT('Ctrl Pts',(8.62843609809529,-0.548054535901959,
3.56033138942427));
#21914=CARTESIAN_POINT('Ctrl Pts',(8.67615193415812,0.0734047453217555,
3.30122678585069));
#21915=CARTESIAN_POINT('Ctrl Pts',(8.72386777022095,0.627455319439314,3.68381637683837));
#21916=CARTESIAN_POINT('Ctrl Pts',(8.7715836062838,0.605304019074675,4.35676225408577));
#21917=CARTESIAN_POINT('Ctrl Pts',(8.81929944234663,0.0272927241942496,
4.70208786391332));
#21918=CARTESIAN_POINT('Ctrl Pts',(8.86701527840948,-0.575781899266294,
4.40267538529889));
#21919=CARTESIAN_POINT('Ctrl Pts',(8.9147311144723,-0.650107145087294,3.73347990440727));
#21920=CARTESIAN_POINT('Ctrl Pts',(8.96244695053515,-0.127428996390418,
3.30903392823725));
#21921=CARTESIAN_POINT('Ctrl Pts',(9.01016278659798,0.512269160438921,3.51911272764658));
#21922=CARTESIAN_POINT('Ctrl Pts',(9.05787862266082,0.681542664962993,4.17079770865984));
#21923=CARTESIAN_POINT('Ctrl Pts',(9.10559445872366,0.224945053369686,4.66563652575022));
#21924=CARTESIAN_POINT('Ctrl Pts',(9.1533102947865,-0.438223061957547,4.54921107910972));
#21925=CARTESIAN_POINT('Ctrl Pts',(9.20102613084934,-0.698964196560635,
3.92843664782408));
#21926=CARTESIAN_POINT('Ctrl Pts',(9.24874196691217,-0.317835754515511,
3.3733799439853));
#21927=CARTESIAN_POINT('Ctrl Pts',(9.29645780297501,0.355166151432911,3.39375807937372));
#21928=CARTESIAN_POINT('Ctrl Pts',(9.34417363903786,0.702013515586798,3.97085749870423));
#21929=CARTESIAN_POINT('Ctrl Pts',(9.39188947510068,0.404191066510942,4.57471892538967));
#21930=CARTESIAN_POINT('Ctrl Pts',(9.43960531116354,-0.264806258220881,
4.65080711970243));
#21931=CARTESIAN_POINT('Ctrl Pts',(9.48732114722635,-0.690627921460452,
4.12924912203773));
#21932=CARTESIAN_POINT('Ctrl Pts',(9.53503698328922,-0.482235337746388,
3.48899966685243));
#21933=CARTESIAN_POINT('Ctrl Pts',(9.58275281935202,0.169001376764621,3.31800968034731));
#21934=CARTESIAN_POINT('Ctrl Pts',(9.63046865541491,0.665041526572246,3.77330189814918));
#21935=CARTESIAN_POINT('Ctrl Pts',(9.6781844914777,0.550363809549371,4.43677447107931));
#21936=CARTESIAN_POINT('Ctrl Pts',(9.72590032754056,-0.0697214622184181,
4.69915032657822));
#21937=CARTESIAN_POINT('Ctrl Pts',(9.7736161636034,-0.625780442428439,4.31948567936979));
#21938=CARTESIAN_POINT('Ctrl Pts',(9.82133199966623,-0.607175613486645,
3.64643241687702));
#21939=CARTESIAN_POINT('Ctrl Pts',(9.86904783572907,-0.030992076082374,
3.29806570630264));
#21940=CARTESIAN_POINT('Ctrl Pts',(9.91676367179191,0.573651961662729,3.59429605827795));
#21941=CARTESIAN_POINT('Ctrl Pts',(9.96447950785474,0.651502576242943,4.26309058249416));
#21942=CARTESIAN_POINT('Ctrl Pts',(10.0121953439176,0.131068350403577,4.69028497663703));
#21943=CARTESIAN_POINT('Ctrl Pts',(10.0599111799804,-0.50972795835719,4.48358005533451));
#21944=CARTESIAN_POINT('Ctrl Pts',(10.1076270160433,-0.682433239785766,
3.83279612838271));
#21945=CARTESIAN_POINT('Ctrl Pts',(10.1553428521061,-0.228449576533966,
3.33555808949935));
#21946=CARTESIAN_POINT('Ctrl Pts',(10.2030586881689,0.435322847997542,3.44848728078164));
#21947=CARTESIAN_POINT('Ctrl Pts',(10.2507745242318,0.699331602909907,4.06787908823615));
#21948=CARTESIAN_POINT('Ctrl Pts',(10.2984903602946,0.321133386270249,4.62493648450936));
#21949=CARTESIAN_POINT('Ctrl Pts',(10.3462061963575,-0.351966560253669,
4.60810509117381));
#21950=CARTESIAN_POINT('Ctrl Pts',(10.3939220324203,-0.701850198794989,
4.03284143571381));
#21951=CARTESIAN_POINT('Ctrl Pts',(10.4416378684831,-0.407214000429435,
3.42741898450738));
#21952=CARTESIAN_POINT('Ctrl Pts',(10.489353704546,0.261373080323254,3.34780649011919));
#21953=CARTESIAN_POINT('Ctrl Pts',(10.5370695406088,0.689937239673316,3.86711333114163));
#21954=CARTESIAN_POINT('Ctrl Pts',(10.5847853766716,0.484921415782374,4.50845204490092));
#21955=CARTESIAN_POINT('Ctrl Pts',(10.6325012127345,-0.165405205696588,
4.68287142228737));
#21956=CARTESIAN_POINT('Ctrl Pts',(10.6802170487973,-0.66383768169814,4.23019946525991));
#21957=CARTESIAN_POINT('Ctrl Pts',(10.7279328848602,-0.552657800140614,
3.5661317972102));
#21958=CARTESIAN_POINT('Ctrl Pts',(10.775648720923,0.0660362430193439,3.30049197570278));
#21959=CARTESIAN_POINT('Ctrl Pts',(10.8233645569858,0.624088188116435,3.67722113622194));
#21960=CARTESIAN_POINT('Ctrl Pts',(10.8710803930487,0.609030347235101,4.3503630939397));
#21961=CARTESIAN_POINT('Ctrl Pts',(10.9187962291115,0.0346905673513346,
4.70176123146349));
#21962=CARTESIAN_POINT('Ctrl Pts',(10.9665120651743,-0.57150609431415,4.40872123214985));
#21963=CARTESIAN_POINT('Ctrl Pts',(11.0142279012372,-0.65287991581936,3.74034623636848));
#21964=CARTESIAN_POINT('Ctrl Pts',(11.0619437373,-0.134704064778877,3.31041528701663));
#21965=CARTESIAN_POINT('Ctrl Pts',(11.1096595733629,0.507172601636502,3.51374059022208));
#21966=CARTESIAN_POINT('Ctrl Pts',(11.1573754094257,0.68330486411552,4.16360539148934));
#21967=CARTESIAN_POINT('Ctrl Pts',(11.2050912454885,0.231947755880478,4.66322884435941));
#21968=CARTESIAN_POINT('Ctrl Pts',(11.2528070815514,-0.432410545554582,
4.55379904436673));
#21969=CARTESIAN_POINT('Ctrl Pts',(11.3005229176142,-0.699679589515398,
3.93580706063847));
#21970=CARTESIAN_POINT('Ctrl Pts',(11.348238753677,-0.324422100469907,3.37676444086124));
#21971=CARTESIAN_POINT('Ctrl Pts',(11.3959545897399,0.348757195312759,3.39004862475285));
#21972=CARTESIAN_POINT('Ctrl Pts',(11.4436704258027,0.701667392320496,3.9634605418422));
#21973=CARTESIAN_POINT('Ctrl Pts',(11.4913862618656,0.410225626419724,4.57042720558968));
#21974=CARTESIAN_POINT('Ctrl Pts',(11.5391020979284,-0.257932644354891,
4.65356178929341));
#21975=CARTESIAN_POINT('Ctrl Pts',(11.5868179339912,-0.689227399014534,
4.13652052554825));
#21976=CARTESIAN_POINT('Ctrl Pts',(11.6345337700541,-0.487594028032435,
3.49411036255383));
#21977=CARTESIAN_POINT('Ctrl Pts',(11.6822496061169,0.161804441490335,3.31626643773886));
#21978=CARTESIAN_POINT('Ctrl Pts',(11.7299654421798,0.662615402711184,3.76630556374144));
#21979=CARTESIAN_POINT('Ctrl Pts',(11.7776812782426,0.554936443973853,4.43094988641136));
#21980=CARTESIAN_POINT('Ctrl Pts',(11.8253971143054,-0.062349190059417,
4.69984629737339));
#21981=CARTESIAN_POINT('Ctrl Pts',(11.8731129503683,-0.622378603495518,
4.32606308493799));
#21982=CARTESIAN_POINT('Ctrl Pts',(11.9208287864311,-0.610868168815925,
3.65285112447858));
#21983=CARTESIAN_POINT('Ctrl Pts',(11.9685446224939,-0.0383880952977111,
3.29843131798253));
#21984=CARTESIAN_POINT('Ctrl Pts',(12.0162604585568,0.569344356809164,3.58827282720487));
#21985=CARTESIAN_POINT('Ctrl Pts',(12.0639762946196,0.654239125569198,4.25620973444184));
#21986=CARTESIAN_POINT('Ctrl Pts',(12.1116921306825,0.138336038556134,4.68886530024737));
#21987=CARTESIAN_POINT('Ctrl Pts',(12.1594079667453,-0.50460316123658,4.48892526128066));
#21988=CARTESIAN_POINT('Ctrl Pts',(12.2071238028081,-0.684157513748105,
3.83999763179777));
#21989=CARTESIAN_POINT('Ctrl Pts',(12.254839638871,-0.235439494268261,3.33800263898788));
#21990=CARTESIAN_POINT('Ctrl Pts',(12.3025554749338,0.429486235500398,3.44393000893412));
#21991=CARTESIAN_POINT('Ctrl Pts',(12.3502713109967,0.700008146713868,4.06050500791278));
#21992=CARTESIAN_POINT('Ctrl Pts',(12.3979871470595,0.327701805790174,4.62151732713591));
#21993=CARTESIAN_POINT('Ctrl Pts',(12.4457029831223,-0.345538145731053,
4.61178072157682));
#21994=CARTESIAN_POINT('Ctrl Pts',(12.4934188191852,-0.701465101239671,
4.04023646593735));
#21995=CARTESIAN_POINT('Ctrl Pts',(12.541134655248,-0.413225860851952,3.43174244451));
#21996=CARTESIAN_POINT('Ctrl Pts',(12.5888504913108,0.254485045853264,3.34508808005552));
#21997=CARTESIAN_POINT('Ctrl Pts',(12.6365663273737,0.688498419195676,3.85984940880123));
#21998=CARTESIAN_POINT('Ctrl Pts',(12.6842821634365,0.490253100280801,4.50331318193882));
#21999=CARTESIAN_POINT('Ctrl Pts',(12.7319979994994,-0.158199184135511,
4.68457671563321));
#22000=CARTESIAN_POINT('Ctrl Pts',(12.7797138355622,-0.661374723552845,
4.23718291779492));
#22001=CARTESIAN_POINT('Ctrl Pts',(12.827429671625,-0.557199677773407,3.57198039701723));
#22002=CARTESIAN_POINT('Ctrl Pts',(12.8751455076879,0.058660405724426,3.29983486358678));
#22003=CARTESIAN_POINT('Ctrl Pts',(12.9228613437507,0.62065173603916,3.67066174834999));
#22004=CARTESIAN_POINT('Ctrl Pts',(12.9705771798135,0.612689027194643,4.34392501712378));
#22005=CARTESIAN_POINT('Ctrl Pts',(13.0182930158764,0.0420845572448178,
4.7013566507062));
#22006=CARTESIAN_POINT('Ctrl Pts',(13.0660088519392,-0.567166809177069,
4.4147216801859));
#22007=CARTESIAN_POINT('Ctrl Pts',(13.1137246880021,-0.655580167748548,
3.74724140943759));
#22008=CARTESIAN_POINT('Ctrl Pts',(13.1614405240649,-0.141964170879043,
3.31187324159358));
#22009=CARTESIAN_POINT('Ctrl Pts',(13.2091563601277,0.502019708508231,3.50842246418533));
#22010=CARTESIAN_POINT('Ctrl Pts',(13.2568721961906,0.684991165006287,4.15639490180834));
#22011=CARTESIAN_POINT('Ctrl Pts',(13.3045880322534,0.238924694735218,4.66074749465585));
#22012=CARTESIAN_POINT('Ctrl Pts',(13.3523038683163,-0.426549999040181,
4.55832549625387));
#22013=CARTESIAN_POINT('Ctrl Pts',(13.4000197043791,-0.700317265381609,
3.94318460369993));
#22014=CARTESIAN_POINT('Ctrl Pts',(13.4477355404419,-0.330972411156884,
3.38021816378559));
#22015=CARTESIAN_POINT('Ctrl Pts',(13.4954513765048,0.342309500898352,3.3864069206363));
#22016=CARTESIAN_POINT('Ctrl Pts',(13.5431672125676,0.70124333116994,3.95606764360979));
#22017=CARTESIAN_POINT('Ctrl Pts',(13.5908830486304,0.416214620412595,4.5660721254426));
#22018=CARTESIAN_POINT('Ctrl Pts',(13.6385988846933,-0.251030380554765,
4.65624386434224));
#22019=CARTESIAN_POINT('Ctrl Pts',(13.6863147207561,-0.687750320459788,
4.14377676500662));
#22020=CARTESIAN_POINT('Ctrl Pts',(13.734030556819,-0.492898558687668,3.49927725007553));
#22021=CARTESIAN_POINT('Ctrl Pts',(13.7817463928818,0.15458953374652,3.31459914100992));
#22022=CARTESIAN_POINT('Ctrl Pts',(13.8294622289446,0.660115678675556,3.75933518700271));
#22023=CARTESIAN_POINT('Ctrl Pts',(13.8771780650075,0.559447438691528,4.42507743387505));
#22024=CARTESIAN_POINT('Ctrl Pts',(13.9248939010703,-0.0549699924482557,
4.7004645325629));
#22025=CARTESIAN_POINT('Ctrl Pts',(13.9726097371331,-0.61890763370075,4.33260427296601));
#22026=CARTESIAN_POINT('Ctrl Pts',(14.020325573196,-0.614492871807821,3.65930839172987));
#22027=CARTESIAN_POINT('Ctrl Pts',(14.0680414092588,-0.0457798505455885,
3.29887485658241));
#22028=CARTESIAN_POINT('Ctrl Pts',(14.1157572453217,0.564973511886205,3.58229532883235));
#22029=CARTESIAN_POINT('Ctrl Pts',(14.1634730813845,0.656903005118004,4.24930042782804));
#22030=CARTESIAN_POINT('Ctrl Pts',(14.2111889174473,0.145588360997982,4.6873691079691));
#22031=CARTESIAN_POINT('Ctrl Pts',(14.2589047535102,-0.499422315191365,
4.49421615972892));
#22032=CARTESIAN_POINT('Ctrl Pts',(14.306620589573,-0.685805794740406,3.8472169075166));
#22033=CARTESIAN_POINT('Ctrl Pts',(14.3543364256359,-0.242403260500786,
3.34052072000184));
#22034=CARTESIAN_POINT('Ctrl Pts',(14.4020522616987,0.423601917710294,3.43943450270243));
#22035=CARTESIAN_POINT('Ctrl Pts',(14.4497680977615,0.700606936934704,4.05312420698026));
#22036=CARTESIAN_POINT('Ctrl Pts',(14.4974839338244,0.334233825748585,4.61802913456711));
#22037=CARTESIAN_POINT('Ctrl Pts',(14.5451997698872,-0.339071350470923,
4.61538839828042));
#22038=CARTESIAN_POINT('Ctrl Pts',(14.59291560595,-0.701002088269634,4.04762702688518));
#22039=CARTESIAN_POINT('Ctrl Pts',(14.6406314420129,-0.419191822106764,
3.43612902386528));
#22040=CARTESIAN_POINT('Ctrl Pts',(14.6883472780757,0.24756874439201,3.34244241450009));
#22041=CARTESIAN_POINT('Ctrl Pts',(14.7360631141386,0.686983123580828,3.85260105372344));
#22042=CARTESIAN_POINT('Ctrl Pts',(14.7837789502014,0.495530329791292,4.49811841333687));
#22043=CARTESIAN_POINT('Ctrl Pts',(14.8314947862642,-0.150975590559777,
4.68620596944608));
#22044=CARTESIAN_POINT('Ctrl Pts',(14.8792106223271,-0.658838303041738,
4.24414002517693));
#22045=CARTESIAN_POINT('Ctrl Pts',(14.9269264583899,-0.561679664310124,
3.57787653921065));
#22046=CARTESIAN_POINT('Ctrl Pts',(14.9746422944528,0.0512780527100071,
3.29925552249156));
#22047=CARTESIAN_POINT('Ctrl Pts',(15.0223581305156,0.617146344912281,3.6641389418082));
#22048=CARTESIAN_POINT('Ctrl Pts',(15.0700739665784,0.616279652564493,4.337448738749));
#22049=CARTESIAN_POINT('Ctrl Pts',(15.1177898026413,0.0494738725853903,
4.70087416658037));
#22050=CARTESIAN_POINT('Ctrl Pts',(15.1655056387041,-0.562764525842253,
4.42067606290572));
#22051=CARTESIAN_POINT('Ctrl Pts',(15.2132214747669,-0.658207600943685,
3.75416465773151));
#22052=CARTESIAN_POINT('Ctrl Pts',(15.2609373108298,-0.14920850827279,3.31340763002542));
#22053=CARTESIAN_POINT('Ctrl Pts',(15.3086531468926,0.496811053413015,3.50315894024854));
#22054=CARTESIAN_POINT('Ctrl Pts',(15.3563689829554,0.686601380328997,4.14916704052379));
#22055=CARTESIAN_POINT('Ctrl Pts',(15.4040848190183,0.245875094968658,4.6581927522561));
#22056=CARTESIAN_POINT('Ctrl Pts',(15.4518006550811,-0.420642073376032,
4.56278993199436));
#22057=CARTESIAN_POINT('Ctrl Pts',(15.499516491144,-0.700877153329261,3.95056845754601));
#22058=CARTESIAN_POINT('Ctrl Pts',(15.5472323272068,-0.337485958999024,
3.3837407291352));
#22059=CARTESIAN_POINT('Ctrl Pts',(15.5949481632696,0.335823784368978,3.38283337152726));
#22060=CARTESIAN_POINT('Ctrl Pts',(15.6426639993325,0.70074137923783,3.94867962517506));
#22061=CARTESIAN_POINT('Ctrl Pts',(15.6903798353953,0.422157383260532,4.56165416869007));
#22062=CARTESIAN_POINT('Ctrl Pts',(15.7380956714582,-0.244100233491204,
4.65885304693675));
#22063=CARTESIAN_POINT('Ctrl Pts',(15.785811507521,-0.686196849863089,4.15101703442422));
#22064=CARTESIAN_POINT('Ctrl Pts',(15.8335273435838,-0.498148340509996,
3.50449975550414));
#22065=CARTESIAN_POINT('Ctrl Pts',(15.8812431796467,0.147357454930898,3.3130079753559));
#22066=CARTESIAN_POINT('Ctrl Pts',(15.9289590157095,0.657542632122849,3.75239154216938));
#22067=CARTESIAN_POINT('Ctrl Pts',(15.9766748517723,0.563896292642505,4.41915776575455));
#22068=CARTESIAN_POINT('Ctrl Pts',(16.0243906878352,-0.0475846890311933,
4.70100496347609));
#22069=CARTESIAN_POINT('Ctrl Pts',(16.072106523898,-0.615367918582998,4.33910851688972));
#22070=CARTESIAN_POINT('Ctrl Pts',(16.1198223599609,-0.618049319847516,
3.66580350138828));
#22071=CARTESIAN_POINT('Ctrl Pts',(16.1675381960237,-0.0531665207849041,
3.29939627283611));
#22072=CARTESIAN_POINT('Ctrl Pts',(16.2152540320865,0.560539912386559,3.57636422711252));
#22073=CARTESIAN_POINT('Ctrl Pts',(16.2629698681494,0.659493918998266,4.24236343010572));
#22074=CARTESIAN_POINT('Ctrl Pts',(16.3106857042122,0.152824512175573,4.68579656599215));
#22075=CARTESIAN_POINT('Ctrl Pts',(16.358401540275,-0.494185995685336,4.49945216299141));
#22076=CARTESIAN_POINT('Ctrl Pts',(16.4061173763379,-0.687377899679438,
3.85445315365633));
#22077=CARTESIAN_POINT('Ctrl Pts',(16.4538332124007,-0.249340101729437,
3.34311205284473));
#22078=CARTESIAN_POINT('Ctrl Pts',(16.5015490484636,0.417670548229327,3.43500126142608));
#22079=CARTESIAN_POINT('Ctrl Pts',(16.5492648845264,0.701127907061643,4.04573750526291));
#22080=CARTESIAN_POINT('Ctrl Pts',(16.5969807205892,0.340728720599694,4.61447229425484));
#22081=CARTESIAN_POINT('Ctrl Pts',(16.6446965566521,-0.3325668927742,4.61892772056098));
#22082=CARTESIAN_POINT('Ctrl Pts',(16.6924123927149,-0.700461211314163,
4.05501229764889));
#22083=CARTESIAN_POINT('Ctrl Pts',(16.7401282287777,-0.425111221523205,
3.4405782353328));
#22084=CARTESIAN_POINT('Ctrl Pts',(16.7878440648406,0.240624944169445,3.3398697873209));
#22085=CARTESIAN_POINT('Ctrl Pts',(16.8355599009034,0.685391521140609,3.84536907102113));
#22086=CARTESIAN_POINT('Ctrl Pts',(16.8832757369663,0.500752518144239,4.49286831610534));
#22087=CARTESIAN_POINT('Ctrl Pts',(16.9309915730291,-0.143735227331884,
4.68775900275617));
#22088=CARTESIAN_POINT('Ctrl Pts',(16.978707409092,-0.656228701898373,4.25107001464348));
#22089=CARTESIAN_POINT('Ctrl Pts',(17.0264232451548,-0.566097262135119,
3.58381956887496));
#22090=CARTESIAN_POINT('Ctrl Pts',(17.0741390812176,0.0438900039728252,
3.29875401676759));
#22091=CARTESIAN_POINT('Ctrl Pts',(17.1218549172805,0.613572404098014,3.65765344111895));
#22092=CARTESIAN_POINT('Ctrl Pts',(17.1695707533433,0.619801824515016,4.33093497816967));
#22093=CARTESIAN_POINT('Ctrl Pts',(17.2172865894061,0.0568576926029748,
4.70031383267802));
#22094=CARTESIAN_POINT('Ctrl Pts',(17.265002425469,-0.558299733294432,4.42658371892475));
#22095=CARTESIAN_POINT('Ctrl Pts',(17.3127182615318,-0.66076192356197,3.76111521224867));
#22096=CARTESIAN_POINT('Ctrl Pts',(17.3604340975947,-0.156436272293483,
3.31501828187956));
#22097=CARTESIAN_POINT('Ctrl Pts',(17.4081499336575,0.491547214903555,3.49795060305896));
#22098=CARTESIAN_POINT('Ctrl Pts',(17.4558657697204,0.688135331228569,4.14192261047223));
#22099=CARTESIAN_POINT('Ctrl Pts',(17.5035816057831,0.252798184563325,4.65556490092881));
#22100=CARTESIAN_POINT('Ctrl Pts',(17.551297441846,-0.414687424786488,4.56719185569987));
#22101=CARTESIAN_POINT('Ctrl Pts',(17.5990132779088,-0.701359191168653,
3.95795780201324));
#22102=CARTESIAN_POINT('Ctrl Pts',(17.6467291139717,-0.343962020502345,
3.38733174564023));
#22103=CARTESIAN_POINT('Ctrl Pts',(17.6944449500345,0.329300766127249,3.37932837435862));
#22104=CARTESIAN_POINT('Ctrl Pts',(17.7421607860974,0.700161592278611,3.94129730716402));
#22105=CARTESIAN_POINT('Ctrl Pts',(17.7898766221602,0.428053254869629,4.55717382605774));
#22106=CARTESIAN_POINT('Ctrl Pts',(17.837592458223,-0.23714297293205,4.66138904726133));
#22107=CARTESIAN_POINT('Ctrl Pts',(17.8853082942859,-0.684567159776581,
4.15824052958626));
#22108=CARTESIAN_POINT('Ctrl Pts',(17.9330241303487,-0.503342790378573,
3.50977729874859));
#22109=CARTESIAN_POINT('Ctrl Pts',(17.9807399664116,0.140109008348428,3.31149311751593));
#22110=CARTESIAN_POINT('Ctrl Pts',(18.0284558024744,0.654896548854854,3.7454754005085));
#22111=CARTESIAN_POINT('Ctrl Pts',(18.0761716385372,0.568282511669218,4.41319153957849));
#22112=CARTESIAN_POINT('Ctrl Pts',(18.1238874746001,-0.040194100132671,
4.70146753008449));
#22113=CARTESIAN_POINT('Ctrl Pts',(18.1716033106629,-0.611759851316993,
4.34557509424858));
#22114=CARTESIAN_POINT('Ctrl Pts',(18.2193191467258,-0.621537117901666,
3.67233573200791));
#22115=CARTESIAN_POINT('Ctrl Pts',(18.2670349827885,-0.0605472855394143,
3.29999550882718));
#22116=CARTESIAN_POINT('Ctrl Pts',(18.3147508188514,0.556044050773433,3.57048018084402));
#22117=CARTESIAN_POINT('Ctrl Pts',(18.3624666549143,0.662011579423562,4.23539951180373));
#22118=CARTESIAN_POINT('Ctrl Pts',(18.4101824909771,0.160043688331546,4.684147848987));
#22119=CARTESIAN_POINT('Ctrl Pts',(18.4578983270399,-0.488894784343999,
4.50463268947774));
#22120=CARTESIAN_POINT('Ctrl Pts',(18.5056141631028,-0.68887365394326,3.86170556644909));
#22121=CARTESIAN_POINT('Ctrl Pts',(18.5533299991656,-0.256249247442801,
3.34577634968359));
#22122=CARTESIAN_POINT('Ctrl Pts',(18.6010458352284,0.41169278588589,3.4306307775285));
#22123=CARTESIAN_POINT('Ctrl Pts',(18.6487616712913,0.701570999227752,4.03834572324048));
#22124=CARTESIAN_POINT('Ctrl Pts',(18.6964775073541,0.347185768921481,4.6108472012761));
#22125=CARTESIAN_POINT('Ctrl Pts',(18.744193343417,-0.326025495125306,4.62239829528727));
#22126=CARTESIAN_POINT('Ctrl Pts',(18.7919091794798,-0.699842530451103,
4.06239145790787));
#22127=CARTESIAN_POINT('Ctrl Pts',(18.8396250155426,-0.430983401602837,
3.44508958471478));
#22128=CARTESIAN_POINT('Ctrl Pts',(18.8873408516055,0.233654416470602,3.33737048427408));
#22129=CARTESIAN_POINT('Ctrl Pts',(18.9350566876683,0.683723788661416,3.83815426398688));
#22130=CARTESIAN_POINT('Ctrl Pts',(18.9827725237312,0.505919085286118,4.48756347340344));
#22131=CARTESIAN_POINT('Ctrl Pts',(19.030488359794,-0.136478898681533,4.68923564305365));
#22132=CARTESIAN_POINT('Ctrl Pts',(19.0782041958568,-0.653546209976322,
4.2579721164561));
#22133=CARTESIAN_POINT('Ctrl Pts',(19.1259200319197,-0.570451980578726,
3.58980882586423));
#22134=CARTESIAN_POINT('Ctrl Pts',(19.1736358679825,0.0364970801727598,
3.29833040216201));
#22135=CARTESIAN_POINT('Ctrl Pts',(19.2213517040453,0.609930310515188,3.65120596658116));
#22136=CARTESIAN_POINT('Ctrl Pts',(19.2690675401082,0.623255151928734,4.32438445905389));
#22137=CARTESIAN_POINT('Ctrl Pts',(19.316783376171,0.0642351969327414,4.69967571095415));
#22138=CARTESIAN_POINT('Ctrl Pts',(19.3644992122339,-0.553772927074266,
4.43244399258532));
#22139=CARTESIAN_POINT('Ctrl Pts',(19.4122150482967,-0.663242852612724,
3.76809229994096));
#22140=CARTESIAN_POINT('Ctrl Pts',(19.4599308843595,-0.163646658734412,
3.3167050201661));
#22141=CARTESIAN_POINT('Ctrl Pts',(19.5076467204224,0.486228775054438,3.49279802752061));
#22142=CARTESIAN_POINT('Ctrl Pts',(19.5553625564852,0.689592852244711,4.13466242315333));
#22143=CARTESIAN_POINT('Ctrl Pts',(19.6030783925481,0.259693185238344,4.65286421968052));
#22144=CARTESIAN_POINT('Ctrl Pts',(19.6507942286109,-0.408686697131164,
4.57153080275077));
#22145=CARTESIAN_POINT('Ctrl Pts',(19.6985100646738,-0.701763358503738,
3.96535177039745));
#22146=CARTESIAN_POINT('Ctrl Pts',(19.7462259007365,-0.350399813749482,
3.39099090115443));
#22147=CARTESIAN_POINT('Ctrl Pts',(19.7939417367994,0.322741052541778,3.37589215469092));
#22148=CARTESIAN_POINT('Ctrl Pts',(19.8416575728622,0.699504257835039,3.93392181877779));
#22149=CARTESIAN_POINT('Ctrl Pts',(19.8893734089251,0.433901159015506,4.55263101135276));
#22150=CARTESIAN_POINT('Ctrl Pts',(19.9370892449879,-0.23015857608315,4.663852686053));
#22151=CARTESIAN_POINT('Ctrl Pts',(19.9848050810507,-0.682862933423436,
4.16544436654047));
#22152=CARTESIAN_POINT('Ctrl Pts',(20.0325209171136,-0.508478494849655,
3.51511322409123));
#22153=CARTESIAN_POINT('Ctrl Pts',(20.0802367531764,0.132839643288252,3.31004731418368));
#22154=CARTESIAN_POINT('Ctrl Pts',(20.1279525892393,0.652187835720725,3.73860154375571));
#22155=CARTESIAN_POINT('Ctrl Pts',(20.1756684253021,0.572586513039731,4.4071529569233));
#22156=CARTESIAN_POINT('Ctrl Pts',(20.2233842613649,-0.0327629883405684,
4.70190215105461));
#22157=CARTESIAN_POINT('Ctrl Pts',(20.2711000974278,-0.608151935097038,
4.35190888358257));
#22158=CARTESIAN_POINT('Ctrl Pts',(20.3188159334906,-0.624827148513498,
3.67908301574286));
#22159=CARTESIAN_POINT('Ctrl Pts',(20.3665317695535,-0.0681655280739813,
3.30033184185188));
#22160=CARTESIAN_POINT('Ctrl Pts',(20.4142476056163,0.551956769749184,3.56531418539817));
#22161=CARTESIAN_POINT('Ctrl Pts',(20.4540108023353,0.644905999548395,4.11665253813788));
#22162=CARTESIAN_POINT('Ctrl Pts',(20.4858213597105,0.416382673412033,4.45708139504444));
#22163=CARTESIAN_POINT('Ctrl Pts',(20.509679277742,0.148137151166912,4.60177085628536));
#22164=CARTESIAN_POINT('Ctrl Pts',(20.5335371957734,-0.159214575149101,
4.59858486262053));
#22165=CARTESIAN_POINT('Ctrl Pts',(20.5573951138048,-0.426074836374489,
4.44942877587387));
#22166=CARTESIAN_POINT('Ctrl Pts',(20.5812530318362,-0.589577924844292,
4.19016123618585));
#22167=CARTESIAN_POINT('Ctrl Pts',(20.6051109498677,-0.608473233900696,
3.88450759853215));
#22168=CARTESIAN_POINT('Ctrl Pts',(20.6289688678991,-0.478813304308425,
3.60703485797333));
#22169=CARTESIAN_POINT('Ctrl Pts',(20.6528267859305,-0.231947052182395,
3.42568465323223));
#22170=CARTESIAN_POINT('Ctrl Pts',(20.6766847039619,0.0715712039811096,
3.38475332414555));
#22171=CARTESIAN_POINT('Ctrl Pts',(20.7005426219933,0.357622970648114,3.49427550111266));
#22172=CARTESIAN_POINT('Ctrl Pts',(20.7244005400248,0.556207844932749,3.72745636179159));
#22173=CARTESIAN_POINT('Ctrl Pts',(20.7482584580561,0.618794460414918,4.02728407199912));
#22174=CARTESIAN_POINT('Ctrl Pts',(20.7721163760876,0.530063832205264,4.32043875618714));
#22175=CARTESIAN_POINT('Ctrl Pts',(20.7959742941189,0.311720881859749,4.53523813880796));
#22176=CARTESIAN_POINT('Ctrl Pts',(20.8198322121505,0.01715224242355,4.619156844639));
#22177=CARTESIAN_POINT('Ctrl Pts',(20.8436901301818,-0.281609823618225,
4.55167503361081));
#22178=CARTESIAN_POINT('Ctrl Pts',(20.8675480482133,-0.511511021444125,
4.34929354512778));
#22179=CARTESIAN_POINT('Ctrl Pts',(20.8914059662447,-0.616333626991818,
4.06150032559224));
#22180=CARTESIAN_POINT('Ctrl Pts',(20.9152638842761,-0.570445985619195,
3.75866857192897));
#22181=CARTESIAN_POINT('Ctrl Pts',(20.9391218023075,-0.385068702031786,
3.51484894167474));
#22182=CARTESIAN_POINT('Ctrl Pts',(20.9629797203389,-0.105531663562905,
3.38966195221662));
#22183=CARTESIAN_POINT('Ctrl Pts',(20.9868376383704,0.199810758127152,3.41371924506628));
#22184=CARTESIAN_POINT('Ctrl Pts',(21.0106955564018,0.456293997792742,3.58113815016051));
#22185=CARTESIAN_POINT('Ctrl Pts',(21.0345534744332,0.60120093052663,3.85098018832832));
#22186=CARTESIAN_POINT('Ctrl Pts',(21.0584113924646,0.599097856858477,4.15726162902184));
#22187=CARTESIAN_POINT('Ctrl Pts',(21.082269310496,0.450499039416452,4.42508831804098));
#22188=CARTESIAN_POINT('Ctrl Pts',(21.1061272285275,0.191740934787398,4.58896933394457));
#22189=CARTESIAN_POINT('Ctrl Pts',(21.1299851465589,-0.113903050943465,
4.60883130459215));
#22190=CARTESIAN_POINT('Ctrl Pts',(21.1538430645903,-0.391694638258801,
4.47981743698434));
#22191=CARTESIAN_POINT('Ctrl Pts',(21.1777009826217,-0.573706216867813,
4.23347513609622));
#22192=CARTESIAN_POINT('Ctrl Pts',(21.2015589006531,-0.615430998064313,
3.9300418046833));
#22193=CARTESIAN_POINT('Ctrl Pts',(21.2254168186846,-0.506666136201032,
3.64371515765586));
#22194=CARTESIAN_POINT('Ctrl Pts',(21.2492747367159,-0.27400760274365,3.44450985958179));
#22195=CARTESIAN_POINT('Ctrl Pts',(21.2731326547474,0.0256532534100022,
3.38113703208972));
#22196=CARTESIAN_POINT('Ctrl Pts',(21.2969905727788,0.319041190319967,3.46909305773936));
#22197=CARTESIAN_POINT('Ctrl Pts',(21.3208484908102,0.534414865691478,3.68687029238709));
#22198=CARTESIAN_POINT('Ctrl Pts',(21.3447064088416,0.619109549231529,3.98121627002784));
#22199=CARTESIAN_POINT('Ctrl Pts',(21.3685643268731,0.552415083779586,4.28015538130547));
#22200=CARTESIAN_POINT('Ctrl Pts',(21.3924222449044,0.350640082858436,4.51058887057447));
#22201=CARTESIAN_POINT('Ctrl Pts',(21.4162801629359,0.0631240304344945,
4.61616947282646));
#22202=CARTESIAN_POINT('Ctrl Pts',(21.4401380809673,-0.239827566894842,
4.57107985485291));
#22203=CARTESIAN_POINT('Ctrl Pts',(21.4639959989987,-0.484134791346583,
4.38634565646493));
#22204=CARTESIAN_POINT('Ctrl Pts',(21.4878539170302,-0.610057871747176,
4.10713942122688));
#22205=CARTESIAN_POINT('Ctrl Pts',(21.5117118350615,-0.586805184862796,
3.80173467907963));
#22206=CARTESIAN_POINT('Ctrl Pts',(21.535569753093,-0.420062646027161,3.5448112085363));
#22207=CARTESIAN_POINT('Ctrl Pts',(21.5594276711244,-0.150603347961132,
3.39919379659958));
#22208=CARTESIAN_POINT('Ctrl Pts',(21.5832855891558,0.155682571034224,3.40048986702667));
#22209=CARTESIAN_POINT('Ctrl Pts',(21.6071435071872,0.423899860703612,3.54838249529388));
#22210=CARTESIAN_POINT('Ctrl Pts',(21.6310014252187,0.588462087630599,3.80670790527556));
#22211=CARTESIAN_POINT('Ctrl Pts',(21.6548593432501,0.609129304746478,4.11229849758833));
#22212=CARTESIAN_POINT('Ctrl Pts',(21.6787172612815,0.480847814502724,4.39042904829107));
#22213=CARTESIAN_POINT('Ctrl Pts',(21.7025751793129,0.234985935581564,4.57308906161293));
#22214=CARTESIAN_POINT('Ctrl Pts',(21.7264330973443,-0.0683364054776661,
4.61561318873779));
#22215=CARTESIAN_POINT('Ctrl Pts',(21.7502910153758,-0.35494863395129,4.5076031222497));
#22216=CARTESIAN_POINT('Ctrl Pts',(21.7741489334072,-0.554766252817153,
4.2754702655401));
#22217=CARTESIAN_POINT('Ctrl Pts',(21.7980068514386,-0.618928411339905,
3.9759774252466));
#22218=CARTESIAN_POINT('Ctrl Pts',(21.82186476947,-0.531745714018629,3.68235875884208));
#22219=CARTESIAN_POINT('Ctrl Pts',(21.8457226875014,-0.314536705157368,
3.46641202827438));
#22220=CARTESIAN_POINT('Ctrl Pts',(21.8695806055329,-0.0204149040773093,
3.3809420914381));
#22221=CARTESIAN_POINT('Ctrl Pts',(21.8934385235643,0.278698897140474,3.44684867604406));
#22222=CARTESIAN_POINT('Ctrl Pts',(21.9172964415957,0.509663226401888,3.6480158268968));
#22223=CARTESIAN_POINT('Ctrl Pts',(21.9411543596271,0.616001013860485,3.93525269592965));
#22224=CARTESIAN_POINT('Ctrl Pts',(21.9650122776585,0.571709773899469,4.23832204448885));
#22225=CARTESIAN_POINT('Ctrl Pts',(21.98887019569,0.387619921158457,4.48311516140836));
#22226=CARTESIAN_POINT('Ctrl Pts',(22.0127281137213,0.108746439139576,4.60977346157076));
#22227=CARTESIAN_POINT('Ctrl Pts',(22.0365860317528,-0.196718509442517,
4.5873255404835));
#22228=CARTESIAN_POINT('Ctrl Pts',(22.0604439497842,-0.454080423961193,
4.42126052632156));
#22229=CARTESIAN_POINT('Ctrl Pts',(22.0843018678156,-0.600407305919173,
4.15218583856754));
#22230=CARTESIAN_POINT('Ctrl Pts',(22.1081597858471,-0.599918246812857,
3.84589756782496));
#22231=CARTESIAN_POINT('Ctrl Pts',(22.1320177038785,-0.452732834916613,
3.57729153941473));
#22232=CARTESIAN_POINT('Ctrl Pts',(22.1558756219099,-0.194841912687001,
3.41204924396571));
#22233=CARTESIAN_POINT('Ctrl Pts',(22.1797335399413,0.110693164578993,3.39057692382254));
#22234=CARTESIAN_POINT('Ctrl Pts',(22.2035914579728,0.389160747889314,3.51812514615901));
#22235=CARTESIAN_POINT('Ctrl Pts',(22.2274493760041,0.572467927805029,3.76350489626149));
#22236=CARTESIAN_POINT('Ctrl Pts',(22.2513072940356,0.615791105677536,4.06671414123586));
#22237=CARTESIAN_POINT('Ctrl Pts',(22.2751652120669,0.508536584364246,4.35360996140145));
#22238=CARTESIAN_POINT('Ctrl Pts',(22.2990231300984,0.276931015980992,4.55403851389998));
#22239=CARTESIAN_POINT('Ctrl Pts',(22.3228810481298,-0.0223917293827815,
4.61898955797298));
#22240=CARTESIAN_POINT('Ctrl Pts',(22.3467389661613,-0.31623908674035,4.53258079431836));
#22241=CARTESIAN_POINT('Ctrl Pts',(22.3705968841927,-0.532757373651304,
4.31594151899069));
#22242=CARTESIAN_POINT('Ctrl Pts',(22.3944548022241,-0.619001969851995,
4.02204593667267));
#22243=CARTESIAN_POINT('Ctrl Pts',(22.4183127202555,-0.553883724721699,
3.72275952141814));
#22244=CARTESIAN_POINT('Ctrl Pts',(22.4421706382869,-0.35332581843718,3.49126595675675));
#22245=CARTESIAN_POINT('Ctrl Pts',(22.4660285563184,-0.0663701307507445,
3.38417172009386));
#22246=CARTESIAN_POINT('Ctrl Pts',(22.4898864743497,0.236814872379406,3.42766427875767));
#22247=CARTESIAN_POINT('Ctrl Pts',(22.5137443923812,0.482092168510832,3.61110849992699));
#22248=CARTESIAN_POINT('Ctrl Pts',(22.5376023104126,0.609484835267769,3.88964730767638));
#22249=CARTESIAN_POINT('Ctrl Pts',(22.561460228444,0.587841786482003,4.19517031382209));
#22250=CARTESIAN_POINT('Ctrl Pts',(22.5853181464754,0.422455543015367,4.45296893898932));
#22251=CARTESIAN_POINT('Ctrl Pts',(22.6091760645069,0.153767157666155,4.60000417439789));
#22252=CARTESIAN_POINT('Ctrl Pts',(22.6330339825383,-0.152521006364708,
4.60032232020799));
#22253=CARTESIAN_POINT('Ctrl Pts',(22.6568919005697,-0.421514535902825,
4.45384478734481));
#22254=CARTESIAN_POINT('Ctrl Pts',(22.6807498186011,-0.587434568575047,
4.19639082134502));
#22255=CARTESIAN_POINT('Ctrl Pts',(22.7046077366325,-0.60971407867596,3.89091209973551));
#22256=CARTESIAN_POINT('Ctrl Pts',(22.728465654664,-0.482895786937606,3.61211183522625));
#22257=CARTESIAN_POINT('Ctrl Pts',(22.7523235726954,-0.23800784887647,3.4281541921173));
#22258=CARTESIAN_POINT('Ctrl Pts',(22.7761814907268,0.0651013135850054,
3.38404091701771));
#22259=CARTESIAN_POINT('Ctrl Pts',(22.8000394087582,0.352249768808992,3.49052260401466));
#22260=CARTESIAN_POINT('Ctrl Pts',(22.8238973267896,0.553345940411564,3.72163220123786));
#22261=CARTESIAN_POINT('Ctrl Pts',(22.8398026054772,0.597082876783669,3.92101540361374));
#22262=CARTESIAN_POINT('Ctrl Pts',(22.847755244821,0.593766187829899,4.01991291515446));
#22263=CARTESIAN_POINT('',(22.8,0.337479661717902,3.51106003648017));
#22264=CARTESIAN_POINT('Ctrl Pts',(22.8,0.337504360408405,3.51101527402275));
#22265=CARTESIAN_POINT('Ctrl Pts',(22.8,0.337610992569967,3.51114843896934));
#22266=CARTESIAN_POINT('Ctrl Pts',(22.8,0.337717562131928,3.51128164981369));
#22267=CARTESIAN_POINT('Ctrl Pts',(22.8,0.337824069051012,3.51141490653789));
#22268=CARTESIAN_POINT('Ctrl Pts',(22.8,0.354145371784291,3.53183539523119));
#22269=CARTESIAN_POINT('Ctrl Pts',(22.8,0.368999739942303,3.55333386321799));
#22270=CARTESIAN_POINT('Ctrl Pts',(22.8,0.382262544471458,3.57576050230915));
#22271=CARTESIAN_POINT('Ctrl Pts',(22.8,0.395177725624396,3.59759933027929));
#22272=CARTESIAN_POINT('Ctrl Pts',(22.8,0.406583379369087,3.62031953557487));
#22273=CARTESIAN_POINT('Ctrl Pts',(22.8,0.416319965152677,3.64376476659274));
#22274=CARTESIAN_POINT('Ctrl Pts',(22.8,0.420499854003763,3.65382973822867));
#22275=CARTESIAN_POINT('Ctrl Pts',(22.8,0.424371599987778,3.66402799385056));
#22276=CARTESIAN_POINT('Ctrl Pts',(22.8,0.42792023461967,3.67434527679585));
#22277=CARTESIAN_POINT('Ctrl Pts',(22.8,0.430015882150509,3.68043815216119));
#22278=CARTESIAN_POINT('Ctrl Pts',(22.8,0.431995626466768,3.68656321156818));
#22279=CARTESIAN_POINT('Ctrl Pts',(22.8,0.433857425300493,3.69271766785326));
#22280=CARTESIAN_POINT('Ctrl Pts',(22.8,0.440667704273582,3.71523007009016));
#22281=CARTESIAN_POINT('Ctrl Pts',(22.8,0.445903532435623,3.73813926926309));
#22282=CARTESIAN_POINT('Ctrl Pts',(22.8,0.449441836754149,3.76130640751661));
#22283=CARTESIAN_POINT('Ctrl Pts',(22.8,0.450038513826676,3.76521316594877));
#22284=CARTESIAN_POINT('Ctrl Pts',(22.8,0.450586822418701,3.76912718643627));
#22285=CARTESIAN_POINT('Ctrl Pts',(22.8,0.451086059471329,3.77304770583064));
#22286=CARTESIAN_POINT('Ctrl Pts',(22.8,0.453684096906641,3.79345015011803));
#22287=CARTESIAN_POINT('Ctrl Pts',(22.8,0.454954433743694,3.81403106227893));
#22288=CARTESIAN_POINT('Ctrl Pts',(22.8,0.45484641916779,3.83463783350426));
#22289=CARTESIAN_POINT('Ctrl Pts',(22.8,0.454808390965019,3.84189276616533));
#22290=CARTESIAN_POINT('Ctrl Pts',(22.8,0.454599381710613,3.84915061719132));
#22291=CARTESIAN_POINT('Ctrl Pts',(22.8,0.454216814112443,3.8564037154462));
#22292=CARTESIAN_POINT('Ctrl Pts',(22.8,0.453866695925276,3.86304160538904));
#22293=CARTESIAN_POINT('Ctrl Pts',(22.8,0.453371644107099,3.86966645154658));
#22294=CARTESIAN_POINT('Ctrl Pts',(22.8,0.452731182295137,3.87626933737115));
#22295=CARTESIAN_POINT('Ctrl Pts',(22.8,0.450713457978438,3.89707120727158));
#22296=CARTESIAN_POINT('Ctrl Pts',(22.8,0.447253508643,3.9176725514372));
#22297=CARTESIAN_POINT('Ctrl Pts',(22.8,0.442312061254715,3.9379035771693));
#22298=CARTESIAN_POINT('Ctrl Pts',(22.8,0.437564183511961,3.95734209977996));
#22299=CARTESIAN_POINT('Ctrl Pts',(22.8,0.431447509288203,3.97643919003209));
#22300=CARTESIAN_POINT('Ctrl Pts',(22.8,0.423915075143768,3.9949978423605));
#22301=CARTESIAN_POINT('Ctrl Pts',(22.8,0.421325190817866,4.00137888225459));
#22302=CARTESIAN_POINT('Ctrl Pts',(22.8,0.418567902041021,4.00769582483512));
#22303=CARTESIAN_POINT('Ctrl Pts',(22.8,0.415641328671541,4.01393920819689));
#22304=CARTESIAN_POINT('Ctrl Pts',(22.6211545887425,-1.51173456864708E-7,
4.59404872180247));
#22305=CARTESIAN_POINT('Ctrl Pts',(22.6251143866744,-0.0492822808754852,
4.59404929162283));
#22306=CARTESIAN_POINT('Ctrl Pts',(22.6290741846063,-0.0985642856931001,
4.58798571459226));
#22307=CARTESIAN_POINT('Ctrl Pts',(22.6330339825383,-0.14630523394925,4.57585637376244));
#22308=CARTESIAN_POINT('Ctrl Pts',(22.6409866218821,-0.242185516210759,
4.55149647592026));
#22309=CARTESIAN_POINT('Ctrl Pts',(22.6489392612259,-0.331850026056775,
4.50267063163255));
#22310=CARTESIAN_POINT('Ctrl Pts',(22.6568919005697,-0.404335619758509,
4.43534871515538));
#22311=CARTESIAN_POINT('Ctrl Pts',(22.6648445399135,-0.476821213460227,
4.36802679867822));
#22312=CARTESIAN_POINT('Ctrl Pts',(22.6727971792573,-0.532127891017642,
4.28220881001161));
#22313=CARTESIAN_POINT('Ctrl Pts',(22.6807498186011,-0.563494481479829,
4.18838669541007));
#22314=CARTESIAN_POINT('Ctrl Pts',(22.6887024579449,-0.594861071942019,
4.09456458080851));
#22315=CARTESIAN_POINT('Ctrl Pts',(22.6966550972887,-0.602287575308989,
3.99273834027202));
#22316=CARTESIAN_POINT('Ctrl Pts',(22.7046077366325,-0.584864445036083,
3.89535850925222));
#22317=CARTESIAN_POINT('Ctrl Pts',(22.7125603759763,-0.567441314763176,
3.79797867823242));
#22318=CARTESIAN_POINT('Ctrl Pts',(22.7205130153201,-0.525168550850394,
3.70504525672934));
#22319=CARTESIAN_POINT('Ctrl Pts',(22.7284656546639,-0.463217512550482,
3.62791893879298));
#22320=CARTESIAN_POINT('Ctrl Pts',(22.7364182940078,-0.401266474250563,
3.5507926208566));
#22321=CARTESIAN_POINT('Ctrl Pts',(22.7443709333516,-0.319637161563486,
3.48947340648693));
#22322=CARTESIAN_POINT('Ctrl Pts',(22.7523235726954,-0.228304311476372,
3.45146158678551));
#22323=CARTESIAN_POINT('Ctrl Pts',(22.7602762120392,-0.136971461389268,
3.41344976708409));
#22324=CARTESIAN_POINT('Ctrl Pts',(22.768228851383,-0.0359350739021178,
3.3987453420509));
#22325=CARTESIAN_POINT('Ctrl Pts',(22.7761814907268,0.062441195712126,3.40914007736714));
#22326=CARTESIAN_POINT('Ctrl Pts',(22.7841209938178,0.160654966376612,3.41951764255099));
#22327=CARTESIAN_POINT('Ctrl Pts',(22.7920604969089,0.256217399931083,3.45491151845628));
#22328=CARTESIAN_POINT('Ctrl Pts',(22.8,0.337504360408238,3.51101527402264));
#22329=CARTESIAN_POINT('',(4.,-0.219892372742957,4.3529863453938));
#22330=CARTESIAN_POINT('Ctrl Pts',(4.,-0.219914231356238,4.35301468169996));
#22331=CARTESIAN_POINT('Ctrl Pts',(4.,-0.219843051329574,4.3531167999744));
#22332=CARTESIAN_POINT('Ctrl Pts',(4.,-0.219771822781512,4.35321888245988));
#22333=CARTESIAN_POINT('Ctrl Pts',(4.,-0.21970054575756,4.3533209291203));
#22334=CARTESIAN_POINT('Ctrl Pts',(4.,-0.207925336055227,4.3701793886806));
#22335=CARTESIAN_POINT('Ctrl Pts',(4.,-0.194831304039315,4.38605734350833));
#22336=CARTESIAN_POINT('Ctrl Pts',(4.,-0.18064579384139,4.40088380688851));
#22337=CARTESIAN_POINT('Ctrl Pts',(4.,-0.168975273508986,4.41308164397169));
#22338=CARTESIAN_POINT('Ctrl Pts',(4.,-0.156565051628872,4.42456888924957));
#22339=CARTESIAN_POINT('Ctrl Pts',(4.,-0.143515931303371,4.43531683418355));
#22340=CARTESIAN_POINT('Ctrl Pts',(4.,-0.133182439541062,4.44382804395605));
#22341=CARTESIAN_POINT('Ctrl Pts',(4.,-0.122447811630206,4.45187590303098));
#22342=CARTESIAN_POINT('Ctrl Pts',(4.,-0.111352162047151,4.45944712768208));
#22343=CARTESIAN_POINT('Ctrl Pts',(4.,-0.105068105051177,4.46373511522897));
#22344=CARTESIAN_POINT('Ctrl Pts',(4.,-0.0986661212125077,4.46787107983396));
#22345=CARTESIAN_POINT('Ctrl Pts',(4.,-0.0921733602714696,4.47184061613108));
#22346=CARTESIAN_POINT('Ctrl Pts',(4.,-0.0718171345235072,4.48428598070136));
#22347=CARTESIAN_POINT('Ctrl Pts',(4.,-0.0505350523745213,4.49512244469223));
#22348=CARTESIAN_POINT('Ctrl Pts',(4.,-0.0285775088988711,4.50429938857761));
#22349=CARTESIAN_POINT('Ctrl Pts',(4.,-0.00645956782426854,4.51354336909515));
#22350=CARTESIAN_POINT('Ctrl Pts',(4.,0.0163444141029789,4.52110543571878));
#22351=CARTESIAN_POINT('Ctrl Pts',(4.,0.0396343143342583,4.52702898180467));
#22352=CARTESIAN_POINT('Ctrl Pts',(4.,0.0479455316904685,4.52914285427945));
#22353=CARTESIAN_POINT('Ctrl Pts',(4.,0.0563191235587283,4.53104786585874));
#22354=CARTESIAN_POINT('Ctrl Pts',(4.,0.0647475081636451,4.53274519105122));
#22355=CARTESIAN_POINT('Ctrl Pts',(4.,0.0709442475001029,4.53399310299165));
#22356=CARTESIAN_POINT('Ctrl Pts',(4.,0.0771669940275102,4.53512789739638));
#22357=CARTESIAN_POINT('Ctrl Pts',(4.,0.0834037601527001,4.53614909266968));
#22358=CARTESIAN_POINT('Ctrl Pts',(4.,0.108500755516298,4.54025842313435));
#22359=CARTESIAN_POINT('Ctrl Pts',(4.,0.133859781029961,4.54253781872753));
#22360=CARTESIAN_POINT('Ctrl Pts',(3.99999999999999,0.159256593756596,4.54305292380224));
#22361=CARTESIAN_POINT('Ctrl Pts',(3.99999999999999,0.185497795908202,4.5435851550133));
#22362=CARTESIAN_POINT('Ctrl Pts',(3.99999999999998,0.211780221987087,4.54223483664603));
#22363=CARTESIAN_POINT('Ctrl Pts',(3.99999999999998,0.237902321580844,4.5390442708621));
#22364=CARTESIAN_POINT('Ctrl Pts',(3.99999999999998,0.243507595489062,4.53835964001621));
#22365=CARTESIAN_POINT('Ctrl Pts',(3.99999999999998,0.249105619801251,4.53759013757336));
#22366=CARTESIAN_POINT('Ctrl Pts',(3.99999999999998,0.254694598474614,4.53673594206822));
#22367=CARTESIAN_POINT('Ctrl Pts',(4.,-0.219914231356244,4.35301468169996));
#22368=CARTESIAN_POINT('Ctrl Pts',(4.00793950309107,-0.278596966840389,
4.31645650682028));
#22369=CARTESIAN_POINT('Ctrl Pts',(4.02383164552594,-0.377405665439666,
4.21337674819164));
#22370=CARTESIAN_POINT('Ctrl Pts',(4.04767642730463,-0.433534992178268,
4.00656196868444));
#22371=CARTESIAN_POINT('Ctrl Pts',(4.07153434533603,-0.383670022685343,
3.79803920418254));
#22372=CARTESIAN_POINT('Ctrl Pts',(4.09539226336747,-0.239994733226421,
3.63889579340969));
#22373=CARTESIAN_POINT('Ctrl Pts',(4.11925018139887,-0.0376302499649443,
3.56805514133307));
#22374=CARTESIAN_POINT('Ctrl Pts',(4.1431080994303,0.173933765839147,3.60283521426327));
#22375=CARTESIAN_POINT('Ctrl Pts',(4.16696601746172,0.342967344134064,3.73473372141871));
#22376=CARTESIAN_POINT('Ctrl Pts',(4.19082393549313,0.428135478754777,3.93149662217858));
#22377=CARTESIAN_POINT('Ctrl Pts',(4.21468185352456,0.40861313688017,4.1450106963618));
#22378=CARTESIAN_POINT('Ctrl Pts',(4.23853977155597,0.289173588337559,4.32306558264197));
#22379=CARTESIAN_POINT('Ctrl Pts',(4.25811226835493,0.13317859508208,4.40432939198872));
#22380=CARTESIAN_POINT('Ctrl Pts',(4.26973212581007,0.0319512750557707,
4.41584666103033));
#22381=CARTESIAN_POINT('Ctrl Pts',(4.2733993439214,2.51014653359152E-6,
4.41583996132385));
#22382=CARTESIAN_POINT('Origin',(3.42660065607856,0.,4.));
#22383=CARTESIAN_POINT('',(4.,-0.219892372743086,3.64701365460628));
#22384=CARTESIAN_POINT('Origin',(4.,0.,4.));
#22385=CARTESIAN_POINT('Ctrl Pts',(4.,-0.219892372743211,3.64701365460636));
#22386=CARTESIAN_POINT('Ctrl Pts',(4.00795263934381,-0.161099076858729,
3.61038844940468));
#22387=CARTESIAN_POINT('Ctrl Pts',(4.02385791803142,-0.0249198690254346,
3.56711791692558));
#22388=CARTESIAN_POINT('Ctrl Pts',(4.04771583606284,0.185569069288609,3.60813812632505));
#22389=CARTESIAN_POINT('Ctrl Pts',(4.07157375409426,0.350624105231944,3.74494568050885));
#22390=CARTESIAN_POINT('Ctrl Pts',(4.09543167212568,0.429971014252744,3.94413788601839));
#22391=CARTESIAN_POINT('Ctrl Pts',(4.1192895901571,0.40416308778273,4.15698104289539));
#22392=CARTESIAN_POINT('Ctrl Pts',(4.14314750818851,0.279534313346206,4.3314427366163));
#22393=CARTESIAN_POINT('Ctrl Pts',(4.16225119682902,0.125004509401131,4.40624063703925));
#22394=CARTESIAN_POINT('Ctrl Pts',(4.1734022461257,0.0278694809177792,4.41585864517498));
#22395=CARTESIAN_POINT('Ctrl Pts',(4.17660065607858,5.88453344126799E-6,
4.41584444980552));
#22396=CARTESIAN_POINT('Ctrl Pts',(3.95224475517896,-0.314128184302177,
3.49573985500833));
#22397=CARTESIAN_POINT('Ctrl Pts',(3.96019739452277,-0.230138771413741,
3.44341876234755));
#22398=CARTESIAN_POINT('Ctrl Pts',(3.97610267321038,-0.0355993848822847,
3.38160445914153));
#22399=CARTESIAN_POINT('Ctrl Pts',(3.9999605912418,0.265095483172694,3.44020405374152));
#22400=CARTESIAN_POINT('Ctrl Pts',(4.02381850927322,0.500885556761892,3.63564106712445));
#22401=CARTESIAN_POINT('Ctrl Pts',(4.04767642730465,0.614236921112272,3.92019793948569));
#22402=CARTESIAN_POINT('Ctrl Pts',(4.07153434533605,0.577368897990231,4.22425593648149));
#22403=CARTESIAN_POINT('Ctrl Pts',(4.09539226336749,0.399329932212592,4.47348393104611));
#22404=CARTESIAN_POINT('Ctrl Pts',(4.11925018139889,0.123637843932736,4.60692867011962));
#22405=CARTESIAN_POINT('Ctrl Pts',(4.14310809943032,-0.182283847264271,
4.59196468982869));
#22406=CARTESIAN_POINT('Ctrl Pts',(4.16696601746173,-0.443633876576525,
4.43224822622665));
#22407=CARTESIAN_POINT('Ctrl Pts',(4.19082393549315,-0.596502436238336,
4.16683582239239));
#22408=CARTESIAN_POINT('Ctrl Pts',(4.21468185352458,-0.603510379797736,
3.86062723727387));
#22409=CARTESIAN_POINT('Ctrl Pts',(4.23853977155598,-0.462943343075553,
3.58849923641164));
#22410=CARTESIAN_POINT('Ctrl Pts',(4.26239768958742,-0.209174182705692,
3.41699430327496));
#22411=CARTESIAN_POINT('Ctrl Pts',(4.28625560761882,0.0957438341235747,
3.38805018506757));
#22412=CARTESIAN_POINT('Ctrl Pts',(4.31011352565025,0.377249837899377,3.50874444390425));
#22413=CARTESIAN_POINT('Ctrl Pts',(4.33397144368167,0.566508000142931,3.7495640793295));
#22414=CARTESIAN_POINT('Ctrl Pts',(4.35782936171309,0.617239514437223,4.05162211295782));
#22415=CARTESIAN_POINT('Ctrl Pts',(4.3816872797445,0.517039159770137,4.34105713706075));
#22416=CARTESIAN_POINT('Ctrl Pts',(4.40554519777592,0.290408643717306,4.54709439922074));
#22417=CARTESIAN_POINT('Ctrl Pts',(4.42940311580735,-0.00723469473045889,
4.61935217913086));
#22418=CARTESIAN_POINT('Ctrl Pts',(4.45326103383876,-0.303108954077165,
4.54016147994594));
#22419=CARTESIAN_POINT('Ctrl Pts',(4.47711895187019,-0.524864817190473,
4.3288865854667));
#22420=CARTESIAN_POINT('Ctrl Pts',(4.5009768699016,-0.618276935702851,4.03718996201469));
#22421=CARTESIAN_POINT('Ctrl Pts',(4.52483478793302,-0.560503501787052,
3.7363993798876));
#22422=CARTESIAN_POINT('Ctrl Pts',(4.54869270596444,-0.365671693940747,
3.50006632967672));
#22423=CARTESIAN_POINT('Ctrl Pts',(4.57255062399586,-0.0814231961944085,
3.38598067979976));
#22424=CARTESIAN_POINT('Ctrl Pts',(4.59640854202727,0.222735490926488,3.42203947925158));
#22425=CARTESIAN_POINT('Ctrl Pts',(4.6202664600587,0.472429283332598,3.59942536936051));
#22426=CARTESIAN_POINT('Ctrl Pts',(4.64412437809011,0.606601247243452,3.87476266809168));
#22427=CARTESIAN_POINT('Ctrl Pts',(4.66798229612153,0.592442682719785,4.18072390587243));
#22428=CARTESIAN_POINT('Ctrl Pts',(4.69184021415295,0.433415744455024,4.44249322584619));
#22429=CARTESIAN_POINT('Ctrl Pts',(4.71569813218437,0.168406850663934,4.59606089882753));
#22430=CARTESIAN_POINT('Ctrl Pts',(4.7395560502158,-0.1377821054254,4.60387544567241));
#22431=CARTESIAN_POINT('Ctrl Pts',(4.7634139682472,-0.410279583628813,4.46402599681362));
#22432=CARTESIAN_POINT('Ctrl Pts',(4.78727188627863,-0.582452527843622,
4.21070955191949));
#22433=CARTESIAN_POINT('Ctrl Pts',(4.81112980431005,-0.612199963312297,
3.9058688819681));
#22434=CARTESIAN_POINT('Ctrl Pts',(4.83498772234147,-0.492247831758966,
3.62404583445569));
#22435=CARTESIAN_POINT('Ctrl Pts',(4.85884564037289,-0.251927696778831,
3.4341538212047));
#22436=CARTESIAN_POINT('Ctrl Pts',(4.88270355840431,0.0499956224363984,
3.38262661200963));
#22437=CARTESIAN_POINT('Ctrl Pts',(4.90656147643572,0.339693650112522,3.48206401309162));
#22438=CARTESIAN_POINT('Ctrl Pts',(4.93041939446714,0.546327327266884,3.70815087126575));
#22439=CARTESIAN_POINT('Ctrl Pts',(4.95427731249857,0.619369091246891,4.00560279122603));
#22440=CARTESIAN_POINT('Ctrl Pts',(4.97813523052998,0.540958241141728,4.3016846761146));
#22441=CARTESIAN_POINT('Ctrl Pts',(5.00199314856141,0.330268365670778,4.52399643996756));
#22442=CARTESIAN_POINT('Ctrl Pts',(5.02585106659282,0.0388188784636707,
4.61817680087201));
#22443=CARTESIAN_POINT('Ctrl Pts',(5.04970898462424,-0.262122881932824,
4.56119609516527));
#22444=CARTESIAN_POINT('Ctrl Pts',(5.07356690265566,-0.498968457612796,
4.36698765751594));
#22445=CARTESIAN_POINT('Ctrl Pts',(5.09742482068708,-0.613802653778546,
4.08304074106085));
#22446=CARTESIAN_POINT('Ctrl Pts',(5.12128273871849,-0.578545381446849,
3.77878810143205));
#22447=CARTESIAN_POINT('Ctrl Pts',(5.14514065674992,-0.40181800409162,3.52862779669421));
#22448=CARTESIAN_POINT('Ctrl Pts',(5.16899857478133,-0.126835179433317,
3.39373083558568));
#22449=CARTESIAN_POINT('Ctrl Pts',(5.19285649281276,0.179162301517353,3.4070831996169));
#22450=CARTESIAN_POINT('Ctrl Pts',(5.21671441084417,0.441349719463922,3.56541987207117));
#22451=CARTESIAN_POINT('Ctrl Pts',(5.24057232887559,0.595615108876583,3.83002322352904));
#22452=CARTESIAN_POINT('Ctrl Pts',(5.26443024690701,0.604236379939102,4.13619052690848));
#22453=CARTESIAN_POINT('Ctrl Pts',(5.28828816493843,0.465105397037983,4.40905553670335));
#22454=CARTESIAN_POINT('Ctrl Pts',(5.31214608296985,0.21224347534444,4.58189532532512));
#22455=CARTESIAN_POINT('Ctrl Pts',(5.33600400100126,-0.0925177574670201,
4.61244585639451));
#22456=CARTESIAN_POINT('Ctrl Pts',(5.35986191903269,-0.37465587844466,4.49323669288525));
#22457=CARTESIAN_POINT('Ctrl Pts',(5.3837198370641,-0.565180431721392,4.25341772246777));
#22458=CARTESIAN_POINT('Ctrl Pts',(5.40757775509553,-0.617502974236318,
3.95163121594683));
#22459=CARTESIAN_POINT('Ctrl Pts',(5.43143567312694,-0.518829219107294,
3.66167219466597));
#22460=CARTESIAN_POINT('Ctrl Pts',(5.45529359115837,-0.293287587282116,
3.45444353765392));
#22461=CARTESIAN_POINT('Ctrl Pts',(5.47915150918978,0.00397084862654925,
3.38061829634467));
#22462=CARTESIAN_POINT('Ctrl Pts',(5.50300942722121,0.300258303883157,3.45824875319892));
#22463=CARTESIAN_POINT('Ctrl Pts',(5.52686734525262,0.523124424966688,3.66835214690199));
#22464=CARTESIAN_POINT('Ctrl Pts',(5.55072526328404,0.618072374525773,3.95955247459688));
#22465=CARTESIAN_POINT('Ctrl Pts',(5.57458318131546,0.561884792553919,4.26064332401524));
#22466=CARTESIAN_POINT('Ctrl Pts',(5.59844109934688,0.368301073379394,4.49799978094171));
#22467=CARTESIAN_POINT('Ctrl Pts',(5.62229901737829,0.0846577094226282,
4.61358172616469));
#22468=CARTESIAN_POINT('Ctrl Pts',(5.64615693540972,-0.219686770477705,
4.57912622575047));
#22469=CARTESIAN_POINT('Ctrl Pts',(5.67001485344113,-0.470311850924231,
4.40305858798173));
#22470=CARTESIAN_POINT('Ctrl Pts',(5.69387277147256,-0.605932872639677,
4.12843214650112));
#22471=CARTESIAN_POINT('Ctrl Pts',(5.71773068950397,-0.593386801983745,
3.82240054650545));
#22472=CARTESIAN_POINT('Ctrl Pts',(5.74158860753539,-0.435741494202748,
3.55979685111874));
#22473=CARTESIAN_POINT('Ctrl Pts',(5.76544652556682,-0.171545522688555,
3.40483481554927));
#22474=CARTESIAN_POINT('Ctrl Pts',(5.78930444359822,0.134598003740687,3.39540688139736));
#22475=CARTESIAN_POINT('Ctrl Pts',(5.81316236162965,0.407828648458881,3.53381843004554));
#22476=CARTESIAN_POINT('Ctrl Pts',(5.83702027966106,0.58133408605803,3.78622407765735));
#22477=CARTESIAN_POINT('Ctrl Pts',(5.86087819769249,0.612687492198482,4.09090374899912));
#22478=CARTESIAN_POINT('Ctrl Pts',(5.8847361157239,0.494222140250734,4.3733550009975));
#22479=CARTESIAN_POINT('Ctrl Pts',(5.90859403375532,0.254905969192102,4.56451074097759));
#22480=CARTESIAN_POINT('Ctrl Pts',(5.93245195178675,-0.0467415727364197,
4.61762831145024));
#22481=CARTESIAN_POINT('Ctrl Pts',(5.95630986981815,-0.336959681931401,
4.51971877801409));
#22482=CARTESIAN_POINT('Ctrl Pts',(5.98016778784959,-0.544781677596122,
4.29472414464893));
#22483=CARTESIAN_POINT('Ctrl Pts',(6.00402570588099,-0.61939026621187,3.99766086682344));
#22484=CARTESIAN_POINT('Ctrl Pts',(6.02788362391242,-0.542540019317823,
3.70117063377655));
#22485=CARTESIAN_POINT('Ctrl Pts',(6.05174154194384,-0.333025929677459,
3.47775031355921));
#22486=CARTESIAN_POINT('Ctrl Pts',(6.07559945997526,-0.042074208138152,
3.38203805739984));
#22487=CARTESIAN_POINT('Ctrl Pts',(6.09945737800668,0.259158778028439,3.43742717299816));
#22488=CARTESIAN_POINT('Ctrl Pts',(6.12331529603809,0.497033648893269,3.63039418124561));
#22489=CARTESIAN_POINT('Ctrl Pts',(6.14717321406952,0.613345206175343,3.91371436613889));
#22490=CARTESIAN_POINT('Ctrl Pts',(6.17103113210093,0.579724447951105,4.21818191418763));
#22491=CARTESIAN_POINT('Ctrl Pts',(6.19488905013236,0.40425597056565,4.46920707734689));
#22492=CARTESIAN_POINT('Ctrl Pts',(6.21874696816377,0.13010450107023,4.60567007851858));
#22493=CARTESIAN_POINT('Ctrl Pts',(6.24260488619519,-0.176179318911185,
4.59370602015056));
#22494=CARTESIAN_POINT('Ctrl Pts',(6.26646280422661,-0.438782409775579,
4.43717629804221));
#22495=CARTESIAN_POINT('Ctrl Pts',(6.29032072225803,-0.595217424383659,
4.17259489198797));
#22496=CARTESIAN_POINT('Ctrl Pts',(6.31417864028945,-0.604035436411749,
3.86794272465182));
#22497=CARTESIAN_POINT('Ctrl Pts',(6.34598919766468,-0.423477061217623,
3.4998212904071));
#22498=CARTESIAN_POINT('Ctrl Pts',(6.3857523943837,0.100470573235224,3.30464850830547));
#22499=CARTESIAN_POINT('Ctrl Pts',(6.43346823044655,0.640013163212275,3.70919899990029));
#22500=CARTESIAN_POINT('Ctrl Pts',(6.48118406650937,0.590335835129396,4.3806576914582));
#22501=CARTESIAN_POINT('Ctrl Pts',(6.52889990257223,-0.000686065451295705,
4.70262946694599));
#22502=CARTESIAN_POINT('Ctrl Pts',(6.57661573863505,-0.591483599613884,
4.37932465573422));
#22503=CARTESIAN_POINT('Ctrl Pts',(6.6243315746979,-0.638898060441451,3.70770201230499));
#22504=CARTESIAN_POINT('Ctrl Pts',(6.67204741076074,-0.0997162142428727,
3.30448953810453));
#22505=CARTESIAN_POINT('Ctrl Pts',(6.71976324682356,0.531096731682035,3.53998115137447));
#22506=CARTESIAN_POINT('Ctrl Pts',(6.76747908288643,0.674163513320998,4.19791190586338));
#22507=CARTESIAN_POINT('Ctrl Pts',(6.81519491894923,0.19815244237474,4.67409883091767));
#22508=CARTESIAN_POINT('Ctrl Pts',(6.86291075501209,-0.459834002450772,
4.53124951681343));
#22509=CARTESIAN_POINT('Ctrl Pts',(6.91062659107492,-0.695543074258338,
3.90054607923755));
#22510=CARTESIAN_POINT('Ctrl Pts',(6.95834242713776,-0.292526745343327,
3.36117245204842));
#22511=CARTESIAN_POINT('Ctrl Pts',(7.00605826320061,0.379122722467859,3.40844412700009));
#22512=CARTESIAN_POINT('Ctrl Pts',(7.05377409926343,0.702617257610868,3.99895059076549));
#22513=CARTESIAN_POINT('Ctrl Pts',(7.10148993532628,0.380887926283931,4.59042078110798));
#22514=CARTESIAN_POINT('Ctrl Pts',(7.14920577138911,-0.290616845661789,
4.63969846327979));
#22515=CARTESIAN_POINT('Ctrl Pts',(7.19692160745196,-0.695243592084394,
4.10153121423426));
#22516=CARTESIAN_POINT('Ctrl Pts',(7.24463744351478,-0.461417505508394,
3.47012628326466));
#22517=CARTESIAN_POINT('Ctrl Pts',(7.29235327957764,0.196135405489393,3.32531254251214));
#22518=CARTESIAN_POINT('Ctrl Pts',(7.34006911564046,0.673574140181709,3.80007467379138));
#22519=CARTESIAN_POINT('Ctrl Pts',(7.38778495170331,0.532459385890787,4.45843130921146));
#22520=CARTESIAN_POINT('Ctrl Pts',(7.43550078776614,-0.0976210197556089,
4.69580341906706));
#22521=CARTESIAN_POINT('Ctrl Pts',(7.48321662382899,-0.638054538563543,
4.29420854311633));
#22522=CARTESIAN_POINT('Ctrl Pts',(7.53093245989182,-0.592552758097988,
3.62243743491725));
#22523=CARTESIAN_POINT('Ctrl Pts',(7.57864829595465,-0.00290066162856385,
3.29738783984629));
#22524=CARTESIAN_POINT('Ctrl Pts',(7.6263641320175,0.589415156704478,3.61755780248734));
#22525=CARTESIAN_POINT('Ctrl Pts',(7.67407996808033,0.64046196749915,4.28893031975233));
#22526=CARTESIAN_POINT('Ctrl Pts',(7.72179580414318,0.103362698669259,4.69497367861456));
#22527=CARTESIAN_POINT('Ctrl Pts',(7.769511640206,-0.528656126737314,4.46281201486565));
#22528=CARTESIAN_POINT('Ctrl Pts',(7.81722747626886,-0.675201896567852,
3.80564295658466));
#22529=CARTESIAN_POINT('Ctrl Pts',(7.86494331233168,-0.201699375449268,
3.32695496184095));
#22530=CARTESIAN_POINT('Ctrl Pts',(7.91265914839452,0.457026785680635,3.46633458176699));
#22531=CARTESIAN_POINT('Ctrl Pts',(7.96037498445737,0.696058217263005,4.09578736675475));
#22532=CARTESIAN_POINT('Ctrl Pts',(8.0080908205202,0.295888677698302,4.63727713897333));
#22533=CARTESIAN_POINT('Ctrl Pts',(8.05580665658303,-0.375999987428149,
4.59354550870361));
#22534=CARTESIAN_POINT('Ctrl Pts',(8.10352249264589,-0.702602078596463,
4.00475190491975));
#22535=CARTESIAN_POINT('Ctrl Pts',(8.1512383287087,-0.383993870066737,3.41159455373064));
#22536=CARTESIAN_POINT('Ctrl Pts',(8.19895416477156,0.287241817850264,3.35877897763223));
#22537=CARTESIAN_POINT('Ctrl Pts',(8.24667000083438,0.694698924651979,3.89480653282778));
#22538=CARTESIAN_POINT('Ctrl Pts',(8.29438583689724,0.464203319628796,4.52743486753713));
#22539=CARTESIAN_POINT('Ctrl Pts',(8.34210167296006,-0.192577336495663,
4.67571164775853));
#22540=CARTESIAN_POINT('Ctrl Pts',(8.3898175090229,-0.672511261332963,4.20347202468314));
#22541=CARTESIAN_POINT('Ctrl Pts',(8.43753334508575,-0.534867746972347,
3.54438091052171));
#22542=CARTESIAN_POINT('Ctrl Pts',(8.48524918114857,0.0939530494311211,
3.303691816829));
#22543=CARTESIAN_POINT('Ctrl Pts',(8.53296501721143,0.636495314888509,3.70243324182078));
#22544=CARTESIAN_POINT('Ctrl Pts',(8.58068085327425,0.594534138944492,4.37443479950165));
#22545=CARTESIAN_POINT('Ctrl Pts',(8.6283966893371,0.00660311512414562,
4.7025871193802));
#22546=CARTESIAN_POINT('Ctrl Pts',(8.67611252539993,-0.58739165091669,4.3855428768395));
#22547=CARTESIAN_POINT('Ctrl Pts',(8.72382836146277,-0.64197562573843,3.71444867815739));
#22548=CARTESIAN_POINT('Ctrl Pts',(8.77154419752561,-0.107023505379864,
3.30558065209521));
#22549=CARTESIAN_POINT('Ctrl Pts',(8.81926003358845,0.526209946737336,3.53440859822909));
#22550=CARTESIAN_POINT('Ctrl Pts',(8.86697586965128,0.676216707984864,4.19079629265377));
#22551=CARTESIAN_POINT('Ctrl Pts',(8.91469170571413,0.20524326135842,4.67197281575615));
#22552=CARTESIAN_POINT('Ctrl Pts',(8.96240754177695,-0.45420823024697,4.53606636251889));
#22553=CARTESIAN_POINT('Ctrl Pts',(9.0101233778398,-0.69655331512461,3.90788192013928));
#22554=CARTESIAN_POINT('Ctrl Pts',(9.05783921390263,-0.299242772872918,
3.36429092791464));
#22555=CARTESIAN_POINT('Ctrl Pts',(9.10555504996548,0.37286701214988,3.40448135822736));
#22556=CARTESIAN_POINT('Ctrl Pts',(9.15327088602831,0.702567282619003,3.99154572051203));
#22557=CARTESIAN_POINT('Ctrl Pts',(9.20098672209116,0.387089207071907,4.58637377773631));
#22558=CARTESIAN_POINT('Ctrl Pts',(9.24870255815397,-0.28385884346236,4.64272577234503));
#22559=CARTESIAN_POINT('Ctrl Pts',(9.29641839421684,-0.694134950315416,
4.10885280060212));
#22560=CARTESIAN_POINT('Ctrl Pts',(9.34413423027966,-0.46697625165475,3.47501862715065));
#22561=CARTESIAN_POINT('Ctrl Pts',(9.39185006634251,0.189013924253689,3.32328292626348));
#22562=CARTESIAN_POINT('Ctrl Pts',(9.43956590240535,0.671429705166911,3.79298692681914));
#22563=CARTESIAN_POINT('Ctrl Pts',(9.48728173846818,0.537261256551386,4.45279421778236));
#22564=CARTESIAN_POINT('Ctrl Pts',(9.53499757453101,-0.090282470782305,
4.69679361142145));
#22565=CARTESIAN_POINT('Ctrl Pts',(9.58271341059386,-0.634918416022234,
4.30091671014441));
#22566=CARTESIAN_POINT('Ctrl Pts',(9.63042924665669,-0.596499010353368,
3.62870336374299));
#22567=CARTESIAN_POINT('Ctrl Pts',(9.67814508271953,-0.0103053851599677,
3.29745743154951));
#22568=CARTESIAN_POINT('Ctrl Pts',(9.72586091878236,0.585351833794561,3.61136714997101));
#22569=CARTESIAN_POINT('Ctrl Pts',(9.77357675484522,0.643471456979869,4.28216439445919));
#22570=CARTESIAN_POINT('Ctrl Pts',(9.82129259090803,0.110681340139534,4.69384573385819));
#22571=CARTESIAN_POINT('Ctrl Pts',(9.8690084269709,-0.523749154402255,4.46835785966634));
#22572=CARTESIAN_POINT('Ctrl Pts',(9.91672426303372,-0.677212741539845,
3.81276975633088));
#22573=CARTESIAN_POINT('Ctrl Pts',(9.96444009909655,-0.208781447863971,
3.32911806666439));
#22574=CARTESIAN_POINT('Ctrl Pts',(10.0121559351594,0.451377061900895,3.4615475792254));
#22575=CARTESIAN_POINT('Ctrl Pts',(10.0598717712222,0.697029070393332,4.08844623493918));
#22576=CARTESIAN_POINT('Ctrl Pts',(10.1075876072851,0.302588558372737,4.63412335218805));
#22577=CARTESIAN_POINT('Ctrl Pts',(10.1553034433479,-0.369723682724971,
4.5974752378807));
#22578=CARTESIAN_POINT('Ctrl Pts',(10.2030192794108,-0.702512977046242,
4.01215641928927));
#22579=CARTESIAN_POINT('Ctrl Pts',(10.2507351154736,-0.390173794994359,
3.41567417381395));
#22580=CARTESIAN_POINT('Ctrl Pts',(10.2984509515364,0.280467986596366,3.3557873255338));
#22581=CARTESIAN_POINT('Ctrl Pts',(10.3461667875993,0.693551700540965,3.8874908887021));
#22582=CARTESIAN_POINT('Ctrl Pts',(10.3938826236621,0.469736216214169,4.52251329995044));
#22583=CARTESIAN_POINT('Ctrl Pts',(10.441598459725,-0.185445263282835,4.67770370795377));
#22584=CARTESIAN_POINT('Ctrl Pts',(10.4893142957878,-0.670329504065059,
4.21054837313121));
#22585=CARTESIAN_POINT('Ctrl Pts',(10.5370301318506,-0.539639846919137,
3.55004322755915));
#22586=CARTESIAN_POINT('Ctrl Pts',(10.5847459679134,0.0866093850789692,
3.30274030959437));
#22587=CARTESIAN_POINT('Ctrl Pts',(10.6324618039763,0.633323886102378,3.69574169404847));
#22588=CARTESIAN_POINT('Ctrl Pts',(10.6801776400391,0.598447317577389,4.36814816247366));
#22589=CARTESIAN_POINT('Ctrl Pts',(10.727893476102,0.0140073690254923,4.70247850861168));
#22590=CARTESIAN_POINT('Ctrl Pts',(10.7756093121648,-0.583295762033595,
4.39171203127037));
#22591=CARTESIAN_POINT('Ctrl Pts',(10.8233251482277,-0.644949419658282,
3.72123036834915));
#22592=CARTESIAN_POINT('Ctrl Pts',(10.8710409842905,-0.114336101388361,
3.30674714759503));
#22593=CARTESIAN_POINT('Ctrl Pts',(10.9187568203533,0.521273818073547,3.52888868827067));
#22594=CARTESIAN_POINT('Ctrl Pts',(10.9664726564162,0.678189969569843,4.18365899548663));
#22595=CARTESIAN_POINT('Ctrl Pts',(11.014188492479,0.212313836716152,4.66977242119035));
#22596=CARTESIAN_POINT('Ctrl Pts',(11.0619043285418,-0.44853335926228,4.54082352674158));
#22597=CARTESIAN_POINT('Ctrl Pts',(11.1096201646047,-0.697485469857315,
3.91522806604643));
#22598=CARTESIAN_POINT('Ctrl Pts',(11.1573360006675,-0.305925941288932,
3.36747997668469));
#22599=CARTESIAN_POINT('Ctrl Pts',(11.2050518367303,0.36657008644075,3.40058475730499));
#22600=CARTESIAN_POINT('Ctrl Pts',(11.2527676727932,0.702439163386103,3.98414177848112));
#22601=CARTESIAN_POINT('Ctrl Pts',(11.300483508856,0.393247548178179,4.58226164848818));
#22602=CARTESIAN_POINT('Ctrl Pts',(11.3481993449189,-0.277069341413063,
4.64568168744144));
#22603=CARTESIAN_POINT('Ctrl Pts',(11.3959151809817,-0.692949191524882,
4.11616229772746));
#22604=CARTESIAN_POINT('Ctrl Pts',(11.4436310170446,-0.47248313666557,3.47996928262364));
#22605=CARTESIAN_POINT('Ctrl Pts',(11.4913468531074,0.181871452681271,3.32132847698764));
#22606=CARTESIAN_POINT('Ctrl Pts',(11.5390626891702,0.669210688578896,3.78592217363756));
#22607=CARTESIAN_POINT('Ctrl Pts',(11.586778525233,0.54200345202451,4.44710683224685));
#22608=CARTESIAN_POINT('Ctrl Pts',(11.6344943612959,-0.082933894319074,
4.69770640718098));
#22609=CARTESIAN_POINT('Ctrl Pts',(11.6822101973587,-0.631711769407458,
4.30759145280778));
#22610=CARTESIAN_POINT('Ctrl Pts',(11.7299260334216,-0.600379006513997,
3.63501053441836));
#22611=CARTESIAN_POINT('Ctrl Pts',(11.7776418694844,-0.0177089639202829,
3.29760505835735));
#22612=CARTESIAN_POINT('Ctrl Pts',(11.8253577055473,0.581223492728864,3.60521966494218));
#22613=CARTESIAN_POINT('Ctrl Pts',(11.8730735416101,0.646409472732109,4.27536712768685));
#22614=CARTESIAN_POINT('Ctrl Pts',(11.9207893776729,0.11798768763725,4.69264072000881));
#22615=CARTESIAN_POINT('Ctrl Pts',(11.9685052137358,-0.518784006488825,
4.4738516814993));
#22616=CARTESIAN_POINT('Ctrl Pts',(12.0162210497986,-0.679148364938221,
3.81991735272367));
#22617=CARTESIAN_POINT('Ctrl Pts',(12.0639368858614,-0.215840329824027,
3.33135568986959));
#22618=CARTESIAN_POINT('Ctrl Pts',(12.1116527219243,0.445677201297934,3.45682038542343));
#22619=CARTESIAN_POINT('Ctrl Pts',(12.1593685579871,0.697922500842799,4.08109527893561));
#22620=CARTESIAN_POINT('Ctrl Pts',(12.2070843940499,0.309254828945687,4.63089912998995));
#22621=CARTESIAN_POINT('Ctrl Pts',(12.2548002301128,-0.36340631086944,4.60133860234362));
#22622=CARTESIAN_POINT('Ctrl Pts',(12.3025160661756,-0.702345843688318,
4.0195595833814));
#22623=CARTESIAN_POINT('Ctrl Pts',(12.3502319022385,-0.396310381268302,
3.41981869803717));
#22624=CARTESIAN_POINT('Ctrl Pts',(12.3979477383013,0.273663002289436,3.35286722952223));
#22625=CARTESIAN_POINT('Ctrl Pts',(12.4456635743641,0.69232743999824,3.88018774155459));
#22626=CARTESIAN_POINT('Ctrl Pts',(12.493379410427,0.475216936729713,4.51753369406595));
#22627=CARTESIAN_POINT('Ctrl Pts',(12.5410952464898,-0.178292591690169,
4.67962049203707));
#22628=CARTESIAN_POINT('Ctrl Pts',(12.5888110825527,-0.66807328977682,4.21760133486514));
#22629=CARTESIAN_POINT('Ctrl Pts',(12.6365269186155,-0.544352006232531,
3.55575552365962));
#22630=CARTESIAN_POINT('Ctrl Pts',(12.6842427546784,0.0792561005673328,
3.3018662506574));
#22631=CARTESIAN_POINT('Ctrl Pts',(12.7319585907411,0.630082110704352,3.68908394184497));
#22632=CARTESIAN_POINT('Ctrl Pts',(12.779674426804,0.60229402352211,4.36182063329482));
#22633=CARTESIAN_POINT('Ctrl Pts',(12.8273902628668,0.0214100670547408,
4.70229186986395));
#22634=CARTESIAN_POINT('Ctrl Pts',(12.8751060989297,-0.579135083425219,
4.39783767618763));
#22635=CARTESIAN_POINT('Ctrl Pts',(12.9228219349925,-0.647851575657132,
3.7280430229487));
#22636=CARTESIAN_POINT('Ctrl Pts',(12.9705377710554,-0.121635997485283,
3.30799064633195));
#22637=CARTESIAN_POINT('Ctrl Pts',(13.0182536071182,0.516279788787698,3.52342110712114));
#22638=CARTESIAN_POINT('Ctrl Pts',(13.065969443181,0.68008790103128,4.17650129834983));
#22639=CARTESIAN_POINT('Ctrl Pts',(13.1136852792439,0.219360829260397,4.66749763148232));
#22640=CARTESIAN_POINT('Ctrl Pts',(13.1614011153067,-0.44280866732052,4.54552061885334));
#22641=CARTESIAN_POINT('Ctrl Pts',(13.2091169513696,-0.698340151213866,
3.92258362801769));
#22642=CARTESIAN_POINT('Ctrl Pts',(13.2568327874324,-0.31257512890311,3.37073928277739));
#22643=CARTESIAN_POINT('Ctrl Pts',(13.3045486234952,0.36023244386594,3.39675473658331));
#22644=CARTESIAN_POINT('Ctrl Pts',(13.3522644595581,0.702233020544282,3.97673959790624));
#22645=CARTESIAN_POINT('Ctrl Pts',(13.3999802956209,0.39936220921291,4.57808484437918));
#22646=CARTESIAN_POINT('Ctrl Pts',(13.4476961316837,-0.270249063816132,
4.64856588328003));
#22647=CARTESIAN_POINT('Ctrl Pts',(13.4954119677466,-0.691686463226468,
4.123458892096));
#22648=CARTESIAN_POINT('Ctrl Pts',(13.5431278038094,-0.47793754049168,3.48497770064095));
#22649=CARTESIAN_POINT('Ctrl Pts',(13.5908436398723,0.174708779690948,3.31944941132403));
#22650=CARTESIAN_POINT('Ctrl Pts',(13.6385594759351,0.666917339243262,3.77888119920505));
#22651=CARTESIAN_POINT('Ctrl Pts',(13.6862753119979,0.54668544432619,4.44136978420615));
#22652=CARTESIAN_POINT('Ctrl Pts',(13.7339911480608,-0.075576105952426,
4.69854170502367));
#22653=CARTESIAN_POINT('Ctrl Pts',(13.7817069841236,-0.62843495524706,4.31423202967224));
#22654=CARTESIAN_POINT('Ctrl Pts',(13.8294228201864,-0.604192315423611,
3.64135824639153));
#22655=CARTESIAN_POINT('Ctrl Pts',(13.8771386562493,-0.025110575652917,
3.29783070386218));
#22656=CARTESIAN_POINT('Ctrl Pts',(13.9248544923121,0.577030592115723,3.59911603023956));
#22657=CARTESIAN_POINT('Ctrl Pts',(13.972570328375,0.649275688387581,4.26853927444071));
#22658=CARTESIAN_POINT('Ctrl Pts',(14.0202861644378,0.125280929622514,4.69135877091509));
#22659=CARTESIAN_POINT('Ctrl Pts',(14.0680020005006,-0.513761234509794,
4.47929287013608));
#22660=CARTESIAN_POINT('Ctrl Pts',(14.1157178365635,-0.681008551759042,
3.82708495184235));
#22661=CARTESIAN_POINT('Ctrl Pts',(14.1634336726263,-0.222875237264486,
3.33366758291179));
#22662=CARTESIAN_POINT('Ctrl Pts',(14.2111495086891,0.439927836986373,3.45215352543546));
#22663=CARTESIAN_POINT('Ctrl Pts',(14.258865344752,0.698738409372782,4.07373531525328));
#22664=CARTESIAN_POINT('Ctrl Pts',(14.3065811808148,0.315886748959774,4.62760483051036));
#22665=CARTESIAN_POINT('Ctrl Pts',(14.3542970168777,-0.357048573565392,
4.60513517296818));
#22666=CARTESIAN_POINT('Ctrl Pts',(14.4020128529405,-0.702100697086982,
4.02696057488784));
#22667=CARTESIAN_POINT('Ctrl Pts',(14.4497286890033,-0.402402947265751,
3.42402766604624));
#22668=CARTESIAN_POINT('Ctrl Pts',(14.4974445250662,0.266827620794843,3.35001901394789));
#22669=CARTESIAN_POINT('Ctrl Pts',(14.545160361129,0.691026279008849,3.87289790258421));
#22670=CARTESIAN_POINT('Ctrl Pts',(14.5928761971919,0.480644872403009,4.51249660299459));
#22671=CARTESIAN_POINT('Ctrl Pts',(14.6405920332547,-0.171120116202498,
4.6814617871012));
#22672=CARTESIAN_POINT('Ctrl Pts',(14.6883078693176,-0.665742869077823,
4.22463012647536));
#22673=CARTESIAN_POINT('Ctrl Pts',(14.7360237053803,-0.549003701508229,
3.56151716432844));
#22674=CARTESIAN_POINT('Ctrl Pts',(14.7837395414432,0.0718940126641393,
3.30106973710437));
#22675=CARTESIAN_POINT('Ctrl Pts',(14.831455377506,0.626770348775451,3.68246072472179));
#22676=CARTESIAN_POINT('Ctrl Pts',(14.8791712135689,0.606073829504824,4.35545291479698));
#22677=CARTESIAN_POINT('Ctrl Pts',(14.9268870496317,0.0288103869553486,
4.70202722386799));
#22678=CARTESIAN_POINT('Ctrl Pts',(14.9746028856946,-0.574910077240004,
4.4039191311837));
#22679=CARTESIAN_POINT('Ctrl Pts',(15.0223187217574,-0.650681771377263,
3.73488588523872));
#22680=CARTESIAN_POINT('Ctrl Pts',(15.0700345578202,-0.128922382832804,
3.30931101018402));
#22681=CARTESIAN_POINT('Ctrl Pts',(15.1177503938831,0.511228413592865,3.51800646209349));
#22682=CARTESIAN_POINT('Ctrl Pts',(15.1654662299459,0.681910291555949,4.16932399628639));
#22683=CARTESIAN_POINT('Ctrl Pts',(15.2131820660088,0.226383456244684,4.6651486993049));
#22684=CARTESIAN_POINT('Ctrl Pts',(15.2608979020716,-0.437034790293287,
4.55015711712348));
#22685=CARTESIAN_POINT('Ctrl Pts',(15.3086137381344,-0.699117264260319,
3.92994778903219));
#22686=CARTESIAN_POINT('Ctrl Pts',(15.3563295741972,-0.319189597155267,
3.37406848416447));
#22687=CARTESIAN_POINT('Ctrl Pts',(15.4040454102601,0.353854788380711,3.39299172148285));
#22688=CARTESIAN_POINT('Ctrl Pts',(15.4517612463229,0.70194887699091,3.96934000098645));
#22689=CARTESIAN_POINT('Ctrl Pts',(15.4994770823858,0.40543251098856,4.57384382934891));
#22690=CARTESIAN_POINT('Ctrl Pts',(15.5471929184486,-0.263398768235635,
4.65137803949801));
#22691=CARTESIAN_POINT('Ctrl Pts',(15.5949087545115,-0.690346905678043,
4.13074177323664));
#22692=CARTESIAN_POINT('Ctrl Pts',(15.6426245905743,-0.483338857283784,
3.4900433248913));
#22693=CARTESIAN_POINT('Ctrl Pts',(15.6903404266371,0.167526700878456,3.31764593799033));
#22694=CARTESIAN_POINT('Ctrl Pts',(15.7380562627,0.664549911894371,3.77186478559966));
#22695=CARTESIAN_POINT('Ctrl Pts',(15.7857720987628,0.551306713402943,4.43558371090429));
#22696=CARTESIAN_POINT('Ctrl Pts',(15.8334879348256,-0.0682099229505586,
4.69929941216862));
#22697=CARTESIAN_POINT('Ctrl Pts',(15.8812037708885,-0.625088337514006,
4.32083770313399));
#22698=CARTESIAN_POINT('Ctrl Pts',(15.9289196069513,-0.607938513517956,
3.64774579458877));
#22699=CARTESIAN_POINT('Ctrl Pts',(15.9766354430142,-0.0325093982219456,
3.29813434300035));
#22700=CARTESIAN_POINT('Ctrl Pts',(16.024351279077,0.572773597682653,3.59305692382598));
#22701=CARTESIAN_POINT('Ctrl Pts',(16.0720671151399,0.652069785580651,4.2616815931263));
#22702=CARTESIAN_POINT('Ctrl Pts',(16.1197829512026,0.132560255996602,4.69000002896988));
#22703=CARTESIAN_POINT('Ctrl Pts',(16.1674987872655,-0.508681396370837,
4.48468082119526));
#22704=CARTESIAN_POINT('Ctrl Pts',(16.2152146233283,-0.682793095381579,
3.83427175754402));
#22705=CARTESIAN_POINT('Ctrl Pts',(16.2629304593912,-0.229885388781225,
3.33605348899688));
#22706=CARTESIAN_POINT('Ctrl Pts',(16.310646295454,0.434129607578297,3.44754751763412));
#22707=CARTESIAN_POINT('Ctrl Pts',(16.3583621315168,0.699476705356048,4.06636716140204));
#22708=CARTESIAN_POINT('Ctrl Pts',(16.4060779675797,0.322483581772784,4.62424081966442));
#22709=CARTESIAN_POINT('Ctrl Pts',(16.4537938036425,-0.350651177000141,
4.60886452804932));
#22710=CARTESIAN_POINT('Ctrl Pts',(16.5015096397054,-0.701777564471952,
4.03435857174156));
#22711=CARTESIAN_POINT('Ctrl Pts',(16.5492254757682,-0.408450816253369,
3.42830061032894));
#22712=CARTESIAN_POINT('Ctrl Pts',(16.596941311831,0.259962601354342,3.34724299517707));
#22713=CARTESIAN_POINT('Ctrl Pts',(16.6446571478939,0.689648362099571,3.86562218151166));
#22714=CARTESIAN_POINT('Ctrl Pts',(16.6923729839567,0.486019420324727,4.50740258623259));
#22715=CARTESIAN_POINT('Ctrl Pts',(16.7400888200196,-0.163928633504336,
4.6832273886238));
#22716=CARTESIAN_POINT('Ctrl Pts',(16.7878046560824,-0.663338500820136,
4.23163396723712));
#22717=CARTESIAN_POINT('Ctrl Pts',(16.8355204921452,-0.553594416058007,
3.56732750958986));
#22718=CARTESIAN_POINT('Ctrl Pts',(16.8832363282081,0.064523939115192,3.30035085740826));
#22719=CARTESIAN_POINT('Ctrl Pts',(16.9309521642709,0.623388968170475,3.67587277835446));
#22720=CARTESIAN_POINT('Ctrl Pts',(16.9786680003338,0.609786315682611,4.34904571427615));
#22721=CARTESIAN_POINT('Ctrl Pts',(17.0263838363966,0.0362075067348799,
4.70168460001938));
#22722=CARTESIAN_POINT('Ctrl Pts',(17.0740996724594,-0.570621212771584,
4.40995572075944));
#22723=CARTESIAN_POINT('Ctrl Pts',(17.1218155085223,-0.653439692453966,
3.74175819514654));
#22724=CARTESIAN_POINT('Ctrl Pts',(17.1695313445851,-0.136194448093839,
3.31070809249149));
#22725=CARTESIAN_POINT('Ctrl Pts',(17.2172471806479,0.50612025357182,3.51264535462077));
#22726=CARTESIAN_POINT('Ctrl Pts',(17.2649630167108,0.683656938721366,4.16212788651693));
#22727=CARTESIAN_POINT('Ctrl Pts',(17.3126788527736,0.233380937628925,4.66272588556639));
#22728=CARTESIAN_POINT('Ctrl Pts',(17.3603946888365,-0.431212369515449,
4.55473250655174));
#22729=CARTESIAN_POINT('Ctrl Pts',(17.4081105248993,-0.699816722678643,
3.93731973111387));
#22730=CARTESIAN_POINT('Ctrl Pts',(17.4558263609621,-0.325768611341644,
3.37746721105403));
#22731=CARTESIAN_POINT('Ctrl Pts',(17.503542197025,0.347437828384778,3.38929612998149));
#22732=CARTESIAN_POINT('Ctrl Pts',(17.5512580330878,0.701586764287296,3.96194380963385));
#22733=CARTESIAN_POINT('Ctrl Pts',(17.5989738691507,0.411457779244836,4.56953907446917));
#22734=CARTESIAN_POINT('Ctrl Pts',(17.6466897052135,-0.256519215569882,
4.65411784373439));
#22735=CARTESIAN_POINT('Ctrl Pts',(17.6944055412764,-0.688930667671302,
4.13801013220155));
#22736=CARTESIAN_POINT('Ctrl Pts',(17.7421213773391,-0.488686487089258,
3.49516559270919));
#22737=CARTESIAN_POINT('Ctrl Pts',(17.789837213402,0.160326013994967,3.3159182573078));
#22738=CARTESIAN_POINT('Ctrl Pts',(17.8375530494648,0.662108669494809,3.76487371217125));
#22739=CARTESIAN_POINT('Ctrl Pts',(17.8852688855277,0.555866745946156,4.42974925503083));
#22740=CARTESIAN_POINT('Ctrl Pts',(17.9329847215905,-0.060836163514142,
4.69997944445332));
#22741=CARTESIAN_POINT('Ctrl Pts',(17.9807005576534,-0.621672287934692,
4.32740773946617));
#22742=CARTESIAN_POINT('Ctrl Pts',(18.0284163937162,-0.611617184687133,
3.65417246951162));
#22743=CARTESIAN_POINT('Ctrl Pts',(18.0761322297791,-0.0399046098013318,
3.29851594204507));
#22744=CARTESIAN_POINT('Ctrl Pts',(18.1238480658419,0.568452982276385,3.58704301871817));
#22745=CARTESIAN_POINT('Ctrl Pts',(18.1715639019047,0.65479145395626,4.25479484546229));
#22746=CARTESIAN_POINT('Ctrl Pts',(18.2192797379675,0.139824858206545,4.68856464509573));
#22747=CARTESIAN_POINT('Ctrl Pts',(18.2669955740304,-0.503545056316242,
4.49001493620888));
#22748=CARTESIAN_POINT('Ctrl Pts',(18.3147114100932,-0.684501797587214,
3.84147697155243));
#22749=CARTESIAN_POINT('Ctrl Pts',(18.3624272461561,-0.236870005719869,
3.33851314310973));
#22750=CARTESIAN_POINT('Ctrl Pts',(18.4101430822189,0.42828315711354,3.44300287363294));
#22751=CARTESIAN_POINT('Ctrl Pts',(18.4578589182817,0.70013730678616,4.05899163580144));
#22752=CARTESIAN_POINT('Ctrl Pts',(18.5055747543446,0.32904459463985,4.62080747111051));
#22753=CARTESIAN_POINT('Ctrl Pts',(18.5532905904074,-0.34421483176614,4.61252625334797));
#22754=CARTESIAN_POINT('Ctrl Pts',(18.6010064264702,-0.701376481735239,
4.0417527522082));
#22755=CARTESIAN_POINT('Ctrl Pts',(18.6487222625331,-0.414453316462639,
3.43263705626685));
#22756=CARTESIAN_POINT('Ctrl Pts',(18.6964380985959,0.253068706501803,3.34453948155689));
#22757=CARTESIAN_POINT('Ctrl Pts',(18.7441539346588,0.68819384232267,3.85836138648927));
#22758=CARTESIAN_POINT('Ctrl Pts',(18.7918697707216,0.491339983515996,4.50225220959958));
#22759=CARTESIAN_POINT('Ctrl Pts',(18.8395856067844,-0.156718942392259,
4.68491710048942));
#22760=CARTESIAN_POINT('Ctrl Pts',(18.8873014428473,-0.660860452068119,
4.23861207919858));
#22761=CARTESIAN_POINT('Ctrl Pts',(18.9350172789101,-0.558123639969822,
3.57318591405529));
#22762=CARTESIAN_POINT('Ctrl Pts',(18.9827331149729,0.0571466985584877,
3.29970969142451));
#22763=CARTESIAN_POINT('Ctrl Pts',(19.0304489510358,0.619938344467307,3.66932083449001));
#22764=CARTESIAN_POINT('Ctrl Pts',(19.0781647870986,0.613431069708698,4.3425997434341));
#22765=CARTESIAN_POINT('Ctrl Pts',(19.1258806231615,0.0436006047213211,
4.70126403633668));
#22766=CARTESIAN_POINT('Ctrl Pts',(19.1735964592243,-0.566268966340429,
4.41594677447179));
#22767=CARTESIAN_POINT('Ctrl Pts',(19.2213122952871,-0.656125032675529,
3.74865918919138));
#22768=CARTESIAN_POINT('Ctrl Pts',(19.26902813135,-0.143451385285705,3.31218173833215));
#22769=CARTESIAN_POINT('Ctrl Pts',(19.3167439674128,0.500955875668841,3.50733837970023));
#22770=CARTESIAN_POINT('Ctrl Pts',(19.3644598034757,0.68532764936022,4.15491376927485));
#22771=CARTESIAN_POINT('Ctrl Pts',(19.4121756395385,0.240352494576274,4.66022945763735));
#22772=CARTESIAN_POINT('Ctrl Pts',(19.4598914756013,-0.425342048711971,
4.55924628221868));
#22773=CARTESIAN_POINT('Ctrl Pts',(19.5076073116642,-0.700438454444525,
3.94469862920436));
#22774=CARTESIAN_POINT('Ctrl Pts',(19.555323147727,-0.332311429993836,3.3809350976725));
#22775=CARTESIAN_POINT('Ctrl Pts',(19.6030389837899,0.340982256434611,3.38566835039883));
#22776=CARTESIAN_POINT('Ctrl Pts',(19.6507548198527,0.701146760813864,3.95455188724214));
#22777=CARTESIAN_POINT('Ctrl Pts',(19.6984706559155,0.417437272672218,4.56517097885182));
#22778=CARTESIAN_POINT('Ctrl Pts',(19.7461864919784,-0.249611033919464,
4.6567851409082));
#22779=CARTESIAN_POINT('Ctrl Pts',(19.7939023280412,-0.687438163400574,
4.14526287985386));
#22780=CARTESIAN_POINT('Ctrl Pts',(19.841618164104,-0.493979350866992,3.5003444672369));
#22781=CARTESIAN_POINT('Ctrl Pts',(19.8893340001669,0.153106602982307,3.31426555646693));
#22782=CARTESIAN_POINT('Ctrl Pts',(19.9370498362297,0.659595612567133,3.75791065255607));
#22783=CARTESIAN_POINT('Ctrl Pts',(19.9847656722925,0.560361770063263,4.42386348253578));
#22784=CARTESIAN_POINT('Ctrl Pts',(20.0324815083554,-0.0534494809679074,
4.70058849011268));
#22785=CARTESIAN_POINT('Ctrl Pts',(20.0801973444182,-0.618198828117398,
4.33392863744107));
#22786=CARTESIAN_POINT('Ctrl Pts',(20.1279131804811,-0.615205937201001,
3.66066167313574));
#22787=CARTESIAN_POINT('Ctrl Pts',(20.1756290165439,-0.0473369003220797,
3.29892991724937));
#22788=CARTESIAN_POINT('Ctrl Pts',(20.2233448526068,0.564147630203746,3.58116102158214));
#22789=CARTESIAN_POINT('Ctrl Pts',(20.2710606886696,0.657292163719816,4.24771695100806));
#22790=CARTESIAN_POINT('Ctrl Pts',(20.3187765247324,0.147355317357748,4.68736342730055));
#22791=CARTESIAN_POINT('Ctrl Pts',(20.3664923607953,-0.498896366832293,
4.49468216892218));
#22792=CARTESIAN_POINT('Ctrl Pts',(20.4062555575143,-0.653992183610565,
3.9575054511282));
#22793=CARTESIAN_POINT('Ctrl Pts',(20.4380661148895,-0.465699721472375,
3.59327933193152));
#22794=CARTESIAN_POINT('Ctrl Pts',(20.461924032921,-0.215665100260693,3.41899970433759));
#22795=CARTESIAN_POINT('Ctrl Pts',(20.4857819509523,0.0900520562992202,
3.38718375849312));
#22796=CARTESIAN_POINT('Ctrl Pts',(20.5096398689838,0.372154449079436,3.50499792242313));
#22797=CARTESIAN_POINT('Ctrl Pts',(20.5334977870152,0.564103623124681,3.74397162737493));
#22798=CARTESIAN_POINT('Ctrl Pts',(20.5573557050466,0.61766411855396,4.04548854604559));
#22799=CARTESIAN_POINT('Ctrl Pts',(20.581213623078,0.520427284318709,4.33591550271974));
#22800=CARTESIAN_POINT('Ctrl Pts',(20.6050715411094,0.295805552416038,4.5441843692251));
#22801=CARTESIAN_POINT('Ctrl Pts',(20.6289294591409,-0.00108183093298003,
4.61939465531364));
#22802=CARTESIAN_POINT('Ctrl Pts',(20.6527873771723,-0.297740088546312,
4.543141139652));
#22803=CARTESIAN_POINT('Ctrl Pts',(20.6766452952037,-0.521574030203058,
4.33407743490148));
#22804=CARTESIAN_POINT('Ctrl Pts',(20.7005032132351,-0.617878846294169,
4.04332131262121));
#22805=CARTESIAN_POINT('Ctrl Pts',(20.7243611312665,-0.563090193646282,
3.74197268265107));
#22806=CARTESIAN_POINT('Ctrl Pts',(20.748219049298,-0.370613436173077,3.50371837193987));
#22807=CARTESIAN_POINT('Ctrl Pts',(20.7720769673294,-0.0875101228827464,
3.38681864340431));
#22808=CARTESIAN_POINT('Ctrl Pts',(20.7959348853608,0.216991017820888,3.41985835035499));
#22809=CARTESIAN_POINT('Ctrl Pts',(20.8197928033922,0.468432357761717,3.59475855107288));
#22810=CARTESIAN_POINT('Ctrl Pts',(20.8436507214236,0.605329007232586,3.86875129405724));
#22811=CARTESIAN_POINT('Ctrl Pts',(20.8675086394551,0.594206341669864,4.17483793696784));
#22812=CARTESIAN_POINT('Ctrl Pts',(20.8913665574864,0.437783978244149,4.43817193323088));
#22813=CARTESIAN_POINT('Ctrl Pts',(20.9152244755179,0.174311539695801,4.5943609607934));
#22814=CARTESIAN_POINT('Ctrl Pts',(20.9390823935493,-0.13178483570001,4.60521254097096));
#22815=CARTESIAN_POINT('Ctrl Pts',(20.9629403115808,-0.405656219889506,
4.46807317049539));
#22816=CARTESIAN_POINT('Ctrl Pts',(20.9867982296121,-0.580333613298163,
4.21647715910241));
#22817=CARTESIAN_POINT('Ctrl Pts',(21.0106561476436,-0.613103627724174,
3.91194658594648));
#22818=CARTESIAN_POINT('Ctrl Pts',(21.034514065675,-0.495953105920446,3.62894747086441));
#22819=CARTESIAN_POINT('Ctrl Pts',(21.0583719837064,-0.257528539509485,
3.43668080652407));
#22820=CARTESIAN_POINT('Ctrl Pts',(21.0822299017379,0.0438687693677006,
3.38216102944232));
#22821=CARTESIAN_POINT('Ctrl Pts',(21.1060878197692,0.334538969374667,3.47871971028568));
#22822=CARTESIAN_POINT('Ctrl Pts',(21.1299457378007,0.543405278604256,3.7027456213393));
#22823=CARTESIAN_POINT('Ctrl Pts',(21.153803655832,0.619394195209021,3.99945832503004));
#22824=CARTESIAN_POINT('Ctrl Pts',(21.1776615738635,0.543924359096133,4.29630348300169));
#22825=CARTESIAN_POINT('Ctrl Pts',(21.2015194918949,0.33545020099803,4.52069436823682));
#22826=CARTESIAN_POINT('Ctrl Pts',(21.2253774099264,0.0449493312674926,
4.61776129700707));
#22827=CARTESIAN_POINT('Ctrl Pts',(21.2492353279577,-0.256542874348706,
4.56376876117982));
#22828=CARTESIAN_POINT('Ctrl Pts',(21.2730932459892,-0.495303359101402,
4.37191940649105));
#22829=CARTESIAN_POINT('Ctrl Pts',(21.2969511640206,-0.612948680759938,
4.08912562603418));
#22830=CARTESIAN_POINT('Ctrl Pts',(21.320809082052,-0.580711353586496,3.78453820227854));
#22831=CARTESIAN_POINT('Ctrl Pts',(21.3446670000834,-0.406474282201139,
3.53263705712739));
#22832=CARTESIAN_POINT('Ctrl Pts',(21.3685249181149,-0.132843176680646,
3.39501888221951));
#22833=CARTESIAN_POINT('Ctrl Pts',(21.3923828361463,0.17327170411384,3.40533506996376));
#22834=CARTESIAN_POINT('Ctrl Pts',(21.4162407541777,0.437016933425986,3.56106303144932));
#22835=CARTESIAN_POINT('Ctrl Pts',(21.4400986722091,0.593899618413251,3.82412303814848));
#22836=CARTESIAN_POINT('Ctrl Pts',(21.4639565902405,0.605557669197671,4.13018975281259));
#22837=CARTESIAN_POINT('Ctrl Pts',(21.4878145082719,0.469140374803543,4.40442152661638));
#22838=CARTESIAN_POINT('Ctrl Pts',(21.5116724263034,0.218005479642704,4.57976122094124));
#22839=CARTESIAN_POINT('Ctrl Pts',(21.5355303443348,-0.0864376936408111,
4.61333350436739));
#22840=CARTESIAN_POINT('Ctrl Pts',(21.5593882623662,-0.369744496313637,
4.49692903910649));
#22841=CARTESIAN_POINT('Ctrl Pts',(21.5832461803976,-0.562638697999917,
4.2590118877088));
#22842=CARTESIAN_POINT('Ctrl Pts',(21.607104098429,-0.617952412054802,3.95775927442416));
#22843=CARTESIAN_POINT('Ctrl Pts',(21.6309620164605,-0.522159928676552,
3.66683566915707));
#22844=CARTESIAN_POINT('Ctrl Pts',(21.6548199344919,-0.298685119385998,
3.45737981799522));
#22845=CARTESIAN_POINT('Ctrl Pts',(21.6786778525233,-0.00217366238626178,
3.38060938201055));
#22846=CARTESIAN_POINT('Ctrl Pts',(21.7025357705547,0.294869314276287,3.45529682398599));
#22847=CARTESIAN_POINT('Ctrl Pts',(21.7263936885862,0.519808711519421,3.66317902991346));
#22848=CARTESIAN_POINT('Ctrl Pts',(21.7502516066175,0.617640719491047,3.95342313784609));
#22849=CARTESIAN_POINT('Ctrl Pts',(21.774109524649,0.564442747351711,4.25505655730362));
#22850=CARTESIAN_POINT('Ctrl Pts',(21.7979674426804,0.373223148373148,4.49432170089927));
#22851=CARTESIAN_POINT('Ctrl Pts',(21.8218253607118,0.0907403232229101,
4.61271172357229));
#22852=CARTESIAN_POINT('Ctrl Pts',(21.8456832787432,-0.213930982672105,
4.58127703989962));
#22853=CARTESIAN_POINT('Ctrl Pts',(21.8695411967746,-0.466290335940828,
4.40770428630285));
#22854=CARTESIAN_POINT('Ctrl Pts',(21.8933991148061,-0.604629000578284,
4.13443672906324));
#22855=CARTESIAN_POINT('Ctrl Pts',(21.9172570328375,-0.595119404811066,
3.82829572958469));
#22856=CARTESIAN_POINT('Ctrl Pts',(21.9411149508689,-0.440086903840403,
3.56414110135311));
#22857=CARTESIAN_POINT('Ctrl Pts',(21.9649728689003,-0.177441167154219,
3.40656584639871));
#22858=CARTESIAN_POINT('Ctrl Pts',(21.9888307869318,0.128593768301574,3.39410140682164));
#22859=CARTESIAN_POINT('Ctrl Pts',(22.0126887049631,0.403184024583593,3.52979567762293));
#22860=CARTESIAN_POINT('Ctrl Pts',(22.0365466229946,0.579184804342829,3.7804677133541));
#22861=CARTESIAN_POINT('Ctrl Pts',(22.060404541026,0.613559122762511,4.08482137310942));
#22862=CARTESIAN_POINT('Ctrl Pts',(22.0842624590574,0.497901522652627,4.36843389665204));
#22863=CARTESIAN_POINT('Ctrl Pts',(22.1081203770888,0.260493437687466,4.56195429652472));
#22864=CARTESIAN_POINT('Ctrl Pts',(22.1319782951203,-0.0406123884881684,
4.61806156357065));
#22865=CARTESIAN_POINT('Ctrl Pts',(22.1558362131517,-0.33178737942464,4.52303594266224));
#22866=CARTESIAN_POINT('Ctrl Pts',(22.1796941311831,-0.541831318374727,
4.30011378656432));
#22867=CARTESIAN_POINT('Ctrl Pts',(22.2035520492145,-0.619382740812877,
4.00380563470766));
#22868=CARTESIAN_POINT('Ctrl Pts',(22.2274099672459,-0.545478211438426,
3.70656690151735));
#22869=CARTESIAN_POINT('Ctrl Pts',(22.2512678852774,-0.338189400908512,
3.48108055383335));
#22870=CARTESIAN_POINT('Ctrl Pts',(22.2751258033088,-0.0482040696311437,
3.38248414587532));
#22871=CARTESIAN_POINT('Ctrl Pts',(22.2989837213402,0.253568469476171,3.43488718493857));
#22872=CARTESIAN_POINT('Ctrl Pts',(22.3228416393716,0.493336611197201,3.62547570084914));
#22873=CARTESIAN_POINT('Ctrl Pts',(22.346699557403,0.612470512379129,3.90764560936005));
#22874=CARTESIAN_POINT('Ctrl Pts',(22.3705574754344,0.581838691587799,4.21239868278141));
#22875=CARTESIAN_POINT('Ctrl Pts',(22.3944153934659,0.408931458591185,4.46521449128699));
#22876=CARTESIAN_POINT('Ctrl Pts',(22.4182733114973,0.13602935083686,4.60427268703701));
#22877=CARTESIAN_POINT('Ctrl Pts',(22.4421312295287,-0.170135649772668,
4.59556974592947));
#22878=CARTESIAN_POINT('Ctrl Pts',(22.4659891475601,-0.434697828443077,
4.44123378804823));
#22879=CARTESIAN_POINT('Ctrl Pts',(22.4898470655916,-0.592964587096883,
4.17900413283907));
#22880=CARTESIAN_POINT('Ctrl Pts',(22.513704983623,-0.606235276705168,3.87300312362118));
#22881=CARTESIAN_POINT('Ctrl Pts',(22.5375629016543,-0.471265070143009,
3.59805624874041));
#22882=CARTESIAN_POINT('Ctrl Pts',(22.5614208196858,-0.22105744785653,3.4213956854475));
#22883=CARTESIAN_POINT('Ctrl Pts',(22.5852787377172,0.0832042338527798,
3.38621941950615));
#22884=CARTESIAN_POINT('Ctrl Pts',(22.6091366557487,0.36712117327337,3.50112963696785));
#22885=CARTESIAN_POINT('Ctrl Pts',(22.63299457378,0.561265174232679,3.7380264683998));
#22886=CARTESIAN_POINT('Ctrl Pts',(22.6568524918115,0.618167971965146,4.03898443479498));
#22887=CARTESIAN_POINT('Ctrl Pts',(22.6807104098429,0.523905402647805,4.33040686810369));
#22888=CARTESIAN_POINT('Ctrl Pts',(22.7045683278744,0.301545895245711,4.54104106792393));
#22889=CARTESIAN_POINT('Ctrl Pts',(22.7284262459057,0.00542710047790416,
4.61936606261506));
#22890=CARTESIAN_POINT('Ctrl Pts',(22.7522841639372,-0.291974666000346,
4.54625809930836));
#22891=CARTESIAN_POINT('Ctrl Pts',(22.7761420819686,-0.518067845615496,
4.33953802216683));
#22892=CARTESIAN_POINT('Ctrl Pts',(22.7920473606562,-0.584213376873476,
4.14642833911731));
#22893=CARTESIAN_POINT('Ctrl Pts',(22.8,-0.592174260192535,4.04779597854866));
#22894=CARTESIAN_POINT('Ctrl Pts',(3.96816317011931,-0.282716247115855,
3.54616445487434));
#22895=CARTESIAN_POINT('Ctrl Pts',(3.97611580946312,-0.207125539895404,
3.49907532469992));
#22896=CARTESIAN_POINT('Ctrl Pts',(3.99202108815073,-0.0320395462633344,
3.44344227840288));
#22897=CARTESIAN_POINT('Ctrl Pts',(4.01587900618214,0.238586678544665,3.49618207793602));
#22898=CARTESIAN_POINT('Ctrl Pts',(4.03973692421357,0.450798406251909,3.67207593825259));
#22899=CARTESIAN_POINT('Ctrl Pts',(4.06359484224498,0.552814952159096,3.92817792166325));
#22900=CARTESIAN_POINT('Ctrl Pts',(4.0874527602764,0.519633627921064,4.20183097195279));
#22901=CARTESIAN_POINT('Ctrl Pts',(4.11131067830782,0.359398059257131,4.42613686623617));
#22902=CARTESIAN_POINT('Ctrl Pts',(4.13516859633924,0.11127440638865,4.54623750576341));
#22903=CARTESIAN_POINT('Ctrl Pts',(4.15902651437066,-0.164055973910312,
4.53276988152218));
#22904=CARTESIAN_POINT('Ctrl Pts',(4.18288443240208,-0.399271733473279,
4.38902461621758));
#22905=CARTESIAN_POINT('Ctrl Pts',(4.2067423504335,-0.536853866020863,4.15015270818839));
#22906=CARTESIAN_POINT('Ctrl Pts',(4.23060026846491,-0.543161034884179,
3.87456412255522));
#22907=CARTESIAN_POINT('Ctrl Pts',(4.25445818649634,-0.416650307492554,
3.62964815836115));
#22908=CARTESIAN_POINT('Ctrl Pts',(4.27831610452775,-0.188257351244862,
3.47529323740438));
#22909=CARTESIAN_POINT('Ctrl Pts',(4.30217402255918,0.0861697193074588,
3.44924344981891));
#22910=CARTESIAN_POINT('Ctrl Pts',(4.32603194059059,0.339525912432458,3.55786862136322));
#22911=CARTESIAN_POINT('Ctrl Pts',(4.34988985862202,0.509858789389686,3.77460696883261));
#22912=CARTESIAN_POINT('Ctrl Pts',(4.37374777665342,0.555517294574929,4.0464600464808));
#22913=CARTESIAN_POINT('Ctrl Pts',(4.39760569468486,0.465336694276122,4.30695238014399));
#22914=CARTESIAN_POINT('Ctrl Pts',(4.42146361271626,0.261368594047533,4.4923864940975));
#22915=CARTESIAN_POINT('Ctrl Pts',(4.4453215307477,-0.00651124555331369,
4.55741869872598));
#22916=CARTESIAN_POINT('Ctrl Pts',(4.4691794487791,-0.272798909000308,4.48614684730087));
#22917=CARTESIAN_POINT('Ctrl Pts',(4.49303736681053,-0.472379807908186,
4.29599884956661));
#22918=CARTESIAN_POINT('Ctrl Pts',(4.51689528484195,-0.55645097662433,4.03347107014466));
#22919=CARTESIAN_POINT('Ctrl Pts',(4.54075320287336,-0.504454724024634,
3.76275870240323));
#22920=CARTESIAN_POINT('Ctrl Pts',(4.56461112090479,-0.329105550388866,
3.55005829421323));
#22921=CARTESIAN_POINT('Ctrl Pts',(4.5884690389362,-0.0732811049967102,
3.44738088927219));
#22922=CARTESIAN_POINT('Ctrl Pts',(4.61232695696762,0.200462566687888,3.47983390993684));
#22923=CARTESIAN_POINT('Ctrl Pts',(4.63618487499904,0.425187680335341,3.63948170866684));
#22924=CARTESIAN_POINT('Ctrl Pts',(4.66004279303046,0.54594282425631,3.88728604994618));
#22925=CARTESIAN_POINT('Ctrl Pts',(4.68390071106188,0.533200076465109,4.16265202228146));
#22926=CARTESIAN_POINT('Ctrl Pts',(4.7077586290933,0.390075385898422,4.39824514461603));
#22927=CARTESIAN_POINT('Ctrl Pts',(4.73161654712472,0.151566638040082,4.53645648111246));
#22928=CARTESIAN_POINT('Ctrl Pts',(4.75547446515614,-0.124004281411749,
4.54348959519552));
#22929=CARTESIAN_POINT('Ctrl Pts',(4.77933238318755,-0.369252776249408,
4.41762469889406));
#22930=CARTESIAN_POINT('Ctrl Pts',(4.80319030121898,-0.524208909050512,
4.18963918784455));
#22931=CARTESIAN_POINT('Ctrl Pts',(4.82704821925039,-0.550981684424725,
3.91528172969931));
#22932=CARTESIAN_POINT('Ctrl Pts',(4.85090613728181,-0.443024429517375,
3.66164019632193));
#22933=CARTESIAN_POINT('Ctrl Pts',(4.87476405531323,-0.226735633849849,
3.49073685167984));
#22934=CARTESIAN_POINT('Ctrl Pts',(4.89862197334465,0.0449962004486201,
3.44436221885167));
#22935=CARTESIAN_POINT('Ctrl Pts',(4.92247989137607,0.305725238065515,3.53385615878353));
#22936=CARTESIAN_POINT('Ctrl Pts',(4.94633780940749,0.491696127187109,3.73733496539613));
#22937=CARTESIAN_POINT('Ctrl Pts',(4.9701957274389,0.557433919677865,4.00504252782125));
#22938=CARTESIAN_POINT('Ctrl Pts',(4.99405364547033,0.486863934612277,4.27151705483839));
#22939=CARTESIAN_POINT('Ctrl Pts',(5.01791156350174,0.297242455626679,4.47159826597145));
#22940=CARTESIAN_POINT('Ctrl Pts',(5.04176948153317,0.0349370995184326,
4.55636085499566));
#22941=CARTESIAN_POINT('Ctrl Pts',(5.06562739956458,-0.235911329089554,
4.505078060008));
#22942=CARTESIAN_POINT('Ctrl Pts',(5.08948531759601,-0.449073011639563,
4.33028992129829));
#22943=CARTESIAN_POINT('Ctrl Pts',(5.11334323562741,-0.552424110340463,
4.07473689991432));
#22944=CARTESIAN_POINT('Ctrl Pts',(5.13720115365885,-0.520692466332485,
3.80090867070902));
#22945=CARTESIAN_POINT('Ctrl Pts',(5.16105907169026,-0.361637330928202,
3.57576369465428));
#22946=CARTESIAN_POINT('Ctrl Pts',(5.18491698972168,-0.114152017308863,
3.45435605122152));
#22947=CARTESIAN_POINT('Ctrl Pts',(5.2087749077531,0.161246573981014,3.46637321630784));
#22948=CARTESIAN_POINT('Ctrl Pts',(5.23263282578452,0.397215985664045,3.60887666570863));
#22949=CARTESIAN_POINT('Ctrl Pts',(5.25649074381594,0.536055268906009,3.84702042432939));
#22950=CARTESIAN_POINT('Ctrl Pts',(5.28034866184735,0.543814437048104,4.12257185628156));
#22951=CARTESIAN_POINT('Ctrl Pts',(5.30420657987878,0.418596162124088,4.3681511305826));
#22952=CARTESIAN_POINT('Ctrl Pts',(5.32806449791019,0.191019723230217,4.5237074252207));
#22953=CARTESIAN_POINT('Ctrl Pts',(5.35192241594161,-0.0832662412662402,
4.55120298888854));
#22954=CARTESIAN_POINT('Ctrl Pts',(5.37578033397303,-0.337191341646214,
4.44391440730515));
#22955=CARTESIAN_POINT('Ctrl Pts',(5.39963825200445,-0.508663974085987,
4.22807666114996));
#22956=CARTESIAN_POINT('Ctrl Pts',(5.42349617003587,-0.555754409133215,
3.95646795866016));
#22957=CARTESIAN_POINT('Ctrl Pts',(5.4473540880673,-0.466947752701331,3.69550402606682));
#22958=CARTESIAN_POINT('Ctrl Pts',(5.47121200609871,-0.263959651332346,
3.50899765340418));
#22959=CARTESIAN_POINT('Ctrl Pts',(5.49506992413013,0.00357377490351851,
3.44255472911916));
#22960=CARTESIAN_POINT('Ctrl Pts',(5.51892784216155,0.270233315828591,3.51242235806964));
#22961=CARTESIAN_POINT('Ctrl Pts',(5.54278576019296,0.470813450024345,3.70151600181885));
#22962=CARTESIAN_POINT('Ctrl Pts',(5.56664367822439,0.556266870991092,3.96359711366712));
#22963=CARTESIAN_POINT('Ctrl Pts',(5.5905015962558,0.505697889589837,4.23457972281303));
#22964=CARTESIAN_POINT('Ctrl Pts',(5.61435951428722,0.331471999260015,4.4482011999181));
#22965=CARTESIAN_POINT('Ctrl Pts',(5.63821743231864,0.0761921759760934,
4.55222527486821));
#22966=CARTESIAN_POINT('Ctrl Pts',(5.66207535035006,-0.197718709731212,
4.52121522783523));
#22967=CARTESIAN_POINT('Ctrl Pts',(5.68593326838148,-0.423281985227643,
4.3627538599096));
#22968=CARTESIAN_POINT('Ctrl Pts',(5.70979118641289,-0.545341285237878,
4.11558929214995));
#22969=CARTESIAN_POINT('Ctrl Pts',(5.73364910444432,-0.534049786451273,
3.84015999362387));
#22970=CARTESIAN_POINT('Ctrl Pts',(5.75750702247573,-0.392168567195948,
3.6038159310769));
#22971=CARTESIAN_POINT('Ctrl Pts',(5.78136494050716,-0.154391451667357,
3.46434966433946));
#22972=CARTESIAN_POINT('Ctrl Pts',(5.80522285853857,0.121138580962943,3.45586449715393));
#22973=CARTESIAN_POINT('Ctrl Pts',(5.82908077656999,0.367046927720705,3.58043527923202));
#22974=CARTESIAN_POINT('Ctrl Pts',(5.85293869460141,0.523202308305842,3.80760107017232));
#22975=CARTESIAN_POINT('Ctrl Pts',(5.87679661263283,0.551420461789987,4.08181362911724));
#22976=CARTESIAN_POINT('Ctrl Pts',(5.90065453066425,0.44480131269862,4.33602054829434));
#22977=CARTESIAN_POINT('Ctrl Pts',(5.92451244869567,0.229416087376931,4.50806125053784));
#22978=CARTESIAN_POINT('Ctrl Pts',(5.94837036672709,-0.042067546589846,
4.55586721297736));
#22979=CARTESIAN_POINT('Ctrl Pts',(5.97222828475851,-0.30326465903273,4.46774835821298));
#22980=CARTESIAN_POINT('Ctrl Pts',(5.99608620278993,-0.490305038147314,
4.26525255699254));
#22981=CARTESIAN_POINT('Ctrl Pts',(6.01994412082133,-0.557452977205748,
3.99789477357902));
#22982=CARTESIAN_POINT('Ctrl Pts',(6.04380203885278,-0.488287539408226,
3.73105273207384));
#22983=CARTESIAN_POINT('Ctrl Pts',(6.06765995688417,-0.299724270968661,
3.52997381710292));
#22984=CARTESIAN_POINT('Ctrl Pts',(6.09151787491561,-0.0378669053578504,
3.44383251805177));
#22985=CARTESIAN_POINT('Ctrl Pts',(6.11537579294702,0.233243627260218,3.49368287747685));
#22986=CARTESIAN_POINT('Ctrl Pts',(6.13923371097844,0.447331678364145,3.6673537262422));
#22987=CARTESIAN_POINT('Ctrl Pts',(6.16309162900986,0.552012406214274,3.92234268746235));
#22988=CARTESIAN_POINT('Ctrl Pts',(6.18694954704127,0.521753629494025,4.19636433484848));
#22989=CARTESIAN_POINT('Ctrl Pts',(6.2108074650727,0.363831507594212,4.42228768590875));
#22990=CARTESIAN_POINT('Ctrl Pts',(6.23466538310411,0.117094415953721,4.54510476979165));
#22991=CARTESIAN_POINT('Ctrl Pts',(6.25852330113554,-0.158561881267111,
4.53433708369694));
#22992=CARTESIAN_POINT('Ctrl Pts',(6.28238121916695,-0.394905399742298,
4.39345989467659));
#22993=CARTESIAN_POINT('Ctrl Pts',(6.30623913719837,-0.535697351746728,
4.1553358869807));
#22994=CARTESIAN_POINT('Ctrl Pts',(6.33009705522979,-0.543633587309765,
3.88114808171798));
#22995=CARTESIAN_POINT('Ctrl Pts',(6.36190761260502,-0.381130543103143,
3.54983775818315));
#22996=CARTESIAN_POINT('Ctrl Pts',(6.40167080932404,0.0904237977681596,
3.37418170676098));
#22997=CARTESIAN_POINT('Ctrl Pts',(6.4493866453869,0.576013642360818,3.73827828410759));
#22998=CARTESIAN_POINT('Ctrl Pts',(6.49710248144972,0.531303907723303,4.34259299019566));
#22999=CARTESIAN_POINT('Ctrl Pts',(6.54481831751257,-0.000617460830772086,
4.63236849138271));
#23000=CARTESIAN_POINT('Ctrl Pts',(6.5925341535754,-0.532336898979176,4.34139325430452));
#23001=CARTESIAN_POINT('Ctrl Pts',(6.64024998963824,-0.575010046738857,
3.73693099107234));
#23002=CARTESIAN_POINT('Ctrl Pts',(6.68796582570108,-0.0897448725589052,
3.37403863313417));
#23003=CARTESIAN_POINT('Ctrl Pts',(6.73568166176391,0.477988548433368,3.58598174571673));
#23004=CARTESIAN_POINT('Ctrl Pts',(6.78339749782676,0.606749053262868,4.17812127049189));
#23005=CARTESIAN_POINT('Ctrl Pts',(6.83111333388958,0.178337754027021,4.60669083891839));
#23006=CARTESIAN_POINT('Ctrl Pts',(6.87882916995244,-0.413851892207341,
4.47812605548031));
#23007=CARTESIAN_POINT('Ctrl Pts',(6.92654500601527,-0.625990718083913,
3.91049119230943));
#23008=CARTESIAN_POINT('Ctrl Pts',(6.97426084207811,-0.263274891453005,
3.42505341469988));
#23009=CARTESIAN_POINT('Ctrl Pts',(7.02197667814094,0.341211513798207,3.46759805477058));
#23010=CARTESIAN_POINT('Ctrl Pts',(7.06969251420378,0.63235750294684,3.99905552874491));
#23011=CARTESIAN_POINT('Ctrl Pts',(7.11740835026662,0.342800202184808,4.53138035934227));
#23012=CARTESIAN_POINT('Ctrl Pts',(7.16512418632946,-0.261555976381552,
4.57573041153878));
#23013=CARTESIAN_POINT('Ctrl Pts',(7.2128400223923,-0.625721183287191,4.0913783776429));
#23014=CARTESIAN_POINT('Ctrl Pts',(7.26055585845514,-0.41527704940159,3.52311216844965));
#23015=CARTESIAN_POINT('Ctrl Pts',(7.30827169451797,0.176522415171576,3.39277939551711));
#23016=CARTESIAN_POINT('Ctrl Pts',(7.35598753058081,0.606218615784068,3.8200666455489));
#23017=CARTESIAN_POINT('Ctrl Pts',(7.40370336664364,0.479214941044062,4.4125894643569));
#23018=CARTESIAN_POINT('Ctrl Pts',(7.4514192027065,-0.0878591916424711,
4.62622502914213));
#23019=CARTESIAN_POINT('Ctrl Pts',(7.49913503876932,-0.574250874682306,
4.26478851416677));
#23020=CARTESIAN_POINT('Ctrl Pts',(7.54685087483217,-0.53329914461431,3.6601926322252));
#23021=CARTESIAN_POINT('Ctrl Pts',(7.594566710895,-0.00261060360317682,
3.36764708477891));
#23022=CARTESIAN_POINT('Ctrl Pts',(7.64228254695784,0.530475294557976,3.65580094934904));
#23023=CARTESIAN_POINT('Ctrl Pts',(7.68999838302067,0.576417567478113,4.26003809833172));
#23024=CARTESIAN_POINT('Ctrl Pts',(7.73771421908353,0.093026718772369,4.62547826040714));
#23025=CARTESIAN_POINT('Ctrl Pts',(7.78543005514634,-0.475791997136335,
4.41653211173522));
#23026=CARTESIAN_POINT('Ctrl Pts',(7.8331458912092,-0.607683601098078,3.82507811568403));
#23027=CARTESIAN_POINT('Ctrl Pts',(7.88086172727203,-0.181530003744534,
3.39425757752065));
#23028=CARTESIAN_POINT('Ctrl Pts',(7.92857756333487,0.411325389238953,3.51969962646458));
#23029=CARTESIAN_POINT('Ctrl Pts',(7.97629339939771,0.626454348233276,4.08620889879763));
#23030=CARTESIAN_POINT('Ctrl Pts',(8.02400923546054,0.266300640003926,4.57355121287022));
#23031=CARTESIAN_POINT('Ctrl Pts',(8.07172507152339,-0.338401043502061,
4.5341926229444));
#23032=CARTESIAN_POINT('Ctrl Pts',(8.11944090758622,-0.632343841791292,
4.00427672775865));
#23033=CARTESIAN_POINT('Ctrl Pts',(8.16715674364906,-0.345595560302635,
3.47043344766624));
#23034=CARTESIAN_POINT('Ctrl Pts',(8.2148725797119,0.258518441882999,3.42289928101069));
#23035=CARTESIAN_POINT('Ctrl Pts',(8.26258841577473,0.625230981070026,3.90532558443901));
#23036=CARTESIAN_POINT('Ctrl Pts',(8.31030425183758,0.417784289925175,4.47469286043008));
#23037=CARTESIAN_POINT('Ctrl Pts',(8.35802008790041,-0.173320143095541,
4.60814237859973));
#23038=CARTESIAN_POINT('Ctrl Pts',(8.40573592396325,-0.605262021838435,
4.18312539302794));
#23039=CARTESIAN_POINT('Ctrl Pts',(8.45345176002609,-0.481382472773795,
3.58994154129225));
#23040=CARTESIAN_POINT('Ctrl Pts',(8.50116759608892,0.0845580080604409,
3.37332068174828));
#23041=CARTESIAN_POINT('Ctrl Pts',(8.54888343215178,0.572847569000584,3.73218908285563));
#23042=CARTESIAN_POINT('Ctrl Pts',(8.59659926821459,0.535082392934658,4.33699236997728));
#23043=CARTESIAN_POINT('Ctrl Pts',(8.64431510427745,0.00594282213592907,
4.6323303784547));
#23044=CARTESIAN_POINT('Ctrl Pts',(8.69203094034027,-0.528654133672296,
4.34698967074364));
#23045=CARTESIAN_POINT('Ctrl Pts',(8.73974677640312,-0.577779864139828,
3.74300300926635));
#23046=CARTESIAN_POINT('Ctrl Pts',(8.78746261246595,-0.0963214550818077,
3.37502063878676));
#23047=CARTESIAN_POINT('Ctrl Pts',(8.8351784485288,0.473590428273928,3.58096643225285));
#23048=CARTESIAN_POINT('Ctrl Pts',(8.88289428459164,0.608596934220305,4.17171719864135));
#23049=CARTESIAN_POINT('Ctrl Pts',(8.93061012065447,0.184719511004659,4.60477741930878));
#23050=CARTESIAN_POINT('Ctrl Pts',(8.97832595671731,-0.408788681441581,
4.48246123012823));
#23051=CARTESIAN_POINT('Ctrl Pts',(9.02604179278014,-0.626899937697651,
3.91709346970068));
#23052=CARTESIAN_POINT('Ctrl Pts',(9.07375762884299,-0.269319335070538,
3.42786005172794));
#23053=CARTESIAN_POINT('Ctrl Pts',(9.12147346490582,0.335581356962483,3.46403155175812));
#23054=CARTESIAN_POINT('Ctrl Pts',(9.16918930096866,0.632312525313962,3.99239112474344));
#23055=CARTESIAN_POINT('Ctrl Pts',(9.21690513703149,0.348381372290835,4.52773804495445));
#23056=CARTESIAN_POINT('Ctrl Pts',(9.26462097309434,-0.255473755443411,
4.5784549981902));
#23057=CARTESIAN_POINT('Ctrl Pts',(9.31233680915717,-0.624723402584967,
4.09796782591368));
#23058=CARTESIAN_POINT('Ctrl Pts',(9.36005264522002,-0.420279936527615,
3.52751529167185));
#23059=CARTESIAN_POINT('Ctrl Pts',(9.40776848128285,0.170113062081096,3.39095273519949));
#23060=CARTESIAN_POINT('Ctrl Pts',(9.45548431734569,0.604288618254829,3.81368765339017));
#23061=CARTESIAN_POINT('Ctrl Pts',(9.50320015340853,0.483536638109595,4.40751606625661));
#23062=CARTESIAN_POINT('Ctrl Pts',(9.55091598947137,-0.0812544769791981,
4.62711620503893));
#23063=CARTESIAN_POINT('Ctrl Pts',(9.5986318255342,-0.571428355597161,4.27082588331087));
#23064=CARTESIAN_POINT('Ctrl Pts',(9.64634766159704,-0.536850782714826,
3.66583198574659));
#23065=CARTESIAN_POINT('Ctrl Pts',(9.69406349765987,-0.0092748755543832,
3.36770971750703));
#23066=CARTESIAN_POINT('Ctrl Pts',(9.74177933372272,0.52681829253995,3.65022934471732));
#23067=CARTESIAN_POINT('Ctrl Pts',(9.78949516978555,0.579126116453474,4.253948746587));
#23068=CARTESIAN_POINT('Ctrl Pts',(9.83721100584839,0.099613516627068,4.62446310696212));
#23069=CARTESIAN_POINT('Ctrl Pts',(9.88492684191123,-0.471375708268938,
4.42152338761395));
#23070=CARTESIAN_POINT('Ctrl Pts',(9.93264267797408,-0.609493367214024,
3.83149225544889));
#23071=CARTESIAN_POINT('Ctrl Pts',(9.9803585140369,-0.187903888785556,3.39620437793004));
#23072=CARTESIAN_POINT('Ctrl Pts',(10.0280743500997,0.406240621987656,3.51539131074786));
#23073=CARTESIAN_POINT('Ctrl Pts',(10.0757901861626,0.627328118774167,4.07960185956908));
#23074=CARTESIAN_POINT('Ctrl Pts',(10.1235060222254,0.27233055140652,4.57071279591595));
#23075=CARTESIAN_POINT('Ctrl Pts',(10.1712218582883,-0.332752351661881,
4.5377293902281));
#23076=CARTESIAN_POINT('Ctrl Pts',(10.2189376943511,-0.632263650146131,
4.01094081146358));
#23077=CARTESIAN_POINT('Ctrl Pts',(10.2666535304139,-0.351157510074434,
3.47410511718603));
#23078=CARTESIAN_POINT('Ctrl Pts',(10.3143693664768,0.252421974751429,3.42020678572945));
#23079=CARTESIAN_POINT('Ctrl Pts',(10.3620852025396,0.624198476151732,3.89874148420283));
#23080=CARTESIAN_POINT('Ctrl Pts',(10.4098010386024,0.422763912373798,4.47026343579529));
#23081=CARTESIAN_POINT('Ctrl Pts',(10.4575168746653,-0.166901257195935,
4.60993523836389));
#23082=CARTESIAN_POINT('Ctrl Pts',(10.5052327107281,-0.603298434176698,
4.18949412648294));
#23083=CARTESIAN_POINT('Ctrl Pts',(10.552948546791,-0.485677376113382,3.5950376425108));
#23084=CARTESIAN_POINT('Ctrl Pts',(10.6006643828538,0.0779486895418537,
3.3724643225678));
#23085=CARTESIAN_POINT('Ctrl Pts',(10.6483802189166,0.569993274196054,3.72616667108832));
#23086=CARTESIAN_POINT('Ctrl Pts',(10.6960960549795,0.538604264682155,4.3313343790158));
#23087=CARTESIAN_POINT('Ctrl Pts',(10.7438118910423,0.0126066714187673,
4.63223262845832));
#23088=CARTESIAN_POINT('Ctrl Pts',(10.7915277271052,-0.524967822187051,
4.35254192703816));
#23089=CARTESIAN_POINT('Ctrl Pts',(10.839243563168,-0.580456287010268,3.74910654946403));
#23090=CARTESIAN_POINT('Ctrl Pts',(10.8869593992308,-0.102902812003948,
3.37607048800905));
#23091=CARTESIAN_POINT('Ctrl Pts',(10.9346752352937,0.469147898628881,3.5759984978049));
#23092=CARTESIAN_POINT('Ctrl Pts',(10.9823910713565,0.610372875182502,4.16529361116822));
#23093=CARTESIAN_POINT('Ctrl Pts',(11.0301069074193,0.191083048662156,4.60279705802663));
#23094=CARTESIAN_POINT('Ctrl Pts',(11.0778227434822,-0.403681281635282,
4.48674269127424));
#23095=CARTESIAN_POINT('Ctrl Pts',(11.125538579545,-0.627738879572117,3.92370502162571));
#23096=CARTESIAN_POINT('Ctrl Pts',(11.1732544156079,-0.275334205393669,
3.43073020456744));
#23097=CARTESIAN_POINT('Ctrl Pts',(11.2209702516707,0.329914106159097,3.46052459999659));
#23098=CARTESIAN_POINT('Ctrl Pts',(11.2686860877335,0.632197217644931,3.98572755614488));
#23099=CARTESIAN_POINT('Ctrl Pts',(11.3164019237964,0.353923896562866,4.52403711709511));
#23100=CARTESIAN_POINT('Ctrl Pts',(11.3641177598592,-0.24936318455202,4.58111533006939));
#23101=CARTESIAN_POINT('Ctrl Pts',(11.411833595922,-0.623656216347001,4.10454639383227));
#23102=CARTESIAN_POINT('Ctrl Pts',(11.4595494319849,-0.425236148486169,
3.53197089548594));
#23103=CARTESIAN_POINT('Ctrl Pts',(11.5072652680477,0.163684817628688,3.3891937253683));
#23104=CARTESIAN_POINT('Ctrl Pts',(11.5549811041106,0.602291497100466,3.80732935570755));
#23105=CARTESIAN_POINT('Ctrl Pts',(11.6026969401734,0.487804627338989,4.40239740331947));
#23106=CARTESIAN_POINT('Ctrl Pts',(11.6504127762363,-0.0746407375468588,
4.62793772378323));
#23107=CARTESIAN_POINT('Ctrl Pts',(11.6981286122991,-0.568542364648052,
4.276833170433));
#23108=CARTESIAN_POINT('Ctrl Pts',(11.7458444483619,-0.540342790144192,
3.67150845704832));
#23109=CARTESIAN_POINT('Ctrl Pts',(11.7935602844247,-0.0159381172083995,
3.36784258204823));
#23110=CARTESIAN_POINT('Ctrl Pts',(11.8412761204876,0.523102773999324,3.64469659094542));
#23111=CARTESIAN_POINT('Ctrl Pts',(11.8889919565504,0.581770338872691,4.24783118742311));
#23112=CARTESIAN_POINT('Ctrl Pts',(11.9367077926133,0.106189249871976,4.62337859111715));
#23113=CARTESIAN_POINT('Ctrl Pts',(11.9844236286761,-0.466907061217805,
4.4264678426758));
#23114=CARTESIAN_POINT('Ctrl Pts',(12.0321394647389,-0.611235433702689,
3.83792511225401));
#23115=CARTESIAN_POINT('Ctrl Pts',(12.0798553008018,-0.19425690235234,3.39821824509208));
#23116=CARTESIAN_POINT('Ctrl Pts',(12.1275711368646,0.401110731454808,3.51113682306459));
#23117=CARTESIAN_POINT('Ctrl Pts',(12.1752869729275,0.628132208685083,4.07298597854376));
#23118=CARTESIAN_POINT('Ctrl Pts',(12.2230028089903,0.27833021362349,4.56781098689255));
#23119=CARTESIAN_POINT('Ctrl Pts',(12.2707186450531,-0.327066699269377,
4.54120642908287));
#23120=CARTESIAN_POINT('Ctrl Pts',(12.3184344811159,-0.632113229655128,
4.01760367991507));
#23121=CARTESIAN_POINT('Ctrl Pts',(12.3661503171788,-0.356680454936339,
3.47783520061383));
#23122=CARTESIAN_POINT('Ctrl Pts',(12.4138661532416,0.246297469784735,3.4175786911271));
#23123=CARTESIAN_POINT('Ctrl Pts',(12.4615819893045,0.623096638228782,3.89216863128209));
#23124=CARTESIAN_POINT('Ctrl Pts',(12.5092978253673,0.427696576213203,4.46578177652963));
#23125=CARTESIAN_POINT('Ctrl Pts',(12.5570136614302,-0.16046383269669,4.61166034941614));
#23126=CARTESIAN_POINT('Ctrl Pts',(12.604729497493,-0.601267834987779,4.1958418118296));
#23127=CARTESIAN_POINT('Ctrl Pts',(12.6524453335558,-0.489918332714758,
3.60017872502631));
#23128=CARTESIAN_POINT('Ctrl Pts',(12.7001611696187,0.0713307128527425,
3.37167766707246));
#23129=CARTESIAN_POINT('Ctrl Pts',(12.7478770056815,0.56707566724347,3.72017467542775));
#23130=CARTESIAN_POINT('Ctrl Pts',(12.7955928417444,0.542066310823814,4.32563958500381));
#23131=CARTESIAN_POINT('Ctrl Pts',(12.8433086778072,0.0192691204123526,
4.63206465306178));
#23132=CARTESIAN_POINT('Ctrl Pts',(12.89102451387,-0.521223199767296,4.35805502464836));
#23133=CARTESIAN_POINT('Ctrl Pts',(12.9387403499329,-0.583068235550835,
3.7552379577156));
#23134=CARTESIAN_POINT('Ctrl Pts',(12.9864561859957,-0.109472738970043,
3.37718964036075));
#23135=CARTESIAN_POINT('Ctrl Pts',(13.0341720220585,0.464653258261548,3.57107765943178));
#23136=CARTESIAN_POINT('Ctrl Pts',(13.0818878581214,0.612081018822183,4.15885166366515));
#23137=CARTESIAN_POINT('Ctrl Pts',(13.1296036941842,0.197425361721354,4.6007497409078));
#23138=CARTESIAN_POINT('Ctrl Pts',(13.177319530247,-0.398529042827853,4.49097008735187));
#23139=CARTESIAN_POINT('Ctrl Pts',(13.2250353663099,-0.628508095190705,
3.93032504803489));
#23140=CARTESIAN_POINT('Ctrl Pts',(13.2727512023727,-0.281318492899819,
3.4336635891944));
#23141=CARTESIAN_POINT('Ctrl Pts',(13.3204670384356,0.324210210062374,3.45707757060249));
#23142=CARTESIAN_POINT('Ctrl Pts',(13.3681828744984,0.632011688508986,3.97906557286167));
#23143=CARTESIAN_POINT('Ctrl Pts',(13.4158987105612,0.359427108647973,4.52027798167956));
#23144=CARTESIAN_POINT('Ctrl Pts',(13.4636145466241,-0.243224915581421,
4.58371111441534));
#23145=CARTESIAN_POINT('Ctrl Pts',(13.5113303826869,-0.622519757336015,
4.11111334923356));
#23146=CARTESIAN_POINT('Ctrl Pts',(13.5590462187498,-0.430145127231255,
3.53647848575196));
#23147=CARTESIAN_POINT('Ctrl Pts',(13.6067620548126,0.157238391843492,3.38750256099959));
#23148=CARTESIAN_POINT('Ctrl Pts',(13.6544778908755,0.600227476264717,3.8009924589658));
#23149=CARTESIAN_POINT('Ctrl Pts',(13.7021937269383,0.492018433545193,4.39723404398833));
#23150=CARTESIAN_POINT('Ctrl Pts',(13.7499095630011,-0.0680187073756014,
4.62868949418496));
#23151=CARTESIAN_POINT('Ctrl Pts',(13.797625399064,-0.565593222711038,4.28280970824024));
#23152=CARTESIAN_POINT('Ctrl Pts',(13.8453412351268,-0.543774778860562,
3.67722141563181));
#23153=CARTESIAN_POINT('Ctrl Pts',(13.8930570711896,-0.0225995885319848,
3.36804566363559));
#23154=CARTESIAN_POINT('Ctrl Pts',(13.9407729072525,0.519329151684885,3.63920330259016));
#23155=CARTESIAN_POINT('Ctrl Pts',(13.9884887433153,0.584349941003394,4.24168610034696));
#23156=CARTESIAN_POINT('Ctrl Pts',(14.0362045793781,0.112753188118911,4.62222483333648));
#23157=CARTESIAN_POINT('Ctrl Pts',(14.083920415441,-0.462386552345973,4.43136492771341));
#23158=CARTESIAN_POINT('Ctrl Pts',(14.1316362515038,-0.612909607059929,
3.84437597156854));
#23159=CARTESIAN_POINT('Ctrl Pts',(14.1793520875667,-0.200588338784227,
3.40029895531576));
#23160=CARTESIAN_POINT('Ctrl Pts',(14.2270679236295,0.395936287445344,3.50693663598317));
#23161=CARTESIAN_POINT('Ctrl Pts',(14.2747837596923,0.628866528650988,4.06636199058228));
#23162=CARTESIAN_POINT('Ctrl Pts',(14.3224995957552,0.284298960241116,4.5648461081192));
#23163=CARTESIAN_POINT('Ctrl Pts',(14.370215431818,-0.321344717859966,4.54462335329573));
#23164=CARTESIAN_POINT('Ctrl Pts',(14.4179312678809,-0.631892597026201,
4.02426459303334));
#23165=CARTESIAN_POINT('Ctrl Pts',(14.4656471039437,-0.362163781425906,
3.48162328362967));
#23166=CARTESIAN_POINT('Ctrl Pts',(14.5133629400065,0.240145607263868,3.41501528911991));
#23167=CARTESIAN_POINT('Ctrl Pts',(14.5610787760693,0.6219255896881,3.8856077557581));
#23168=CARTESIAN_POINT('Ctrl Pts',(14.6087946121322,0.432581733546503,4.46124838043455));
#23169=CARTESIAN_POINT('Ctrl Pts',(14.656510448195,-0.154008584636381,4.61331752013935));
#23170=CARTESIAN_POINT('Ctrl Pts',(14.7042262842579,-0.599170449821005,
4.20216774399712));
#23171=CARTESIAN_POINT('Ctrl Pts',(14.7519421203207,-0.494104871512583,
3.60536421779174));
#23172=CARTESIAN_POINT('Ctrl Pts',(14.7996579563836,0.0647048130865326,
3.37096080264023));
#23173=CARTESIAN_POINT('Ctrl Pts',(14.8473737924464,0.564095072216763,3.71421376143635));
#23174=CARTESIAN_POINT('Ctrl Pts',(14.8950896285093,0.545468146811986,4.319908620492));
#23175=CARTESIAN_POINT('Ctrl Pts',(14.942805464572,0.0259294290834894,4.63182647092298));
#23176=CARTESIAN_POINT('Ctrl Pts',(14.9905213006349,-0.517420682347921,
4.36352835120552));
#23177=CARTESIAN_POINT('Ctrl Pts',(15.0382371366977,-0.585615419638682,
3.76139655297334));
#23178=CARTESIAN_POINT('Ctrl Pts',(15.0859529727606,-0.116030506223773,
3.3783779715317));
#23179=CARTESIAN_POINT('Ctrl Pts',(15.1336688088234,0.460107006415252,3.56620446371685));
#23180=CARTESIAN_POINT('Ctrl Pts',(15.1813846448862,0.613721175406852,4.15239207167311));
#23181=CARTESIAN_POINT('Ctrl Pts',(15.2291004809491,0.203745745708236,4.59863569535852));
#23182=CARTESIAN_POINT('Ctrl Pts',(15.2768163170119,-0.393332537305518,
4.49514294880206));
#23183=CARTESIAN_POINT('Ctrl Pts',(15.3245321530748,-0.629207499112597,
3.93695281360709));
#23184=CARTESIAN_POINT('Ctrl Pts',(15.3722479891376,-0.287271532882751,
3.43665987978239));
#23185=CARTESIAN_POINT('Ctrl Pts',(15.4199638252004,0.318470302234025,3.45369084645546));
#23186=CARTESIAN_POINT('Ctrl Pts',(15.4676796612633,0.631755958513824,3.97240591487529));
#23187=CARTESIAN_POINT('Ctrl Pts',(15.5153954973261,0.364890397275464,4.51646105625472));
#23188=CARTESIAN_POINT('Ctrl Pts',(15.563111333389,-0.237059630341402,4.58624206290064));
#23189=CARTESIAN_POINT('Ctrl Pts',(15.6108271694518,-0.621314151784485,
4.11766796269128));
#23190=CARTESIAN_POINT('Ctrl Pts',(15.6585430055147,-0.435006327496808,
3.54103756178819));
#23191=CARTESIAN_POINT('Ctrl Pts',(15.7062588415774,0.150774500763906,3.38587942993986));
#23192=CARTESIAN_POINT('Ctrl Pts',(15.7539746776403,0.598096785009218,3.79467766703735));
#23193=CARTESIAN_POINT('Ctrl Pts',(15.8016905137032,0.496177588678611,4.39202656178461));
#23194=CARTESIAN_POINT('Ctrl Pts',(15.849406349766,-0.0613891220090978,
4.62937143274106));
#23195=CARTESIAN_POINT('Ctrl Pts',(15.8971221858288,-0.562581257362808,
4.28875483288714));
#23196=CARTESIAN_POINT('Ctrl Pts',(15.9448380218917,-0.547146367654922,
3.68297022692873));
#23197=CARTESIAN_POINT('Ctrl Pts',(15.9925538579545,-0.0292585496004989,
3.36831893971177));
#23198=CARTESIAN_POINT('Ctrl Pts',(16.0402696940173,0.515497844752703,3.63375008981994));
#23199=CARTESIAN_POINT('Ctrl Pts',(16.0879855300802,0.586864636315616,4.23551416792571));
#23200=CARTESIAN_POINT('Ctrl Pts',(16.135701366143,0.119304602276749,4.62100196177401));
#23201=CARTESIAN_POINT('Ctrl Pts',(16.1834172022059,-0.457814683770117,
4.43621409878185));
#23202=CARTESIAN_POINT('Ctrl Pts',(16.2311330382687,-0.614515701326505,
3.85084411686165));
#23203=CARTESIAN_POINT('Ctrl Pts',(16.2788488743316,-0.206897494815317,
3.40244627748567));
#23204=CARTESIAN_POINT('Ctrl Pts',(16.3265647103943,0.390717864711932,3.50279121604045));
#23205=CARTESIAN_POINT('Ctrl Pts',(16.3742805464572,0.629530997107116,4.05973063144581));
#23206=CARTESIAN_POINT('Ctrl Pts',(16.42199638252,0.290236128279341,4.56181848892059));
#23207=CARTESIAN_POINT('Ctrl Pts',(16.4697122185829,-0.315587043004215,
4.54797978333095));
#23208=CARTESIAN_POINT('Ctrl Pts',(16.5174280546457,-0.631601776766168,
4.03092281095576));
#23209=CARTESIAN_POINT('Ctrl Pts',(16.5651438907086,-0.367606880481235,
3.48546894547127));
#23210=CARTESIAN_POINT('Ctrl Pts',(16.6128597267714,0.233967070508539,3.41251686443844));
#23211=CARTESIAN_POINT('Ctrl Pts',(16.6605755628343,0.620685460604191,3.87905958638177));
#23212=CARTESIAN_POINT('Ctrl Pts',(16.7082913988971,0.437418841753611,4.45666375105816));
#23213=CARTESIAN_POINT('Ctrl Pts',(16.7560072349599,-0.147536230033309,
4.61490656646286));
#23214=CARTESIAN_POINT('Ctrl Pts',(16.8037230710227,-0.597006511643959,
4.20847122033102));
#23215=CARTESIAN_POINT('Ctrl Pts',(16.8514389070856,-0.498236527486006,
3.61059354482716));
#23216=CARTESIAN_POINT('Ctrl Pts',(16.8991547431484,0.058071726216741,3.37031380889701));
#23217=CARTESIAN_POINT('Ctrl Pts',(16.9468705792113,0.561051820186282,3.70828459122417));
#23218=CARTESIAN_POINT('Ctrl Pts',(16.9945864152741,0.548809394786867,4.31414212204871));
#23219=CARTESIAN_POINT('Ctrl Pts',(17.0423022513369,0.0325868576366809,
4.63151810849805));
#23220=CARTESIAN_POINT('Ctrl Pts',(17.0900180873998,-0.513560692294518,
4.3689612987585));
#23221=CARTESIAN_POINT('Ctrl Pts',(17.1377339234626,-0.588097556344686,
3.76758165116972));
#23222=CARTESIAN_POINT('Ctrl Pts',(17.1854497595255,-0.122575385359494,
3.37963534952775));
#23223=CARTESIAN_POINT('Ctrl Pts',(17.2331655955883,0.455509648066065,3.56137945195155));
#23224=CARTESIAN_POINT('Ctrl Pts',(17.2808814316511,0.615293162755707,4.14591555269289));
#23225=CARTESIAN_POINT('Ctrl Pts',(17.328597267714,0.210043498584534,4.59645515619697));
#23226=CARTESIAN_POINT('Ctrl Pts',(17.3763131037768,-0.388092342271454,
4.49926081212312));
#23227=CARTESIAN_POINT('Ctrl Pts',(17.4240289398397,-0.629837013651323,
3.94358758216158));
#23228=CARTESIAN_POINT('Ctrl Pts',(17.4717447759025,-0.293192664107019,
3.43971874351766));
#23229=CARTESIAN_POINT('Ctrl Pts',(17.5194606119653,0.312695020235776,3.45036480373676));
#23230=CARTESIAN_POINT('Ctrl Pts',(17.5671764480282,0.631430056064715,3.96574932190893));
#23231=CARTESIAN_POINT('Ctrl Pts',(17.614892284091,0.370313155609181,4.51258676478657));
#23232=CARTESIAN_POINT('Ctrl Pts',(17.6626081201539,-0.230868013642575,
4.58870789439952));
#23233=CARTESIAN_POINT('Ctrl Pts',(17.7103239562166,-0.620039533605355,
4.12420950615009));
#23234=CARTESIAN_POINT('Ctrl Pts',(17.7580397922796,-0.43981920932378,3.54564761719411));
#23235=CARTESIAN_POINT('Ctrl Pts',(17.8057556283423,0.144293862368219,3.38432451247882));
#23236=CARTESIAN_POINT('Ctrl Pts',(17.8534714644052,0.595899660001039,3.78838568133928));
#23237=CARTESIAN_POINT('Ctrl Pts',(17.901187300468,0.500281630760053,4.38677553513073));
#23238=CARTESIAN_POINT('Ctrl Pts',(17.9489031365309,-0.0547527178302441,
4.62998346370502));
#23239=CARTESIAN_POINT('Ctrl Pts',(17.9966189725937,-0.559506803158163,
4.29466788401745));
#23240=CARTESIAN_POINT('Ctrl Pts',(18.0443348086565,-0.550457182027191,
3.68875425238845));
#23241=CARTESIAN_POINT('Ctrl Pts',(18.0920506447194,-0.0359142607682062,
3.36866237992255));
#23242=CARTESIAN_POINT('Ctrl Pts',(18.1397664807822,0.511609278766163,3.62833755835171));
#23243=CARTESIAN_POINT('Ctrl Pts',(18.187482316845,0.589314145488933,4.22931607570827));
#23244=CARTESIAN_POINT('Ctrl Pts',(18.2351981529079,0.12584276464555,4.61971011226051));
#23245=CARTESIAN_POINT('Ctrl Pts',(18.2829139889707,-0.453191963311679,
4.44101481725822));
#23246=CARTESIAN_POINT('Ctrl Pts',(18.3306298250336,-0.616053538105107,
3.85732882968247));
#23247=CARTESIAN_POINT('Ctrl Pts',(18.3783456610964,-0.213183669654489,
3.40465997308746));
#23248=CARTESIAN_POINT('Ctrl Pts',(18.4260614971592,0.385456042892229,3.49870102369));
#23249=CARTESIAN_POINT('Ctrl Pts',(18.4737773332221,0.630125540247444,4.05309263771424));
#23250=CARTESIAN_POINT('Ctrl Pts',(18.5214931692849,0.296141058265729,4.55872846559028));
#23251=CARTESIAN_POINT('Ctrl Pts',(18.5692090053478,-0.309794314237323,
4.55127534637221));
#23252=CARTESIAN_POINT('Ctrl Pts',(18.6169248414106,-0.631240801177943,
4.0375775941191));
#23253=CARTESIAN_POINT('Ctrl Pts',(18.6646406774734,-0.373009147508776,
3.4893717589807));
#23254=CARTESIAN_POINT('Ctrl Pts',(18.7123565135363,0.227762545801372,3.41008369459593));
#23255=CARTESIAN_POINT('Ctrl Pts',(18.7600723495991,0.619376388724522,3.87252485049244));
#23256=CARTESIAN_POINT('Ctrl Pts',(18.8077881856619,0.442207363551868,4.45202839763978));
#23257=CARTESIAN_POINT('Ctrl Pts',(18.8555040217248,-0.141047487806633,
4.61642731188217));
#23258=CARTESIAN_POINT('Ctrl Pts',(18.9032198577876,-0.594776260815313,
4.21475154067248));
#23259=CARTESIAN_POINT('Ctrl Pts',(18.9509356938505,-0.502312841712761,
3.615866125281));
#23260=CARTESIAN_POINT('Ctrl Pts',(18.9986515299133,0.0514321890198641,
3.36973675771293));
#23261=CARTESIAN_POINT('Ctrl Pts',(19.0463673659762,0.557946249173174,3.70238782336559));
#23262=CARTESIAN_POINT('Ctrl Pts',(19.0940832020389,0.552089683635207,4.30834073020757));
#23263=CARTESIAN_POINT('Ctrl Pts',(19.1417990381018,0.0392406665648073,
4.63113960000379));
#23264=CARTESIAN_POINT('Ctrl Pts',(19.1895148741646,-0.509643658296843,
4.3743532639067));
#23265=CARTESIAN_POINT('Ctrl Pts',(19.2372307102275,-0.590514370077448,
3.77379256516987));
#23266=CARTESIAN_POINT('Ctrl Pts',(19.2849465462903,-0.129106649190522,
3.38096163491845));
#23267=CARTESIAN_POINT('Ctrl Pts',(19.3326623823532,0.450861693465423,3.55660315963506));
#23268=CARTESIAN_POINT('Ctrl Pts',(19.380378218416,0.616796807017627,4.1394228269368));
#23269=CARTESIAN_POINT('Ctrl Pts',(19.4280940544789,0.216317919394901,4.59420836405745));
#23270=CARTESIAN_POINT('Ctrl Pts',(19.4758098905416,-0.382809037079938,
4.50332322288615));
#23271=CARTESIAN_POINT('Ctrl Pts',(19.5235257266046,-0.630396573984801,
3.95022861114352));
#23272=CARTESIAN_POINT('Ctrl Pts',(19.5712415626673,-0.299081219248977,
3.44283985120298));
#23273=CARTESIAN_POINT('Ctrl Pts',(19.6189573987302,0.306884987370396,3.44709979193512));
#23274=CARTESIAN_POINT('Ctrl Pts',(19.666673234793,0.631034051704256,3.95909657101937));
#23275=CARTESIAN_POINT('Ctrl Pts',(19.7143890708559,0.375694716468479,4.50865546647685));
#23276=CARTESIAN_POINT('Ctrl Pts',(19.7621049069187,-0.224650630777236,
4.59110846933868));
#23277=CARTESIAN_POINT('Ctrl Pts',(19.8098207429815,-0.618696275574682,
4.13073699938377));
#23278=CARTESIAN_POINT('Ctrl Pts',(19.8575365790444,-0.44458280157215,3.55030861879767));
#23279=CARTESIAN_POINT('Ctrl Pts',(19.9052524151072,0.13779637220375,3.3828370770856));
#23280=CARTESIAN_POINT('Ctrl Pts',(19.9529682511701,0.593637901716091,3.7821189081517));
#23281=CARTESIAN_POINT('Ctrl Pts',(20.0006840872329,0.504327165075627,4.38147832337345));
#23282=CARTESIAN_POINT('Ctrl Pts',(20.0483999232957,-0.0481046828163007,
4.63053160650705));
#23283=CARTESIAN_POINT('Ctrl Pts',(20.0961157593586,-0.556380679578279,
4.30053671048834));
#23284=CARTESIAN_POINT('Ctrl Pts',(20.1438315954214,-0.553687069357429,
3.69459455385474));
#23285=CARTESIAN_POINT('Ctrl Pts',(20.1915474314843,-0.0426033430871586,
3.36903495876776));
#23286=CARTESIAN_POINT('Ctrl Pts',(20.2392632675471,0.507734449822709,3.62304374442814));
#23287=CARTESIAN_POINT('Ctrl Pts',(20.2869791036099,0.591564791291533,4.22294595084339));
#23288=CARTESIAN_POINT('Ctrl Pts',(20.3346949396728,0.132620199007312,4.618629012875));
#23289=CARTESIAN_POINT('Ctrl Pts',(20.3824107757356,-0.449008129734859,
4.44521533979349));
#23290=CARTESIAN_POINT('Ctrl Pts',(20.4221739724547,-0.588594799935545,
3.96175478680276));
#23291=CARTESIAN_POINT('Ctrl Pts',(20.4539845298298,-0.419131055782338,
3.63395025773895));
#23292=CARTESIAN_POINT('Ctrl Pts',(20.4778424478613,-0.194099195253748,
3.47709810398663));
#23293=CARTESIAN_POINT('Ctrl Pts',(20.5017003658927,0.0810471032980313,
3.44846366347126));
#23294=CARTESIAN_POINT('Ctrl Pts',(20.5255582839241,0.334940048200093,3.55449674151986));
#23295=CARTESIAN_POINT('Ctrl Pts',(20.5494162019556,0.507694843328107,3.76957374638464));
#23296=CARTESIAN_POINT('Ctrl Pts',(20.5732741199869,0.555899439471162,4.04093981905292));
#23297=CARTESIAN_POINT('Ctrl Pts',(20.5971320380184,0.468386015874758,4.30232489481291));
#23298=CARTESIAN_POINT('Ctrl Pts',(20.6209899560498,0.266225827016684,4.48976745893774));
#23299=CARTESIAN_POINT('Ctrl Pts',(20.6448478740812,-0.000973650874560818,
4.55745692740964));
#23300=CARTESIAN_POINT('Ctrl Pts',(20.6687057921126,-0.267966914960919,
4.48882854939535));
#23301=CARTESIAN_POINT('Ctrl Pts',(20.6925637101441,-0.469418090387657,
4.30067062862012));
#23302=CARTESIAN_POINT('Ctrl Pts',(20.7164216281755,-0.556092695039732,
4.03898930289119));
#23303=CARTESIAN_POINT('Ctrl Pts',(20.7402795462069,-0.506782753954552,
3.7677746905255));
#23304=CARTESIAN_POINT('Ctrl Pts',(20.7641374642383,-0.333553132261349,
3.55334514249538));
#23305=CARTESIAN_POINT('Ctrl Pts',(20.7879953822697,-0.0787593560922578,
3.44813505886707));
#23306=CARTESIAN_POINT('Ctrl Pts',(20.8118533003012,0.19529252477751,3.47787088781106));
#23307=CARTESIAN_POINT('Ctrl Pts',(20.8357112183325,0.421590436108717,3.63528155911584));
#23308=CARTESIAN_POINT('Ctrl Pts',(20.859569136364,0.544797804677434,3.8818757964511));
#23309=CARTESIAN_POINT('Ctrl Pts',(20.8834270543954,0.534787374467886,4.15735463375504));
#23310=CARTESIAN_POINT('Ctrl Pts',(20.9072849724269,0.394006808563119,4.39435596913946));
#23311=CARTESIAN_POINT('Ctrl Pts',(20.9311428904582,0.156880874733563,4.53492653211281));
#23312=CARTESIAN_POINT('Ctrl Pts',(20.9550008084897,-0.118606721834374,
4.54469298471526));
#23313=CARTESIAN_POINT('Ctrl Pts',(20.9788587265211,-0.365091735913813,
4.42126716656144));
#23314=CARTESIAN_POINT('Ctrl Pts',(21.0027166445525,-0.522301880015273,
4.19483005048941));
#23315=CARTESIAN_POINT('Ctrl Pts',(21.0265745625839,-0.55179498493052,3.92075168033001));
#23316=CARTESIAN_POINT('Ctrl Pts',(21.0504324806153,-0.446359186657349,
3.66605168284066));
#23317=CARTESIAN_POINT('Ctrl Pts',(21.0742903986468,-0.231776408019839,
3.49301114555638));
#23318=CARTESIAN_POINT('Ctrl Pts',(21.0981483166782,0.0394820154987394,
3.44394319323497));
#23319=CARTESIAN_POINT('Ctrl Pts',(21.1220062347096,0.301086010940692,3.5308462768762));
#23320=CARTESIAN_POINT('Ctrl Pts',(21.145864152741,0.489066275193333,3.73247022529863));
#23321=CARTESIAN_POINT('Ctrl Pts',(21.1697220707724,0.557456513314207,3.9995124910074));
#23322=CARTESIAN_POINT('Ctrl Pts',(21.1935799888039,0.489533449092281,4.26667396594056));
#23323=CARTESIAN_POINT('Ctrl Pts',(21.2174379068352,0.30190612195814,4.46862639215028));
#23324=CARTESIAN_POINT('Ctrl Pts',(21.2412958248667,0.0404545242400231,
4.55598690035157));
#23325=CARTESIAN_POINT('Ctrl Pts',(21.2651537428981,-0.230889306609896,
4.50739346663836));
#23326=CARTESIAN_POINT('Ctrl Pts',(21.2890116609295,-0.445774412697373,
4.33472850921124));
#23327=CARTESIAN_POINT('Ctrl Pts',(21.312869578961,-0.551655532228011,4.08021331346062));
#23328=CARTESIAN_POINT('Ctrl Pts',(21.3367274969923,-0.522641847334507,
3.80608377760199));
#23329=CARTESIAN_POINT('Ctrl Pts',(21.3605854150238,-0.365827994289322,
3.57937204029158));
#23330=CARTESIAN_POINT('Ctrl Pts',(21.3844433330552,-0.119559231686077,
3.45551529680541));
#23331=CARTESIAN_POINT('Ctrl Pts',(21.4083012510867,0.155945019792583,3.46479989471587));
#23332=CARTESIAN_POINT('Ctrl Pts',(21.432159169118,0.393316466074861,3.60495549692644));
#23333=CARTESIAN_POINT('Ctrl Pts',(21.4560170871495,0.534511322676435,3.84171024093472));
#23334=CARTESIAN_POINT('Ctrl Pts',(21.4798750051809,0.545003601087511,4.11717114276091));
#23335=CARTESIAN_POINT('Ctrl Pts',(21.5037329232123,0.422227653432673,4.36398050850424));
#23336=CARTESIAN_POINT('Ctrl Pts',(21.5275908412437,0.196205543263173,4.52178672528827));
#23337=CARTESIAN_POINT('Ctrl Pts',(21.5514487592751,-0.0777941667658609,
4.5520018745543));
#23338=CARTESIAN_POINT('Ctrl Pts',(21.5753066773066,-0.332771083950078,
4.44723752926263));
#23339=CARTESIAN_POINT('Ctrl Pts',(21.5991645953379,-0.506376406606172,
4.23311142556056));
#23340=CARTESIAN_POINT('Ctrl Pts',(21.6230225133694,-0.556158904430687,
3.96198322848119));
#23341=CARTESIAN_POINT('Ctrl Pts',(21.6468804314008,-0.469945400657515,
3.70015116759423));
#23342=CARTESIAN_POINT('Ctrl Pts',(21.6707383494323,-0.268817445367881,
3.51164031394868));
#23343=CARTESIAN_POINT('Ctrl Pts',(21.6945962674636,-0.00195630224560004,
3.44254670619344));
#23344=CARTESIAN_POINT('Ctrl Pts',(21.7184541854951,0.26538321006433,3.50976561349676));
#23345=CARTESIAN_POINT('Ctrl Pts',(21.7423121035264,0.467829298620023,3.6968601820167));
#23346=CARTESIAN_POINT('Ctrl Pts',(21.766170021558,0.555878380248887,3.95808069339639));
#23347=CARTESIAN_POINT('Ctrl Pts',(21.7900279395893,0.508000056083844,4.22955161709966));
#23348=CARTESIAN_POINT('Ctrl Pts',(21.8138858576208,0.335901880562604,4.44489091756156));
#23349=CARTESIAN_POINT('Ctrl Pts',(21.8377437756521,0.0816665454602928,
4.55144227009437));
#23350=CARTESIAN_POINT('Ctrl Pts',(21.8616016936836,-0.192538484559094,
4.52315096660328));
#23351=CARTESIAN_POINT('Ctrl Pts',(21.885459611715,-0.419662610460766,4.36693500143146));
#23352=CARTESIAN_POINT('Ctrl Pts',(21.9093175297464,-0.544167796724789,
4.12099343330092));
#23353=CARTESIAN_POINT('Ctrl Pts',(21.9331754477779,-0.535609133856441,
3.84546567493331));
#23354=CARTESIAN_POINT('Ctrl Pts',(21.9570333658092,-0.396079448060293,
3.60772576847503));
#23355=CARTESIAN_POINT('Ctrl Pts',(21.9808912838407,-0.159697548225882,
3.46590759696012));
#23356=CARTESIAN_POINT('Ctrl Pts',(22.0047492018721,0.115734752223676,3.45468956637345));
#23357=CARTESIAN_POINT('Ctrl Pts',(22.0286071199035,0.362866753203085,3.5768147907664));
#23358=CARTESIAN_POINT('Ctrl Pts',(22.0524650379349,0.521267948732644,3.80242032615069));
#23359=CARTESIAN_POINT('Ctrl Pts',(22.0763229559664,0.552204931742854,4.07633947375325));
#23360=CARTESIAN_POINT('Ctrl Pts',(22.1001808739978,0.448112767182329,4.33159154057792));
#23361=CARTESIAN_POINT('Ctrl Pts',(22.1240387920292,0.23444482469764,4.5057604433585));
#23362=CARTESIAN_POINT('Ctrl Pts',(22.1478967100606,-0.0365512635718279,
4.55625714110116));
#23363=CARTESIAN_POINT('Ctrl Pts',(22.171754628092,-0.298609572266455,4.47073381570218));
#23364=CARTESIAN_POINT('Ctrl Pts',(22.1956125461234,-0.487649706571227,
4.2701032498363));
#23365=CARTESIAN_POINT('Ctrl Pts',(22.2194704641549,-0.557446204325542,
4.00342508191314));
#23366=CARTESIAN_POINT('Ctrl Pts',(22.2433283821863,-0.490931920559466,
3.73590938817905));
#23367=CARTESIAN_POINT('Ctrl Pts',(22.2671863002177,-0.304371409562025,
3.53297104269219));
#23368=CARTESIAN_POINT('Ctrl Pts',(22.2910442182491,-0.0433837978980346,
3.44423399893113));
#23369=CARTESIAN_POINT('Ctrl Pts',(22.3149021362806,0.228212333880327,3.49139688109763));
#23370=CARTESIAN_POINT('Ctrl Pts',(22.3387600543119,0.444004334066149,3.66292708008725));
#23371=CARTESIAN_POINT('Ctrl Pts',(22.3626179723434,0.551225179343846,3.91688078933633));
#23372=CARTESIAN_POINT('Ctrl Pts',(22.3864758903748,0.523656454698273,4.19115941035881));
#23373=CARTESIAN_POINT('Ctrl Pts',(22.4103338084062,0.368039459933637,4.41869434725418));
#23374=CARTESIAN_POINT('Ctrl Pts',(22.4341917264376,0.122426797365049,4.54384711353805));
#23375=CARTESIAN_POINT('Ctrl Pts',(22.458049644469,-0.153122562087755,4.53601444212637));
#23376=CARTESIAN_POINT('Ctrl Pts',(22.4819075625005,-0.391229265084309,
4.39711164706476));
#23377=CARTESIAN_POINT('Ctrl Pts',(22.5057654805319,-0.533669791868601,
4.16110422172694));
#23378=CARTESIAN_POINT('Ctrl Pts',(22.5296233985633,-0.545613449745194,
3.88570245498666));
#23379=CARTESIAN_POINT('Ctrl Pts',(22.5534813165947,-0.424139885198736,
3.63824949626794));
#23380=CARTESIAN_POINT('Ctrl Pts',(22.5773392346261,-0.198952323217499,
3.47925449370713));
#23381=CARTESIAN_POINT('Ctrl Pts',(22.6011971526576,0.0748840438856019,
3.44759575567767));
#23382=CARTESIAN_POINT('Ctrl Pts',(22.625055070689,0.330410085854462,3.55101527375816));
#23383=CARTESIAN_POINT('Ctrl Pts',(22.6489129887204,0.505140231362423,3.7642230866287));
#23384=CARTESIAN_POINT('Ctrl Pts',(22.6727709067518,0.556352908954721,4.03508610068096));
#23385=CARTESIAN_POINT('Ctrl Pts',(22.6966288247833,0.471516332128332,4.29736710820476));
#23386=CARTESIAN_POINT('Ctrl Pts',(22.7204867428146,0.27139215166714,4.48693847894857));
#23387=CARTESIAN_POINT('Ctrl Pts',(22.7443446608461,0.00488440565515616,
4.55743119390072));
#23388=CARTESIAN_POINT('Ctrl Pts',(22.7682025788775,-0.262778018495442,
4.49163382183027));
#23389=CARTESIAN_POINT('Ctrl Pts',(22.7920604969089,-0.466262514422727,
4.30558517247789));
#23390=CARTESIAN_POINT('Ctrl Pts',(22.8079657755965,-0.525793678117208,
4.1317859159904));
#23391=CARTESIAN_POINT('Ctrl Pts',(22.8159184149403,-0.532958495437544,
4.04301651477895));
#23392=CARTESIAN_POINT('Ctrl Pts',(3.98408158505965,-0.251304309929533,
3.59658905474035));
#23393=CARTESIAN_POINT('Ctrl Pts',(3.99203422440346,-0.184112308377066,
3.5547318870523));
#23394=CARTESIAN_POINT('Ctrl Pts',(4.00793950309107,-0.0284797076443847,
3.50528009766423));
#23395=CARTESIAN_POINT('Ctrl Pts',(4.03179742112249,0.212077873916637,3.55216010213054));
#23396=CARTESIAN_POINT('Ctrl Pts',(4.05565533915392,0.400711255741927,3.70851080938071));
#23397=CARTESIAN_POINT('Ctrl Pts',(4.07951325718533,0.49139298320592,3.93615790384083));
#23398=CARTESIAN_POINT('Ctrl Pts',(4.10337117521676,0.461898357851897,4.17940600742409));
#23399=CARTESIAN_POINT('Ctrl Pts',(4.12722909324816,0.319466186301668,4.37878980142624));
#23400=CARTESIAN_POINT('Ctrl Pts',(4.15108701127959,0.0989109688445654,
4.48554634140719));
#23401=CARTESIAN_POINT('Ctrl Pts',(4.174944929311,-0.145828100556353,4.47357507321567));
#23402=CARTESIAN_POINT('Ctrl Pts',(4.19880284734243,-0.354909590370033,
4.34580100620849));
#23403=CARTESIAN_POINT('Ctrl Pts',(4.22266076537384,-0.477205295803391,
4.13346959398438));
#23404=CARTESIAN_POINT('Ctrl Pts',(4.24651868340526,-0.482811689970624,
3.88850100783657));
#23405=CARTESIAN_POINT('Ctrl Pts',(4.27037660143669,-0.370357271909554,
3.67079708031066));
#23406=CARTESIAN_POINT('Ctrl Pts',(4.2942345194681,-0.167340519784032,3.53359217153378));
#23407=CARTESIAN_POINT('Ctrl Pts',(4.31809243749953,0.0765956044913427,
3.51043671457025));
#23408=CARTESIAN_POINT('Ctrl Pts',(4.34195035553093,0.301801986965541,3.60699279882218));
#23409=CARTESIAN_POINT('Ctrl Pts',(4.36580827356237,0.453209578636439,3.79964985833574));
#23410=CARTESIAN_POINT('Ctrl Pts',(4.38966619159377,0.493795074712635,4.04129798000377));
#23411=CARTESIAN_POINT('Ctrl Pts',(4.4135241096252,0.413634228782107,4.27284762322724));
#23412=CARTESIAN_POINT('Ctrl Pts',(4.43738202765661,0.23232854437776,4.43767858897425));
#23413=CARTESIAN_POINT('Ctrl Pts',(4.46123994568804,-0.00578779637616802,
4.49548521832112));
#23414=CARTESIAN_POINT('Ctrl Pts',(4.48509786371945,-0.242488863923451,
4.43213221465579));
#23415=CARTESIAN_POINT('Ctrl Pts',(4.50895578175088,-0.419894798625899,
4.26311111366653));
#23416=CARTESIAN_POINT('Ctrl Pts',(4.53281369978229,-0.494625017545811,
4.02975217827461));
#23417=CARTESIAN_POINT('Ctrl Pts',(4.55667161781372,-0.448405946262215,
3.78911802491887));
#23418=CARTESIAN_POINT('Ctrl Pts',(4.58052953584513,-0.292539406836986,
3.60005025874973));
#23419=CARTESIAN_POINT('Ctrl Pts',(4.60438745387655,-0.0651390137990107,
3.50878109874461));
#23420=CARTESIAN_POINT('Ctrl Pts',(4.62824537190797,0.178189642449287,3.53762834062211));
#23421=CARTESIAN_POINT('Ctrl Pts',(4.65210328993938,0.377946077338085,3.67953804797316));
#23422=CARTESIAN_POINT('Ctrl Pts',(4.67596120797081,0.485284401269169,3.89980943180067));
#23423=CARTESIAN_POINT('Ctrl Pts',(4.69981912600222,0.473957470210434,4.14458013869048));
#23424=CARTESIAN_POINT('Ctrl Pts',(4.72367704403364,0.34673502734182,4.35399706338589));
#23425=CARTESIAN_POINT('Ctrl Pts',(4.74753496206506,0.134726425416229,4.47685206339739));
#23426=CARTESIAN_POINT('Ctrl Pts',(4.77139288009648,-0.110226457398098,
4.48310374471865));
#23427=CARTESIAN_POINT('Ctrl Pts',(4.7952507981279,-0.328225968870003,4.37122340097448));
#23428=CARTESIAN_POINT('Ctrl Pts',(4.81910871615932,-0.465965290257402,
4.16856882376961));
#23429=CARTESIAN_POINT('Ctrl Pts',(4.84296663419074,-0.489763405537152,
3.92469457743051));
#23430=CARTESIAN_POINT('Ctrl Pts',(4.86682455222216,-0.393801027275785,
3.69923455818817));
#23431=CARTESIAN_POINT('Ctrl Pts',(4.89068247025357,-0.201543570920867,
3.54731988215497));
#23432=CARTESIAN_POINT('Ctrl Pts',(4.914540388285,0.039996778460842,3.50609782569371));
#23433=CARTESIAN_POINT('Ctrl Pts',(4.93839830631641,0.271756826018508,3.58564830447545));
#23434=CARTESIAN_POINT('Ctrl Pts',(4.96225622434784,0.437064927107334,3.76651905952651));
#23435=CARTESIAN_POINT('Ctrl Pts',(4.98611414237925,0.495498748108838,4.00448226441646));
#23436=CARTESIAN_POINT('Ctrl Pts',(5.00997206041068,0.432769628082826,4.24134943356216));
#23437=CARTESIAN_POINT('Ctrl Pts',(5.03382997844209,0.26421654558258,4.41920009197534));
#23438=CARTESIAN_POINT('Ctrl Pts',(5.05768789647352,0.031055320573195,4.49454490911931));
#23439=CARTESIAN_POINT('Ctrl Pts',(5.08154581450493,-0.209699776246285,
4.44896002485074));
#23440=CARTESIAN_POINT('Ctrl Pts',(5.10540373253635,-0.399177565666329,
4.29359218508065));
#23441=CARTESIAN_POINT('Ctrl Pts',(5.12926165056777,-0.491045566902382,
4.06643305876778));
#23442=CARTESIAN_POINT('Ctrl Pts',(5.15311956859918,-0.462839551218119,
3.823029239986));
#23443=CARTESIAN_POINT('Ctrl Pts',(5.17697748663061,-0.321456657764784,
3.62289959261435));
#23444=CARTESIAN_POINT('Ctrl Pts',(5.20083540466202,-0.101468855184408,
3.51498126685736));
#23445=CARTESIAN_POINT('Ctrl Pts',(5.22469332269345,0.143330846444675,3.52566323299877));
#23446=CARTESIAN_POINT('Ctrl Pts',(5.24855124072486,0.353082251864168,3.6523334593461));
#23447=CARTESIAN_POINT('Ctrl Pts',(5.27240915875629,0.476495428935435,3.86401762512973));
#23448=CARTESIAN_POINT('Ctrl Pts',(5.2962670767877,0.483392494157105,4.10895318565465));
#23449=CARTESIAN_POINT('Ctrl Pts',(5.32012499481913,0.372086927210194,4.32724672446184));
#23450=CARTESIAN_POINT('Ctrl Pts',(5.34398291285054,0.169795971115995,4.46551952511629));
#23451=CARTESIAN_POINT('Ctrl Pts',(5.36784083088196,-0.0740147250654609,
4.48996012138256));
#23452=CARTESIAN_POINT('Ctrl Pts',(5.39169874891337,-0.299726804847767,
4.39459212172504));
#23453=CARTESIAN_POINT('Ctrl Pts',(5.4155566669448,-0.452147516450583,4.20273559983216));
#23454=CARTESIAN_POINT('Ctrl Pts',(5.43941458497621,-0.494005844030112,
3.96130470137348));
#23455=CARTESIAN_POINT('Ctrl Pts',(5.46327250300764,-0.415066286295368,
3.72933585746768));
#23456=CARTESIAN_POINT('Ctrl Pts',(5.48713042103905,-0.234631715382576,
3.56355176915442));
#23457=CARTESIAN_POINT('Ctrl Pts',(5.51098833907048,0.00317670118048804,
3.50449116189365));
#23458=CARTESIAN_POINT('Ctrl Pts',(5.53484625710188,0.240208327774024,3.56659596294035));
#23459=CARTESIAN_POINT('Ctrl Pts',(5.55870417513332,0.418502475082003,3.73467985673571));
#23460=CARTESIAN_POINT('Ctrl Pts',(5.58256209316472,0.494461367456411,3.96764175273735));
#23461=CARTESIAN_POINT('Ctrl Pts',(5.60642001119615,0.449510986625754,4.20851612161082));
#23462=CARTESIAN_POINT('Ctrl Pts',(5.63027792922757,0.294642925140636,4.39840261889448));
#23463=CARTESIAN_POINT('Ctrl Pts',(5.65413584725899,0.0677266425295592,
4.49086882357174));
#23464=CARTESIAN_POINT('Ctrl Pts',(5.6779937652904,-0.17575064898472,4.46330422991997));
#23465=CARTESIAN_POINT('Ctrl Pts',(5.70185168332183,-0.376252119531055,
4.32244913183746));
#23466=CARTESIAN_POINT('Ctrl Pts',(5.72570960135325,-0.48474969783608,4.10274643779879));
#23467=CARTESIAN_POINT('Ctrl Pts',(5.74956751938466,-0.474712770918799,
3.85791944074229));
#23468=CARTESIAN_POINT('Ctrl Pts',(5.77342543741608,-0.348595640189148,
3.64783501103505));
#23469=CARTESIAN_POINT('Ctrl Pts',(5.7972833554475,-0.13723738064616,3.52386451312966));
#23470=CARTESIAN_POINT('Ctrl Pts',(5.82114127347893,0.1076791581852,3.5163221129105));
#23471=CARTESIAN_POINT('Ctrl Pts',(5.84499919151033,0.326265206982528,3.62705212841851));
#23472=CARTESIAN_POINT('Ctrl Pts',(5.86885710954176,0.465070530553655,3.82897806268729));
#23473=CARTESIAN_POINT('Ctrl Pts',(5.89271502757317,0.490153431381492,4.07272350923538));
#23474=CARTESIAN_POINT('Ctrl Pts',(5.9165729456046,0.395380485146506,4.29868609559117));
#23475=CARTESIAN_POINT('Ctrl Pts',(5.94043086363601,0.203926205561759,4.45161176009809));
#23476=CARTESIAN_POINT('Ctrl Pts',(5.96428878166744,-0.0373935204432717,
4.49410611450448));
#23477=CARTESIAN_POINT('Ctrl Pts',(5.98814669969885,-0.26956963613406,4.41577793841189));
#23478=CARTESIAN_POINT('Ctrl Pts',(6.01200461773027,-0.435828398698505,
4.23578096933615));
#23479=CARTESIAN_POINT('Ctrl Pts',(6.0358625357617,-0.495515688199628,3.99812868033461));
#23480=CARTESIAN_POINT('Ctrl Pts',(6.0597204537931,-0.434035059498629,3.76093483037113));
#23481=CARTESIAN_POINT('Ctrl Pts',(6.08357837182454,-0.266422612259865,
3.58219732064663));
#23482=CARTESIAN_POINT('Ctrl Pts',(6.10743628985594,-0.0336596025775484,
3.50562697870369));
#23483=CARTESIAN_POINT('Ctrl Pts',(6.13129420788738,0.207328476491996,3.54993858195554));
#23484=CARTESIAN_POINT('Ctrl Pts',(6.15515212591877,0.397629707835022,3.70431327123879));
#23485=CARTESIAN_POINT('Ctrl Pts',(6.17901004395022,0.490679606253205,3.93097100878581));
#23486=CARTESIAN_POINT('Ctrl Pts',(6.20286796198161,0.463782811036945,4.17454675550933));
#23487=CARTESIAN_POINT('Ctrl Pts',(6.22672588001306,0.323407044622774,4.3753682944706));
#23488=CARTESIAN_POINT('Ctrl Pts',(6.25058379804445,0.104084330837213,4.48453946106473));
#23489=CARTESIAN_POINT('Ctrl Pts',(6.27444171607588,-0.140944443623038,
4.4749681472433));
#23490=CARTESIAN_POINT('Ctrl Pts',(6.29829963410731,-0.351028389709017,
4.349743491311));
#23491=CARTESIAN_POINT('Ctrl Pts',(6.32215755213872,-0.476177279109797,
4.13807688197341));
#23492=CARTESIAN_POINT('Ctrl Pts',(6.34601547017014,-0.483231738207782,
3.89435343878414));
#23493=CARTESIAN_POINT('Ctrl Pts',(6.37782602754537,-0.338784024988664,
3.5998542259592));
#23494=CARTESIAN_POINT('Ctrl Pts',(6.41758922426439,0.0803770223010952,
3.44371490521648));
#23495=CARTESIAN_POINT('Ctrl Pts',(6.46530506032724,0.512014121509362,3.7673575683149));
#23496=CARTESIAN_POINT('Ctrl Pts',(6.51302089639006,0.472271980317209,4.30452828893312));
#23497=CARTESIAN_POINT('Ctrl Pts',(6.56073673245292,-0.000548856210248058,
4.56210751581942));
#23498=CARTESIAN_POINT('Ctrl Pts',(6.60845256851575,-0.473190198344468,
4.30346185287483));
#23499=CARTESIAN_POINT('Ctrl Pts',(6.65616840457859,-0.511122033036262,
3.76615996983968));
#23500=CARTESIAN_POINT('Ctrl Pts',(6.70388424064142,-0.0797735308749388,
3.44358772816382));
#23501=CARTESIAN_POINT('Ctrl Pts',(6.75160007670426,0.424880365184703,3.63198234005898));
#23502=CARTESIAN_POINT('Ctrl Pts',(6.7993159127671,0.539334593204737,4.15833063512042));
#23503=CARTESIAN_POINT('Ctrl Pts',(6.84703174882994,0.158523065679302,4.53928284691909));
#23504=CARTESIAN_POINT('Ctrl Pts',(6.89474758489278,-0.367869781963911,
4.42500259414721));
#23505=CARTESIAN_POINT('Ctrl Pts',(6.94246342095561,-0.556438361909488,
3.92043630538129));
#23506=CARTESIAN_POINT('Ctrl Pts',(6.99017925701846,-0.234023037562683,
3.48893437735136));
#23507=CARTESIAN_POINT('Ctrl Pts',(7.03789509308128,0.303300305128555,3.52675198254107));
#23508=CARTESIAN_POINT('Ctrl Pts',(7.08561092914413,0.562097748282813,3.99916046672433));
#23509=CARTESIAN_POINT('Ctrl Pts',(7.13332676520696,0.304712478085684,4.47233993757656));
#23510=CARTESIAN_POINT('Ctrl Pts',(7.18104260126981,-0.232495107101315,
4.51176235979777));
#23511=CARTESIAN_POINT('Ctrl Pts',(7.22875843733264,-0.556198774489988,
4.08122554105153));
#23512=CARTESIAN_POINT('Ctrl Pts',(7.27647427339549,-0.369136593294786,
3.57609805363465));
#23513=CARTESIAN_POINT('Ctrl Pts',(7.32419010945832,0.156909424853758,3.46024624852207));
#23514=CARTESIAN_POINT('Ctrl Pts',(7.37190594552116,0.538863091386428,3.84005861730642));
#23515=CARTESIAN_POINT('Ctrl Pts',(7.41962178158399,0.425970496197337,4.36674761950234));
#23516=CARTESIAN_POINT('Ctrl Pts',(7.46733761764684,-0.0780973635293338,
4.55664663921719));
#23517=CARTESIAN_POINT('Ctrl Pts',(7.51505345370967,-0.510447210801067,
4.2353684852172));
#23518=CARTESIAN_POINT('Ctrl Pts',(7.56276928977251,-0.474045531130633,
3.69794782953315));
#23519=CARTESIAN_POINT('Ctrl Pts',(7.61048512583535,-0.00232054557778912,
3.43790632971152));
#23520=CARTESIAN_POINT('Ctrl Pts',(7.65820096189818,0.471535432411473,3.69404409621074));
#23521=CARTESIAN_POINT('Ctrl Pts',(7.70591679796103,0.512373167457076,4.23114587691112));
#23522=CARTESIAN_POINT('Ctrl Pts',(7.75363263402387,0.0826907388754792,
4.55598284219971));
#23523=CARTESIAN_POINT('Ctrl Pts',(7.80134847008669,-0.422927867535356,
4.3702522086048));
#23524=CARTESIAN_POINT('Ctrl Pts',(7.84906430614955,-0.540165305628305,
3.84451327478339));
#23525=CARTESIAN_POINT('Ctrl Pts',(7.89678014221237,-0.161360632039799,
3.46156019320034));
#23526=CARTESIAN_POINT('Ctrl Pts',(7.94449597827521,0.365623992797271,3.57306467116217));
#23527=CARTESIAN_POINT('Ctrl Pts',(7.99221181433806,0.556850479203549,4.07663043084052));
#23528=CARTESIAN_POINT('Ctrl Pts',(8.03992765040089,0.236712602309549,4.50982528676712));
#23529=CARTESIAN_POINT('Ctrl Pts',(8.08764348646373,-0.300802099575971,
4.47483973718518));
#23530=CARTESIAN_POINT('Ctrl Pts',(8.13535932252656,-0.562085604986122,
4.00380155059756));
#23531=CARTESIAN_POINT('Ctrl Pts',(8.18307515858941,-0.307197250538534,
3.52927234160183));
#23532=CARTESIAN_POINT('Ctrl Pts',(8.23079099465223,0.229795065915734,3.48701958438918));
#23533=CARTESIAN_POINT('Ctrl Pts',(8.27850683071509,0.555763037488074,3.91584463605021));
#23534=CARTESIAN_POINT('Ctrl Pts',(8.32622266677791,0.371365260221553,4.42195085332305));
#23535=CARTESIAN_POINT('Ctrl Pts',(8.37393850284076,-0.154062949695418,
4.54057310944092));
#23536=CARTESIAN_POINT('Ctrl Pts',(8.4216543389036,-0.538012782343907,4.16277876137275));
#23537=CARTESIAN_POINT('Ctrl Pts',(8.46937017496643,-0.427897198575242,
3.6355021720628));
#23538=CARTESIAN_POINT('Ctrl Pts',(8.51708601102927,0.0751629666897603,
3.44294954666756));
#23539=CARTESIAN_POINT('Ctrl Pts',(8.56480184709211,0.50919982311266,3.76194492389047));
#23540=CARTESIAN_POINT('Ctrl Pts',(8.61251768315494,0.475630646924824,4.29954994045293));
#23541=CARTESIAN_POINT('Ctrl Pts',(8.66023351921779,0.00528252914771292,
4.56207363752918));
#23542=CARTESIAN_POINT('Ctrl Pts',(8.70794935528062,-0.469916616427902,
4.30843646464781));
#23543=CARTESIAN_POINT('Ctrl Pts',(8.75566519134346,-0.513584102541225,
3.7715573403753));
#23544=CARTESIAN_POINT('Ctrl Pts',(8.8033810274063,-0.0856194047837525,
3.44446062547832));
#23545=CARTESIAN_POINT('Ctrl Pts',(8.85109686346913,0.420970909810523,3.6275242662766));
#23546=CARTESIAN_POINT('Ctrl Pts',(8.89881269953199,0.540977160455745,4.15263810462895));
#23547=CARTESIAN_POINT('Ctrl Pts',(8.9465285355948,0.1641957606509,4.5375820228614));
#23548=CARTESIAN_POINT('Ctrl Pts',(8.99424437165766,-0.363369132636193,
4.42885609773758));
#23549=CARTESIAN_POINT('Ctrl Pts',(9.04196020772048,-0.557246560270691,
3.92630501926208));
#23550=CARTESIAN_POINT('Ctrl Pts',(9.08967604378333,-0.239395897268157,
3.49142917554125));
#23551=CARTESIAN_POINT('Ctrl Pts',(9.13739187984617,0.298295701775085,3.52358174528888));
#23552=CARTESIAN_POINT('Ctrl Pts',(9.18510771590899,0.562057768008922,3.99323652897485));
#23553=CARTESIAN_POINT('Ctrl Pts',(9.23282355197185,0.309673537509763,4.46910231217259));
#23554=CARTESIAN_POINT('Ctrl Pts',(9.28053938803466,-0.227088667424462,
4.51418422403538));
#23555=CARTESIAN_POINT('Ctrl Pts',(9.32825522409753,-0.555311854854516,
4.08708285122523));
#23556=CARTESIAN_POINT('Ctrl Pts',(9.37597106016035,-0.373583621400482,
3.58001195619306));
#23557=CARTESIAN_POINT('Ctrl Pts',(9.4236868962232,0.151212199908504,3.45862254413551));
#23558=CARTESIAN_POINT('Ctrl Pts',(9.47140273228603,0.537147531342748,3.83438837996121));
#23559=CARTESIAN_POINT('Ctrl Pts',(9.51911856834887,0.429812019667804,4.36223791473086));
#23560=CARTESIAN_POINT('Ctrl Pts',(9.5668344044117,-0.0722264831760907,
4.5574387986564));
#23561=CARTESIAN_POINT('Ctrl Pts',(9.61455024047456,-0.507938295172089,
4.24073505647735));
#23562=CARTESIAN_POINT('Ctrl Pts',(9.66226607653738,-0.477202555076283,
3.70296060775017));
#23563=CARTESIAN_POINT('Ctrl Pts',(9.70998191260023,-0.00824436594879979,
3.43796200346455));
#23564=CARTESIAN_POINT('Ctrl Pts',(9.75769774866306,0.46828475128534,3.68909153946361));
#23565=CARTESIAN_POINT('Ctrl Pts',(9.80541358472589,0.514780775927077,4.22573309871483));
#23566=CARTESIAN_POINT('Ctrl Pts',(9.85312942078874,0.0885456931146035,
4.55508048006603));
#23567=CARTESIAN_POINT('Ctrl Pts',(9.90084525685159,-0.419002262135622,
4.37468891556157));
#23568=CARTESIAN_POINT('Ctrl Pts',(9.9485610929144,-0.541773992888202,3.8502147545669));
#23569=CARTESIAN_POINT('Ctrl Pts',(9.99627692897727,-0.167026329707142,
3.46329068919569));
#23570=CARTESIAN_POINT('Ctrl Pts',(10.0439927650401,0.361104182074418,3.56923504227033));
#23571=CARTESIAN_POINT('Ctrl Pts',(10.0917086011029,0.557627167155001,4.07075748419897));
#23572=CARTESIAN_POINT('Ctrl Pts',(10.1394244371657,0.242072544440304,4.50730223964386));
#23573=CARTESIAN_POINT('Ctrl Pts',(10.1871402732286,-0.295781020598791,
4.47798354257549));
#23574=CARTESIAN_POINT('Ctrl Pts',(10.2348561092914,-0.56201432324602,4.00972520363789));
#23575=CARTESIAN_POINT('Ctrl Pts',(10.2825719453543,-0.312141225154507,
3.53253606055812));
#23576=CARTESIAN_POINT('Ctrl Pts',(10.3302877814171,0.224375962906492,3.48462624592509));
#23577=CARTESIAN_POINT('Ctrl Pts',(10.37800361748,0.554845251762499,3.90999207970357));
#23578=CARTESIAN_POINT('Ctrl Pts',(10.4257194535428,0.375791608533427,4.41801357164013));
#23579=CARTESIAN_POINT('Ctrl Pts',(10.4734352896056,-0.148357251109035,
4.54216676877402));
#23580=CARTESIAN_POINT('Ctrl Pts',(10.5211511256685,-0.536267364288337,
4.16843987983467));
#23581=CARTESIAN_POINT('Ctrl Pts',(10.5688669617313,-0.431714905307627,
3.64003205746247));
#23582=CARTESIAN_POINT('Ctrl Pts',(10.6165827977942,0.0692879940047382,
3.44218833554121));
#23583=CARTESIAN_POINT('Ctrl Pts',(10.664298633857,0.50666266228973,3.75659164812817));
#23584=CARTESIAN_POINT('Ctrl Pts',(10.7120144699198,0.478761211786921,4.29452059555793));
#23585=CARTESIAN_POINT('Ctrl Pts',(10.7597303059827,0.0112059738120427,
4.56198674830498));
#23586=CARTESIAN_POINT('Ctrl Pts',(10.8074461420455,-0.466639882340508,
4.31337182280594));
#23587=CARTESIAN_POINT('Ctrl Pts',(10.8551619781083,-0.515963154362253,
3.77698273057893));
#23588=CARTESIAN_POINT('Ctrl Pts',(10.9028778141712,-0.0914695226195351,
3.44539382842306));
#23589=CARTESIAN_POINT('Ctrl Pts',(10.950593650234,0.417021979184216,3.62310830733915));
#23590=CARTESIAN_POINT('Ctrl Pts',(10.9983094862969,0.542555780795161,4.14692822684982));
#23591=CARTESIAN_POINT('Ctrl Pts',(11.0460253223597,0.169852260608159,4.53582169486292));
#23592=CARTESIAN_POINT('Ctrl Pts',(11.0937411584225,-0.358829204008283,
4.43266185580689));
#23593=CARTESIAN_POINT('Ctrl Pts',(11.1414569944853,-0.55799228928692,3.93218197720501));
#23594=CARTESIAN_POINT('Ctrl Pts',(11.1891728305482,-0.244742469498405,
3.49398043245019));
#23595=CARTESIAN_POINT('Ctrl Pts',(11.236888666611,0.293258125877444,3.5204644426882));
#23596=CARTESIAN_POINT('Ctrl Pts',(11.2846045026739,0.561955271903759,3.98731333380864));
#23597=CARTESIAN_POINT('Ctrl Pts',(11.3323203387367,0.314600244947554,4.46581258570203));
#23598=CARTESIAN_POINT('Ctrl Pts',(11.3800361747996,-0.221657027690976,
4.51654897269734));
#23599=CARTESIAN_POINT('Ctrl Pts',(11.4277520108624,-0.554363241169119,
4.0929304899371));
#23600=CARTESIAN_POINT('Ctrl Pts',(11.4754678469252,-0.377989160306769,
3.58397250834823));
#23601=CARTESIAN_POINT('Ctrl Pts',(11.5231836829881,0.145498182576105,3.45705897374896));
#23602=CARTESIAN_POINT('Ctrl Pts',(11.5708995190509,0.535372305622036,3.82873653777755));
#23603=CARTESIAN_POINT('Ctrl Pts',(11.6186153551137,0.43360580265347,4.35768797439208));
#23604=CARTESIAN_POINT('Ctrl Pts',(11.6663311911766,-0.0663475807746441,
4.55816904038548));
#23605=CARTESIAN_POINT('Ctrl Pts',(11.7140470272394,-0.505372959888646,
4.24607488805821));
#23606=CARTESIAN_POINT('Ctrl Pts',(11.7617628633023,-0.480306573774387,
3.70800637967828));
#23607=CARTESIAN_POINT('Ctrl Pts',(11.8094786993651,-0.0141672704965164,
3.43808010573911));
#23608=CARTESIAN_POINT('Ctrl Pts',(11.8571945354279,0.464982055269784,3.68417351694868));
#23609=CARTESIAN_POINT('Ctrl Pts',(11.9049103714908,0.517131205013274,4.22029524715934));
#23610=CARTESIAN_POINT('Ctrl Pts',(11.9526262075536,0.0943908121067024,
4.55411646222552));
#23611=CARTESIAN_POINT('Ctrl Pts',(12.0003420436165,-0.415030115946784,
4.37908400385228));
#23612=CARTESIAN_POINT('Ctrl Pts',(12.0480578796793,-0.543322502467158,
3.85593287178435));
#23613=CARTESIAN_POINT('Ctrl Pts',(12.0957737157421,-0.172673474880652,
3.46508080031456));
#23614=CARTESIAN_POINT('Ctrl Pts',(12.143489551805,0.356544261611682,3.56545326070575));
#23615=CARTESIAN_POINT('Ctrl Pts',(12.1912053878678,0.558341916527368,4.06487667815191));
#23616=CARTESIAN_POINT('Ctrl Pts',(12.2389212239306,0.247405598301292,4.50472284379514));
#23617=CARTESIAN_POINT('Ctrl Pts',(12.2866370599935,-0.290727087669313,
4.48107425582212));
#23618=CARTESIAN_POINT('Ctrl Pts',(12.3343528960563,-0.56188061562194,4.01564777644873));
#23619=CARTESIAN_POINT('Ctrl Pts',(12.3820687321191,-0.317050528604376,
3.5358517031905));
#23620=CARTESIAN_POINT('Ctrl Pts',(12.429784568182,0.218931937280033,3.48229015273196));
#23621=CARTESIAN_POINT('Ctrl Pts',(12.4775004042448,0.553865836459325,3.90414952100961));
#23622=CARTESIAN_POINT('Ctrl Pts',(12.5252162403077,0.380176215696692,4.4140298589933));
#23623=CARTESIAN_POINT('Ctrl Pts',(12.5729320763705,-0.142635073703209,
4.54370020679522));
#23624=CARTESIAN_POINT('Ctrl Pts',(12.6206479124333,-0.53446238019874,4.17408228879405));
#23625=CARTESIAN_POINT('Ctrl Pts',(12.6683637484962,-0.435484659196984,
3.644601926393));
#23626=CARTESIAN_POINT('Ctrl Pts',(12.716079584559,0.0634053251381518,3.44148908348752));
#23627=CARTESIAN_POINT('Ctrl Pts',(12.7637954206219,0.504069223782589,3.75126540901054));
#23628=CARTESIAN_POINT('Ctrl Pts',(12.8115112566847,0.481838598125516,4.2894585367128));
#23629=CARTESIAN_POINT('Ctrl Pts',(12.8592270927475,0.0171281737699642,
4.56183743625962));
#23630=CARTESIAN_POINT('Ctrl Pts',(12.9069429288104,-0.463311316109371,
4.31827237310907));
#23631=CARTESIAN_POINT('Ctrl Pts',(12.9546587648732,-0.518284895444539,
3.78243289248252));
#23632=CARTESIAN_POINT('Ctrl Pts',(13.0023746009361,-0.0973094804548018,
3.44638863438952));
#23633=CARTESIAN_POINT('Ctrl Pts',(13.0500904369989,0.413026727735397,3.61873421174243));
#23634=CARTESIAN_POINT('Ctrl Pts',(13.0978062730617,0.544074136613086,4.14120202898048));
#23635=CARTESIAN_POINT('Ctrl Pts',(13.1455221091246,0.17548989418231,4.53400185033327));
#23636=CARTESIAN_POINT('Ctrl Pts',(13.1932379451874,-0.354249418335187,
4.4364195558504));
#23637=CARTESIAN_POINT('Ctrl Pts',(13.2409537812502,-0.558676039167545,
3.93806646805208));
#23638=CARTESIAN_POINT('Ctrl Pts',(13.2886696173131,-0.250061856896528,
3.49658789561142));
#23639=CARTESIAN_POINT('Ctrl Pts',(13.3363854533759,0.288187976258808,3.51740040462167));
#23640=CARTESIAN_POINT('Ctrl Pts',(13.3841012894388,0.56179035647369,3.9813915478171));
#23641=CARTESIAN_POINT('Ctrl Pts',(13.4318171255016,0.319492008083037,4.46247111897993));
#23642=CARTESIAN_POINT('Ctrl Pts',(13.4795329615644,-0.21620076734671,4.51885634555065));
#23643=CARTESIAN_POINT('Ctrl Pts',(13.5272487976273,-0.553353051445561,
4.09876780637113));
#23644=CARTESIAN_POINT('Ctrl Pts',(13.5749646336901,-0.382352713970831,
3.58797927086295));
#23645=CARTESIAN_POINT('Ctrl Pts',(13.6226804697529,0.139768003996038,3.45555571067516));
#23646=CARTESIAN_POINT('Ctrl Pts',(13.6703963058158,0.53353761328617,3.82310371872654));
#23647=CARTESIAN_POINT('Ctrl Pts',(13.7181121418786,0.437351422764197,4.35309830377052));
#23648=CARTESIAN_POINT('Ctrl Pts',(13.7658279779415,-0.0604613087987784,
4.55883728334624));
#23649=CARTESIAN_POINT('Ctrl Pts',(13.8135438140043,-0.502751490175015,
4.25138738680826));
#23650=CARTESIAN_POINT('Ctrl Pts',(13.8612596500671,-0.483357242297515,
3.71308458487209));
#23651=CARTESIAN_POINT('Ctrl Pts',(13.90897548613,-0.0200886014110514,3.43826062340902));
#23652=CARTESIAN_POINT('Ctrl Pts',(13.9566913221928,0.461627711254046,3.67929057494076));
#23653=CARTESIAN_POINT('Ctrl Pts',(14.0044071582557,0.519424193619207,4.21483292625321));
#23654=CARTESIAN_POINT('Ctrl Pts',(14.0521229943185,0.100225446615308,4.55309089575788));
#23655=CARTESIAN_POINT('Ctrl Pts',(14.0998388303813,-0.411011870182152,
4.38343698529073));
#23656=CARTESIAN_POINT('Ctrl Pts',(14.1475546664441,-0.544810662360815,
3.86166699129474));
#23657=CARTESIAN_POINT('Ctrl Pts',(14.195270502507,-0.178301440303968,3.46693032771971));
#23658=CARTESIAN_POINT('Ctrl Pts',(14.2429863385698,0.351944737904315,3.5617197465309));
#23659=CARTESIAN_POINT('Ctrl Pts',(14.2907021746327,0.558994647929194,4.05898866591129));
#23660=CARTESIAN_POINT('Ctrl Pts',(14.3384180106955,0.252711171522458,4.50208738572805));
#23661=CARTESIAN_POINT('Ctrl Pts',(14.3861338467583,-0.28564086215454,4.48411153362329));
#23662=CARTESIAN_POINT('Ctrl Pts',(14.4338496828212,-0.561684496965419,
4.02156861117883));
#23663=CARTESIAN_POINT('Ctrl Pts',(14.481565518884,-0.321924615586062,3.53921890121312));
#23664=CARTESIAN_POINT('Ctrl Pts',(14.5292813549469,0.213463593732893,3.48001156429194));
#23665=CARTESIAN_POINT('Ctrl Pts',(14.5769971910097,0.552824900367352,3.89831760893199));
#23666=CARTESIAN_POINT('Ctrl Pts',(14.6247130270725,0.384518594689996,4.4100001578745));
#23667=CARTESIAN_POINT('Ctrl Pts',(14.6724288631354,-0.136897053070264,
4.54517325317752));
#23668=CARTESIAN_POINT('Ctrl Pts',(14.7201446991982,-0.532598030564186,
4.17970536151887));
#23669=CARTESIAN_POINT('Ctrl Pts',(14.7678605352611,-0.439206041516937,
3.64921127125505));
#23670=CARTESIAN_POINT('Ctrl Pts',(14.8155763713239,0.0575156135089261,
3.44085186817608));
#23671=CARTESIAN_POINT('Ctrl Pts',(14.8632922073868,0.501419795658073,3.74596679815093));
#23672=CARTESIAN_POINT('Ctrl Pts',(14.9110080434496,0.484862464119148,4.284364326187));
#23673=CARTESIAN_POINT('Ctrl Pts',(14.9587238795124,0.0230484712116303,
4.56162571797798));
#23674=CARTESIAN_POINT('Ctrl Pts',(15.0064397155752,-0.459931287455839,
4.32313757122732));
#23675=CARTESIAN_POINT('Ctrl Pts',(15.0541555516381,-0.5205490679001,3.78790722070797));
#23676=CARTESIAN_POINT('Ctrl Pts',(15.1018713877009,-0.103138629614742,
3.44744493287938));
#23677=CARTESIAN_POINT('Ctrl Pts',(15.1495872237638,0.40898559923764,3.61440246534021));
#23678=CARTESIAN_POINT('Ctrl Pts',(15.1973030598266,0.545532059257757,4.13546014705983));
#23679=CARTESIAN_POINT('Ctrl Pts',(15.2450188958894,0.181108035171788,4.53212269141213));
#23680=CARTESIAN_POINT('Ctrl Pts',(15.2927347319523,-0.349630284317748,
4.44012878048063));
#23681=CARTESIAN_POINT('Ctrl Pts',(15.3404505680151,-0.559297733964875,
3.94395783818199));
#23682=CARTESIAN_POINT('Ctrl Pts',(15.3881664040779,-0.255353468610234,
3.49925127540033));
#23683=CARTESIAN_POINT('Ctrl Pts',(15.4358822401408,0.283085816087337,3.51438997142805));
#23684=CARTESIAN_POINT('Ctrl Pts',(15.4835980762036,0.561563040036739,3.97547182876414));
#23685=CARTESIAN_POINT('Ctrl Pts',(15.5313139122665,0.324348283562367,4.45907828316053));
#23686=CARTESIAN_POINT('Ctrl Pts',(15.5790297483293,-0.210720492447169,
4.52110608630326));
#23687=CARTESIAN_POINT('Ctrl Pts',(15.6267455843921,-0.552281397890927,
4.10459415214592));
#23688=CARTESIAN_POINT('Ctrl Pts',(15.674461420455,-0.386673797709831,3.59203179868507));
#23689=CARTESIAN_POINT('Ctrl Pts',(15.7221772565178,0.134022300649356,3.45411292188939));
#23690=CARTESIAN_POINT('Ctrl Pts',(15.7698930925807,0.531643658124066,3.81749054847505));
#23691=CARTESIAN_POINT('Ctrl Pts',(15.8176089286435,0.441048463954279,4.34846941266494));
#23692=CARTESIAN_POINT('Ctrl Pts',(15.8653247647064,-0.054568321067637,
4.5594434533135));
#23693=CARTESIAN_POINT('Ctrl Pts',(15.9130406007692,-0.500074177211609,
4.25667196264028));
#23694=CARTESIAN_POINT('Ctrl Pts',(15.960756436832,-0.486354221791887,3.71819465926869));
#23695=CARTESIAN_POINT('Ctrl Pts',(16.0084722728949,-0.0260077009790528,
3.4385035364232));
#23696=CARTESIAN_POINT('Ctrl Pts',(16.0561881089577,0.458222091822753,3.6744432558139));
#23697=CARTESIAN_POINT('Ctrl Pts',(16.1039039450206,0.52165948705058,4.2093467427251));
#23698=CARTESIAN_POINT('Ctrl Pts',(16.1516197810833,0.106048948556897,4.55200389457816));
#23699=CARTESIAN_POINT('Ctrl Pts',(16.1993356171462,-0.406947971169398,
4.38774737636841));
#23700=CARTESIAN_POINT('Ctrl Pts',(16.247051453209,-0.546238307271431,3.86741647617928));
#23701=CARTESIAN_POINT('Ctrl Pts',(16.2947672892719,-0.183909600849411,
3.46883906597446));
#23702=CARTESIAN_POINT('Ctrl Pts',(16.3424831253347,0.347306121845567,3.55803491444678));
#23703=CARTESIAN_POINT('Ctrl Pts',(16.3901989613975,0.559585288858183,4.05309410148958));
#23704=CARTESIAN_POINT('Ctrl Pts',(16.4379147974604,0.257988674785898,4.49939615817675));
#23705=CARTESIAN_POINT('Ctrl Pts',(16.4856306335232,-0.280522909008289,
4.4870950386126));
#23706=CARTESIAN_POINT('Ctrl Pts',(16.5333464695861,-0.561425989060384,
4.02748705016995));
#23707=CARTESIAN_POINT('Ctrl Pts',(16.5810623056489,-0.326762944709103,
3.54263728061361));
#23708=CARTESIAN_POINT('Ctrl Pts',(16.6287781417117,0.207971539662738,3.4777907336998));
#23709=CARTESIAN_POINT('Ctrl Pts',(16.6764939777746,0.551722559108811,3.89249699125187));
#23710=CARTESIAN_POINT('Ctrl Pts',(16.7242098138374,0.388818263182495,4.40592491588375));
#23711=CARTESIAN_POINT('Ctrl Pts',(16.7719256499003,-0.131143826562283,
4.54658574430191));
#23712=CARTESIAN_POINT('Ctrl Pts',(16.8196414859631,-0.53067452246778,4.18530847342493));
#23713=CARTESIAN_POINT('Ctrl Pts',(16.8673573220259,-0.442878638914007,
3.65385958006445));
#23714=CARTESIAN_POINT('Ctrl Pts',(16.9150731580888,0.0516195133182915,
3.44027676038576));
#23715=CARTESIAN_POINT('Ctrl Pts',(16.9627889941516,0.498714672202087,3.74069640409388));
#23716=CARTESIAN_POINT('Ctrl Pts',(17.0105048302145,0.487832473891125,4.27923852982128));
#23717=CARTESIAN_POINT('Ctrl Pts',(17.0582206662773,0.0289662085384809,
4.56135161697672));
#23718=CARTESIAN_POINT('Ctrl Pts',(17.1059365023401,-0.456500171817451,
4.32796687675757));
#23719=CARTESIAN_POINT('Ctrl Pts',(17.1536523384029,-0.522755420235406,
3.79340510719289));
#23720=CARTESIAN_POINT('Ctrl Pts',(17.2013681744658,-0.108956322625149,
3.44856260656401));
#23721=CARTESIAN_POINT('Ctrl Pts',(17.2490840105286,0.404899042560309,3.61011354928233));
#23722=CARTESIAN_POINT('Ctrl Pts',(17.2967998465915,0.54692938679005,4.12970321886885));
#23723=CARTESIAN_POINT('Ctrl Pts',(17.3445156826543,0.186706059540143,4.53018442682757));
#23724=CARTESIAN_POINT('Ctrl Pts',(17.3922315187172,-0.344972315027459,
4.4437891176945));
#23725=CARTESIAN_POINT('Ctrl Pts',(17.43994735478,-0.559857304624004,3.94985543320929));
#23726=CARTESIAN_POINT('Ctrl Pts',(17.4876631908428,-0.260616716872392,
3.5019702759813));
#23727=CARTESIAN_POINT('Ctrl Pts',(17.5353790269057,0.277952212086773,3.51143347749201));
#23728=CARTESIAN_POINT('Ctrl Pts',(17.5830948629685,0.561273347842132,3.96955483418404));
#23729=CARTESIAN_POINT('Ctrl Pts',(17.6308106990313,0.329168531973526,4.45563445510394));
#23730=CARTESIAN_POINT('Ctrl Pts',(17.6785265350942,-0.205216811715269,
4.52329794506467));
#23731=CARTESIAN_POINT('Ctrl Pts',(17.726242371157,-0.551148399539408,4.11040888009862));
#23732=CARTESIAN_POINT('Ctrl Pts',(17.7739582072198,-0.390951931558304,
3.59612964167903));
#23733=CARTESIAN_POINT('Ctrl Pts',(17.8216740432827,0.128261710741471,3.45273076764982));
#23734=CARTESIAN_POINT('Ctrl Pts',(17.8693898793456,0.529690650507269,3.81189765050732));
#23735=CARTESIAN_POINT('Ctrl Pts',(17.9171057154083,0.44469651557395,4.34380181523062));
#23736=CARTESIAN_POINT('Ctrl Pts',(17.9648215514712,-0.0486692721463468,
4.55998748295674));
#23737=CARTESIAN_POINT('Ctrl Pts',(18.012537387534,-0.497341318381634,4.26192802856871));
#23738=CARTESIAN_POINT('Ctrl Pts',(18.0602532235969,-0.489297179367249,
3.72333603526529));
#23739=CARTESIAN_POINT('Ctrl Pts',(18.1079690596597,-0.0319239117350811,
3.43880881780002));
#23740=CARTESIAN_POINT('Ctrl Pts',(18.1556848957225,0.454765575255941,3.66963209798526));
#23741=CARTESIAN_POINT('Ctrl Pts',(18.2034007317854,0.523836837021606,4.20383730595423));
#23742=CARTESIAN_POINT('Ctrl Pts',(18.2511165678483,0.111860671084556,4.5508555794253));
#23743=CARTESIAN_POINT('Ctrl Pts',(18.298832403911,-0.402838870307115,4.39201469830757));
#23744=CARTESIAN_POINT('Ctrl Pts',(18.346548239974,-0.547605278623001,3.87318068781251));
#23745=CARTESIAN_POINT('Ctrl Pts',(18.3942640760367,-0.189497333589109,
3.47080680306518));
#23746=CARTESIAN_POINT('Ctrl Pts',(18.4419799120997,0.342628928670919,3.55439917374707));
#23747=CARTESIAN_POINT('Ctrl Pts',(18.4896957481624,0.560113773708727,4.04719363962704));
#23748=CARTESIAN_POINT('Ctrl Pts',(18.5374115842253,0.263237521891608,4.49664946007004));
#23749=CARTESIAN_POINT('Ctrl Pts',(18.5851274202881,-0.275373796708506,
4.49002443939646));
#23750=CARTESIAN_POINT('Ctrl Pts',(18.632843256351,-0.561105120620647,4.03340243603));
#23751=CARTESIAN_POINT('Ctrl Pts',(18.6805590924138,-0.331564978554912,
3.54610646169455));
#23752=CARTESIAN_POINT('Ctrl Pts',(18.7282749284766,0.202456385100939,3.47562790763498));
#23753=CARTESIAN_POINT('Ctrl Pts',(18.7759907645394,0.550558935126376,3.8866883144956));
#23754=CARTESIAN_POINT('Ctrl Pts',(18.8237066006023,0.393074743587739,4.40180458567998));
#23755=CARTESIAN_POINT('Ctrl Pts',(18.8714224366651,-0.125376033221007,
4.54793752327491));
#23756=CARTESIAN_POINT('Ctrl Pts',(18.919138272728,-0.528692069562509,4.19089100214638));
#23757=CARTESIAN_POINT('Ctrl Pts',(18.9668541087908,-0.4465020434557,3.6585463365067));
#23758=CARTESIAN_POINT('Ctrl Pts',(19.0145699448537,0.0457176794812401,
3.43976382400136));
#23759=CARTESIAN_POINT('Ctrl Pts',(19.0622857809165,0.495954153879041,3.73545481224116));
#23760=CARTESIAN_POINT('Ctrl Pts',(19.1100016169793,0.490748297561716,4.27408171698104));
#23761=CARTESIAN_POINT('Ctrl Pts',(19.1577174530421,0.0348807284082936,
4.5610151636709));
#23762=CARTESIAN_POINT('Ctrl Pts',(19.205433289105,-0.453018350253257,4.33275975334162));
#23763=CARTESIAN_POINT('Ctrl Pts',(19.2531491251678,-0.524903707479367,
3.79892594114836));
#23764=CARTESIAN_POINT('Ctrl Pts',(19.3008649612307,-0.11476191309534,3.44974153150476));
#23765=CARTESIAN_POINT('Ctrl Pts',(19.3485807972935,0.400767511262006,3.60586793956989));
#23766=CARTESIAN_POINT('Ctrl Pts',(19.3962966333564,0.548265964675035,4.12393188459875));
#23767=CARTESIAN_POINT('Ctrl Pts',(19.4440124694192,0.192283344213529,4.52818727047755));
#23768=CARTESIAN_POINT('Ctrl Pts',(19.491728305482,-0.340276025447905,4.44740016355363));
#23769=CARTESIAN_POINT('Ctrl Pts',(19.5394441415448,-0.560354693525076,
3.95575859308266));
#23770=CARTESIAN_POINT('Ctrl Pts',(19.5871599776077,-0.265851008504119,
3.50474460473346));
#23771=CARTESIAN_POINT('Ctrl Pts',(19.6348758136705,0.272787718306182,3.5085312334714));
#23772=CARTESIAN_POINT('Ctrl Pts',(19.6825916497334,0.560921342594646,3.96364125479661));
#23773=CARTESIAN_POINT('Ctrl Pts',(19.7303074857962,0.33395216026474,4.45213995410186));
#23774=CARTESIAN_POINT('Ctrl Pts',(19.7780233218591,-0.199690227635008,
4.52543179776919));
#23775=CARTESIAN_POINT('Ctrl Pts',(19.8257391579219,-0.549954387748789,
4.11621111891367));
#23776=CARTESIAN_POINT('Ctrl Pts',(19.8734549939848,-0.395186252277308,
3.60027277035845));
#23777=CARTESIAN_POINT('Ctrl Pts',(19.9211708300475,0.122486141425193,3.45140859770427));
#23778=CARTESIAN_POINT('Ctrl Pts',(19.9688866661104,0.527680190865048,3.80632716374734));
#23779=CARTESIAN_POINT('Ctrl Pts',(20.0166025021732,0.448292560087992,4.33909316421112));
#23780=CARTESIAN_POINT('Ctrl Pts',(20.0643183382361,-0.0427598846646947,
4.56047472290141));
#23781=CARTESIAN_POINT('Ctrl Pts',(20.1120341742989,-0.49456253103916,4.26714478353561));
#23782=CARTESIAN_POINT('Ctrl Pts',(20.1597500103618,-0.492168201513856,
3.72852743457374));
#23783=CARTESIAN_POINT('Ctrl Pts',(20.2074658464246,-0.0378697858522375,
3.43914000028616));
#23784=CARTESIAN_POINT('Ctrl Pts',(20.2551816824874,0.451321269441671,3.66492646727415));
#23785=CARTESIAN_POINT('Ctrl Pts',(20.3028975185503,0.52583741886325,4.1981749506787));
#23786=CARTESIAN_POINT('Ctrl Pts',(20.3506133546131,0.117885080656874,4.54989459844945));
#23787=CARTESIAN_POINT('Ctrl Pts',(20.398329190676,-0.399119892637424,4.39574851066478));
#23788=CARTESIAN_POINT('Ctrl Pts',(20.438092387395,-0.523197416260526,3.96600412247733));
#23789=CARTESIAN_POINT('Ctrl Pts',(20.4699029447702,-0.3725623900923,3.67462118354637));
#23790=CARTESIAN_POINT('Ctrl Pts',(20.4937608628016,-0.172533290246804,
3.53519650363565));
#23791=CARTESIAN_POINT('Ctrl Pts',(20.5176187808331,0.0720421502968434,
3.50974356844941));
#23792=CARTESIAN_POINT('Ctrl Pts',(20.5414766988645,0.297725647320748,3.60399556061657));
#23793=CARTESIAN_POINT('Ctrl Pts',(20.5653346168959,0.451286063531533,3.79517586539437));
#23794=CARTESIAN_POINT('Ctrl Pts',(20.5891925349273,0.494134760388362,4.03639109206021));
#23795=CARTESIAN_POINT('Ctrl Pts',(20.6130504529587,0.416344747430809,4.26873428690612));
#23796=CARTESIAN_POINT('Ctrl Pts',(20.6369083709901,0.23664610161733,4.43535054865035));
#23797=CARTESIAN_POINT('Ctrl Pts',(20.6607662890216,-0.000865470816140784,
4.49551919950567));
#23798=CARTESIAN_POINT('Ctrl Pts',(20.684624207053,-0.238193741375527,4.43451595913869));
#23799=CARTESIAN_POINT('Ctrl Pts',(20.7084821250844,-0.417262150572256,
4.26726382233879));
#23800=CARTESIAN_POINT('Ctrl Pts',(20.7323400431158,-0.494306543785295,
4.03465729316116));
#23801=CARTESIAN_POINT('Ctrl Pts',(20.7561979611472,-0.45047531426282,3.79357669839993));
#23802=CARTESIAN_POINT('Ctrl Pts',(20.7800558791787,-0.296492828349621,
3.60297191305088));
#23803=CARTESIAN_POINT('Ctrl Pts',(20.80391379721,-0.0700085893017688,3.50945147432983));
#23804=CARTESIAN_POINT('Ctrl Pts',(20.8277717152415,0.173594031734132,3.53588342526713));
#23805=CARTESIAN_POINT('Ctrl Pts',(20.8516296332729,0.374748514455718,3.6758045671588));
#23806=CARTESIAN_POINT('Ctrl Pts',(20.8754875513043,0.484266602122282,3.89500029884494));
#23807=CARTESIAN_POINT('Ctrl Pts',(20.8993454693358,0.475368407265908,4.13987133054223));
#23808=CARTESIAN_POINT('Ctrl Pts',(20.9232033873671,0.350229638882089,4.35054000504804));
#23809=CARTESIAN_POINT('Ctrl Pts',(20.9470613053986,0.139450209771325,4.47549210343221));
#23810=CARTESIAN_POINT('Ctrl Pts',(20.97091922343,-0.105428607968738,4.48417342845956));
#23811=CARTESIAN_POINT('Ctrl Pts',(20.9947771414615,-0.324527251938122,
4.37446116262749));
#23812=CARTESIAN_POINT('Ctrl Pts',(21.0186350594928,-0.464270146732381,
4.17318294187641));
#23813=CARTESIAN_POINT('Ctrl Pts',(21.0424929775243,-0.490486342136868,
3.92955677471355));
#23814=CARTESIAN_POINT('Ctrl Pts',(21.0663508955557,-0.396765267394252,
3.7031558948169));
#23815=CARTESIAN_POINT('Ctrl Pts',(21.0902088135871,-0.206024276530194,
3.54934148458869));
#23816=CARTESIAN_POINT('Ctrl Pts',(21.1140667316185,0.0350952616297792,
3.50572535702762));
#23817=CARTESIAN_POINT('Ctrl Pts',(21.1379246496499,0.267633052506714,3.58297284346672));
#23818=CARTESIAN_POINT('Ctrl Pts',(21.1617825676814,0.434727271782411,3.76219482925797));
#23819=CARTESIAN_POINT('Ctrl Pts',(21.1856404857128,0.495518831419392,3.99956665698474));
#23820=CARTESIAN_POINT('Ctrl Pts',(21.2094984037442,0.43514253908843,4.23704444887943));
#23821=CARTESIAN_POINT('Ctrl Pts',(21.2333563217756,0.268362042918248,4.41655841606373));
#23822=CARTESIAN_POINT('Ctrl Pts',(21.257214239807,0.0359597172125542,4.49421250369607));
#23823=CARTESIAN_POINT('Ctrl Pts',(21.2810721578384,-0.205235738871087,
4.45101817209691));
#23824=CARTESIAN_POINT('Ctrl Pts',(21.3049300758699,-0.396245466293343,
4.29753761193144));
#23825=CARTESIAN_POINT('Ctrl Pts',(21.3287879939013,-0.490362383696085,
4.07130100088706));
#23826=CARTESIAN_POINT('Ctrl Pts',(21.3526459119327,-0.464572341082516,
3.82762935292545));
#23827=CARTESIAN_POINT('Ctrl Pts',(21.3765038299641,-0.325181706377507,
3.62610702345576));
#23828=CARTESIAN_POINT('Ctrl Pts',(21.4003617479955,-0.106275286691508,
3.51601171139131));
#23829=CARTESIAN_POINT('Ctrl Pts',(21.424219666027,0.138618335471326,3.52426471946798));
#23830=CARTESIAN_POINT('Ctrl Pts',(21.4480775840584,0.349615998723735,3.64884796240357));
#23831=CARTESIAN_POINT('Ctrl Pts',(21.4719355020898,0.475123026939619,3.85929744372095));
#23832=CARTESIAN_POINT('Ctrl Pts',(21.4957934201212,0.484449532977353,4.10415253270923));
#23833=CARTESIAN_POINT('Ctrl Pts',(21.5196513381527,0.375314932061802,4.32353949039209));
#23834=CARTESIAN_POINT('Ctrl Pts',(21.543509256184,0.174405606883644,4.4638122296353));
#23835=CARTESIAN_POINT('Ctrl Pts',(21.5673671742155,-0.069150639890911,
4.49067024474121));
#23836=CARTESIAN_POINT('Ctrl Pts',(21.5912250922469,-0.29579767158652,4.39754601941878));
#23837=CARTESIAN_POINT('Ctrl Pts',(21.6150830102783,-0.450114115212426,
4.20721096341231));
#23838=CARTESIAN_POINT('Ctrl Pts',(21.6389409283097,-0.494365396806572,
3.96620718253823));
#23839=CARTESIAN_POINT('Ctrl Pts',(21.6627988463412,-0.417730872638478,
3.73346666603139));
#23840=CARTESIAN_POINT('Ctrl Pts',(21.6866567643726,-0.238949771349764,
3.56590080990214));
#23841=CARTESIAN_POINT('Ctrl Pts',(21.710514682404,-0.00173894210493873,
3.50448403037633));
#23842=CARTESIAN_POINT('Ctrl Pts',(21.7343726004354,0.235897105852373,3.56423440300754));
#23843=CARTESIAN_POINT('Ctrl Pts',(21.7582305184669,0.415849885720624,3.73054133411992));
#23844=CARTESIAN_POINT('Ctrl Pts',(21.7820884364982,0.49411604100673,3.96273824894669));
#23845=CARTESIAN_POINT('Ctrl Pts',(21.8059463545297,0.451557364815975,4.20404667689569));
#23846=CARTESIAN_POINT('Ctrl Pts',(21.8298042725611,0.29858061275206,4.39546013422383));
#23847=CARTESIAN_POINT('Ctrl Pts',(21.8536621905925,0.0725927676976751,
4.49017281661646));
#23848=CARTESIAN_POINT('Ctrl Pts',(21.8775201086239,-0.171145986446082,
4.46502489330693));
#23849=CARTESIAN_POINT('Ctrl Pts',(21.9013780266554,-0.373034884980705,
4.32616571656009));
#23850=CARTESIAN_POINT('Ctrl Pts',(21.9252359446868,-0.483706592871294,
4.10755013753858));
#23851=CARTESIAN_POINT('Ctrl Pts',(21.9490938627182,-0.476098862901817,
3.86263562028194));
#23852=CARTESIAN_POINT('Ctrl Pts',(21.9729517807496,-0.352071992280181,
3.65131043559696));
#23853=CARTESIAN_POINT('Ctrl Pts',(21.996809698781,-0.141953929297546,3.52524934752154));
#23854=CARTESIAN_POINT('Ctrl Pts',(22.0206676168125,0.102875736145779,3.51527772592526));
#23855=CARTESIAN_POINT('Ctrl Pts',(22.0445255348438,0.322549481822576,3.62383390390986));
#23856=CARTESIAN_POINT('Ctrl Pts',(22.0683834528753,0.46335109312246,3.82437293894729));
#23857=CARTESIAN_POINT('Ctrl Pts',(22.0922413709067,0.490850740723195,4.06785757439707));
#23858=CARTESIAN_POINT('Ctrl Pts',(22.1160992889381,0.398324011712033,4.29474918450382));
#23859=CARTESIAN_POINT('Ctrl Pts',(22.1399572069695,0.208396211707814,4.44956659019228));
#23860=CARTESIAN_POINT('Ctrl Pts',(22.163815125001,-0.0324901386554863,
4.49445271863166));
#23861=CARTESIAN_POINT('Ctrl Pts',(22.1876730430324,-0.265431765108271,
4.41843168874211));
#23862=CARTESIAN_POINT('Ctrl Pts',(22.2115309610638,-0.433468094767725,
4.24009271310828));
#23863=CARTESIAN_POINT('Ctrl Pts',(22.2353888790952,-0.495509667838209,
4.00304452911861));
#23864=CARTESIAN_POINT('Ctrl Pts',(22.2592467971266,-0.436385629680506,
3.76525187484075));
#23865=CARTESIAN_POINT('Ctrl Pts',(22.2831047151581,-0.270553418215538,
3.58486153155103));
#23866=CARTESIAN_POINT('Ctrl Pts',(22.3069626331895,-0.0385635261649252,
3.50598385198694));
#23867=CARTESIAN_POINT('Ctrl Pts',(22.3308205512209,0.202856198284482,3.54790657725669));
#23868=CARTESIAN_POINT('Ctrl Pts',(22.3546784692523,0.394672056935096,3.70037845932536));
#23869=CARTESIAN_POINT('Ctrl Pts',(22.3785363872837,0.489979846308564,3.9261159693126));
#23870=CARTESIAN_POINT('Ctrl Pts',(22.4023943053151,0.465474217808745,4.1699201379362));
#23871=CARTESIAN_POINT('Ctrl Pts',(22.4262522233466,0.327147461276091,4.37217420322137));
#23872=CARTESIAN_POINT('Ctrl Pts',(22.450110141378,0.108824243893236,4.4834215400391));
#23873=CARTESIAN_POINT('Ctrl Pts',(22.4739680594094,-0.136109474402841,
4.47645913832327));
#23874=CARTESIAN_POINT('Ctrl Pts',(22.4978259774408,-0.347760701725541,
4.3529895060813));
#23875=CARTESIAN_POINT('Ctrl Pts',(22.5216838954723,-0.474374996640319,
4.1432043106148));
#23876=CARTESIAN_POINT('Ctrl Pts',(22.5455418135036,-0.484991622785221,
3.89840178635216));
#23877=CARTESIAN_POINT('Ctrl Pts',(22.5693997315351,-0.377014700254462,
3.67844274379546));
#23878=CARTESIAN_POINT('Ctrl Pts',(22.5932576495665,-0.176847198578467,
3.53711330196678));
#23879=CARTESIAN_POINT('Ctrl Pts',(22.6171155675979,0.0665638539184235,
3.50897209184919));
#23880=CARTESIAN_POINT('Ctrl Pts',(22.6409734856293,0.293698998435555,3.60090091054846));
#23881=CARTESIAN_POINT('Ctrl Pts',(22.6648314036608,0.449015288492166,3.79041970485759));
#23882=CARTESIAN_POINT('Ctrl Pts',(22.6886893216922,0.494537845944295,4.03118776656693));
#23883=CARTESIAN_POINT('Ctrl Pts',(22.7125472397236,0.419127261608858,4.26432734830583));
#23884=CARTESIAN_POINT('Ctrl Pts',(22.736405157755,0.241238408088568,4.43283588997321));
#23885=CARTESIAN_POINT('Ctrl Pts',(22.7602630757865,0.00434171083240793,
4.49549632518638));
#23886=CARTESIAN_POINT('Ctrl Pts',(22.7841209938178,-0.233581370990537,
4.43700954435219));
#23887=CARTESIAN_POINT('Ctrl Pts',(22.8079789118493,-0.414457183229959,
4.27163232278894));
#23888=CARTESIAN_POINT('Ctrl Pts',(22.8238841905369,-0.46737397936094,4.11714349286348));
#23889=CARTESIAN_POINT('Ctrl Pts',(22.8318368298807,-0.473742730682552,
4.03823705100924));
#23890=CARTESIAN_POINT('Ctrl Pts',(4.,-0.219892372743211,3.64701365460636));
#23891=CARTESIAN_POINT('Ctrl Pts',(4.00795263934381,-0.161099076858729,
3.61038844940468));
#23892=CARTESIAN_POINT('Ctrl Pts',(4.02385791803142,-0.0249198690254346,
3.56711791692558));
#23893=CARTESIAN_POINT('Ctrl Pts',(4.04771583606284,0.185569069288609,3.60813812632505));
#23894=CARTESIAN_POINT('Ctrl Pts',(4.07157375409426,0.350624105231944,3.74494568050885));
#23895=CARTESIAN_POINT('Ctrl Pts',(4.09543167212568,0.429971014252744,3.94413788601839));
#23896=CARTESIAN_POINT('Ctrl Pts',(4.1192895901571,0.40416308778273,4.15698104289539));
#23897=CARTESIAN_POINT('Ctrl Pts',(4.14314750818851,0.279534313346206,4.3314427366163));
#23898=CARTESIAN_POINT('Ctrl Pts',(4.16700542621994,0.0865475313004802,
4.42485517705098));
#23899=CARTESIAN_POINT('Ctrl Pts',(4.19086334425134,-0.127600227202394,
4.41438026490915));
#23900=CARTESIAN_POINT('Ctrl Pts',(4.21472126228278,-0.310547447266788,
4.30257739619942));
#23901=CARTESIAN_POINT('Ctrl Pts',(4.23857918031418,-0.417556725585918,
4.11678647978038));
#23902=CARTESIAN_POINT('Ctrl Pts',(4.26243709834561,-0.422462345057068,
3.90243789311793));
#23903=CARTESIAN_POINT('Ctrl Pts',(4.28629501637703,-0.324064236326554,
3.71194600226016));
#23904=CARTESIAN_POINT('Ctrl Pts',(4.31015293440845,-0.146423688323203,
3.59189110566319));
#23905=CARTESIAN_POINT('Ctrl Pts',(4.33401085243986,0.0670214896752265,
3.5716299793216));
#23906=CARTESIAN_POINT('Ctrl Pts',(4.35786877047129,0.264078061498623,3.65611697628114));
#23907=CARTESIAN_POINT('Ctrl Pts',(4.38172668850271,0.396560367883193,3.82469274783887));
#23908=CARTESIAN_POINT('Ctrl Pts',(4.40558460653412,0.432072854850341,4.03613591352675));
#23909=CARTESIAN_POINT('Ctrl Pts',(4.42944252456555,0.361931763288092,4.23874286631049));
#23910=CARTESIAN_POINT('Ctrl Pts',(4.45330044259696,0.203288494707987,4.382970683851));
#23911=CARTESIAN_POINT('Ctrl Pts',(4.47715836062838,-0.00506434719902249,
4.43355173791626));
#23912=CARTESIAN_POINT('Ctrl Pts',(4.5010162786598,-0.212178818846594,4.37811758201071));
#23913=CARTESIAN_POINT('Ctrl Pts',(4.52487419669122,-0.367409789343613,
4.23022337776645));
#23914=CARTESIAN_POINT('Ctrl Pts',(4.54873211472264,-0.432799058467291,
4.02603328640456));
#23915=CARTESIAN_POINT('Ctrl Pts',(4.57259003275406,-0.392357168499796,
3.8154773474345));
#23916=CARTESIAN_POINT('Ctrl Pts',(4.59644795078547,-0.255973263285106,
3.65004222328625));
#23917=CARTESIAN_POINT('Ctrl Pts',(4.6203058688169,-0.0569969226013119,
3.57018130821703));
#23918=CARTESIAN_POINT('Ctrl Pts',(4.64416378684831,0.155916718210686,3.59542277130738));
#23919=CARTESIAN_POINT('Ctrl Pts',(4.66802170487973,0.330704474340828,3.71959438727947));
#23920=CARTESIAN_POINT('Ctrl Pts',(4.69187962291115,0.424625978282027,3.91233281365517));
#23921=CARTESIAN_POINT('Ctrl Pts',(4.71573754094257,0.41471486395576,4.1265082550995));
#23922=CARTESIAN_POINT('Ctrl Pts',(4.73959545897399,0.303394668785218,4.30974898215573));
#23923=CARTESIAN_POINT('Ctrl Pts',(4.76345337700541,0.117886212792376,4.41724764568232));
#23924=CARTESIAN_POINT('Ctrl Pts',(4.78731129503683,-0.0964486333844469,
4.42271789424177));
#23925=CARTESIAN_POINT('Ctrl Pts',(4.81116921306824,-0.287199161490599,
4.32482210305491));
#23926=CARTESIAN_POINT('Ctrl Pts',(4.83502713109967,-0.407721671464292,
4.14749845969467));
#23927=CARTESIAN_POINT('Ctrl Pts',(4.85888504913109,-0.42854512664958,3.93410742516172));
#23928=CARTESIAN_POINT('Ctrl Pts',(4.8827429671625,-0.344577625034195,3.73682892005441));
#23929=CARTESIAN_POINT('Ctrl Pts',(4.90660088519393,-0.176351507991885,
3.60390291263011));
#23930=CARTESIAN_POINT('Ctrl Pts',(4.93045880322534,0.0349973564730633,
3.56783343253575));
#23931=CARTESIAN_POINT('Ctrl Pts',(4.95431672125677,0.237788413971502,3.63744045016736));
#23932=CARTESIAN_POINT('Ctrl Pts',(4.97817463928818,0.382433727027559,3.79570315365689));
#23933=CARTESIAN_POINT('Ctrl Pts',(5.0020325573196,0.433563576539811,4.00392200101168));
#23934=CARTESIAN_POINT('Ctrl Pts',(5.02589047535102,0.378675321553375,4.21118181228595));
#23935=CARTESIAN_POINT('Ctrl Pts',(5.04974839338244,0.231190635538481,4.36680191797922));
#23936=CARTESIAN_POINT('Ctrl Pts',(5.07360631141386,0.0271735416279573,
4.43272896324296));
#23937=CARTESIAN_POINT('Ctrl Pts',(5.09746422944527,-0.183488223403015,
4.39284198969348));
#23938=CARTESIAN_POINT('Ctrl Pts',(5.1213221474767,-0.349282119693095,4.256894448863));
#23939=CARTESIAN_POINT('Ctrl Pts',(5.1451800655081,-0.4296670234643,4.05812921762123));
#23940=CARTESIAN_POINT('Ctrl Pts',(5.16903798353954,-0.404986636103755,
3.84514980926298));
#23941=CARTESIAN_POINT('Ctrl Pts',(5.19289590157095,-0.281275984601366,
3.67003549057442));
#23942=CARTESIAN_POINT('Ctrl Pts',(5.21675381960238,-0.0887856930599551,
3.5756064824932));
#23943=CARTESIAN_POINT('Ctrl Pts',(5.24061173763379,0.125415118908336,3.58495324968971));
#23944=CARTESIAN_POINT('Ctrl Pts',(5.26446965566521,0.308948518064291,3.69579025298356));
#23945=CARTESIAN_POINT('Ctrl Pts',(5.28832757369662,0.416935588964862,3.88101482593007));
#23946=CARTESIAN_POINT('Ctrl Pts',(5.31218549172805,0.422970551266107,4.09533451502773));
#23947=CARTESIAN_POINT('Ctrl Pts',(5.33604340975946,0.325577692296299,4.28634231834109));
#23948=CARTESIAN_POINT('Ctrl Pts',(5.35990132779089,0.148572219001774,4.40733162501188));
#23949=CARTESIAN_POINT('Ctrl Pts',(5.3837592458223,-0.0647632088646815,
4.42871725387658));
#23950=CARTESIAN_POINT('Ctrl Pts',(5.40761716385372,-0.26226226804932,4.34526983614494));
#23951=CARTESIAN_POINT('Ctrl Pts',(5.43147508188515,-0.395631058815178,
4.17739453851434));
#23952=CARTESIAN_POINT('Ctrl Pts',(5.45533299991656,-0.432257278927009,
3.96614144408682));
#23953=CARTESIAN_POINT('Ctrl Pts',(5.47919091794798,-0.363184819889405,
3.76316768886851));
#23954=CARTESIAN_POINT('Ctrl Pts',(5.5030488359794,-0.205303779432806,3.61810588490468));
#23955=CARTESIAN_POINT('Ctrl Pts',(5.52690675401082,0.00277962745745752,
3.56642759466814));
#23956=CARTESIAN_POINT('Ctrl Pts',(5.55076467204224,0.210183339719457,3.62076956781107));
#23957=CARTESIAN_POINT('Ctrl Pts',(5.57462259007365,0.36619150013966,3.76784371165257));
#23958=CARTESIAN_POINT('Ctrl Pts',(5.59848050810508,0.432655863921731,3.97168639180759));
#23959=CARTESIAN_POINT('Ctrl Pts',(5.62233842613649,0.393324083661671,4.18245252040861));
#23960=CARTESIAN_POINT('Ctrl Pts',(5.64619634416792,0.257813851021257,4.34860403787086));
#23961=CARTESIAN_POINT('Ctrl Pts',(5.67005426219933,0.0592611090830247,
4.42951237227525));
#23962=CARTESIAN_POINT('Ctrl Pts',(5.69391218023075,-0.153782588238227,
4.40539323200473));
#23963=CARTESIAN_POINT('Ctrl Pts',(5.71777009826218,-0.329222253834466,
4.28214440376531));
#23964=CARTESIAN_POINT('Ctrl Pts',(5.74162801629359,-0.424158110434281,
4.08990358344764));
#23965=CARTESIAN_POINT('Ctrl Pts',(5.76548593432501,-0.415375755386326,
3.8756788878607));
#23966=CARTESIAN_POINT('Ctrl Pts',(5.78934385235642,-0.305022713182347,
3.69185409099321));
#23967=CARTESIAN_POINT('Ctrl Pts',(5.81320177038785,-0.120083309624962,
3.58337936191985));
#23968=CARTESIAN_POINT('Ctrl Pts',(5.83705968841926,0.0942197354074567,
3.57677972866706));
#23969=CARTESIAN_POINT('Ctrl Pts',(5.86091760645069,0.285483486244351,3.673668977605));
#23970=CARTESIAN_POINT('Ctrl Pts',(5.8847755244821,0.406938752801468,3.85035505520226));
#23971=CARTESIAN_POINT('Ctrl Pts',(5.90863344251353,0.428886400972996,4.06363338935351));
#23972=CARTESIAN_POINT('Ctrl Pts',(5.93249136054494,0.345959657594393,4.261351642888));
#23973=CARTESIAN_POINT('Ctrl Pts',(5.95634927857636,0.178436323746589,4.39516226965834));
#23974=CARTESIAN_POINT('Ctrl Pts',(5.98020719660778,-0.0327194942966983,
4.4323450160316));
#23975=CARTESIAN_POINT('Ctrl Pts',(6.0040651146392,-0.23587461323539,4.36380751861078));
#23976=CARTESIAN_POINT('Ctrl Pts',(6.02792303267061,-0.381351759249696,
4.20630938167977));
#23977=CARTESIAN_POINT('Ctrl Pts',(6.05178095070204,-0.433578399193506,
3.9983625870902));
#23978=CARTESIAN_POINT('Ctrl Pts',(6.07563886873346,-0.379782579589031,
3.79081692866841));
#23979=CARTESIAN_POINT('Ctrl Pts',(6.09949678676487,-0.233120953551068,
3.63442082419035));
#23980=CARTESIAN_POINT('Ctrl Pts',(6.12335470479629,-0.0294522997972467,
3.5674214393556));
#23981=CARTESIAN_POINT('Ctrl Pts',(6.14721262282771,0.181413325723775,3.60619428643423));
#23982=CARTESIAN_POINT('Ctrl Pts',(6.17107054085913,0.347927737305898,3.74127281623538));
#23983=CARTESIAN_POINT('Ctrl Pts',(6.19492845889055,0.429346806292137,3.93959933010928));
#23984=CARTESIAN_POINT('Ctrl Pts',(6.21878637692197,0.405811992579865,4.15272917617017));
#23985=CARTESIAN_POINT('Ctrl Pts',(6.24264429495339,0.282982581651336,4.32844890303245));
#23986=CARTESIAN_POINT('Ctrl Pts',(6.26650221298481,0.0910742457207041,
4.42397415233781));
#23987=CARTESIAN_POINT('Ctrl Pts',(6.29036013101623,-0.123327005978964,
4.41559921078967));
#23988=CARTESIAN_POINT('Ctrl Pts',(6.31421804904765,-0.307151379675736,
4.3060270879454));
#23989=CARTESIAN_POINT('Ctrl Pts',(6.33807596707907,-0.416657206472865,
4.12081787696614));
#23990=CARTESIAN_POINT('Ctrl Pts',(6.36193388511048,-0.422829889105799,
3.9075587958503));
#23991=CARTESIAN_POINT('Ctrl Pts',(6.39374444248571,-0.296437506874183,
3.64987069373525));
#23992=CARTESIAN_POINT('Ctrl Pts',(6.43350763920474,0.0703302468340302,
3.51324810367198));
#23993=CARTESIAN_POINT('Ctrl Pts',(6.48122347526758,0.448014600657906,3.7964368525222));
#23994=CARTESIAN_POINT('Ctrl Pts',(6.52893931133042,0.413240052911115,4.26646358767058));
#23995=CARTESIAN_POINT('Ctrl Pts',(6.57665514739325,-0.000480251589724132,
4.49184654025612));
#23996=CARTESIAN_POINT('Ctrl Pts',(6.62437098345609,-0.41404349770976,4.26553045144514));
#23997=CARTESIAN_POINT('Ctrl Pts',(6.67208681951894,-0.447234019333667,
3.79538894860702));
#23998=CARTESIAN_POINT('Ctrl Pts',(6.71980265558177,-0.0698021891909718,
3.51313682319347));
#23999=CARTESIAN_POINT('Ctrl Pts',(6.76751849164461,0.371772181936036,3.67798293440124));
#24000=CARTESIAN_POINT('Ctrl Pts',(6.81523432770745,0.471920133146607,4.13853999974893));
#24001=CARTESIAN_POINT('Ctrl Pts',(6.86295016377028,0.138708377331583,4.4718748549198));
#24002=CARTESIAN_POINT('Ctrl Pts',(6.91066599983312,-0.32188767172048,4.37187913281409));
#24003=CARTESIAN_POINT('Ctrl Pts',(6.95838183589596,-0.486886005735063,
3.93038141845316));
#24004=CARTESIAN_POINT('Ctrl Pts',(7.0060976719588,-0.204771183672361,3.55281534000283));
#24005=CARTESIAN_POINT('Ctrl Pts',(7.05381350802163,0.265389096458903,3.58590591031157));
#24006=CARTESIAN_POINT('Ctrl Pts',(7.10152934408448,0.491837993618785,3.99926540470374));
#24007=CARTESIAN_POINT('Ctrl Pts',(7.14924518014731,0.266624753986561,4.41329951581085));
#24008=CARTESIAN_POINT('Ctrl Pts',(7.19696101621015,-0.203434237821079,
4.44779430805676));
#24009=CARTESIAN_POINT('Ctrl Pts',(7.24467685227299,-0.486676365692783,
4.07107270446015));
#24010=CARTESIAN_POINT('Ctrl Pts',(7.29239268833582,-0.322996137187983,
3.62908393881966));
#24011=CARTESIAN_POINT('Ctrl Pts',(7.34010852439867,0.137296434535941,3.52771310152703));
#24012=CARTESIAN_POINT('Ctrl Pts',(7.3878243604615,0.471507566988788,3.86005058906394));
#24013=CARTESIAN_POINT('Ctrl Pts',(7.43554019652434,0.372726051350611,4.32090577464778));
#24014=CARTESIAN_POINT('Ctrl Pts',(7.48325603258718,-0.0683355354161961,
4.48706824929225));
#24015=CARTESIAN_POINT('Ctrl Pts',(7.53097186865002,-0.44664354691983,4.20594845626764));
#24016=CARTESIAN_POINT('Ctrl Pts',(7.57868770471286,-0.414791917646955,
3.73570302684109));
#24017=CARTESIAN_POINT('Ctrl Pts',(7.62640354077569,-0.00203048755240202,
3.50816557464413));
#24018=CARTESIAN_POINT('Ctrl Pts',(7.67411937683853,0.412595570264971,3.73228724307244));
#24019=CARTESIAN_POINT('Ctrl Pts',(7.72183521290137,0.448328767436039,4.20225365549051));
#24020=CARTESIAN_POINT('Ctrl Pts',(7.7695510489642,0.0723547589785895,4.48648742399228));
#24021=CARTESIAN_POINT('Ctrl Pts',(7.81726688502705,-0.370063737934377,
4.32397230547438));
#24022=CARTESIAN_POINT('Ctrl Pts',(7.86498272108989,-0.472647010158531,
3.86394843388276));
#24023=CARTESIAN_POINT('Ctrl Pts',(7.91269855715272,-0.141191260335066,
3.52886280888004));
#24024=CARTESIAN_POINT('Ctrl Pts',(7.96041439321556,0.31992259635559,3.62642971585976));
#24025=CARTESIAN_POINT('Ctrl Pts',(8.0081302292784,0.48724661017382,4.0670519628834));
#24026=CARTESIAN_POINT('Ctrl Pts',(8.05584606534124,0.207124564615173,4.44609936066402));
#24027=CARTESIAN_POINT('Ctrl Pts',(8.10356190140407,-0.263203155649882,
4.41548685142597));
#24028=CARTESIAN_POINT('Ctrl Pts',(8.15127773746691,-0.491827368180951,
4.00332637343646));
#24029=CARTESIAN_POINT('Ctrl Pts',(8.19899357352975,-0.268798940774433,
3.58811123553743));
#24030=CARTESIAN_POINT('Ctrl Pts',(8.24670940959259,0.201071689948468,3.55113988776764));
#24031=CARTESIAN_POINT('Ctrl Pts',(8.29442524565542,0.486295093906121,3.92636368766143));
#24032=CARTESIAN_POINT('Ctrl Pts',(8.34214108171827,0.324946230517931,4.36920884621601));
#24033=CARTESIAN_POINT('Ctrl Pts',(8.3898569177811,-0.134805756295296,4.47300384028212));
#24034=CARTESIAN_POINT('Ctrl Pts',(8.43757275384394,-0.470763542849379,
4.14243212971755));
#24035=CARTESIAN_POINT('Ctrl Pts',(8.48528858990678,-0.37441192437669,3.68106280283335));
#24036=CARTESIAN_POINT('Ctrl Pts',(8.53300442596962,0.0657679253190804,
3.51257841158684));
#24037=CARTESIAN_POINT('Ctrl Pts',(8.58072026203246,0.445552077224736,3.79170076492532));
#24038=CARTESIAN_POINT('Ctrl Pts',(8.62843609809529,0.41617890091499,4.26210751092856));
#24039=CARTESIAN_POINT('Ctrl Pts',(8.67615193415813,0.0046222361594965,
4.49181689660367));
#24040=CARTESIAN_POINT('Ctrl Pts',(8.72386777022097,-0.411179099183508,
4.26988325855195));
#24041=CARTESIAN_POINT('Ctrl Pts',(8.7715836062838,-0.449388340942622,3.80011167148426));
#24042=CARTESIAN_POINT('Ctrl Pts',(8.81929944234665,-0.0749173544856965,
3.51390061216986));
#24043=CARTESIAN_POINT('Ctrl Pts',(8.86701527840948,0.368351391347115,3.67408210030036));
#24044=CARTESIAN_POINT('Ctrl Pts',(8.91473111447233,0.473357386691186,4.13355901061654));
#24045=CARTESIAN_POINT('Ctrl Pts',(8.96244695053515,0.14367201029714,4.47038662641401));
#24046=CARTESIAN_POINT('Ctrl Pts',(9.01016278659801,-0.317949583830803,
4.37525096534692));
#24047=CARTESIAN_POINT('Ctrl Pts',(9.05787862266083,-0.487593182843731,
3.93551656882348));
#24048=CARTESIAN_POINT('Ctrl Pts',(9.10559445872368,-0.209472459465777,
3.55499829935456));
#24049=CARTESIAN_POINT('Ctrl Pts',(9.15331029478651,0.261010046587687,3.58313193881964));
#24050=CARTESIAN_POINT('Ctrl Pts',(9.20102613084934,0.491803010703882,3.99408193320625));
#24051=CARTESIAN_POINT('Ctrl Pts',(9.2487419669122,0.270965702728691,4.41046657939073));
#24052=CARTESIAN_POINT('Ctrl Pts',(9.29645780297501,-0.198703579405513,
4.44991344988054));
#24053=CARTESIAN_POINT('Ctrl Pts',(9.34417363903789,-0.485900307124067,
4.07619787653679));
#24054=CARTESIAN_POINT('Ctrl Pts',(9.39188947510068,-0.326887306273347,
3.63250862071426));
#24055=CARTESIAN_POINT('Ctrl Pts',(9.43960531116356,0.13231133773591,3.52629235307153));
#24056=CARTESIAN_POINT('Ctrl Pts',(9.48732114722637,0.470006444430667,3.85508910653225));
#24057=CARTESIAN_POINT('Ctrl Pts',(9.53503698328922,0.376087401226012,4.31695976320512));
#24058=CARTESIAN_POINT('Ctrl Pts',(9.58275281935206,-0.0631984893729827,
4.48776139227388));
#24059=CARTESIAN_POINT('Ctrl Pts',(9.63046865541489,-0.444448234747017,
4.21064422964382));
#24060=CARTESIAN_POINT('Ctrl Pts',(9.67818449147773,-0.41755432743774,3.74008922975375));
#24061=CARTESIAN_POINT('Ctrl Pts',(9.72590032754057,-0.00721385634321597,
3.50821428942208));
#24062=CARTESIAN_POINT('Ctrl Pts',(9.77361616360341,0.40975121003073,3.72795373420991));
#24063=CARTESIAN_POINT('Ctrl Pts',(9.82133199966624,0.450435435400681,4.19751745084266));
#24064=CARTESIAN_POINT('Ctrl Pts',(9.86904783572909,0.077477869602138,4.48569785316993));
#24065=CARTESIAN_POINT('Ctrl Pts',(9.91676367179192,-0.366628816002305,
4.3278544435092));
#24066=CARTESIAN_POINT('Ctrl Pts',(9.96447950785476,-0.474054618562381,
3.8689372536849));
#24067=CARTESIAN_POINT('Ctrl Pts',(10.0121953439176,-0.146148770628728,
3.53037700046135));
#24068=CARTESIAN_POINT('Ctrl Pts',(10.0599111799804,0.315967742161179,3.62307877379278));
#24069=CARTESIAN_POINT('Ctrl Pts',(10.1076270160433,0.487926215535836,4.06191310882887));
#24070=CARTESIAN_POINT('Ctrl Pts',(10.1553428521061,0.211814537474087,4.44389168337175));
#24071=CARTESIAN_POINT('Ctrl Pts',(10.203058688169,-0.258809689535701,4.4182376949229));
#24072=CARTESIAN_POINT('Ctrl Pts',(10.2507745242318,-0.491764996345908,
4.00850959581219));
#24073=CARTESIAN_POINT('Ctrl Pts',(10.2984903602946,-0.273124940234581,
3.59096700393021));
#24074=CARTESIAN_POINT('Ctrl Pts',(10.3462061963575,0.196329951061554,3.54904570612073));
#24075=CARTESIAN_POINT('Ctrl Pts',(10.3939220324203,0.485492027373267,3.92124267520431));
#24076=CARTESIAN_POINT('Ctrl Pts',(10.4416378684831,0.328819304693055,4.36576370748498));
#24077=CARTESIAN_POINT('Ctrl Pts',(10.489353704546,-0.129813245022134,4.47439829918413));
#24078=CARTESIAN_POINT('Ctrl Pts',(10.5370695406088,-0.469236294399976,
4.14738563318641));
#24079=CARTESIAN_POINT('Ctrl Pts',(10.5847853766716,-0.377752434501872,
3.68502647241413));
#24080=CARTESIAN_POINT('Ctrl Pts',(10.6325012127345,0.0606272984676223,
3.51191234851464));
#24081=CARTESIAN_POINT('Ctrl Pts',(10.6802170487973,0.443332050383407,3.78701662516801));
#24082=CARTESIAN_POINT('Ctrl Pts',(10.7279328848602,0.418918158891686,4.25770681210006));
#24083=CARTESIAN_POINT('Ctrl Pts',(10.775648720923,0.00980527620531799,
4.49174086815163));
#24084=CARTESIAN_POINT('Ctrl Pts',(10.8233645569858,-0.408311942493964,
4.27420171857372));
#24085=CARTESIAN_POINT('Ctrl Pts',(10.8710803930487,-0.451470021714238,
3.80485891169382));
#24086=CARTESIAN_POINT('Ctrl Pts',(10.9187962291115,-0.080036233235122,
3.51471716883706));
#24087=CARTESIAN_POINT('Ctrl Pts',(10.9665120651743,0.364896059739551,3.6702181168734));
#24088=CARTESIAN_POINT('Ctrl Pts',(11.0142279012372,0.47473868640782,4.1285628425314));
#24089=CARTESIAN_POINT('Ctrl Pts',(11.0619437373,0.148621472554162,4.46884633169921));
#24090=CARTESIAN_POINT('Ctrl Pts',(11.1096595733629,-0.313977126381285,
4.37858102033954));
#24091=CARTESIAN_POINT('Ctrl Pts',(11.1573754094257,-0.488245699001722,
3.94065893278431));
#24092=CARTESIAN_POINT('Ctrl Pts',(11.2050912454886,-0.214150733603143,
3.55723066033293));
#24093=CARTESIAN_POINT('Ctrl Pts',(11.2528070815514,0.256602145595791,3.58040428537983));
#24094=CARTESIAN_POINT('Ctrl Pts',(11.3005229176142,0.491713326162588,3.98889911147238));
#24095=CARTESIAN_POINT('Ctrl Pts',(11.3482387536771,0.275276593332242,4.40758805430897));
#24096=CARTESIAN_POINT('Ctrl Pts',(11.3959545897399,-0.193950870829933,
4.45198261532529));
#24097=CARTESIAN_POINT('Ctrl Pts',(11.4436704258028,-0.485070265991237,
4.08131458604192));
#24098=CARTESIAN_POINT('Ctrl Pts',(11.4913862618656,-0.330742172127369,
3.63597412121053));
#24099=CARTESIAN_POINT('Ctrl Pts',(11.5391020979284,0.127311547523522,3.52492422212962));
#24100=CARTESIAN_POINT('Ctrl Pts',(11.5868179339912,0.468453114143607,3.85014371984754));
#24101=CARTESIAN_POINT('Ctrl Pts',(11.6345337700541,0.379406977967949,4.31297854546471));
#24102=CARTESIAN_POINT('Ctrl Pts',(11.6822496061169,-0.0580544240024287,
4.48840035698771));
#24103=CARTESIAN_POINT('Ctrl Pts',(11.7299654421798,-0.44220355512924,4.21531660568344));
#24104=CARTESIAN_POINT('Ctrl Pts',(11.7776812782426,-0.420270357404582,
3.74450430230823));
#24105=CARTESIAN_POINT('Ctrl Pts',(11.8253971143054,-0.0123964237846327,
3.50831762943));
#24106=CARTESIAN_POINT('Ctrl Pts',(11.8731129503683,0.406861336540243,3.72365044295193));
#24107=CARTESIAN_POINT('Ctrl Pts',(11.9208287864311,0.452492071153857,4.1927593068956));
#24108=CARTESIAN_POINT('Ctrl Pts',(11.968544622494,0.0825923743414284,4.48485433333386));
#24109=CARTESIAN_POINT('Ctrl Pts',(12.0162604585568,-0.363153170675764,
4.33170016502878));
#24110=CARTESIAN_POINT('Ctrl Pts',(12.0639762946196,-0.475409571231627,
3.87394063131468));
#24111=CARTESIAN_POINT('Ctrl Pts',(12.1116921306825,-0.151090047408964,
3.53194335553704));
#24112=CARTESIAN_POINT('Ctrl Pts',(12.1594079667453,0.311977791768556,3.61976969834691));
#24113=CARTESIAN_POINT('Ctrl Pts',(12.2071238028081,0.488551624369653,4.05676737776005));
#24114=CARTESIAN_POINT('Ctrl Pts',(12.254839638871,0.216480982979095,4.44163470069774));
#24115=CARTESIAN_POINT('Ctrl Pts',(12.3025554749338,-0.254387476069249,
4.42094208256136));
#24116=CARTESIAN_POINT('Ctrl Pts',(12.3502713109967,-0.49164800158875,4.0136918729824));
#24117=CARTESIAN_POINT('Ctrl Pts',(12.3979871470595,-0.277420602272412,
3.59386820576715));
#24118=CARTESIAN_POINT('Ctrl Pts',(12.4457029831224,0.191566404775332,3.54700161433684));
#24119=CARTESIAN_POINT('Ctrl Pts',(12.4934188191852,0.484635034689867,3.91613041073711));
#24120=CARTESIAN_POINT('Ctrl Pts',(12.541134655248,0.332655855180181,4.362277941457));
#24121=CARTESIAN_POINT('Ctrl Pts',(12.5888504913109,-0.124806314709729,
4.47574006417428));
#24122=CARTESIAN_POINT('Ctrl Pts',(12.6365663273737,-0.4676569254097,4.15232276575852));
#24123=CARTESIAN_POINT('Ctrl Pts',(12.6842821634365,-0.381050985679211,
3.68902512775968));
#24124=CARTESIAN_POINT('Ctrl Pts',(12.7319979994994,0.0554799374235607,
3.5113004999026));
#24125=CARTESIAN_POINT('Ctrl Pts',(12.7797138355622,0.441062780321708,3.78235614259331));
#24126=CARTESIAN_POINT('Ctrl Pts',(12.8274296716251,0.421610885427219,4.2532774884218));
#24127=CARTESIAN_POINT('Ctrl Pts',(12.8751455076879,0.0149872271275763,
4.49161021945745));
#24128=CARTESIAN_POINT('Ctrl Pts',(12.9228613437507,-0.405399432451448,
4.27848972156979));
#24129=CARTESIAN_POINT('Ctrl Pts',(12.9705771798136,-0.453501555338242,
3.80962782724943));
#24130=CARTESIAN_POINT('Ctrl Pts',(13.0182930158764,-0.0851462219395619,
3.51558762841831));
#24131=CARTESIAN_POINT('Ctrl Pts',(13.0660088519392,0.361400197209248,3.66639076405307));
#24132=CARTESIAN_POINT('Ctrl Pts',(13.1137246880021,0.476067254403989,4.1235523942958));
#24133=CARTESIAN_POINT('Ctrl Pts',(13.1614405240649,0.153554426643267,4.46725395975876));
#24134=CARTESIAN_POINT('Ctrl Pts',(13.2091563601278,-0.30996979384252,4.38186902434892));
#24135=CARTESIAN_POINT('Ctrl Pts',(13.2568721961906,-0.488843983144383,
3.94580788806928));
#24136=CARTESIAN_POINT('Ctrl Pts',(13.3045880322534,-0.218805220893238,
3.55951220202843));
#24137=CARTESIAN_POINT('Ctrl Pts',(13.3523038683163,0.252165742455243,3.57772323864086));
#24138=CARTESIAN_POINT('Ctrl Pts',(13.4000197043791,0.491569024438394,3.98371752277252));
#24139=CARTESIAN_POINT('Ctrl Pts',(13.447735540442,0.279556907518101,4.40466425628032));
#24140=CARTESIAN_POINT('Ctrl Pts',(13.4954513765048,-0.189176619112,4.45400157668594));
#24141=CARTESIAN_POINT('Ctrl Pts',(13.5431672125676,-0.484186345555107,
4.08642226350871));
#24142=CARTESIAN_POINT('Ctrl Pts',(13.5908830486304,-0.334560300710407,
3.63948005597396));
#24143=CARTESIAN_POINT('Ctrl Pts',(13.6385988846933,0.122297616148583,3.52360886035071));
#24144=CARTESIAN_POINT('Ctrl Pts',(13.6863147207561,0.466847750307624,3.8452149784873));
#24145=CARTESIAN_POINT('Ctrl Pts',(13.734030556819,0.3826844119832,4.30896256355269));
#24146=CARTESIAN_POINT('Ctrl Pts',(13.7817463928818,-0.0529039102219543,
4.48898507250754));
#24147=CARTESIAN_POINT('Ctrl Pts',(13.8294622289446,-0.439909757638992,
4.21996506537626));
#24148=CARTESIAN_POINT('Ctrl Pts',(13.8771780650075,-0.422939705734467,
3.74894775411238));
#24149=CARTESIAN_POINT('Ctrl Pts',(13.9248939010703,-0.0175776142901187,
3.50847558318244));
#24150=CARTESIAN_POINT('Ctrl Pts',(13.9726097371332,0.403926270823208,3.71937784729135));
#24151=CARTESIAN_POINT('Ctrl Pts',(14.020325573196,0.454498446235019,4.18797975215946));
#24152=CARTESIAN_POINT('Ctrl Pts',(14.0680414092588,0.0876977051117048,
4.48395695817926));
#24153=CARTESIAN_POINT('Ctrl Pts',(14.1157572453217,-0.359637188018331,
4.33550904286807));
#24154=CARTESIAN_POINT('Ctrl Pts',(14.1634730813845,-0.476711717661702,
3.87895801102093));
#24155=CARTESIAN_POINT('Ctrl Pts',(14.2111889174473,-0.156014541823709,
3.53356170012368));
#24156=CARTESIAN_POINT('Ctrl Pts',(14.2589047535102,0.307953188363286,3.61650285707861));
#24157=CARTESIAN_POINT('Ctrl Pts',(14.306620589573,0.4891227672074,4.05161534124029));
#24158=CARTESIAN_POINT('Ctrl Pts',(14.3543364256359,0.2211233828038,4.4393286633369));
#24159=CARTESIAN_POINT('Ctrl Pts',(14.4020522616987,-0.249937006449114,
4.42359971395084));
#24160=CARTESIAN_POINT('Ctrl Pts',(14.4497680977616,-0.491476396904638,
4.01887262932433));
#24161=CARTESIAN_POINT('Ctrl Pts',(14.4974839338244,-0.281685449746218,
3.59681451879656));
#24162=CARTESIAN_POINT('Ctrl Pts',(14.5451997698872,0.186781580201919,3.54500783946397));
#24163=CARTESIAN_POINT('Ctrl Pts',(14.59291560595,0.483724211046603,3.91102746210588));
#24164=CARTESIAN_POINT('Ctrl Pts',(14.6406314420129,0.33645545583349,4.35875193531444));
#24165=CARTESIAN_POINT('Ctrl Pts',(14.6883472780757,-0.119785521504147,
4.47702898621568));
#24166=CARTESIAN_POINT('Ctrl Pts',(14.7360631141386,-0.466025611307368,
4.15724297904063));
#24167=CARTESIAN_POINT('Ctrl Pts',(14.7837789502014,-0.38430721152129,3.69305832471834));
#24168=CARTESIAN_POINT('Ctrl Pts',(14.8314947862642,0.0503264139313189,
3.51074293371195));
#24169=CARTESIAN_POINT('Ctrl Pts',(14.8792106223271,0.438744519099385,3.77771983486548));
#24170=CARTESIAN_POINT('Ctrl Pts',(14.9269264583899,0.42425678142631,4.24882003188202));
#24171=CARTESIAN_POINT('Ctrl Pts',(14.9746422944528,0.0201675133397715,
4.49142496503298));
#24172=CARTESIAN_POINT('Ctrl Pts',(15.0223581305156,-0.402441892563756,
4.28274679124913));
#24173=CARTESIAN_POINT('Ctrl Pts',(15.0700739665785,-0.455482716161518,
3.8144178884426));
#24174=CARTESIAN_POINT('Ctrl Pts',(15.1177898026413,-0.0902467530057116,
3.51651189422706));
#24175=CARTESIAN_POINT('Ctrl Pts',(15.1655056387041,0.357864192060027,3.66260046696357));
#24176=CARTESIAN_POINT('Ctrl Pts',(15.2132214747669,0.47734294310866,4.11852822244656));
#24177=CARTESIAN_POINT('Ctrl Pts',(15.2609373108298,0.15847032463534,4.46560968746574));
#24178=CARTESIAN_POINT('Ctrl Pts',(15.3086531468926,-0.305928031329979,
4.38511461215921));
#24179=CARTESIAN_POINT('Ctrl Pts',(15.3563689829555,-0.489387968817152,
3.95096286275689));
#24180=CARTESIAN_POINT('Ctrl Pts',(15.4040848190183,-0.223435404337718,
3.56184267101825));
#24181=CARTESIAN_POINT('Ctrl Pts',(15.4518006550811,0.24770132994065,3.57508909640066));
#24182=CARTESIAN_POINT('Ctrl Pts',(15.499516491144,0.491370121559653,3.97853774265298));
#24183=CARTESIAN_POINT('Ctrl Pts',(15.5472323272068,0.283806169849271,4.40169551006635));
#24184=CARTESIAN_POINT('Ctrl Pts',(15.5949481632697,-0.184381354552937,
4.4559701097059));
#24185=CARTESIAN_POINT('Ctrl Pts',(15.6426639993325,-0.483248643997369,
4.09152034160055));
#24186=CARTESIAN_POINT('Ctrl Pts',(15.6903798353953,-0.338341267922855,
3.64302603558196));
#24187=CARTESIAN_POINT('Ctrl Pts',(15.7380956714582,0.117270100534806,3.52234641383892));
#24188=CARTESIAN_POINT('Ctrl Pts',(15.785811507521,0.465190531238913,3.84030342991275));
#24189=CARTESIAN_POINT('Ctrl Pts',(15.8335273435838,0.385919339229949,4.30491226354526));
#24190=CARTESIAN_POINT('Ctrl Pts',(15.8812431796467,-0.0477475201261761,
4.48951547388594));
#24191=CARTESIAN_POINT('Ctrl Pts',(15.9289590157095,-0.437567097060412,
4.22458909239344));
#24192=CARTESIAN_POINT('Ctrl Pts',(15.9766748517724,-0.425562075928853,
3.75341909160864));
#24193=CARTESIAN_POINT('Ctrl Pts',(16.0243906878352,-0.0227568523576073,
3.50868813313462));
#24194=CARTESIAN_POINT('Ctrl Pts',(16.072106523898,0.400946338892803,3.71513642180785));
#24195=CARTESIAN_POINT('Ctrl Pts',(16.1198223599609,0.456454337785543,4.1831793175245));
#24196=CARTESIAN_POINT('Ctrl Pts',(16.1675381960237,0.0927932948370443,
4.4830058273823));
#24197=CARTESIAN_POINT('Ctrl Pts',(16.2152540320865,-0.356081258568678,
4.33928065395499));
#24198=CARTESIAN_POINT('Ctrl Pts',(16.2629698681494,-0.477960913216358,
3.88398883549692));
#24199=CARTESIAN_POINT('Ctrl Pts',(16.3106857042122,-0.160921706883503,
3.53523185446324));
#24200=CARTESIAN_POINT('Ctrl Pts',(16.358401540275,0.303894378979202,3.6132786128531));
#24201=CARTESIAN_POINT('Ctrl Pts',(16.4061173763379,0.489639580609251,4.04645757153336));
#24202=CARTESIAN_POINT('Ctrl Pts',(16.4538332124007,0.225741221292456,4.43697382743292));
#24203=CARTESIAN_POINT('Ctrl Pts',(16.5015490484636,-0.245458775012363,
4.42621029389423));
#24204=CARTESIAN_POINT('Ctrl Pts',(16.5492648845264,-0.4912502013546,4.02405128938415));
#24205=CARTESIAN_POINT('Ctrl Pts',(16.5969807205893,-0.285919008936969,
3.59980561575594));
#24206=CARTESIAN_POINT('Ctrl Pts',(16.6446965566521,0.181976008816936,3.54306460296116));
#24207=CARTESIAN_POINT('Ctrl Pts',(16.6924123927149,0.482759657613431,3.90593439612197));
#24208=CARTESIAN_POINT('Ctrl Pts',(16.7401282287778,0.340217684611379,4.35518608070932));
#24209=CARTESIAN_POINT('Ctrl Pts',(16.7878440648406,-0.114751423091257,
4.47826492214097));
#24210=CARTESIAN_POINT('Ctrl Pts',(16.8355599009034,-0.464342533291602,
4.16214572651883));
#24211=CARTESIAN_POINT('Ctrl Pts',(16.8832757369663,-0.387520750342007,
3.69712561530174));
#24212=CARTESIAN_POINT('Ctrl Pts',(16.9309915730291,0.0451673004198413,
3.51023971187451));
#24213=CARTESIAN_POINT('Ctrl Pts',(16.978707409092,0.436377524217892,3.7731082169636));
#24214=CARTESIAN_POINT('Ctrl Pts',(17.0264232451548,0.426855552995382,4.24433493759383));
#24215=CARTESIAN_POINT('Ctrl Pts',(17.0741390812176,0.0253455594402812,
4.49118512545541));
#24216=CARTESIAN_POINT('Ctrl Pts',(17.1218549172805,-0.399439651340385,
4.28697245475663));
#24217=CARTESIAN_POINT('Ctrl Pts',(17.1695707533433,-0.457413284126125,
3.81922856321607));
#24218=CARTESIAN_POINT('Ctrl Pts',(17.2172865894061,-0.0953372598908034,
3.51748986360026));
#24219=CARTESIAN_POINT('Ctrl Pts',(17.265002425469,0.354288437054553,3.6588476466131));
#24220=CARTESIAN_POINT('Ctrl Pts',(17.3127182615318,0.478565610824392,4.11349088504481));
#24221=CARTESIAN_POINT('Ctrl Pts',(17.3604340975947,0.163368620495752,4.46391369745815));
#24222=CARTESIAN_POINT('Ctrl Pts',(17.4081499336575,-0.301852287783465,
4.38831742326589));
#24223=CARTESIAN_POINT('Ctrl Pts',(17.4558657697204,-0.489877595596684,
3.956123284257));
#24224=CARTESIAN_POINT('Ctrl Pts',(17.5035816057832,-0.228040769637767,
3.56422180844494));
#24225=CARTESIAN_POINT('Ctrl Pts',(17.551297441846,0.243209403937772,3.57250215124727));
#24226=CARTESIAN_POINT('Ctrl Pts',(17.5990132779089,0.491116639619549,3.97336034645914));
#24227=CARTESIAN_POINT('Ctrl Pts',(17.6467291139717,0.288023908337871,4.39868214542132));
#24228=CARTESIAN_POINT('Ctrl Pts',(17.6944449500345,-0.179565609787963,
4.45788799572981));
#24229=CARTESIAN_POINT('Ctrl Pts',(17.7421607860973,-0.48225726547346,4.09660825404716));
#24230=CARTESIAN_POINT('Ctrl Pts',(17.7898766221602,-0.342084653792828,
3.64661166616396));
#24231=CARTESIAN_POINT('Ctrl Pts',(17.837592458223,0.112229559114723,3.52113702282083));
#24232=CARTESIAN_POINT('Ctrl Pts',(17.8853082942859,0.463481641013499,3.83540961967535));
#24233=CARTESIAN_POINT('Ctrl Pts',(17.9330241303487,0.389111400387848,4.30082809533052));
#24234=CARTESIAN_POINT('Ctrl Pts',(17.9807399664116,-0.0425858264624495,
4.48999150220845));
#24235=CARTESIAN_POINT('Ctrl Pts',(18.0284558024744,-0.435175833605105,
4.22918817311999));
#24236=CARTESIAN_POINT('Ctrl Pts',(18.0761716385373,-0.428137176707308,
3.75791781814212));
#24237=CARTESIAN_POINT('Ctrl Pts',(18.1238874746,-0.0279335627019553,3.5089552556775));
#24238=CARTESIAN_POINT('Ctrl Pts',(18.1716033106629,0.397921871745719,3.71092663761881));
#24239=CARTESIAN_POINT('Ctrl Pts',(18.2193191467257,0.458359528554279,4.17835853620019));
#24240=CARTESIAN_POINT('Ctrl Pts',(18.2670349827886,0.097878577523561,4.48200104659009));
#24241=CARTESIAN_POINT('Ctrl Pts',(18.3147508188514,-0.352485777302551,
4.34301457935691));
#24242=CARTESIAN_POINT('Ctrl Pts',(18.3624666549143,-0.479157019140895,
3.88903254594255));
#24243=CARTESIAN_POINT('Ctrl Pts',(18.4101824909771,-0.165810997523729,
3.5369536330429));
#24244=CARTESIAN_POINT('Ctrl Pts',(18.4578983270399,0.299801814449608,3.61009732380414));
#24245=CARTESIAN_POINT('Ctrl Pts',(18.5056141631028,0.49010200717001,4.04129464153984));
#24246=CARTESIAN_POINT('Ctrl Pts',(18.5533299991656,0.230333985517487,4.43457045454981));
#24247=CARTESIAN_POINT('Ctrl Pts',(18.6010458352284,-0.24095327917969,4.42877353242069));
#24248=CARTESIAN_POINT('Ctrl Pts',(18.6487616712913,-0.49096944006335,4.0292272779409));
#24249=CARTESIAN_POINT('Ctrl Pts',(18.6964775073541,-0.290120809601049,
3.60284116440841));
#24250=CARTESIAN_POINT('Ctrl Pts',(18.744193343417,0.177150224400508,3.54117212067402));
#24251=CARTESIAN_POINT('Ctrl Pts',(18.7919091794797,0.481741481528227,3.90085177849878));
#24252=CARTESIAN_POINT('Ctrl Pts',(18.8396250155427,0.343942123623612,4.35158077372017));
#24253=CARTESIAN_POINT('Ctrl Pts',(18.8873408516054,-0.109704578635382,
4.47944773466767));
#24254=CARTESIAN_POINT('Ctrl Pts',(18.9350566876684,-0.462607878309702,
4.16703046362027));
#24255=CARTESIAN_POINT('Ctrl Pts',(18.9827725237311,-0.39069124519864,3.70122654773242));
#24256=CARTESIAN_POINT('Ctrl Pts',(19.030488359794,0.0400031699426168,3.50979089028978));
#24257=CARTESIAN_POINT('Ctrl Pts',(19.0782041958568,0.433962058584907,3.76852180111673));
#24258=CARTESIAN_POINT('Ctrl Pts',(19.1259200319197,0.429406911488226,4.23982270375453));
#24259=CARTESIAN_POINT('Ctrl Pts',(19.1736358679825,0.0305207902517796,
4.49089072733801));
#24260=CARTESIAN_POINT('Ctrl Pts',(19.2213517040454,-0.396393042209671,
4.29116624277653));
#24261=CARTESIAN_POINT('Ctrl Pts',(19.2690675401082,-0.459293044881286,
3.82405931712685));
#24262=CARTESIAN_POINT('Ctrl Pts',(19.316783376171,-0.100417177000157,3.51852142809106));
#24263=CARTESIAN_POINT('Ctrl Pts',(19.3644992122339,0.350673329058588,3.65513271950473));
#24264=CARTESIAN_POINT('Ctrl Pts',(19.4122150482967,0.479735122332443,4.10844094226069));
#24265=CARTESIAN_POINT('Ctrl Pts',(19.4599308843596,0.168248769032157,4.46216617689766));
#24266=CARTESIAN_POINT('Ctrl Pts',(19.5076467204224,-0.297743013815871,
4.39147710422109));
#24267=CARTESIAN_POINT('Ctrl Pts',(19.5553625564852,-0.490312813065352,
3.96128857502183));
#24268=CARTESIAN_POINT('Ctrl Pts',(19.603078392548,-0.232620797759261,3.56664935826393));
#24269=CARTESIAN_POINT('Ctrl Pts',(19.6507942286109,0.238690449241969,3.56996267500769));
#24270=CARTESIAN_POINT('Ctrl Pts',(19.6985100646737,0.490808633485035,3.96818593857384));
#24271=CARTESIAN_POINT('Ctrl Pts',(19.7462259007366,0.292209604061002,4.39562444172689));
#24272=CARTESIAN_POINT('Ctrl Pts',(19.7939417367994,-0.174729824492781,
4.45975512619968));
#24273=CARTESIAN_POINT('Ctrl Pts',(19.8416575728622,-0.481212499922896,
4.10168523844358));
#24274=CARTESIAN_POINT('Ctrl Pts',(19.8893734089251,-0.345789702982467,
3.65023692191923));
#24275=CARTESIAN_POINT('Ctrl Pts',(19.9370892449879,0.107175910646637,3.51998011832295));
#24276=CARTESIAN_POINT('Ctrl Pts',(19.9848050810508,0.461722480014006,3.83053541934297));
#24277=CARTESIAN_POINT('Ctrl Pts',(20.0325209171136,0.392257955100357,4.29670800504879));
#24278=CARTESIAN_POINT('Ctrl Pts',(20.0802367531764,-0.0374150865130887,
4.49041783929577));
#24279=CARTESIAN_POINT('Ctrl Pts',(20.1279525892393,-0.432744382500041,
4.23375285658289));
#24280=CARTESIAN_POINT('Ctrl Pts',(20.1756684253021,-0.430649333670284,
3.76246031529274));
#24281=CARTESIAN_POINT('Ctrl Pts',(20.223384261365,-0.033136228617316,3.50924504180455));
#24282=CARTESIAN_POINT('Ctrl Pts',(20.2711000974278,0.394908089060633,3.70680919012016));
#24283=CARTESIAN_POINT('Ctrl Pts',(20.3188159334906,0.460110046434968,4.17340395051402));
#24284=CARTESIAN_POINT('Ctrl Pts',(20.3665317695535,0.103149962306437,4.48116018402389));
#24285=CARTESIAN_POINT('Ctrl Pts',(20.4142476056163,-0.34923165553999,4.34628168153608));
#24286=CARTESIAN_POINT('Ctrl Pts',(20.4540108023354,-0.457800032585507,
3.97025345815189));
#24287=CARTESIAN_POINT('Ctrl Pts',(20.4858213597105,-0.325993724402262,
3.71529210935379));
#24288=CARTESIAN_POINT('Ctrl Pts',(20.509679277742,-0.15096738523986,3.59329490328468));
#24289=CARTESIAN_POINT('Ctrl Pts',(20.5335371957734,0.0630371972956549,
3.57102347342756));
#24290=CARTESIAN_POINT('Ctrl Pts',(20.5573951138048,0.260511246441404,3.65349437971329));
#24291=CARTESIAN_POINT('Ctrl Pts',(20.5812530318362,0.394877283734959,3.82077798440408));
#24292=CARTESIAN_POINT('Ctrl Pts',(20.6051109498677,0.432370081305563,4.03184236506754));
#24293=CARTESIAN_POINT('Ctrl Pts',(20.6289688678991,0.364303478986858,4.23514367899931));
#24294=CARTESIAN_POINT('Ctrl Pts',(20.6528267859305,0.207066376217976,4.38093363836299));
#24295=CARTESIAN_POINT('Ctrl Pts',(20.6766847039619,-0.000757290757721993,
4.43358147160167));
#24296=CARTESIAN_POINT('Ctrl Pts',(20.7005426219933,-0.208420567790133,
4.38020336888205));
#24297=CARTESIAN_POINT('Ctrl Pts',(20.7244005400248,-0.365106210756856,
4.23385701605743));
#24298=CARTESIAN_POINT('Ctrl Pts',(20.7482584580562,-0.432520392530856,
4.03032528343114));
#24299=CARTESIAN_POINT('Ctrl Pts',(20.7721163760876,-0.394167874571092,
3.81937870627435));
#24300=CARTESIAN_POINT('Ctrl Pts',(20.795974294119,-0.259432524437891,3.65259868360638));
#24301=CARTESIAN_POINT('Ctrl Pts',(20.8198322121504,-0.0612578225112809,
3.57076788979259));
#24302=CARTESIAN_POINT('Ctrl Pts',(20.8436901301819,0.151895538690754,3.5938959627232));
#24303=CARTESIAN_POINT('Ctrl Pts',(20.8675480482132,0.327906592802717,3.71632757520176));
#24304=CARTESIAN_POINT('Ctrl Pts',(20.8914059662447,0.423735399567132,3.90812480123879));
#24305=CARTESIAN_POINT('Ctrl Pts',(20.9152638842761,0.415949440063929,4.12238802732943));
#24306=CARTESIAN_POINT('Ctrl Pts',(20.9391218023075,0.30645246920106,4.30672404095661));
#24307=CARTESIAN_POINT('Ctrl Pts',(20.962979720339,0.122019544809087,4.41605767475162));
#24308=CARTESIAN_POINT('Ctrl Pts',(20.9868376383703,-0.0922504941031022,
4.42365387220386));
#24309=CARTESIAN_POINT('Ctrl Pts',(21.0106955564018,-0.28396276796243,4.32765515869354));
#24310=CARTESIAN_POINT('Ctrl Pts',(21.0345534744332,-0.40623841344949,4.15153583326342));
#24311=CARTESIAN_POINT('Ctrl Pts',(21.0584113924646,-0.429177699343215,
3.93836186909709));
#24312=CARTESIAN_POINT('Ctrl Pts',(21.082269310496,-0.347171348131155,3.74026010679315));
#24313=CARTESIAN_POINT('Ctrl Pts',(21.1061272285274,-0.180272145040548,
3.605671823621));
#24314=CARTESIAN_POINT('Ctrl Pts',(21.1299851465589,0.0307085077608185,
3.56750752082027));
#24315=CARTESIAN_POINT('Ctrl Pts',(21.1538430645903,0.234180094072738,3.63509941005724));
#24316=CARTESIAN_POINT('Ctrl Pts',(21.1777009826217,0.380388268371489,3.79191943321731));
#24317=CARTESIAN_POINT('Ctrl Pts',(21.2015589006531,0.433581149524578,3.99962082296209));
#24318=CARTESIAN_POINT('Ctrl Pts',(21.2254168186846,0.380751629084578,4.2074149318183));
#24319=CARTESIAN_POINT('Ctrl Pts',(21.2492747367159,0.234817963878357,4.36449043997717));
#24320=CARTESIAN_POINT('Ctrl Pts',(21.2731326547474,0.0314649101850846,
4.43243810704058));
#24321=CARTESIAN_POINT('Ctrl Pts',(21.2969905727788,-0.179582171132277,
4.39464287755545));
#24322=CARTESIAN_POINT('Ctrl Pts',(21.3208484908102,-0.346716519889314,
4.26034671465164));
#24323=CARTESIAN_POINT('Ctrl Pts',(21.3447064088417,-0.429069235164158,
4.0623886883135));
#24324=CARTESIAN_POINT('Ctrl Pts',(21.368564326873,-0.406502834830527,3.8491749282489));
#24325=CARTESIAN_POINT('Ctrl Pts',(21.3924222449045,-0.284535418465691,
3.67284200661995));
#24326=CARTESIAN_POINT('Ctrl Pts',(21.4162801629359,-0.0929913416969399,
3.5765081259772));
#24327=CARTESIAN_POINT('Ctrl Pts',(21.4401380809674,0.121291651150069,3.58372954422009));
#24328=CARTESIAN_POINT('Ctrl Pts',(21.4639959989987,0.305915531372611,3.69274042788069));
#24329=CARTESIAN_POINT('Ctrl Pts',(21.4878539170302,0.415734731202803,3.87688464650718));
#24330=CARTESIAN_POINT('Ctrl Pts',(21.5117118350615,0.423895464867194,4.09113392265755));
#24331=CARTESIAN_POINT('Ctrl Pts',(21.535569753093,0.328402210690932,4.28309847227994));
#24332=CARTESIAN_POINT('Ctrl Pts',(21.5594276711244,0.152605670504114,4.40583773398234));
#24333=CARTESIAN_POINT('Ctrl Pts',(21.5832855891559,-0.0605071130159612,
4.42933861492812));
#24334=CARTESIAN_POINT('Ctrl Pts',(21.6071435071872,-0.258824259222961,
4.34785450957493));
#24335=CARTESIAN_POINT('Ctrl Pts',(21.6310014252187,-0.39385182381868,4.18131050126406));
#24336=CARTESIAN_POINT('Ctrl Pts',(21.6548593432501,-0.432571889182456,
3.97043113659525));
#24337=CARTESIAN_POINT('Ctrl Pts',(21.6787172612815,-0.365516344619441,
3.76678216446856));
#24338=CARTESIAN_POINT('Ctrl Pts',(21.702575179313,-0.209082097331647,3.62016130585559));
#24339=CARTESIAN_POINT('Ctrl Pts',(21.7264330973443,-0.00152158196427748,
3.56642135455923));
#24340=CARTESIAN_POINT('Ctrl Pts',(21.7502910153758,0.206411001640417,3.61870319251831));
#24341=CARTESIAN_POINT('Ctrl Pts',(21.7741489334072,0.363870472821225,3.76422248622317));
#24342=CARTESIAN_POINT('Ctrl Pts',(21.7980068514386,0.432353701764573,3.96739580449697));
#24343=CARTESIAN_POINT('Ctrl Pts',(21.82186476947,0.395114673548107,4.17854173669174));
#24344=CARTESIAN_POINT('Ctrl Pts',(21.8457226875014,0.261259344941517,4.3460293508861));
#24345=CARTESIAN_POINT('Ctrl Pts',(21.8695806055329,0.0635189899350569,
4.42890336313855));
#24346=CARTESIAN_POINT('Ctrl Pts',(21.8934385235643,-0.14975348833307,4.40689882001058));
#24347=CARTESIAN_POINT('Ctrl Pts',(21.9172964415957,-0.326407159500644,
4.28539643168872));
#24348=CARTESIAN_POINT('Ctrl Pts',(21.9411543596271,-0.423245389017799,
4.09410684177624));
#24349=CARTESIAN_POINT('Ctrl Pts',(21.9650122776585,-0.416588591947193,
3.87980556563057));
#24350=CARTESIAN_POINT('Ctrl Pts',(21.98887019569,-0.30806453650007,3.69489510271888));
#24351=CARTESIAN_POINT('Ctrl Pts',(22.0127281137213,-0.12421031036921,3.58459109808296));
#24352=CARTESIAN_POINT('Ctrl Pts',(22.0365860317528,0.0900167200678817,
3.57586588547707));
#24353=CARTESIAN_POINT('Ctrl Pts',(22.0604439497842,0.282232210442068,3.67085301705332));
#24354=CARTESIAN_POINT('Ctrl Pts',(22.0843018678157,0.405434237512275,3.8463255517439));
#24355=CARTESIAN_POINT('Ctrl Pts',(22.108159785847,0.429496549703537,4.05937567504088));
#24356=CARTESIAN_POINT('Ctrl Pts',(22.1320177038785,0.348535256241736,4.25790682842971));
#24357=CARTESIAN_POINT('Ctrl Pts',(22.1558756219099,0.182347598717988,4.39337273702606));
#24358=CARTESIAN_POINT('Ctrl Pts',(22.1797335399413,-0.0284290137391457,
4.43264829616218));
#24359=CARTESIAN_POINT('Ctrl Pts',(22.2035914579727,-0.232253957950086,
4.36612956178204));
#24360=CARTESIAN_POINT('Ctrl Pts',(22.2274493760041,-0.379286482964224,
4.21008217638027));
#24361=CARTESIAN_POINT('Ctrl Pts',(22.2513072940356,-0.433573131350875,
4.00266397632408));
#24362=CARTESIAN_POINT('Ctrl Pts',(22.275165212067,-0.381839338801546,3.79459436150246));
#24363=CARTESIAN_POINT('Ctrl Pts',(22.2990231300984,-0.236735426869051,
3.63675202040985));
#24364=CARTESIAN_POINT('Ctrl Pts',(22.3228810481298,-0.0337432544318164,
3.56773370504276));
#24365=CARTESIAN_POINT('Ctrl Pts',(22.3467389661613,0.177500062688638,3.60441627341574));
#24366=CARTESIAN_POINT('Ctrl Pts',(22.3705968841926,0.345339779804043,3.73782983856348));
#24367=CARTESIAN_POINT('Ctrl Pts',(22.3944548022241,0.428734513273282,3.93535114928888));
#24368=CARTESIAN_POINT('Ctrl Pts',(22.4183127202555,0.407291980919218,4.1486808655136));
#24369=CARTESIAN_POINT('Ctrl Pts',(22.4421706382869,0.286255462618544,4.32565405918856));
#24370=CARTESIAN_POINT('Ctrl Pts',(22.4660285563183,0.0952216904214238,
4.42299596654013));
#24371=CARTESIAN_POINT('Ctrl Pts',(22.4898864743497,-0.119096386717928,
4.41690383452019));
#24372=CARTESIAN_POINT('Ctrl Pts',(22.5137443923812,-0.304292138366774,
4.30886736509782));
#24373=CARTESIAN_POINT('Ctrl Pts',(22.5376023104126,-0.415080201412036,
4.12530439950267));
#24374=CARTESIAN_POINT('Ctrl Pts',(22.561460228444,-0.424369795825249,3.91110111771763));
#24375=CARTESIAN_POINT('Ctrl Pts',(22.5853181464754,-0.329889515310188,
3.71863599132299));
#24376=CARTESIAN_POINT('Ctrl Pts',(22.6091760645068,-0.154742073939436,
3.59497211022641));
#24377=CARTESIAN_POINT('Ctrl Pts',(22.6330339825383,0.0582436639512456,
3.57034842802071));
#24378=CARTESIAN_POINT('Ctrl Pts',(22.6568919005697,0.256987911016647,3.65078654733876));
#24379=CARTESIAN_POINT('Ctrl Pts',(22.6807498186011,0.39289034562191,3.81661632308649));
#24380=CARTESIAN_POINT('Ctrl Pts',(22.7046077366325,0.432722782933869,4.02728943245291));
#24381=CARTESIAN_POINT('Ctrl Pts',(22.7284656546639,0.366738191089385,4.2312875884069));
#24382=CARTESIAN_POINT('Ctrl Pts',(22.7523235726953,0.211084664509997,4.37873330099785));
#24383=CARTESIAN_POINT('Ctrl Pts',(22.7761814907268,0.00379901600965994,
4.43356145647204));
#24384=CARTESIAN_POINT('Ctrl Pts',(22.8000394087582,-0.204384723485633,
4.3823852668741));
#24385=CARTESIAN_POINT('Ctrl Pts',(22.8238973267896,-0.36265185203719,4.2376794731));
#24386=CARTESIAN_POINT('Ctrl Pts',(22.8398026054772,-0.408954280604672,
4.10250106973657));
#24387=CARTESIAN_POINT('Ctrl Pts',(22.847755244821,-0.414526965927561,4.03345758723954));
#24388=CARTESIAN_POINT('',(22.8,-0.592174260192535,4.04779597854866));
#24389=CARTESIAN_POINT('Ctrl Pts',(22.8,-0.19576256658266,4.36695865185836));
#24390=CARTESIAN_POINT('Ctrl Pts',(22.8,-0.195886593570853,4.36694806728808));
#24391=CARTESIAN_POINT('Ctrl Pts',(22.8,-0.196010613870461,4.36693742279878));
#24392=CARTESIAN_POINT('Ctrl Pts',(22.8,-0.196134627427637,4.36692671841166));
#24393=CARTESIAN_POINT('Ctrl Pts',(22.8,-0.216622178843513,4.36515830948628));
#24394=CARTESIAN_POINT('Ctrl Pts',(22.8,-0.236921239981942,4.36175743074964));
#24395=CARTESIAN_POINT('Ctrl Pts',(22.8,-0.256857422940798,4.35688458679081));
#24396=CARTESIAN_POINT('Ctrl Pts',(22.8,-0.271809560159941,4.35322995382169));
#24397=CARTESIAN_POINT('Ctrl Pts',(22.8,-0.286558947067823,4.34874691155445));
#24398=CARTESIAN_POINT('Ctrl Pts',(22.8,-0.301048271828705,4.34349077646485));
#24399=CARTESIAN_POINT('Ctrl Pts',(22.8,-0.310003423377303,4.3402422133286));
#24400=CARTESIAN_POINT('Ctrl Pts',(22.8,-0.318859482942331,4.33669811041118));
#24401=CARTESIAN_POINT('Ctrl Pts',(22.8,-0.327604744452034,4.33286912874946));
#24402=CARTESIAN_POINT('Ctrl Pts',(22.8,-0.333457186121174,4.33030672489195));
#24403=CARTESIAN_POINT('Ctrl Pts',(22.8,-0.33926207870774,4.32761569029118));
#24404=CARTESIAN_POINT('Ctrl Pts',(22.8,-0.345009487597299,4.32480202294401));
#24405=CARTESIAN_POINT('Ctrl Pts',(22.8,-0.365309066997251,4.31486428146495));
#24406=CARTESIAN_POINT('Ctrl Pts',(22.8,-0.384828901796994,4.30343044333042));
#24407=CARTESIAN_POINT('Ctrl Pts',(22.8,-0.403416958856431,4.29067119823496));
#24408=CARTESIAN_POINT('Ctrl Pts',(22.8,-0.409874425773003,4.28623865303559));
#24409=CARTESIAN_POINT('Ctrl Pts',(22.8,-0.416219739836017,4.28164578247975));
#24410=CARTESIAN_POINT('Ctrl Pts',(22.8,-0.422447327171508,4.27689854297234));
#24411=CARTESIAN_POINT('Ctrl Pts',(22.8,-0.43500295340691,4.2673274905416));
#24412=CARTESIAN_POINT('Ctrl Pts',(22.8,-0.447079966647781,4.25712966465555));
#24413=CARTESIAN_POINT('Ctrl Pts',(22.8,-0.458660056443695,4.24636133358853));
#24414=CARTESIAN_POINT('Ctrl Pts',(22.8,-0.465333929961841,4.24015529539631));
#24415=CARTESIAN_POINT('Ctrl Pts',(22.8,-0.471842796551704,4.23375955955572));
#24416=CARTESIAN_POINT('Ctrl Pts',(22.8,-0.478183280583292,4.22718326898633));
#24417=CARTESIAN_POINT('Ctrl Pts',(22.8,-0.48330469601013,4.22187138494));
#24418=CARTESIAN_POINT('Ctrl Pts',(22.8,-0.488310096860405,4.21644792156372));
#24419=CARTESIAN_POINT('Ctrl Pts',(22.8,-0.49319389770791,4.21092357737429));
#24420=CARTESIAN_POINT('Ctrl Pts',(22.8,-0.509882204568999,4.19204648678071));
#24421=CARTESIAN_POINT('Ctrl Pts',(22.8,-0.525164669297395,4.17198027236651));
#24422=CARTESIAN_POINT('Ctrl Pts',(22.8,-0.538985569877159,4.15095378743758));
#24423=CARTESIAN_POINT('Ctrl Pts',(22.8,-0.553292287721507,4.12918820238033));
#24424=CARTESIAN_POINT('Ctrl Pts',(22.8,-0.566034197593199,4.10639346234103));
#24425=CARTESIAN_POINT('Ctrl Pts',(22.8,-0.577149101532509,4.08276767497818));
#24426=CARTESIAN_POINT('Ctrl Pts',(22.8,-0.582543745751794,4.07130084468266));
#24427=CARTESIAN_POINT('Ctrl Pts',(22.8,-0.587554988912119,4.05963744408228));
#24428=CARTESIAN_POINT('Ctrl Pts',(22.8,-0.592174260192535,4.04779597854866));
#24429=CARTESIAN_POINT('Ctrl Pts',(4.,0.254721014554616,3.46322028700966));
#24430=CARTESIAN_POINT('Ctrl Pts',(4.,0.254552373521139,3.46319452321125));
#24431=CARTESIAN_POINT('Ctrl Pts',(4.,0.254383724765285,3.46316883668624));
#24432=CARTESIAN_POINT('Ctrl Pts',(4.,0.254215068323085,3.46314322746093));
#24433=CARTESIAN_POINT('Ctrl Pts',(4.,0.228435861761457,3.4592288468388));
#24434=CARTESIAN_POINT('Ctrl Pts',(4.,0.202474691352968,3.45711700011808));
#24435=CARTESIAN_POINT('Ctrl Pts',(4.,0.176517231963435,3.45683380906617));
#24436=CARTESIAN_POINT('Ctrl Pts',(4.,0.151199179447316,3.45655759382427));
#24437=CARTESIAN_POINT('Ctrl Pts',(4.,0.125883695414598,3.45802192769867));
#24438=CARTESIAN_POINT('Ctrl Pts',(4.,0.1007794950383,3.46128259448669));
#24439=CARTESIAN_POINT('Ctrl Pts',(4.,0.0854593772715275,3.46327245269535));
#24440=CARTESIAN_POINT('Ctrl Pts',(4.,0.0702187270328167,3.46593187194604));
#24441=CARTESIAN_POINT('Ctrl Pts',(4.,0.0551140352340102,3.4692772918897));
#24442=CARTESIAN_POINT('Ctrl Pts',(4.,0.0468842919617017,3.47110003330284));
#24443=CARTESIAN_POINT('Ctrl Pts',(4.,0.0386923719445779,3.47312744960567));
#24444=CARTESIAN_POINT('Ctrl Pts',(4.,0.0305707631998946,3.47535548770785));
#24445=CARTESIAN_POINT('Ctrl Pts',(4.,0.0102648423897012,3.48092610391051));
#24446=CARTESIAN_POINT('Ctrl Pts',(4.,-0.00963556638195036,3.48775588581666));
#24447=CARTESIAN_POINT('Ctrl Pts',(4.,-0.0289965775380143,3.49587186612014));
#24448=CARTESIAN_POINT('Ctrl Pts',(4.,-0.047965755796229,3.50382359322137));
#24449=CARTESIAN_POINT('Ctrl Pts',(4.,-0.0664174073931304,3.51301096346156));
#24450=CARTESIAN_POINT('Ctrl Pts',(4.,-0.0841982143338667,3.52340033683134));
#24451=CARTESIAN_POINT('Ctrl Pts',(4.,-0.0930898199841631,3.5285957259532));
#24452=CARTESIAN_POINT('Ctrl Pts',(4.,-0.101813128894432,3.53409169793663));
#24453=CARTESIAN_POINT('Ctrl Pts',(4.,-0.110345561972859,3.53988353361915));
#24454=CARTESIAN_POINT('Ctrl Pts',(4.,-0.11586100642067,3.5436274303089));
#24455=CARTESIAN_POINT('Ctrl Pts',(4.,-0.121288652521606,3.54748953413154));
#24456=CARTESIAN_POINT('Ctrl Pts',(4.,-0.126621987542688,3.55146681430013));
#24457=CARTESIAN_POINT('Ctrl Pts',(4.,-0.143297831161627,3.56390265451229));
#24458=CARTESIAN_POINT('Ctrl Pts',(4.,-0.159061930875806,3.57746928852925));
#24459=CARTESIAN_POINT('Ctrl Pts',(4.,-0.173743808224101,3.59211536896244));
#24460=CARTESIAN_POINT('Ctrl Pts',(4.,-0.187864697165731,3.60620182877415));
#24461=CARTESIAN_POINT('Ctrl Pts',(4.,-0.200984288190684,3.62128798311348));
#24462=CARTESIAN_POINT('Ctrl Pts',(4.,-0.212904831975564,3.63731335989365));
#24463=CARTESIAN_POINT('Ctrl Pts',(4.,-0.21528245268753,3.64050971304978));
#24464=CARTESIAN_POINT('Ctrl Pts',(4.,-0.217612227418936,3.64374335030505));
#24465=CARTESIAN_POINT('Ctrl Pts',(4.,-0.219892372743211,3.64701365460636));
#24466=CARTESIAN_POINT('Ctrl Pts',(22.8,-0.592174260192532,4.04779597854869));
#24467=CARTESIAN_POINT('Ctrl Pts',(22.7920473606562,-0.584213376873468,
4.14642833911734));
#24468=CARTESIAN_POINT('Ctrl Pts',(22.7840947213124,-0.551140611244481,
4.24298318064208));
#24469=CARTESIAN_POINT('Ctrl Pts',(22.7761420819686,-0.496922031827459,
4.32571394759471));
#24470=CARTESIAN_POINT('Ctrl Pts',(22.7681894426248,-0.442703452410443,
4.40844471454734));
#24471=CARTESIAN_POINT('Ctrl Pts',(22.760236803281,-0.367339059205388,4.47735140692785));
#24472=CARTESIAN_POINT('Ctrl Pts',(22.7522841639372,-0.280089901523161,
4.52398941366922));
#24473=CARTESIAN_POINT('Ctrl Pts',(22.7444712463773,-0.194373644734646,
4.56980802634291));
#24474=CARTESIAN_POINT('Ctrl Pts',(22.7366583288174,-0.0971865673270821,
4.59413356703531));
#24475=CARTESIAN_POINT('Ctrl Pts',(22.7288454112575,-7.11440487624268E-7,
4.59414971000239));
#24476=CARTESIAN_POINT('Origin',(27.2,0.3,2.9));
#24477=CARTESIAN_POINT('',(29.2,0.3,3.04606079858305));
#24478=CARTESIAN_POINT('',(27.2,0.3,3.04606079858305));
#24479=CARTESIAN_POINT('',(23.3,0.3,3.04606079858305));
#24480=CARTESIAN_POINT('',(29.2,0.3,3.35));
#24481=CARTESIAN_POINT('',(29.2,0.3,2.9));
#24482=CARTESIAN_POINT('',(27.2,0.3,3.35));
#24483=CARTESIAN_POINT('',(27.2,0.3,3.35));
#24484=CARTESIAN_POINT('',(27.2,0.3,2.9));
#24485=CARTESIAN_POINT('Origin',(27.2,0.,3.125));
#24486=CARTESIAN_POINT('',(27.2,-0.3,3.04606079858305));
#24487=CARTESIAN_POINT('Origin',(27.2,0.,4.));
#24488=CARTESIAN_POINT('',(27.2,-0.3,3.35));
#24489=CARTESIAN_POINT('',(27.2,0.3,3.35));
#24490=CARTESIAN_POINT('',(27.2,-0.3,3.35));
#24491=CARTESIAN_POINT('Origin',(27.2,0.3,3.35));
#24492=CARTESIAN_POINT('',(29.2,-0.3,3.35));
#24493=CARTESIAN_POINT('',(29.2,0.3,3.35));
#24494=CARTESIAN_POINT('',(27.2,-0.3,3.35));
#24495=CARTESIAN_POINT('Origin',(27.2,-0.3,3.35));
#24496=CARTESIAN_POINT('',(29.2,-0.3,3.04606079858305));
#24497=CARTESIAN_POINT('',(23.3,-0.3,3.04606079858305));
#24498=CARTESIAN_POINT('',(29.2,-0.3,3.35));
#24499=CARTESIAN_POINT('Origin',(29.2,0.,3.125));
#24500=CARTESIAN_POINT('Origin',(29.2,0.,4.));
#24501=CARTESIAN_POINT('Origin',(23.3,0.,4.));
#24502=CARTESIAN_POINT('',(29.4,-1.22464679914735E-16,5.));
#24503=CARTESIAN_POINT('Origin',(29.4,0.,4.));
#24504=CARTESIAN_POINT('',(23.3,-1.22464679914735E-16,5.));
#24505=CARTESIAN_POINT('',(23.3,-1.22464679914735E-16,5.));
#24506=CARTESIAN_POINT('Origin',(23.3,0.,4.));
#24507=CARTESIAN_POINT('Origin',(29.4,0.,4.));
#24508=CARTESIAN_POINT('Origin',(22.8,0.,4.));
#24509=CARTESIAN_POINT('',(22.8,-1.65327317884893E-16,5.35));
#24510=CARTESIAN_POINT('Origin',(22.8,0.,4.));
#24511=CARTESIAN_POINT('Origin',(22.8,0.,4.));
#24512=CARTESIAN_POINT('Origin',(22.8,0.,4.));
#24513=CARTESIAN_POINT('',(23.3,-1.65327317884893E-16,5.35));
#24514=CARTESIAN_POINT('Origin',(23.3,0.,4.));
#24515=CARTESIAN_POINT('',(22.8,-1.65327317884893E-16,5.35));
#24516=CARTESIAN_POINT('Origin',(23.3,0.,4.));
#24517=CARTESIAN_POINT('Origin',(4.,0.,4.));
#24518=CARTESIAN_POINT('Origin',(4.,0.,4.));
#25030=UNCERTAINTY_MEASURE_WITH_UNIT(LENGTH_MEASURE(0.001),#25075,
'DISTANCE_ACCURACY_VALUE',
'Maximum model space distance between geometric entities at asserted c
onnectivities');
#25040=UNCERTAINTY_MEASURE_WITH_UNIT(LENGTH_MEASURE(0.001),#25075,
'DISTANCE_ACCURACY_VALUE',
'Maximum model space distance between geometric entities at asserted c
onnectivities');
#25064=(
GEOMETRIC_REPRESENTATION_CONTEXT(3)
GLOBAL_UNCERTAINTY_ASSIGNED_CONTEXT((#25030))
GLOBAL_UNIT_ASSIGNED_CONTEXT((#25075,#25077,#25078))
REPRESENTATION_CONTEXT('','3D')
);
#25074=(
GEOMETRIC_REPRESENTATION_CONTEXT(3)
GLOBAL_UNCERTAINTY_ASSIGNED_CONTEXT((#25040))
GLOBAL_UNIT_ASSIGNED_CONTEXT((#25075,#25077,#25078))
REPRESENTATION_CONTEXT('','3D')
);
#25075=(
LENGTH_UNIT()
NAMED_UNIT(*)
SI_UNIT(.CENTI.,.METRE.)
);
#25077=(
NAMED_UNIT(*)
PLANE_ANGLE_UNIT()
SI_UNIT($,.RADIAN.)
);
#25078=(
NAMED_UNIT(*)
SI_UNIT($,.STERADIAN.)
SOLID_ANGLE_UNIT()
);
#25102=SHAPE_DEFINITION_REPRESENTATION(#25151,#25217);
#25151=PRODUCT_DEFINITION_SHAPE('',$,#25251);
#25217=SHAPE_REPRESENTATION('',(#8892),#25064);
#25227=PRODUCT_DEFINITION_CONTEXT('part definition',#25328,'design');
#25251=PRODUCT_DEFINITION('Tr12x3 lead screw','Tr12x3 lead screw',#25284,
#25227);
#25284=PRODUCT_DEFINITION_FORMATION('',$,#25353);
#25328=APPLICATION_CONTEXT(
'Core Data for Automotive Mechanical Design Process');
#25329=PRODUCT_CONTEXT('part definition',#25328,'mechanical');
#25353=PRODUCT('Tr12x3 lead screw','Tr12x3 lead screw',
'Tr12x3 lead screw',(#25329));
#25440=COLOUR_RGB('Black',0.12,0.14,0.17);
#25441=FILL_AREA_STYLE_COLOUR('',#25440);
#25442=FILL_AREA_STYLE('',(#25441));
#25443=SURFACE_STYLE_FILL_AREA(#25442);
#25444=SURFACE_SIDE_STYLE('',(#25443));
#25445=SURFACE_STYLE_USAGE(.BOTH.,#25444);
#25446=PRESENTATION_STYLE_ASSIGNMENT((#25445));
ENDSEC;
END-ISO-10303-21;
